ISO-10303-21;
HEADER;
/* Generated by software containing ST-Developer
 * from STEP Tools, Inc. (www.steptools.com) 
 */

FILE_DESCRIPTION(
/* description */ ('XY cross-slide table'),
/* implementation_level */ '2;1');

FILE_NAME(
/* name */ 'X Stage - 01 Supported TR12x3 screw.step',
/* time_stamp */ '2026-10-28T03:22:46-07:00',
/* author */ (''),
/* organization */ (''),
/* preprocessor_version */ 'ST-DEVELOPER v20.2',
/* originating_system */ 'Autodesk Translation Framework v15.17.0.0',
/* authorisation */ '');

FILE_SCHEMA (('AUTOMOTIVE_DESIGN { 1 0 10303 214 3 1 1 }'));
ENDSEC;

DATA;
#10=MECHANICAL_DESIGN_GEOMETRIC_PRESENTATION_REPRESENTATION('',(#1717),#62984);
#13=B_SPLINE_SURFACE_WITH_KNOTS('',3,3,((#43107,#43108,#43109,#43110,#43111,
#43112,#43113,#43114,#43115,#43116,#43117,#43118,#43119,#43120,#43121,#43122,
#43123,#43124,#43125,#43126,#43127,#43128,#43129,#43130,#43131,#43132,#43133,
#43134,#43135,#43136,#43137,#43138,#43139,#43140,#43141,#43142,#43143,#43144,
#43145,#43146,#43147,#43148,#43149,#43150,#43151,#43152,#43153,#43154,#43155,
#43156,#43157,#43158,#43159,#43160,#43161,#43162,#43163,#43164,#43165,#43166,
#43167,#43168,#43169,#43170,#43171,#43172,#43173,#43174,#43175,#43176,#43177,
#43178,#43179,#43180,#43181,#43182,#43183,#43184,#43185,#43186,#43187,#43188,
#43189,#43190,#43191,#43192,#43193,#43194,#43195,#43196,#43197,#43198,#43199,
#43200,#43201,#43202,#43203,#43204,#43205,#43206,#43207,#43208,#43209,#43210,
#43211,#43212,#43213,#43214,#43215,#43216,#43217,#43218,#43219,#43220,#43221,
#43222,#43223,#43224,#43225,#43226,#43227,#43228,#43229,#43230,#43231,#43232,
#43233,#43234,#43235,#43236,#43237,#43238,#43239,#43240,#43241,#43242,#43243,
#43244,#43245,#43246,#43247,#43248,#43249,#43250,#43251,#43252,#43253,#43254,
#43255,#43256,#43257,#43258,#43259,#43260,#43261,#43262,#43263,#43264,#43265,
#43266,#43267,#43268,#43269,#43270,#43271,#43272,#43273,#43274,#43275,#43276,
#43277,#43278,#43279,#43280,#43281,#43282,#43283,#43284,#43285,#43286,#43287,
#43288,#43289,#43290,#43291,#43292,#43293,#43294,#43295,#43296,#43297,#43298,
#43299,#43300,#43301,#43302,#43303,#43304,#43305,#43306,#43307,#43308,#43309,
#43310,#43311,#43312,#43313,#43314,#43315,#43316,#43317,#43318,#43319,#43320,
#43321,#43322,#43323,#43324,#43325,#43326,#43327,#43328,#43329,#43330,#43331,
#43332,#43333,#43334,#43335,#43336,#43337,#43338,#43339,#43340,#43341,#43342,
#43343,#43344,#43345,#43346,#43347,#43348,#43349,#43350,#43351,#43352,#43353,
#43354,#43355,#43356,#43357,#43358,#43359,#43360,#43361,#43362,#43363,#43364,
#43365,#43366,#43367,#43368,#43369,#43370,#43371,#43372,#43373,#43374,#43375,
#43376,#43377,#43378,#43379,#43380,#43381,#43382,#43383,#43384,#43385,#43386,
#43387,#43388,#43389,#43390,#43391,#43392,#43393,#43394,#43395,#43396,#43397,
#43398,#43399,#43400,#43401,#43402,#43403,#43404,#43405,#43406,#43407,#43408,
#43409,#43410,#43411,#43412,#43413,#43414,#43415,#43416,#43417,#43418,#43419,
#43420,#43421,#43422,#43423,#43424,#43425,#43426,#43427,#43428,#43429,#43430,
#43431,#43432,#43433,#43434,#43435,#43436,#43437,#43438,#43439,#43440,#43441,
#43442,#43443,#43444,#43445,#43446,#43447,#43448,#43449,#43450,#43451,#43452,
#43453,#43454,#43455,#43456,#43457,#43458,#43459,#43460,#43461,#43462,#43463,
#43464,#43465,#43466,#43467,#43468,#43469,#43470,#43471,#43472,#43473,#43474,
#43475,#43476,#43477,#43478,#43479,#43480,#43481,#43482,#43483,#43484,#43485,
#43486,#43487,#43488,#43489,#43490,#43491,#43492,#43493,#43494,#43495,#43496,
#43497,#43498,#43499,#43500,#43501,#43502,#43503,#43504,#43505,#43506,#43507,
#43508,#43509,#43510,#43511,#43512,#43513,#43514,#43515,#43516,#43517,#43518,
#43519,#43520,#43521,#43522,#43523,#43524,#43525,#43526,#43527,#43528,#43529,
#43530,#43531,#43532,#43533,#43534,#43535,#43536,#43537,#43538,#43539,#43540,
#43541,#43542,#43543,#43544,#43545,#43546,#43547,#43548,#43549,#43550,#43551,
#43552,#43553,#43554,#43555,#43556,#43557,#43558,#43559,#43560,#43561,#43562,
#43563,#43564,#43565,#43566,#43567,#43568,#43569,#43570,#43571,#43572,#43573,
#43574,#43575,#43576,#43577,#43578,#43579,#43580,#43581,#43582,#43583,#43584,
#43585,#43586,#43587,#43588,#43589,#43590,#43591,#43592,#43593,#43594,#43595,
#43596,#43597,#43598,#43599,#43600,#43601,#43602,#43603,#43604),(#43605,
#43606,#43607,#43608,#43609,#43610,#43611,#43612,#43613,#43614,#43615,#43616,
#43617,#43618,#43619,#43620,#43621,#43622,#43623,#43624,#43625,#43626,#43627,
#43628,#43629,#43630,#43631,#43632,#43633,#43634,#43635,#43636,#43637,#43638,
#43639,#43640,#43641,#43642,#43643,#43644,#43645,#43646,#43647,#43648,#43649,
#43650,#43651,#43652,#43653,#43654,#43655,#43656,#43657,#43658,#43659,#43660,
#43661,#43662,#43663,#43664,#43665,#43666,#43667,#43668,#43669,#43670,#43671,
#43672,#43673,#43674,#43675,#43676,#43677,#43678,#43679,#43680,#43681,#43682,
#43683,#43684,#43685,#43686,#43687,#43688,#43689,#43690,#43691,#43692,#43693,
#43694,#43695,#43696,#43697,#43698,#43699,#43700,#43701,#43702,#43703,#43704,
#43705,#43706,#43707,#43708,#43709,#43710,#43711,#43712,#43713,#43714,#43715,
#43716,#43717,#43718,#43719,#43720,#43721,#43722,#43723,#43724,#43725,#43726,
#43727,#43728,#43729,#43730,#43731,#43732,#43733,#43734,#43735,#43736,#43737,
#43738,#43739,#43740,#43741,#43742,#43743,#43744,#43745,#43746,#43747,#43748,
#43749,#43750,#43751,#43752,#43753,#43754,#43755,#43756,#43757,#43758,#43759,
#43760,#43761,#43762,#43763,#43764,#43765,#43766,#43767,#43768,#43769,#43770,
#43771,#43772,#43773,#43774,#43775,#43776,#43777,#43778,#43779,#43780,#43781,
#43782,#43783,#43784,#43785,#43786,#43787,#43788,#43789,#43790,#43791,#43792,
#43793,#43794,#43795,#43796,#43797,#43798,#43799,#43800,#43801,#43802,#43803,
#43804,#43805,#43806,#43807,#43808,#43809,#43810,#43811,#43812,#43813,#43814,
#43815,#43816,#43817,#43818,#43819,#43820,#43821,#43822,#43823,#43824,#43825,
#43826,#43827,#43828,#43829,#43830,#43831,#43832,#43833,#43834,#43835,#43836,
#43837,#43838,#43839,#43840,#43841,#43842,#43843,#43844,#43845,#43846,#43847,
#43848,#43849,#43850,#43851,#43852,#43853,#43854,#43855,#43856,#43857,#43858,
#43859,#43860,#43861,#43862,#43863,#43864,#43865,#43866,#43867,#43868,#43869,
#43870,#43871,#43872,#43873,#43874,#43875,#43876,#43877,#43878,#43879,#43880,
#43881,#43882,#43883,#43884,#43885,#43886,#43887,#43888,#43889,#43890,#43891,
#43892,#43893,#43894,#43895,#43896,#43897,#43898,#43899,#43900,#43901,#43902,
#43903,#43904,#43905,#43906,#43907,#43908,#43909,#43910,#43911,#43912,#43913,
#43914,#43915,#43916,#43917,#43918,#43919,#43920,#43921,#43922,#43923,#43924,
#43925,#43926,#43927,#43928,#43929,#43930,#43931,#43932,#43933,#43934,#43935,
#43936,#43937,#43938,#43939,#43940,#43941,#43942,#43943,#43944,#43945,#43946,
#43947,#43948,#43949,#43950,#43951,#43952,#43953,#43954,#43955,#43956,#43957,
#43958,#43959,#43960,#43961,#43962,#43963,#43964,#43965,#43966,#43967,#43968,
#43969,#43970,#43971,#43972,#43973,#43974,#43975,#43976,#43977,#43978,#43979,
#43980,#43981,#43982,#43983,#43984,#43985,#43986,#43987,#43988,#43989,#43990,
#43991,#43992,#43993,#43994,#43995,#43996,#43997,#43998,#43999,#44000,#44001,
#44002,#44003,#44004,#44005,#44006,#44007,#44008,#44009,#44010,#44011,#44012,
#44013,#44014,#44015,#44016,#44017,#44018,#44019,#44020,#44021,#44022,#44023,
#44024,#44025,#44026,#44027,#44028,#44029,#44030,#44031,#44032,#44033,#44034,
#44035,#44036,#44037,#44038,#44039,#44040,#44041,#44042,#44043,#44044,#44045,
#44046,#44047,#44048,#44049,#44050,#44051,#44052,#44053,#44054,#44055,#44056,
#44057,#44058,#44059,#44060,#44061,#44062,#44063,#44064,#44065,#44066,#44067,
#44068,#44069,#44070,#44071,#44072,#44073,#44074,#44075,#44076,#44077,#44078,
#44079,#44080,#44081,#44082,#44083,#44084,#44085,#44086,#44087,#44088,#44089,
#44090,#44091,#44092,#44093,#44094,#44095,#44096,#44097,#44098,#44099,#44100,
#44101,#44102),(#44103,#44104,#44105,#44106,#44107,#44108,#44109,#44110,
#44111,#44112,#44113,#44114,#44115,#44116,#44117,#44118,#44119,#44120,#44121,
#44122,#44123,#44124,#44125,#44126,#44127,#44128,#44129,#44130,#44131,#44132,
#44133,#44134,#44135,#44136,#44137,#44138,#44139,#44140,#44141,#44142,#44143,
#44144,#44145,#44146,#44147,#44148,#44149,#44150,#44151,#44152,#44153,#44154,
#44155,#44156,#44157,#44158,#44159,#44160,#44161,#44162,#44163,#44164,#44165,
#44166,#44167,#44168,#44169,#44170,#44171,#44172,#44173,#44174,#44175,#44176,
#44177,#44178,#44179,#44180,#44181,#44182,#44183,#44184,#44185,#44186,#44187,
#44188,#44189,#44190,#44191,#44192,#44193,#44194,#44195,#44196,#44197,#44198,
#44199,#44200,#44201,#44202,#44203,#44204,#44205,#44206,#44207,#44208,#44209,
#44210,#44211,#44212,#44213,#44214,#44215,#44216,#44217,#44218,#44219,#44220,
#44221,#44222,#44223,#44224,#44225,#44226,#44227,#44228,#44229,#44230,#44231,
#44232,#44233,#44234,#44235,#44236,#44237,#44238,#44239,#44240,#44241,#44242,
#44243,#44244,#44245,#44246,#44247,#44248,#44249,#44250,#44251,#44252,#44253,
#44254,#44255,#44256,#44257,#44258,#44259,#44260,#44261,#44262,#44263,#44264,
#44265,#44266,#44267,#44268,#44269,#44270,#44271,#44272,#44273,#44274,#44275,
#44276,#44277,#44278,#44279,#44280,#44281,#44282,#44283,#44284,#44285,#44286,
#44287,#44288,#44289,#44290,#44291,#44292,#44293,#44294,#44295,#44296,#44297,
#44298,#44299,#44300,#44301,#44302,#44303,#44304,#44305,#44306,#44307,#44308,
#44309,#44310,#44311,#44312,#44313,#44314,#44315,#44316,#44317,#44318,#44319,
#44320,#44321,#44322,#44323,#44324,#44325,#44326,#44327,#44328,#44329,#44330,
#44331,#44332,#44333,#44334,#44335,#44336,#44337,#44338,#44339,#44340,#44341,
#44342,#44343,#44344,#44345,#44346,#44347,#44348,#44349,#44350,#44351,#44352,
#44353,#44354,#44355,#44356,#44357,#44358,#44359,#44360,#44361,#44362,#44363,
#44364,#44365,#44366,#44367,#44368,#44369,#44370,#44371,#44372,#44373,#44374,
#44375,#44376,#44377,#44378,#44379,#44380,#44381,#44382,#44383,#44384,#44385,
#44386,#44387,#44388,#44389,#44390,#44391,#44392,#44393,#44394,#44395,#44396,
#44397,#44398,#44399,#44400,#44401,#44402,#44403,#44404,#44405,#44406,#44407,
#44408,#44409,#44410,#44411,#44412,#44413,#44414,#44415,#44416,#44417,#44418,
#44419,#44420,#44421,#44422,#44423,#44424,#44425,#44426,#44427,#44428,#44429,
#44430,#44431,#44432,#44433,#44434,#44435,#44436,#44437,#44438,#44439,#44440,
#44441,#44442,#44443,#44444,#44445,#44446,#44447,#44448,#44449,#44450,#44451,
#44452,#44453,#44454,#44455,#44456,#44457,#44458,#44459,#44460,#44461,#44462,
#44463,#44464,#44465,#44466,#44467,#44468,#44469,#44470,#44471,#44472,#44473,
#44474,#44475,#44476,#44477,#44478,#44479,#44480,#44481,#44482,#44483,#44484,
#44485,#44486,#44487,#44488,#44489,#44490,#44491,#44492,#44493,#44494,#44495,
#44496,#44497,#44498,#44499,#44500,#44501,#44502,#44503,#44504,#44505,#44506,
#44507,#44508,#44509,#44510,#44511,#44512,#44513,#44514,#44515,#44516,#44517,
#44518,#44519,#44520,#44521,#44522,#44523,#44524,#44525,#44526,#44527,#44528,
#44529,#44530,#44531,#44532,#44533,#44534,#44535,#44536,#44537,#44538,#44539,
#44540,#44541,#44542,#44543,#44544,#44545,#44546,#44547,#44548,#44549,#44550,
#44551,#44552,#44553,#44554,#44555,#44556,#44557,#44558,#44559,#44560,#44561,
#44562,#44563,#44564,#44565,#44566,#44567,#44568,#44569,#44570,#44571,#44572,
#44573,#44574,#44575,#44576,#44577,#44578,#44579,#44580,#44581,#44582,#44583,
#44584,#44585,#44586,#44587,#44588,#44589,#44590,#44591,#44592,#44593,#44594,
#44595,#44596,#44597,#44598,#44599,#44600),(#44601,#44602,#44603,#44604,
#44605,#44606,#44607,#44608,#44609,#44610,#44611,#44612,#44613,#44614,#44615,
#44616,#44617,#44618,#44619,#44620,#44621,#44622,#44623,#44624,#44625,#44626,
#44627,#44628,#44629,#44630,#44631,#44632,#44633,#44634,#44635,#44636,#44637,
#44638,#44639,#44640,#44641,#44642,#44643,#44644,#44645,#44646,#44647,#44648,
#44649,#44650,#44651,#44652,#44653,#44654,#44655,#44656,#44657,#44658,#44659,
#44660,#44661,#44662,#44663,#44664,#44665,#44666,#44667,#44668,#44669,#44670,
#44671,#44672,#44673,#44674,#44675,#44676,#44677,#44678,#44679,#44680,#44681,
#44682,#44683,#44684,#44685,#44686,#44687,#44688,#44689,#44690,#44691,#44692,
#44693,#44694,#44695,#44696,#44697,#44698,#44699,#44700,#44701,#44702,#44703,
#44704,#44705,#44706,#44707,#44708,#44709,#44710,#44711,#44712,#44713,#44714,
#44715,#44716,#44717,#44718,#44719,#44720,#44721,#44722,#44723,#44724,#44725,
#44726,#44727,#44728,#44729,#44730,#44731,#44732,#44733,#44734,#44735,#44736,
#44737,#44738,#44739,#44740,#44741,#44742,#44743,#44744,#44745,#44746,#44747,
#44748,#44749,#44750,#44751,#44752,#44753,#44754,#44755,#44756,#44757,#44758,
#44759,#44760,#44761,#44762,#44763,#44764,#44765,#44766,#44767,#44768,#44769,
#44770,#44771,#44772,#44773,#44774,#44775,#44776,#44777,#44778,#44779,#44780,
#44781,#44782,#44783,#44784,#44785,#44786,#44787,#44788,#44789,#44790,#44791,
#44792,#44793,#44794,#44795,#44796,#44797,#44798,#44799,#44800,#44801,#44802,
#44803,#44804,#44805,#44806,#44807,#44808,#44809,#44810,#44811,#44812,#44813,
#44814,#44815,#44816,#44817,#44818,#44819,#44820,#44821,#44822,#44823,#44824,
#44825,#44826,#44827,#44828,#44829,#44830,#44831,#44832,#44833,#44834,#44835,
#44836,#44837,#44838,#44839,#44840,#44841,#44842,#44843,#44844,#44845,#44846,
#44847,#44848,#44849,#44850,#44851,#44852,#44853,#44854,#44855,#44856,#44857,
#44858,#44859,#44860,#44861,#44862,#44863,#44864,#44865,#44866,#44867,#44868,
#44869,#44870,#44871,#44872,#44873,#44874,#44875,#44876,#44877,#44878,#44879,
#44880,#44881,#44882,#44883,#44884,#44885,#44886,#44887,#44888,#44889,#44890,
#44891,#44892,#44893,#44894,#44895,#44896,#44897,#44898,#44899,#44900,#44901,
#44902,#44903,#44904,#44905,#44906,#44907,#44908,#44909,#44910,#44911,#44912,
#44913,#44914,#44915,#44916,#44917,#44918,#44919,#44920,#44921,#44922,#44923,
#44924,#44925,#44926,#44927,#44928,#44929,#44930,#44931,#44932,#44933,#44934,
#44935,#44936,#44937,#44938,#44939,#44940,#44941,#44942,#44943,#44944,#44945,
#44946,#44947,#44948,#44949,#44950,#44951,#44952,#44953,#44954,#44955,#44956,
#44957,#44958,#44959,#44960,#44961,#44962,#44963,#44964,#44965,#44966,#44967,
#44968,#44969,#44970,#44971,#44972,#44973,#44974,#44975,#44976,#44977,#44978,
#44979,#44980,#44981,#44982,#44983,#44984,#44985,#44986,#44987,#44988,#44989,
#44990,#44991,#44992,#44993,#44994,#44995,#44996,#44997,#44998,#44999,#45000,
#45001,#45002,#45003,#45004,#45005,#45006,#45007,#45008,#45009,#45010,#45011,
#45012,#45013,#45014,#45015,#45016,#45017,#45018,#45019,#45020,#45021,#45022,
#45023,#45024,#45025,#45026,#45027,#45028,#45029,#45030,#45031,#45032,#45033,
#45034,#45035,#45036,#45037,#45038,#45039,#45040,#45041,#45042,#45043,#45044,
#45045,#45046,#45047,#45048,#45049,#45050,#45051,#45052,#45053,#45054,#45055,
#45056,#45057,#45058,#45059,#45060,#45061,#45062,#45063,#45064,#45065,#45066,
#45067,#45068,#45069,#45070,#45071,#45072,#45073,#45074,#45075,#45076,#45077,
#45078,#45079,#45080,#45081,#45082,#45083,#45084,#45085,#45086,#45087,#45088,
#45089,#45090,#45091,#45092,#45093,#45094,#45095,#45096,#45097,#45098)),
 .UNSPECIFIED.,.F.,.F.,.F.,(4,4),(4,1,1,1,1,1,1,1,1,1,1,1,1,1,1,1,1,1,1,
1,1,1,1,1,1,1,1,1,1,1,1,1,1,1,1,1,1,1,1,1,1,1,1,1,1,1,1,1,1,1,1,1,1,1,1,
1,1,1,1,1,1,1,1,1,1,1,1,1,1,1,1,1,1,1,1,1,1,1,1,1,1,1,1,1,1,1,1,1,1,1,1,
1,1,1,1,1,1,1,1,1,1,1,1,1,1,1,1,1,1,1,1,1,1,1,1,1,1,1,1,1,1,1,1,1,1,1,1,
1,1,1,1,1,1,1,1,1,1,1,1,1,1,1,1,1,1,1,1,1,1,1,1,1,1,1,1,1,1,1,1,1,1,1,1,
1,1,1,1,1,1,1,1,1,1,1,1,1,1,1,1,1,1,1,1,1,1,1,1,1,1,1,1,1,1,1,1,1,1,1,1,
1,1,1,1,1,1,1,1,1,1,1,1,1,1,1,1,1,1,1,1,1,1,1,1,1,1,1,1,1,1,1,1,1,1,1,1,
1,1,1,1,1,1,1,1,1,1,1,1,1,1,1,1,1,1,1,1,1,1,1,1,1,1,1,1,1,1,1,1,1,1,1,1,
1,1,1,1,1,1,1,1,1,1,1,1,1,1,1,1,1,1,1,1,1,1,1,1,1,1,1,1,1,1,1,1,1,1,1,1,
1,1,1,1,1,1,1,1,1,1,1,1,1,1,1,1,1,1,1,1,1,1,1,1,1,1,1,1,1,1,1,1,1,1,1,1,
1,1,1,1,1,1,1,1,1,1,1,1,1,1,1,1,1,1,1,1,1,1,1,1,1,1,1,1,1,1,1,1,1,1,1,1,
1,1,1,1,1,1,1,1,1,1,1,1,1,1,1,1,1,1,1,1,1,1,1,1,1,1,1,1,1,1,1,1,1,1,1,1,
1,1,1,1,1,1,1,1,1,1,1,1,1,1,1,1,1,1,1,1,1,1,1,1,1,1,1,1,1,1,1,1,1,1,1,1,
1,1,1,1,1,1,1,1,1,1,1,1,1,1,1,1,1,1,1,1,1,1,1,1,1,1,1,1,1,1,1,1,1,1,1,1,
1,1,1,1,1,1,1,1,4),(0.,0.184512097253587),(8.98171729021681,9.48139635699984,
9.98107542378286,10.4807544905659,10.9804335573489,11.4801126241319,11.979791690915,
12.479470757698,12.979149824481,13.478828891264,13.9785079580471,14.4781870248301,
14.9778660916131,15.4775451583961,15.9772242251791,16.4769032919622,16.9765823587452,
17.4762614255282,17.9759404923112,18.4756195590943,18.9752986258773,19.4749776926603,
19.9746567594433,20.4743358262264,20.9740148930094,21.4736939597924,21.9733730265754,
22.4730520933585,22.9727311601415,23.4724102269245,23.9720892937075,24.4717683604905,
24.9714474272736,25.4711264940566,25.9708055608396,26.4704846276226,26.9701636944057,
27.4698427611887,27.9695218279717,28.4692008947547,28.9688799615378,29.4685590283208,
29.9682380951038,30.4679171618868,30.9675962286699,31.4672752954529,31.9669543622359,
32.4666334290189,32.966312495802,33.465991562585,33.965670629368,34.465349696151,
34.965028762934,35.4647078297171,35.9643868965001,36.4640659632831,36.9637450300661,
37.4634240968492,37.9631031636322,38.4627822304152,38.9624612971982,39.4621403639813,
39.9618194307643,40.4614984975473,40.9611775643303,41.4608566311134,41.9605356978964,
42.4602147646794,42.9598938314624,43.4595728982454,43.9592519650285,44.4589310318115,
44.9586100985945,45.4582891653775,45.9579682321606,46.4576472989436,46.9573263657266,
47.4570054325096,47.9566844992927,48.4563635660757,48.9560426328587,49.4557216996417,
49.9554007664248,50.4550798332078,50.9547588999908,51.4544379667738,51.9541170335568,
52.4537961003399,52.9534751671229,53.4531542339059,53.9528333006889,54.452512367472,
54.952191434255,55.451870501038,55.951549567821,56.4512286346041,56.9509077013871,
57.4505867681701,57.9502658349531,58.4499449017362,58.9496239685192,59.9489821020852,
60.9483402356513,61.9476983692173,62.9470565027834,63.9464146363494,64.9457727699155,
65.9451309034815,66.9444890370476,67.9438471706136,68.9432053041797,69.9425634377457,
70.9419215713118,71.9412797048778,72.9406378384438,73.9399959720099,74.9393541055759,
75.938712239142,76.938070372708,77.9374285062741,78.9367866398401,79.9361447734062,
80.9355029069722,81.9348610405383,82.9342191741043,83.9335773076704,84.9329354412364,
85.9322935748025,86.9316517083685,87.9310098419346,88.9303679755006,89.9297261090666,
90.9290842426327,91.9284423761987,92.9278005097648,93.9271586433308,94.9265167768969,
95.9258749104629,96.925233044029,97.924591177595,98.9239493111611,99.9233074447271,
100.922665578293,101.922023711859,102.921381845425,103.920739978991,104.920098112557,
105.919456246123,106.918814379689,107.918172513255,108.917530646822,109.916888780388,
110.916246913954,111.91560504752,112.914963181086,113.914321314652,114.913679448218,
115.913037581784,116.91239571535,117.911753848916,118.911111982482,119.910470116048,
120.909828249614,121.90918638318,122.908544516746,123.907902650312,124.907260783878,
125.906618917444,126.90597705101,127.905335184576,128.904693318142,129.904051451709,
130.903409585275,131.902767718841,132.902125852407,133.901483985973,134.900842119539,
135.900200253105,136.899558386671,137.898916520237,138.898274653803,139.897632787369,
140.896990920935,141.896349054501,142.895707188067,143.895065321633,144.894423455199,
145.893781588765,146.893139722331,147.892497855897,148.891855989463,149.891214123029,
150.890572256596,151.889930390162,152.889288523728,153.888646657294,154.88800479086,
155.887362924426,156.886721057992,157.886079191558,158.885437325124,159.88479545869,
160.884153592256,161.883511725822,162.882869859388,163.882227992954,164.88158612652,
165.880944260086,166.880302393652,167.879660527218,168.879018660784,169.87837679435,
170.877734927916,171.877093061483,172.876451195049,173.875809328615,174.875167462181,
175.874525595747,176.873883729313,177.873241862879,178.872599996445,179.871958130011,
180.871316263577,181.870674397143,182.870032530709,183.869390664275,184.868748797841,
185.868106931407,186.867465064973,187.866823198539,188.866181332105,189.865539465671,
190.864897599237,191.864255732803,192.86361386637,193.862971999936,194.862330133502,
195.861688267068,196.861046400634,197.8604045342,198.859762667766,199.859120801332,
200.858478934898,201.857837068464,202.85719520203,203.856553335596,204.855911469162,
205.855269602728,206.854627736294,207.85398586986,208.853344003426,209.852702136992,
210.852060270558,211.851418404124,212.85077653769,213.850134671257,214.849492804823,
215.848850938389,216.848209071955,217.847567205521,218.846925339087,219.846283472653,
220.845641606219,221.844999739785,222.844357873351,223.843716006917,224.843074140483,
225.842432274049,226.841790407615,227.841148541181,228.840506674747,229.839864808313,
230.839222941879,231.838581075445,232.837939209011,233.837297342577,234.836655476144,
235.83601360971,236.835371743276,237.834729876842,238.834088010408,239.833446143974,
240.83280427754,241.832162411106,242.831520544672,243.830878678238,244.830236811804,
245.82959494537,246.828953078936,247.828311212502,248.827669346068,249.827027479634,
250.8263856132,251.825743746766,252.825101880332,253.824460013898,254.823818147464,
255.82317628103,256.822534414597,257.821892548163,258.821250681729,259.820608815295,
260.819966948861,261.819325082427,262.818683215993,263.818041349559,264.817399483125,
265.816757616691,266.816115750257,267.815473883823,268.814832017389,269.814190150955,
270.813548284521,271.812906418087,272.812264551653,273.811622685219,274.810980818785,
275.810338952351,276.809697085917,277.809055219484,278.80841335305,279.807771486616,
280.807129620182,281.806487753748,282.805845887314,283.80520402088,284.804562154446,
285.803920288012,286.803278421578,287.802636555144,288.80199468871,289.801352822276,
290.800710955842,291.800069089408,292.799427222974,293.79878535654,294.798143490106,
295.797501623672,296.796859757238,297.796217890804,298.795576024371,299.794934157937,
300.794292291503,301.793650425069,302.793008558635,303.792366692201,304.791724825767,
305.791082959333,306.790441092899,307.789799226465,308.789157360031,309.788515493597,
310.787873627163,311.787231760729,312.786589894295,313.785948027861,314.785306161427,
315.784664294993,316.784022428559,317.783380562125,318.782738695691,319.782096829258,
320.781454962824,321.78081309639,322.780171229956,323.779529363522,324.778887497088,
325.778245630654,326.77760376422,327.776961897786,328.776320031352,329.775678164918,
330.775036298484,331.77439443205,332.773752565616,333.773110699182,334.772468832748,
335.771826966314,336.77118509988,337.770543233446,338.769901367012,339.769259500578,
340.768617634145,341.767975767711,342.767333901277,343.766692034843,344.766050168409,
345.765408301975,346.764766435541,347.764124569107,348.763482702673,349.762840836239,
350.762198969805,351.761557103371,352.760915236937,353.760273370503,354.259952437286,
354.759631504069,355.259310570852,355.758989637635,356.258668704418,356.758347771201,
357.258026837984,357.757705904767,358.25738497155,358.757064038333,359.256743105116,
359.756422171899,360.256101238682,360.755780305465,361.255459372248,361.755138439031,
362.254817505815,362.754496572598,363.254175639381,363.753854706164,364.253533772947,
364.75321283973,365.252891906513,365.752570973296,366.252250040079,366.751929106862,
367.251608173645,367.751287240428,368.250966307211,368.750645373994,369.250324440777,
369.75000350756,370.249682574343,370.749361641126,371.249040707909,371.748719774692,
372.248398841475,372.748077908258,373.247756975041,373.747436041824,374.247115108607,
374.74679417539,375.246473242173,375.746152308956,376.245831375739,376.745510442522,
377.245189509305,377.744868576088,378.244547642871,378.744226709654,379.243905776437,
379.74358484322,380.243263910003,380.742942976786,381.242622043569,381.742301110352,
382.241980177135,382.741659243918,383.241338310702,383.741017377485,384.240696444268,
384.740375511051,385.240054577834,385.739733644617,386.2394127114,386.739091778183,
387.238770844966,387.738449911749,388.238128978532,388.737808045315,389.237487112098,
389.737166178881,390.236845245664,390.736524312447,391.23620337923,391.735882446013,
392.235561512796,392.735240579579,393.234919646362,393.734598713145,394.234277779928,
394.733956846711,395.233635913494,395.733314980277,396.23299404706,396.732673113843,
397.232352180626,397.732031247409,398.231710314192,398.731389380975,399.231068447758,
399.730747514541,400.230426581324,400.730105648107,401.22978471489,401.729463781673,
402.229142848456,402.728821915239,403.228500982022,403.728180048805),
 .UNSPECIFIED.);
#14=B_SPLINE_SURFACE_WITH_KNOTS('',3,3,((#45192,#45193,#45194,#45195,#45196,
#45197,#45198,#45199,#45200,#45201,#45202,#45203,#45204,#45205,#45206,#45207,
#45208,#45209,#45210,#45211,#45212,#45213,#45214,#45215,#45216,#45217,#45218,
#45219,#45220,#45221,#45222,#45223,#45224,#45225,#45226,#45227,#45228,#45229,
#45230,#45231,#45232,#45233,#45234,#45235,#45236,#45237,#45238,#45239,#45240,
#45241,#45242,#45243,#45244,#45245,#45246,#45247,#45248,#45249,#45250,#45251,
#45252,#45253,#45254,#45255,#45256,#45257,#45258,#45259,#45260,#45261,#45262,
#45263,#45264,#45265,#45266,#45267,#45268,#45269,#45270,#45271,#45272,#45273,
#45274,#45275,#45276,#45277,#45278,#45279,#45280,#45281,#45282,#45283,#45284,
#45285,#45286,#45287,#45288,#45289,#45290,#45291,#45292,#45293,#45294,#45295,
#45296,#45297,#45298,#45299,#45300,#45301,#45302,#45303,#45304,#45305,#45306,
#45307,#45308,#45309,#45310,#45311,#45312,#45313,#45314,#45315,#45316,#45317,
#45318,#45319,#45320,#45321,#45322,#45323,#45324,#45325,#45326,#45327,#45328,
#45329,#45330,#45331,#45332,#45333,#45334,#45335,#45336,#45337,#45338,#45339,
#45340,#45341,#45342,#45343,#45344,#45345,#45346,#45347,#45348,#45349,#45350,
#45351,#45352,#45353,#45354,#45355,#45356,#45357,#45358,#45359,#45360,#45361,
#45362,#45363,#45364,#45365,#45366,#45367,#45368,#45369,#45370,#45371,#45372,
#45373,#45374,#45375,#45376,#45377,#45378,#45379,#45380,#45381,#45382,#45383,
#45384,#45385,#45386,#45387,#45388,#45389,#45390,#45391,#45392,#45393,#45394,
#45395,#45396,#45397,#45398,#45399,#45400,#45401,#45402,#45403,#45404,#45405,
#45406,#45407,#45408,#45409,#45410,#45411,#45412,#45413,#45414,#45415,#45416,
#45417,#45418,#45419,#45420,#45421,#45422,#45423,#45424,#45425,#45426,#45427,
#45428,#45429,#45430,#45431,#45432,#45433,#45434,#45435,#45436,#45437,#45438,
#45439,#45440,#45441,#45442,#45443,#45444,#45445,#45446,#45447,#45448,#45449,
#45450,#45451,#45452,#45453,#45454,#45455,#45456,#45457,#45458,#45459,#45460,
#45461,#45462,#45463,#45464,#45465,#45466,#45467,#45468,#45469,#45470,#45471,
#45472,#45473,#45474,#45475,#45476,#45477,#45478,#45479,#45480,#45481,#45482,
#45483,#45484,#45485,#45486,#45487,#45488,#45489,#45490,#45491,#45492,#45493,
#45494,#45495,#45496,#45497,#45498,#45499,#45500,#45501,#45502,#45503,#45504,
#45505,#45506,#45507,#45508,#45509,#45510,#45511,#45512,#45513,#45514,#45515,
#45516,#45517,#45518,#45519,#45520,#45521,#45522,#45523,#45524,#45525,#45526,
#45527,#45528,#45529,#45530,#45531,#45532,#45533,#45534,#45535,#45536,#45537,
#45538,#45539,#45540,#45541,#45542,#45543,#45544,#45545,#45546,#45547,#45548,
#45549,#45550,#45551,#45552,#45553,#45554,#45555,#45556,#45557,#45558,#45559,
#45560,#45561,#45562,#45563,#45564,#45565,#45566,#45567,#45568,#45569,#45570,
#45571,#45572,#45573,#45574,#45575,#45576,#45577,#45578,#45579,#45580,#45581,
#45582,#45583,#45584,#45585,#45586,#45587,#45588,#45589,#45590,#45591,#45592,
#45593,#45594,#45595,#45596,#45597,#45598,#45599,#45600,#45601,#45602,#45603,
#45604,#45605,#45606,#45607,#45608,#45609,#45610,#45611,#45612,#45613,#45614,
#45615,#45616,#45617,#45618,#45619,#45620,#45621,#45622,#45623,#45624,#45625,
#45626,#45627,#45628,#45629,#45630,#45631,#45632,#45633,#45634,#45635,#45636,
#45637,#45638,#45639,#45640,#45641,#45642,#45643,#45644,#45645,#45646,#45647,
#45648,#45649,#45650,#45651,#45652,#45653,#45654,#45655,#45656,#45657,#45658,
#45659,#45660,#45661,#45662,#45663,#45664,#45665,#45666,#45667,#45668,#45669,
#45670,#45671,#45672,#45673,#45674,#45675,#45676,#45677,#45678,#45679,#45680,
#45681,#45682,#45683,#45684,#45685,#45686,#45687,#45688,#45689),(#45690,
#45691,#45692,#45693,#45694,#45695,#45696,#45697,#45698,#45699,#45700,#45701,
#45702,#45703,#45704,#45705,#45706,#45707,#45708,#45709,#45710,#45711,#45712,
#45713,#45714,#45715,#45716,#45717,#45718,#45719,#45720,#45721,#45722,#45723,
#45724,#45725,#45726,#45727,#45728,#45729,#45730,#45731,#45732,#45733,#45734,
#45735,#45736,#45737,#45738,#45739,#45740,#45741,#45742,#45743,#45744,#45745,
#45746,#45747,#45748,#45749,#45750,#45751,#45752,#45753,#45754,#45755,#45756,
#45757,#45758,#45759,#45760,#45761,#45762,#45763,#45764,#45765,#45766,#45767,
#45768,#45769,#45770,#45771,#45772,#45773,#45774,#45775,#45776,#45777,#45778,
#45779,#45780,#45781,#45782,#45783,#45784,#45785,#45786,#45787,#45788,#45789,
#45790,#45791,#45792,#45793,#45794,#45795,#45796,#45797,#45798,#45799,#45800,
#45801,#45802,#45803,#45804,#45805,#45806,#45807,#45808,#45809,#45810,#45811,
#45812,#45813,#45814,#45815,#45816,#45817,#45818,#45819,#45820,#45821,#45822,
#45823,#45824,#45825,#45826,#45827,#45828,#45829,#45830,#45831,#45832,#45833,
#45834,#45835,#45836,#45837,#45838,#45839,#45840,#45841,#45842,#45843,#45844,
#45845,#45846,#45847,#45848,#45849,#45850,#45851,#45852,#45853,#45854,#45855,
#45856,#45857,#45858,#45859,#45860,#45861,#45862,#45863,#45864,#45865,#45866,
#45867,#45868,#45869,#45870,#45871,#45872,#45873,#45874,#45875,#45876,#45877,
#45878,#45879,#45880,#45881,#45882,#45883,#45884,#45885,#45886,#45887,#45888,
#45889,#45890,#45891,#45892,#45893,#45894,#45895,#45896,#45897,#45898,#45899,
#45900,#45901,#45902,#45903,#45904,#45905,#45906,#45907,#45908,#45909,#45910,
#45911,#45912,#45913,#45914,#45915,#45916,#45917,#45918,#45919,#45920,#45921,
#45922,#45923,#45924,#45925,#45926,#45927,#45928,#45929,#45930,#45931,#45932,
#45933,#45934,#45935,#45936,#45937,#45938,#45939,#45940,#45941,#45942,#45943,
#45944,#45945,#45946,#45947,#45948,#45949,#45950,#45951,#45952,#45953,#45954,
#45955,#45956,#45957,#45958,#45959,#45960,#45961,#45962,#45963,#45964,#45965,
#45966,#45967,#45968,#45969,#45970,#45971,#45972,#45973,#45974,#45975,#45976,
#45977,#45978,#45979,#45980,#45981,#45982,#45983,#45984,#45985,#45986,#45987,
#45988,#45989,#45990,#45991,#45992,#45993,#45994,#45995,#45996,#45997,#45998,
#45999,#46000,#46001,#46002,#46003,#46004,#46005,#46006,#46007,#46008,#46009,
#46010,#46011,#46012,#46013,#46014,#46015,#46016,#46017,#46018,#46019,#46020,
#46021,#46022,#46023,#46024,#46025,#46026,#46027,#46028,#46029,#46030,#46031,
#46032,#46033,#46034,#46035,#46036,#46037,#46038,#46039,#46040,#46041,#46042,
#46043,#46044,#46045,#46046,#46047,#46048,#46049,#46050,#46051,#46052,#46053,
#46054,#46055,#46056,#46057,#46058,#46059,#46060,#46061,#46062,#46063,#46064,
#46065,#46066,#46067,#46068,#46069,#46070,#46071,#46072,#46073,#46074,#46075,
#46076,#46077,#46078,#46079,#46080,#46081,#46082,#46083,#46084,#46085,#46086,
#46087,#46088,#46089,#46090,#46091,#46092,#46093,#46094,#46095,#46096,#46097,
#46098,#46099,#46100,#46101,#46102,#46103,#46104,#46105,#46106,#46107,#46108,
#46109,#46110,#46111,#46112,#46113,#46114,#46115,#46116,#46117,#46118,#46119,
#46120,#46121,#46122,#46123,#46124,#46125,#46126,#46127,#46128,#46129,#46130,
#46131,#46132,#46133,#46134,#46135,#46136,#46137,#46138,#46139,#46140,#46141,
#46142,#46143,#46144,#46145,#46146,#46147,#46148,#46149,#46150,#46151,#46152,
#46153,#46154,#46155,#46156,#46157,#46158,#46159,#46160,#46161,#46162,#46163,
#46164,#46165,#46166,#46167,#46168,#46169,#46170,#46171,#46172,#46173,#46174,
#46175,#46176,#46177,#46178,#46179,#46180,#46181,#46182,#46183,#46184,#46185,
#46186,#46187),(#46188,#46189,#46190,#46191,#46192,#46193,#46194,#46195,
#46196,#46197,#46198,#46199,#46200,#46201,#46202,#46203,#46204,#46205,#46206,
#46207,#46208,#46209,#46210,#46211,#46212,#46213,#46214,#46215,#46216,#46217,
#46218,#46219,#46220,#46221,#46222,#46223,#46224,#46225,#46226,#46227,#46228,
#46229,#46230,#46231,#46232,#46233,#46234,#46235,#46236,#46237,#46238,#46239,
#46240,#46241,#46242,#46243,#46244,#46245,#46246,#46247,#46248,#46249,#46250,
#46251,#46252,#46253,#46254,#46255,#46256,#46257,#46258,#46259,#46260,#46261,
#46262,#46263,#46264,#46265,#46266,#46267,#46268,#46269,#46270,#46271,#46272,
#46273,#46274,#46275,#46276,#46277,#46278,#46279,#46280,#46281,#46282,#46283,
#46284,#46285,#46286,#46287,#46288,#46289,#46290,#46291,#46292,#46293,#46294,
#46295,#46296,#46297,#46298,#46299,#46300,#46301,#46302,#46303,#46304,#46305,
#46306,#46307,#46308,#46309,#46310,#46311,#46312,#46313,#46314,#46315,#46316,
#46317,#46318,#46319,#46320,#46321,#46322,#46323,#46324,#46325,#46326,#46327,
#46328,#46329,#46330,#46331,#46332,#46333,#46334,#46335,#46336,#46337,#46338,
#46339,#46340,#46341,#46342,#46343,#46344,#46345,#46346,#46347,#46348,#46349,
#46350,#46351,#46352,#46353,#46354,#46355,#46356,#46357,#46358,#46359,#46360,
#46361,#46362,#46363,#46364,#46365,#46366,#46367,#46368,#46369,#46370,#46371,
#46372,#46373,#46374,#46375,#46376,#46377,#46378,#46379,#46380,#46381,#46382,
#46383,#46384,#46385,#46386,#46387,#46388,#46389,#46390,#46391,#46392,#46393,
#46394,#46395,#46396,#46397,#46398,#46399,#46400,#46401,#46402,#46403,#46404,
#46405,#46406,#46407,#46408,#46409,#46410,#46411,#46412,#46413,#46414,#46415,
#46416,#46417,#46418,#46419,#46420,#46421,#46422,#46423,#46424,#46425,#46426,
#46427,#46428,#46429,#46430,#46431,#46432,#46433,#46434,#46435,#46436,#46437,
#46438,#46439,#46440,#46441,#46442,#46443,#46444,#46445,#46446,#46447,#46448,
#46449,#46450,#46451,#46452,#46453,#46454,#46455,#46456,#46457,#46458,#46459,
#46460,#46461,#46462,#46463,#46464,#46465,#46466,#46467,#46468,#46469,#46470,
#46471,#46472,#46473,#46474,#46475,#46476,#46477,#46478,#46479,#46480,#46481,
#46482,#46483,#46484,#46485,#46486,#46487,#46488,#46489,#46490,#46491,#46492,
#46493,#46494,#46495,#46496,#46497,#46498,#46499,#46500,#46501,#46502,#46503,
#46504,#46505,#46506,#46507,#46508,#46509,#46510,#46511,#46512,#46513,#46514,
#46515,#46516,#46517,#46518,#46519,#46520,#46521,#46522,#46523,#46524,#46525,
#46526,#46527,#46528,#46529,#46530,#46531,#46532,#46533,#46534,#46535,#46536,
#46537,#46538,#46539,#46540,#46541,#46542,#46543,#46544,#46545,#46546,#46547,
#46548,#46549,#46550,#46551,#46552,#46553,#46554,#46555,#46556,#46557,#46558,
#46559,#46560,#46561,#46562,#46563,#46564,#46565,#46566,#46567,#46568,#46569,
#46570,#46571,#46572,#46573,#46574,#46575,#46576,#46577,#46578,#46579,#46580,
#46581,#46582,#46583,#46584,#46585,#46586,#46587,#46588,#46589,#46590,#46591,
#46592,#46593,#46594,#46595,#46596,#46597,#46598,#46599,#46600,#46601,#46602,
#46603,#46604,#46605,#46606,#46607,#46608,#46609,#46610,#46611,#46612,#46613,
#46614,#46615,#46616,#46617,#46618,#46619,#46620,#46621,#46622,#46623,#46624,
#46625,#46626,#46627,#46628,#46629,#46630,#46631,#46632,#46633,#46634,#46635,
#46636,#46637,#46638,#46639,#46640,#46641,#46642,#46643,#46644,#46645,#46646,
#46647,#46648,#46649,#46650,#46651,#46652,#46653,#46654,#46655,#46656,#46657,
#46658,#46659,#46660,#46661,#46662,#46663,#46664,#46665,#46666,#46667,#46668,
#46669,#46670,#46671,#46672,#46673,#46674,#46675,#46676,#46677,#46678,#46679,
#46680,#46681,#46682,#46683,#46684,#46685),(#46686,#46687,#46688,#46689,
#46690,#46691,#46692,#46693,#46694,#46695,#46696,#46697,#46698,#46699,#46700,
#46701,#46702,#46703,#46704,#46705,#46706,#46707,#46708,#46709,#46710,#46711,
#46712,#46713,#46714,#46715,#46716,#46717,#46718,#46719,#46720,#46721,#46722,
#46723,#46724,#46725,#46726,#46727,#46728,#46729,#46730,#46731,#46732,#46733,
#46734,#46735,#46736,#46737,#46738,#46739,#46740,#46741,#46742,#46743,#46744,
#46745,#46746,#46747,#46748,#46749,#46750,#46751,#46752,#46753,#46754,#46755,
#46756,#46757,#46758,#46759,#46760,#46761,#46762,#46763,#46764,#46765,#46766,
#46767,#46768,#46769,#46770,#46771,#46772,#46773,#46774,#46775,#46776,#46777,
#46778,#46779,#46780,#46781,#46782,#46783,#46784,#46785,#46786,#46787,#46788,
#46789,#46790,#46791,#46792,#46793,#46794,#46795,#46796,#46797,#46798,#46799,
#46800,#46801,#46802,#46803,#46804,#46805,#46806,#46807,#46808,#46809,#46810,
#46811,#46812,#46813,#46814,#46815,#46816,#46817,#46818,#46819,#46820,#46821,
#46822,#46823,#46824,#46825,#46826,#46827,#46828,#46829,#46830,#46831,#46832,
#46833,#46834,#46835,#46836,#46837,#46838,#46839,#46840,#46841,#46842,#46843,
#46844,#46845,#46846,#46847,#46848,#46849,#46850,#46851,#46852,#46853,#46854,
#46855,#46856,#46857,#46858,#46859,#46860,#46861,#46862,#46863,#46864,#46865,
#46866,#46867,#46868,#46869,#46870,#46871,#46872,#46873,#46874,#46875,#46876,
#46877,#46878,#46879,#46880,#46881,#46882,#46883,#46884,#46885,#46886,#46887,
#46888,#46889,#46890,#46891,#46892,#46893,#46894,#46895,#46896,#46897,#46898,
#46899,#46900,#46901,#46902,#46903,#46904,#46905,#46906,#46907,#46908,#46909,
#46910,#46911,#46912,#46913,#46914,#46915,#46916,#46917,#46918,#46919,#46920,
#46921,#46922,#46923,#46924,#46925,#46926,#46927,#46928,#46929,#46930,#46931,
#46932,#46933,#46934,#46935,#46936,#46937,#46938,#46939,#46940,#46941,#46942,
#46943,#46944,#46945,#46946,#46947,#46948,#46949,#46950,#46951,#46952,#46953,
#46954,#46955,#46956,#46957,#46958,#46959,#46960,#46961,#46962,#46963,#46964,
#46965,#46966,#46967,#46968,#46969,#46970,#46971,#46972,#46973,#46974,#46975,
#46976,#46977,#46978,#46979,#46980,#46981,#46982,#46983,#46984,#46985,#46986,
#46987,#46988,#46989,#46990,#46991,#46992,#46993,#46994,#46995,#46996,#46997,
#46998,#46999,#47000,#47001,#47002,#47003,#47004,#47005,#47006,#47007,#47008,
#47009,#47010,#47011,#47012,#47013,#47014,#47015,#47016,#47017,#47018,#47019,
#47020,#47021,#47022,#47023,#47024,#47025,#47026,#47027,#47028,#47029,#47030,
#47031,#47032,#47033,#47034,#47035,#47036,#47037,#47038,#47039,#47040,#47041,
#47042,#47043,#47044,#47045,#47046,#47047,#47048,#47049,#47050,#47051,#47052,
#47053,#47054,#47055,#47056,#47057,#47058,#47059,#47060,#47061,#47062,#47063,
#47064,#47065,#47066,#47067,#47068,#47069,#47070,#47071,#47072,#47073,#47074,
#47075,#47076,#47077,#47078,#47079,#47080,#47081,#47082,#47083,#47084,#47085,
#47086,#47087,#47088,#47089,#47090,#47091,#47092,#47093,#47094,#47095,#47096,
#47097,#47098,#47099,#47100,#47101,#47102,#47103,#47104,#47105,#47106,#47107,
#47108,#47109,#47110,#47111,#47112,#47113,#47114,#47115,#47116,#47117,#47118,
#47119,#47120,#47121,#47122,#47123,#47124,#47125,#47126,#47127,#47128,#47129,
#47130,#47131,#47132,#47133,#47134,#47135,#47136,#47137,#47138,#47139,#47140,
#47141,#47142,#47143,#47144,#47145,#47146,#47147,#47148,#47149,#47150,#47151,
#47152,#47153,#47154,#47155,#47156,#47157,#47158,#47159,#47160,#47161,#47162,
#47163,#47164,#47165,#47166,#47167,#47168,#47169,#47170,#47171,#47172,#47173,
#47174,#47175,#47176,#47177,#47178,#47179,#47180,#47181,#47182,#47183)),
 .UNSPECIFIED.,.F.,.F.,.F.,(4,4),(4,1,1,1,1,1,1,1,1,1,1,1,1,1,1,1,1,1,1,
1,1,1,1,1,1,1,1,1,1,1,1,1,1,1,1,1,1,1,1,1,1,1,1,1,1,1,1,1,1,1,1,1,1,1,1,
1,1,1,1,1,1,1,1,1,1,1,1,1,1,1,1,1,1,1,1,1,1,1,1,1,1,1,1,1,1,1,1,1,1,1,1,
1,1,1,1,1,1,1,1,1,1,1,1,1,1,1,1,1,1,1,1,1,1,1,1,1,1,1,1,1,1,1,1,1,1,1,1,
1,1,1,1,1,1,1,1,1,1,1,1,1,1,1,1,1,1,1,1,1,1,1,1,1,1,1,1,1,1,1,1,1,1,1,1,
1,1,1,1,1,1,1,1,1,1,1,1,1,1,1,1,1,1,1,1,1,1,1,1,1,1,1,1,1,1,1,1,1,1,1,1,
1,1,1,1,1,1,1,1,1,1,1,1,1,1,1,1,1,1,1,1,1,1,1,1,1,1,1,1,1,1,1,1,1,1,1,1,
1,1,1,1,1,1,1,1,1,1,1,1,1,1,1,1,1,1,1,1,1,1,1,1,1,1,1,1,1,1,1,1,1,1,1,1,
1,1,1,1,1,1,1,1,1,1,1,1,1,1,1,1,1,1,1,1,1,1,1,1,1,1,1,1,1,1,1,1,1,1,1,1,
1,1,1,1,1,1,1,1,1,1,1,1,1,1,1,1,1,1,1,1,1,1,1,1,1,1,1,1,1,1,1,1,1,1,1,1,
1,1,1,1,1,1,1,1,1,1,1,1,1,1,1,1,1,1,1,1,1,1,1,1,1,1,1,1,1,1,1,1,1,1,1,1,
1,1,1,1,1,1,1,1,1,1,1,1,1,1,1,1,1,1,1,1,1,1,1,1,1,1,1,1,1,1,1,1,1,1,1,1,
1,1,1,1,1,1,1,1,1,1,1,1,1,1,1,1,1,1,1,1,1,1,1,1,1,1,1,1,1,1,1,1,1,1,1,1,
1,1,1,1,1,1,1,1,1,1,1,1,1,1,1,1,1,1,1,1,1,1,1,1,1,1,1,1,1,1,1,1,1,1,1,1,
1,1,1,1,1,1,1,1,4),(0.,0.184512097253587),(12.0092477762453,12.5089268430284,
13.0086059098114,13.5082849765944,14.0079640433774,14.5076431101605,15.0073221769435,
15.5070012437265,16.0066803105095,16.5063593772925,17.0060384440756,17.5057175108586,
18.0053965776416,18.5050756444246,19.0047547112077,19.5044337779907,20.0041128447737,
20.5037919115567,21.0034709783398,21.5031500451228,22.0028291119058,22.5025081786888,
23.0021872454719,23.5018663122549,24.0015453790379,24.5012244458209,25.0009035126039,
25.500582579387,26.00026164617,26.499940712953,26.999619779736,27.4992988465191,
27.9989779133021,28.4986569800851,28.9983360468681,29.4980151136512,29.9976941804342,
30.4973732472172,30.9970523140002,31.4967313807832,31.9964104475663,32.4960895143493,
32.9957685811323,33.4954476479153,33.9951267146984,34.4948057814814,34.9944848482644,
35.4941639150474,35.9938429818305,36.4935220486135,36.9932011153965,37.4928801821795,
37.9925592489626,38.4922383157456,38.9919173825286,39.4915964493116,39.9912755160946,
40.4909545828777,40.9906336496607,41.4903127164437,41.9899917832267,42.4896708500098,
42.9893499167928,43.4890289835758,43.9887080503588,44.4883871171419,44.9880661839249,
45.4877452507079,45.9874243174909,46.4871033842739,46.986782451057,47.48646151784,
47.986140584623,48.485819651406,48.9854987181891,49.4851777849721,49.9848568517551,
50.4845359185381,50.9842149853212,51.4838940521042,51.9835731188872,52.4832521856702,
52.9829312524532,53.4826103192363,53.9822893860193,54.4819684528023,54.9816475195853,
55.4813265863684,55.9810056531514,56.4806847199344,56.9803637867174,57.4800428535005,
57.9797219202835,58.4794009870665,58.9790800538495,59.4787591206325,59.9784381874156,
60.4781172541986,60.9777963209816,61.4774753877646,61.9771544545477,62.9765125881137,
63.9758707216798,64.9752288552458,65.9745869888119,66.9739451223779,67.9733032559439,
68.97266138951,69.972019523076,70.9713776566421,71.9707357902081,72.9700939237742,
73.9694520573402,74.9688101909063,75.9681683244723,76.9675264580384,77.9668845916044,
78.9662427251705,79.9656008587365,80.9649589923026,81.9643171258686,82.9636752594347,
83.9630333930007,84.9623915265667,85.9617496601328,86.9611077936988,87.9604659272649,
88.9598240608309,89.959182194397,90.958540327963,91.9578984615291,92.9572565950951,
93.9566147286612,94.9559728622272,95.9553309957932,96.9546891293593,97.9540472629253,
98.9534053964914,99.9527635300574,100.952121663623,101.95147979719,102.950837930756,
103.950196064322,104.949554197888,105.948912331454,106.94827046502,107.947628598586,
108.946986732152,109.946344865718,110.945702999284,111.94506113285,112.944419266416,
113.943777399982,114.943135533548,115.942493667114,116.94185180068,117.941209934246,
118.940568067812,119.939926201378,120.939284334944,121.93864246851,122.938000602077,
123.937358735643,124.936716869209,125.936075002775,126.935433136341,127.934791269907,
128.934149403473,129.933507537039,130.932865670605,131.932223804171,132.931581937737,
133.930940071303,134.930298204869,135.929656338435,136.929014472001,137.928372605567,
138.927730739133,139.927088872699,140.926447006265,141.925805139831,142.925163273397,
143.924521406963,144.92387954053,145.923237674096,146.922595807662,147.921953941228,
148.921312074794,149.92067020836,150.920028341926,151.919386475492,152.918744609058,
153.918102742624,154.91746087619,155.916819009756,156.916177143322,157.915535276888,
158.914893410454,159.91425154402,160.913609677586,161.912967811152,162.912325944718,
163.911684078284,164.91104221185,165.910400345416,166.909758478983,167.909116612549,
168.908474746115,169.907832879681,170.907191013247,171.906549146813,172.905907280379,
173.905265413945,174.904623547511,175.903981681077,176.903339814643,177.902697948209,
178.902056081775,179.901414215341,180.900772348907,181.900130482473,182.899488616039,
183.898846749605,184.898204883171,185.897563016737,186.896921150303,187.89627928387,
188.895637417436,189.894995551002,190.894353684568,191.893711818134,192.8930699517,
193.892428085266,194.891786218832,195.891144352398,196.890502485964,197.88986061953,
198.889218753096,199.888576886662,200.887935020228,201.887293153794,202.88665128736,
203.886009420926,204.885367554492,205.884725688058,206.884083821624,207.88344195519,
208.882800088756,209.882158222323,210.881516355889,211.880874489455,212.880232623021,
213.879590756587,214.878948890153,215.878307023719,216.877665157285,217.877023290851,
218.876381424417,219.875739557983,220.875097691549,221.874455825115,222.873813958681,
223.873172092247,224.872530225813,225.871888359379,226.871246492945,227.870604626511,
228.869962760077,229.869320893643,230.86867902721,231.868037160776,232.867395294342,
233.866753427908,234.866111561474,235.86546969504,236.864827828606,237.864185962172,
238.863544095738,239.862902229304,240.86226036287,241.861618496436,242.860976630002,
243.860334763568,244.859692897134,245.8590510307,246.858409164266,247.857767297832,
248.857125431398,249.856483564964,250.85584169853,251.855199832097,252.854557965663,
253.853916099229,254.853274232795,255.852632366361,256.851990499927,257.851348633493,
258.850706767059,259.850064900625,260.849423034191,261.848781167757,262.848139301323,
263.847497434889,264.846855568455,265.846213702021,266.845571835587,267.844929969153,
268.844288102719,269.843646236285,270.843004369851,271.842362503417,272.841720636983,
273.84107877055,274.840436904116,275.839795037682,276.839153171248,277.838511304814,
278.83786943838,279.837227571946,280.836585705512,281.835943839078,282.835301972644,
283.83466010621,284.834018239776,285.833376373342,286.832734506908,287.832092640474,
288.83145077404,289.830808907606,290.830167041172,291.829525174738,292.828883308304,
293.82824144187,294.827599575437,295.826957709003,296.826315842569,297.825673976135,
298.825032109701,299.824390243267,300.823748376833,301.823106510399,302.822464643965,
303.821822777531,304.821180911097,305.820539044663,306.819897178229,307.819255311795,
308.818613445361,309.817971578927,310.817329712493,311.816687846059,312.816045979625,
313.815404113191,314.814762246757,315.814120380323,316.81347851389,317.812836647456,
318.812194781022,319.811552914588,320.810911048154,321.81026918172,322.809627315286,
323.808985448852,324.808343582418,325.807701715984,326.80705984955,327.806417983116,
328.805776116682,329.805134250248,330.804492383814,331.80385051738,332.803208650946,
333.802566784512,334.801924918078,335.801283051644,336.80064118521,337.799999318776,
338.799357452343,339.798715585909,340.798073719475,341.797431853041,342.796789986607,
343.796148120173,344.795506253739,345.794864387305,346.794222520871,347.793580654437,
348.792938788003,349.792296921569,350.791655055135,351.791013188701,352.790371322267,
353.789729455833,354.789087589399,355.788445722965,356.787803856531,357.287482923314,
357.787161990097,358.28684105688,358.786520123663,359.286199190446,359.78587825723,
360.285557324013,360.785236390796,361.284915457579,361.784594524362,362.284273591145,
362.783952657928,363.283631724711,363.783310791494,364.282989858277,364.78266892506,
365.282347991843,365.782027058626,366.281706125409,366.781385192192,367.281064258975,
367.780743325758,368.280422392541,368.780101459324,369.279780526107,369.77945959289,
370.279138659673,370.778817726456,371.278496793239,371.778175860022,372.277854926805,
372.777533993588,373.277213060371,373.776892127154,374.276571193937,374.77625026072,
375.275929327503,375.775608394286,376.275287461069,376.774966527852,377.274645594635,
377.774324661418,378.274003728201,378.773682794984,379.273361861767,379.77304092855,
380.272719995333,380.772399062117,381.2720781289,381.771757195683,382.271436262466,
382.771115329249,383.270794396032,383.770473462815,384.270152529598,384.769831596381,
385.269510663164,385.769189729947,386.26886879673,386.768547863513,387.268226930296,
387.767905997079,388.267585063862,388.767264130645,389.266943197428,389.766622264211,
390.266301330994,390.765980397777,391.26565946456,391.765338531343,392.265017598126,
392.764696664909,393.264375731692,393.764054798475,394.263733865258,394.763412932041,
395.263091998824,395.762771065607,396.26245013239,396.762129199173,397.261808265956,
397.761487332739,398.261166399522,398.760845466305,399.260524533088,399.760203599871,
400.259882666654,400.759561733437,401.25924080022,401.758919867003,402.258598933787,
402.75827800057,403.257957067353,403.757636134136,404.257315200919,404.756994267702,
405.256673334485,405.756352401268,406.256031468051,406.755710534834),
 .UNSPECIFIED.);
#768=B_SPLINE_CURVE_WITH_KNOTS('',3,(#37624,#37625,#37626,#37627,#37628,
#37629,#37630,#37631,#37632,#37633,#37634,#37635,#37636,#37637,#37638,#37639,
#37640,#37641,#37642),.UNSPECIFIED.,.F.,.F.,(4,3,3,3,3,3,4),(-3.69871549170445,
-3.49775346748116,-2.99807440069814,-2.49839533391511,-1.99871626713209,
-1.49903720034907,-1.00018350866767),.UNSPECIFIED.);
#769=B_SPLINE_CURVE_WITH_KNOTS('',3,(#37645,#37646,#37647,#37648),
 .UNSPECIFIED.,.F.,.F.,(4,4),(0.,0.443060670554495),.UNSPECIFIED.);
#770=B_SPLINE_CURVE_WITH_KNOTS('',3,(#37653,#37654,#37655,#37656,#37657,
#37658,#37659,#37660,#37661,#37662,#37663,#37664,#37665,#37666,#37667,#37668,
#37669,#37670,#37671,#37672,#37673,#37674,#37675,#37676,#37677,#37678,#37679,
#37680,#37681,#37682,#37683,#37684,#37685,#37686,#37687,#37688,#37689,#37690,
#37691,#37692),.UNSPECIFIED.,.F.,.F.,(4,3,3,3,3,3,3,3,3,3,3,3,3,4),(-9.98190079888403,
-9.49390226887744,-8.99422320209442,-8.4945441353114,-7.99486506852837,
-7.49518600174535,-6.99550693496233,-6.4958278681793,-5.99614880139628,
-5.49646973461325,-4.99679066783023,-4.49711160104721,-3.99743253426419,
-3.69871549170445),.UNSPECIFIED.);
#771=B_SPLINE_CURVE_WITH_KNOTS('',3,(#37693,#37694,#37695,#37696,#37697,
#37698,#37699,#37700,#37701,#37702,#37703,#37704,#37705,#37706,#37707,#37708,
#37709,#37710,#37711,#37712,#37713,#37714,#37715,#37716,#37717,#37718,#37719,
#37720,#37721,#37722,#37723,#37724,#37725,#37726,#37727,#37728,#37729,#37730,
#37731,#37732,#37733,#37734,#37735),.UNSPECIFIED.,.F.,.F.,(4,3,3,3,3,3,
3,3,3,3,3,3,3,3,4),(0.443060670554495,0.49967906678306,0.999358133566079,
1.4990372003491,1.99871626713212,2.49839533391514,2.99807440069816,3.49775346748117,
3.99743253426419,4.49711160104721,4.99679066783023,5.49646973461325,5.99614880139627,
6.49582786817929,6.72624597773408),.UNSPECIFIED.);
#772=B_SPLINE_CURVE_WITH_KNOTS('',3,(#37740,#37741,#37742,#37743,#37744,
#37745,#37746,#37747,#37748,#37749,#37750,#37751,#37752,#37753,#37754,#37755,
#37756,#37757,#37758,#37759,#37760,#37761,#37762,#37763,#37764,#37765,#37766,
#37767,#37768,#37769,#37770,#37771,#37772,#37773,#37774,#37775,#37776,#37777,
#37778,#37779,#37780,#37781,#37782),.UNSPECIFIED.,.F.,.F.,(4,3,3,3,3,3,
3,3,3,3,3,3,3,3,4),(-16.2650861060636,-15.9897301370567,-15.4900510702737,
-14.9903720034907,-14.4906929367077,-13.9910138699247,-13.4913348031416,
-12.9916557363586,-12.4919766695756,-11.9922976027926,-11.4926185360095,
-10.9929394692265,-10.4932604024435,-9.99358133566046,-9.98190079888403),
 .UNSPECIFIED.);
#773=B_SPLINE_CURVE_WITH_KNOTS('',3,(#37783,#37784,#37785,#37786,#37787,
#37788,#37789,#37790,#37791,#37792,#37793,#37794,#37795,#37796,#37797,#37798,
#37799,#37800,#37801,#37802,#37803,#37804,#37805,#37806,#37807,#37808,#37809,
#37810,#37811,#37812,#37813,#37814,#37815,#37816,#37817,#37818,#37819,#37820,
#37821,#37822,#37823,#37824,#37825),.UNSPECIFIED.,.F.,.F.,(4,3,3,3,3,3,
3,3,3,3,3,3,3,3,4),(6.72624597773408,6.99550693496231,7.49518600174534,
7.99486506852837,8.49454413531139,8.99422320209442,9.49390226887745,9.99358133566048,
10.4932604024435,10.9929394692265,11.4926185360096,11.9922976027926,12.4919766695756,
12.9916557363586,13.0094312849137),.UNSPECIFIED.);
#774=B_SPLINE_CURVE_WITH_KNOTS('',3,(#37830,#37831,#37832,#37833,#37834,
#37835,#37836,#37837,#37838,#37839,#37840,#37841,#37842,#37843,#37844,#37845,
#37846,#37847,#37848,#37849,#37850,#37851,#37852,#37853,#37854,#37855,#37856,
#37857,#37858,#37859,#37860,#37861,#37862,#37863,#37864,#37865,#37866,#37867,
#37868,#37869,#37870,#37871,#37872),.UNSPECIFIED.,.F.,.F.,(4,3,3,3,3,3,
3,3,3,3,3,3,3,3,4),(-22.5482714132432,-22.485558005236,-21.985878938453,
-21.48619987167,-20.986520804887,-20.486841738104,-19.9871626713209,-19.4874836045379,
-18.9878045377549,-18.4881254709719,-17.9884464041888,-17.4887673374058,
-16.9890882706228,-16.4894092038398,-16.2650861060636),.UNSPECIFIED.);
#775=B_SPLINE_CURVE_WITH_KNOTS('',3,(#37873,#37874,#37875,#37876,#37877,
#37878,#37879,#37880,#37881,#37882,#37883,#37884,#37885,#37886,#37887,#37888,
#37889,#37890,#37891,#37892,#37893,#37894,#37895,#37896,#37897,#37898,#37899,
#37900,#37901,#37902,#37903,#37904,#37905,#37906,#37907,#37908,#37909,#37910,
#37911,#37912),.UNSPECIFIED.,.F.,.F.,(4,3,3,3,3,3,3,3,3,3,3,3,3,4),(13.0094312849137,
13.4913348031417,13.9910138699247,14.4906929367077,14.9903720034907,15.4900510702737,
15.9897301370568,16.4894092038398,16.9890882706228,17.4887673374058,17.9884464041888,
18.4881254709718,18.9878045377549,19.2926165920933),.UNSPECIFIED.);
#776=B_SPLINE_CURVE_WITH_KNOTS('',3,(#37917,#37918,#37919,#37920,#37921,
#37922,#37923,#37924,#37925,#37926,#37927,#37928,#37929,#37930,#37931,#37932,
#37933,#37934,#37935,#37936,#37937,#37938,#37939,#37940,#37941,#37942,#37943,
#37944,#37945,#37946,#37947,#37948,#37949,#37950,#37951,#37952,#37953,#37954,
#37955,#37956),.UNSPECIFIED.,.F.,.F.,(4,3,3,3,3,3,3,3,3,3,3,3,3,4),(-28.8314567204228,
-28.4817068066323,-27.9820277398493,-27.4823486730663,-26.9826696062833,
-26.4829905395002,-25.9833114727172,-25.4836324059342,-24.9839533391512,
-24.4842742723681,-23.9845952055851,-23.4849161388021,-22.9852370720191,
-22.5482714132432),.UNSPECIFIED.);
#777=B_SPLINE_CURVE_WITH_KNOTS('',3,(#37957,#37958,#37959,#37960,#37961,
#37962,#37963,#37964,#37965,#37966,#37967,#37968,#37969,#37970,#37971,#37972,
#37973,#37974,#37975,#37976,#37977,#37978,#37979,#37980,#37981,#37982,#37983,
#37984,#37985,#37986,#37987,#37988,#37989,#37990,#37991,#37992,#37993,#37994,
#37995,#37996,#37997,#37998,#37999),.UNSPECIFIED.,.F.,.F.,(4,3,3,3,3,3,
3,3,3,3,3,3,3,3,4),(19.2926165920933,19.4874836045379,19.9871626713209,
20.4868417381039,20.986520804887,21.48619987167,21.985878938453,22.4855580052361,
22.9852370720191,23.4849161388021,23.9845952055851,24.4842742723682,24.9839533391512,
25.4836324059342,25.5758018992728),.UNSPECIFIED.);
#778=B_SPLINE_CURVE_WITH_KNOTS('',3,(#38004,#38005,#38006,#38007,#38008,
#38009,#38010,#38011,#38012,#38013,#38014,#38015,#38016,#38017,#38018,#38019,
#38020,#38021,#38022,#38023,#38024,#38025,#38026,#38027,#38028,#38029,#38030,
#38031,#38032,#38033,#38034,#38035,#38036,#38037,#38038,#38039,#38040,#38041,
#38042,#38043,#38044,#38045,#38046),.UNSPECIFIED.,.F.,.F.,(4,3,3,3,3,3,
3,3,3,3,3,3,3,3,4),(-35.1146420276024,-34.9775346748116,-34.4778556080286,
-33.9781765412456,-33.4784974744626,-32.9788184076795,-32.4791393408965,
-31.9794602741135,-31.4797812073305,-30.9801021405474,-30.4804230737644,
-29.9807440069814,-29.4810649401984,-28.9813858734153,-28.8314567204228),
 .UNSPECIFIED.);
#779=B_SPLINE_CURVE_WITH_KNOTS('',3,(#38047,#38048,#38049,#38050,#38051,
#38052,#38053,#38054,#38055,#38056,#38057,#38058,#38059,#38060,#38061,#38062,
#38063,#38064,#38065,#38066,#38067,#38068,#38069,#38070,#38071,#38072,#38073,
#38074,#38075,#38076,#38077,#38078,#38079,#38080,#38081,#38082,#38083,#38084,
#38085,#38086),.UNSPECIFIED.,.F.,.F.,(4,3,3,3,3,3,3,3,3,3,3,3,3,4),(25.5758018992728,
25.9833114727172,26.4829905395003,26.9826696062833,27.4823486730663,27.9820277398493,
28.4817068066324,28.9813858734154,29.4810649401984,29.9807440069814,30.4804230737645,
30.9801021405475,31.4797812073305,31.8589872064524),.UNSPECIFIED.);
#780=B_SPLINE_CURVE_WITH_KNOTS('',3,(#38091,#38092,#38093,#38094,#38095,
#38096,#38097,#38098,#38099,#38100,#38101,#38102,#38103,#38104,#38105,#38106,
#38107,#38108,#38109,#38110,#38111,#38112,#38113,#38114,#38115,#38116,#38117,
#38118,#38119,#38120,#38121,#38122,#38123,#38124,#38125,#38126,#38127,#38128,
#38129,#38130),.UNSPECIFIED.,.F.,.F.,(4,3,3,3,3,3,3,3,3,3,3,3,3,4),(-41.397827334782,
-40.9736834762079,-40.4740044094249,-39.9743253426419,-39.4746462758588,
-38.9749672090758,-38.4752881422928,-37.9756090755098,-37.4759300087267,
-36.9762509419437,-36.4765718751607,-35.9768928083777,-35.4772137415947,
-35.1146420276024),.UNSPECIFIED.);
#781=B_SPLINE_CURVE_WITH_KNOTS('',3,(#38131,#38132,#38133,#38134,#38135,
#38136,#38137,#38138,#38139,#38140,#38141,#38142,#38143,#38144,#38145,#38146,
#38147,#38148,#38149,#38150,#38151,#38152,#38153,#38154,#38155,#38156,#38157,
#38158,#38159,#38160,#38161,#38162,#38163,#38164,#38165,#38166,#38167,#38168,
#38169,#38170,#38171,#38172,#38173),.UNSPECIFIED.,.F.,.F.,(4,3,3,3,3,3,
3,3,3,3,3,3,3,3,4),(31.8589872064524,31.9794602741135,32.4791393408966,
32.9788184076796,33.4784974744626,33.9781765412456,34.4778556080286,34.9775346748117,
35.4772137415947,35.9768928083777,36.4765718751607,36.9762509419437,37.4759300087267,
37.9756090755098,38.142172513632),.UNSPECIFIED.);
#782=B_SPLINE_CURVE_WITH_KNOTS('',3,(#38178,#38179,#38180,#38181,#38182,
#38183,#38184,#38185,#38186,#38187,#38188,#38189,#38190,#38191,#38192,#38193,
#38194,#38195,#38196,#38197,#38198,#38199,#38200,#38201,#38202,#38203,#38204,
#38205,#38206,#38207,#38208,#38209,#38210,#38211,#38212,#38213,#38214,#38215,
#38216,#38217,#38218,#38219,#38220),.UNSPECIFIED.,.F.,.F.,(4,3,3,3,3,3,
3,3,3,3,3,3,3,3,4),(-47.6810126419616,-47.4695113443872,-46.9698322776042,
-46.4701532108212,-45.9704741440381,-45.4707950772551,-44.9711160104721,
-44.4714369436891,-43.971757876906,-43.472078810123,-42.97239974334,-42.472720676557,
-41.973041609774,-41.4733625429909,-41.397827334782),.UNSPECIFIED.);
#783=B_SPLINE_CURVE_WITH_KNOTS('',3,(#38221,#38222,#38223,#38224,#38225,
#38226,#38227,#38228,#38229,#38230,#38231,#38232,#38233,#38234,#38235,#38236,
#38237,#38238,#38239,#38240,#38241,#38242,#38243,#38244,#38245,#38246,#38247,
#38248,#38249,#38250,#38251,#38252,#38253,#38254,#38255,#38256,#38257,#38258,
#38259,#38260),.UNSPECIFIED.,.F.,.F.,(4,3,3,3,3,3,3,3,3,3,3,3,3,4),(38.142172513632,
38.4752881422928,38.9749672090758,39.4746462758589,39.9743253426419,40.4740044094249,
40.973683476208,41.473362542991,41.973041609774,42.472720676557,42.9723997433401,
43.4720788101231,43.9717578769061,44.4253578208116),.UNSPECIFIED.);
#784=B_SPLINE_CURVE_WITH_KNOTS('',3,(#38265,#38266,#38267,#38268,#38269,
#38270,#38271,#38272,#38273,#38274,#38275,#38276,#38277,#38278,#38279,#38280,
#38281,#38282,#38283,#38284,#38285,#38286,#38287,#38288,#38289,#38290,#38291,
#38292),.UNSPECIFIED.,.F.,.F.,(4,3,3,3,3,3,3,3,3,4),(-53.9641979491412,
-52.9659810790005,-51.9666229454344,-50.9672648118684,-49.9679066783023,
-49.4682276115193,-48.9685485447363,-48.4688694779533,-47.9691904111702,
-47.6810126419616),.UNSPECIFIED.);
#785=B_SPLINE_CURVE_WITH_KNOTS('',3,(#38293,#38294,#38295,#38296,#38297,
#38298,#38299,#38300,#38301,#38302,#38303,#38304,#38305,#38306,#38307,#38308,
#38309,#38310,#38311,#38312,#38313,#38314,#38315,#38316,#38317,#38318,#38319,
#38320,#38321,#38322,#38323,#38324,#38325,#38326,#38327,#38328,#38329,#38330,
#38331,#38332),.UNSPECIFIED.,.F.,.F.,(4,3,3,3,3,3,3,3,3,3,3,3,3,4),(44.4253578208116,
44.4714369436892,44.9711160104722,45.4707950772552,45.9704741440382,46.4701532108212,
46.9698322776042,47.4695113443873,47.9691904111703,48.4688694779533,48.9685485447363,
49.4682276115193,49.9679066783024,50.7085431279912),.UNSPECIFIED.);
#786=B_SPLINE_CURVE_WITH_KNOTS('',3,(#38337,#38338,#38339,#38340,#38341,
#38342,#38343,#38344,#38345,#38346,#38347,#38348,#38349,#38350,#38351,#38352,
#38353,#38354,#38355,#38356,#38357,#38358),.UNSPECIFIED.,.F.,.F.,(4,3,3,
3,3,3,3,4),(-60.2473832563207,-59.9614880139628,-58.9621298803968,-57.9627717468307,
-56.9634136132647,-55.9640554796986,-54.9646973461326,-53.9641979491412),
 .UNSPECIFIED.);
#787=B_SPLINE_CURVE_WITH_KNOTS('',3,(#38359,#38360,#38361,#38362,#38363,
#38364,#38365,#38366,#38367,#38368,#38369,#38370,#38371,#38372,#38373,#38374,
#38375,#38376,#38377,#38378,#38379,#38380,#38381,#38382,#38383),
 .UNSPECIFIED.,.F.,.F.,(4,3,3,3,3,3,3,3,4),(50.7085431279912,50.9672648118684,
51.9666229454345,52.9659810790005,53.9653392125666,54.9646973461326,55.9640554796987,
56.9634136132647,56.9917284351708),.UNSPECIFIED.);
#788=B_SPLINE_CURVE_WITH_KNOTS('',3,(#38388,#38389,#38390,#38391,#38392,
#38393,#38394,#38395,#38396,#38397,#38398,#38399,#38400,#38401,#38402,#38403,
#38404,#38405,#38406,#38407,#38408,#38409),.UNSPECIFIED.,.F.,.F.,(4,3,3,
3,3,3,3,4),(-66.5305685635003,-65.9576368153591,-64.958278681793,-63.958920548227,
-62.9595624146609,-61.9602042810949,-60.9608461475288,-60.2473832563207),
 .UNSPECIFIED.);
#789=B_SPLINE_CURVE_WITH_KNOTS('',3,(#38410,#38411,#38412,#38413,#38414,
#38415,#38416,#38417,#38418,#38419,#38420,#38421,#38422,#38423,#38424,#38425,
#38426,#38427,#38428,#38429,#38430,#38431),.UNSPECIFIED.,.F.,.F.,(4,3,3,
3,3,3,3,4),(56.9917284351708,57.9627717468308,58.9621298803968,59.9614880139629,
60.9608461475289,61.960204281095,62.959562414661,63.2749137423504),
 .UNSPECIFIED.);
#790=B_SPLINE_CURVE_WITH_KNOTS('',3,(#38436,#38437,#38438,#38439,#38440,
#38441,#38442,#38443,#38444,#38445,#38446,#38447,#38448,#38449,#38450,#38451,
#38452,#38453,#38454,#38455,#38456,#38457),.UNSPECIFIED.,.F.,.F.,(4,3,3,
3,3,3,3,4),(-72.8137538706799,-71.9537856167554,-70.9544274831893,-69.9550693496233,
-68.9557112160572,-67.9563530824912,-66.9569949489251,-66.5305685635003),
 .UNSPECIFIED.);
#791=B_SPLINE_CURVE_WITH_KNOTS('',3,(#38458,#38459,#38460,#38461,#38462,
#38463,#38464,#38465,#38466,#38467,#38468,#38469,#38470,#38471,#38472,#38473,
#38474,#38475,#38476,#38477,#38478,#38479),.UNSPECIFIED.,.F.,.F.,(4,3,3,
3,3,3,3,4),(63.2749137423504,63.958920548227,64.9582786817931,65.9576368153591,
66.9569949489252,67.9563530824912,68.9557112160573,69.55809904953),
 .UNSPECIFIED.);
#792=B_SPLINE_CURVE_WITH_KNOTS('',3,(#38484,#38485,#38486,#38487,#38488,
#38489,#38490,#38491,#38492,#38493,#38494,#38495,#38496,#38497,#38498,#38499,
#38500,#38501,#38502,#38503,#38504,#38505,#38506,#38507,#38508),
 .UNSPECIFIED.,.F.,.F.,(4,3,3,3,3,3,3,3,4),(-79.0969391778595,-78.9492925517177,
-77.9499344181516,-76.9505762845856,-75.9512181510195,-74.9518600174535,
-73.9525018838875,-72.9531437503214,-72.8137538706799),.UNSPECIFIED.);
#793=B_SPLINE_CURVE_WITH_KNOTS('',3,(#38509,#38510,#38511,#38512,#38513,
#38514,#38515,#38516,#38517,#38518,#38519,#38520,#38521,#38522,#38523,#38524,
#38525,#38526,#38527,#38528,#38529,#38530),.UNSPECIFIED.,.F.,.F.,(4,3,3,
3,3,3,3,4),(69.55809904953,69.9550693496233,70.9544274831893,71.9537856167554,
72.9531437503215,73.9525018838875,74.9518600174536,75.8412843567096),
 .UNSPECIFIED.);
#794=B_SPLINE_CURVE_WITH_KNOTS('',3,(#38535,#38536,#38537,#38538,#38539,
#38540,#38541,#38542,#38543,#38544,#38545,#38546,#38547,#38548,#38549,#38550,
#38551,#38552,#38553,#38554,#38555,#38556),.UNSPECIFIED.,.F.,.F.,(4,3,3,
3,3,3,3,4),(-85.3801244850391,-84.945441353114,-83.9460832195479,-82.9467250859819,
-81.9473669524158,-80.9480088188498,-79.9486506852837,-79.0969391778595),
 .UNSPECIFIED.);
#795=B_SPLINE_CURVE_WITH_KNOTS('',3,(#38557,#38558,#38559,#38560,#38561,
#38562,#38563,#38564,#38565,#38566,#38567,#38568,#38569,#38570,#38571,#38572,
#38573,#38574,#38575,#38576,#38577,#38578,#38579,#38580,#38581),
 .UNSPECIFIED.,.F.,.F.,(4,3,3,3,3,3,3,3,4),(75.8412843567096,75.9512181510196,
76.9505762845857,77.9499344181517,78.9492925517178,79.9486506852838,80.9480088188499,
81.9473669524159,82.1244696638892),.UNSPECIFIED.);
#796=B_SPLINE_CURVE_WITH_KNOTS('',3,(#38586,#38587,#38588,#38589,#38590,
#38591,#38592,#38593,#38594,#38595,#38596,#38597,#38598,#38599,#38600,#38601,
#38602,#38603,#38604,#38605,#38606,#38607),.UNSPECIFIED.,.F.,.F.,(4,3,3,
3,3,3,3,4),(-91.6633097922187,-90.9415901545102,-89.9422320209442,-88.9428738873782,
-87.9435157538121,-86.944157620246,-85.94479948668,-85.3801244850391),
 .UNSPECIFIED.);
#797=B_SPLINE_CURVE_WITH_KNOTS('',3,(#38608,#38609,#38610,#38611,#38612,
#38613,#38614,#38615,#38616,#38617,#38618,#38619,#38620,#38621,#38622,#38623,
#38624,#38625,#38626,#38627,#38628,#38629),.UNSPECIFIED.,.F.,.F.,(4,3,3,
3,3,3,3,4),(82.1244696638892,82.946725085982,83.946083219548,84.9454413531141,
85.9447994866801,86.9441576202461,87.9435157538122,88.4076549710687),
 .UNSPECIFIED.);
#798=B_SPLINE_CURVE_WITH_KNOTS('',3,(#38634,#38635,#38636,#38637,#38638,
#38639,#38640,#38641,#38642,#38643,#38644,#38645,#38646,#38647,#38648,#38649,
#38650,#38651,#38652,#38653,#38654,#38655,#38656,#38657,#38658),
 .UNSPECIFIED.,.F.,.F.,(4,3,3,3,3,3,3,3,4),(-97.9464950993983,-97.9370970894726,
-96.9377389559065,-95.9383808223405,-94.9390226887744,-93.9396645552084,
-92.9403064216423,-91.9409482880763,-91.6633097922187),.UNSPECIFIED.);
#799=B_SPLINE_CURVE_WITH_KNOTS('',3,(#38659,#38660,#38661,#38662,#38663,
#38664,#38665,#38666,#38667,#38668,#38669,#38670,#38671,#38672,#38673,#38674,
#38675,#38676,#38677,#38678,#38679,#38680),.UNSPECIFIED.,.F.,.F.,(4,3,3,
3,3,3,3,4),(88.4076549710687,88.9428738873782,89.9422320209442,90.9415901545103,
91.9409482880763,92.9403064216424,93.9396645552084,94.6908402782483),
 .UNSPECIFIED.);
#800=B_SPLINE_CURVE_WITH_KNOTS('',3,(#38685,#38686,#38687,#38688,#38689,
#38690,#38691,#38692,#38693,#38694,#38695,#38696,#38697,#38698,#38699,#38700,
#38701,#38702,#38703,#38704,#38705,#38706),.UNSPECIFIED.,.F.,.F.,(4,3,3,
3,3,3,3,4),(-104.229680406578,-103.933245890869,-102.933887757303,-101.934529623737,
-100.935171490171,-99.9358133566047,-98.9364552230386,-97.9464950993983),
 .UNSPECIFIED.);
#801=B_SPLINE_CURVE_WITH_KNOTS('',3,(#38707,#38708,#38709,#38710,#38711,
#38712,#38713,#38714,#38715,#38716,#38717,#38718,#38719,#38720,#38721,#38722,
#38723,#38724,#38725,#38726,#38727,#38728,#38729,#38730,#38731),
 .UNSPECIFIED.,.F.,.F.,(4,3,3,3,3,3,3,3,4),(94.6908402782483,94.9390226887745,
95.9383808223405,96.9377389559065,97.9370970894726,98.9364552230386,99.9358133566047,
100.935171490171,100.974025585428),.UNSPECIFIED.);
#802=B_SPLINE_CURVE_WITH_KNOTS('',3,(#38736,#38737,#38738,#38739,#38740,
#38741,#38742,#38743,#38744,#38745,#38746,#38747,#38748,#38749,#38750,#38751,
#38752,#38753,#38754,#38755,#38756,#38757),.UNSPECIFIED.,.F.,.F.,(4,3,3,
3,3,3,3,4),(-110.512865713757,-109.929394692265,-108.930036558699,-107.930678425133,
-106.931320291567,-105.931962158001,-104.932604024435,-104.229680406578),
 .UNSPECIFIED.);
#803=B_SPLINE_CURVE_WITH_KNOTS('',3,(#38758,#38759,#38760,#38761,#38762,
#38763,#38764,#38765,#38766,#38767,#38768,#38769,#38770,#38771,#38772,#38773,
#38774,#38775,#38776,#38777,#38778,#38779),.UNSPECIFIED.,.F.,.F.,(4,3,3,
3,3,3,3,4),(100.974025585428,101.934529623737,102.933887757303,103.933245890869,
104.932604024435,105.931962158001,106.931320291567,107.257210892608),
 .UNSPECIFIED.);
#804=B_SPLINE_CURVE_WITH_KNOTS('',3,(#38784,#38785,#38786,#38787,#38788,
#38789,#38790,#38791,#38792,#38793,#38794,#38795,#38796,#38797,#38798,#38799,
#38800,#38801,#38802,#38803,#38804,#38805),.UNSPECIFIED.,.F.,.F.,(4,3,3,
3,3,3,3,4),(-116.796051020937,-115.925543493661,-114.926185360095,-113.926827226529,
-112.927469092963,-111.928110959397,-110.928752825831,-110.512865713757),
 .UNSPECIFIED.);
#805=B_SPLINE_CURVE_WITH_KNOTS('',3,(#38806,#38807,#38808,#38809,#38810,
#38811,#38812,#38813,#38814,#38815,#38816,#38817,#38818,#38819,#38820,#38821,
#38822,#38823,#38824,#38825,#38826,#38827),.UNSPECIFIED.,.F.,.F.,(4,3,3,
3,3,3,3,4),(107.257210892608,107.930678425133,108.930036558699,109.929394692265,
110.928752825831,111.928110959397,112.927469092963,113.540396199787),
 .UNSPECIFIED.);
#806=B_SPLINE_CURVE_WITH_KNOTS('',3,(#38832,#38833,#38834,#38835,#38836,
#38837,#38838,#38839,#38840,#38841,#38842,#38843,#38844,#38845,#38846,#38847,
#38848,#38849,#38850,#38851,#38852,#38853,#38854,#38855,#38856),
 .UNSPECIFIED.,.F.,.F.,(4,3,3,3,3,3,3,3,4),(-123.079236328117,-122.921050428624,
-121.921692295058,-120.922334161492,-119.922976027926,-118.92361789436,
-117.924259760793,-116.924901627227,-116.796051020937),.UNSPECIFIED.);
#807=B_SPLINE_CURVE_WITH_KNOTS('',3,(#38857,#38858,#38859,#38860,#38861,
#38862,#38863,#38864,#38865,#38866,#38867,#38868,#38869,#38870,#38871,#38872,
#38873,#38874,#38875,#38876,#38877,#38878),.UNSPECIFIED.,.F.,.F.,(4,3,3,
3,3,3,3,4),(113.540396199787,113.926827226529,114.926185360095,115.925543493661,
116.924901627228,117.924259760794,118.92361789436,119.823581506967),
 .UNSPECIFIED.);
#808=B_SPLINE_CURVE_WITH_KNOTS('',3,(#38883,#38884,#38885,#38886,#38887,
#38888,#38889,#38890,#38891,#38892,#38893,#38894,#38895,#38896,#38897,#38898,
#38899,#38900,#38901,#38902,#38903,#38904),.UNSPECIFIED.,.F.,.F.,(4,3,3,
3,3,3,3,4),(-129.362421635296,-128.91719923002,-127.917841096454,-126.918482962888,
-125.919124829322,-124.919766695756,-123.92040856219,-123.079236328117),
 .UNSPECIFIED.);
#809=B_SPLINE_CURVE_WITH_KNOTS('',3,(#38905,#38906,#38907,#38908,#38909,
#38910,#38911,#38912,#38913,#38914,#38915,#38916,#38917,#38918,#38919,#38920,
#38921,#38922,#38923,#38924,#38925,#38926,#38927,#38928,#38929),
 .UNSPECIFIED.,.F.,.F.,(4,3,3,3,3,3,3,3,4),(119.823581506967,119.922976027926,
120.922334161492,121.921692295058,122.921050428624,123.92040856219,124.919766695756,
125.919124829322,126.106766814146),.UNSPECIFIED.);
#810=B_SPLINE_CURVE_WITH_KNOTS('',3,(#38934,#38935,#38936,#38937,#38938,
#38939,#38940,#38941,#38942,#38943,#38944,#38945,#38946,#38947,#38948,#38949,
#38950,#38951,#38952,#38953,#38954,#38955),.UNSPECIFIED.,.F.,.F.,(4,3,3,
3,3,3,3,4),(-135.645606942476,-134.913348031416,-133.91398989785,-132.914631764284,
-131.915273630718,-130.915915497152,-129.916557363586,-129.362421635296),
 .UNSPECIFIED.);
#811=B_SPLINE_CURVE_WITH_KNOTS('',3,(#38956,#38957,#38958,#38959,#38960,
#38961,#38962,#38963,#38964,#38965,#38966,#38967,#38968,#38969,#38970,#38971,
#38972,#38973,#38974,#38975,#38976,#38977),.UNSPECIFIED.,.F.,.F.,(4,3,3,
3,3,3,3,4),(126.106766814146,126.918482962888,127.917841096454,128.91719923002,
129.916557363586,130.915915497152,131.915273630718,132.389952121326),
 .UNSPECIFIED.);
#812=B_SPLINE_CURVE_WITH_KNOTS('',3,(#38982,#38983,#38984,#38985,#38986,
#38987,#38988,#38989,#38990,#38991,#38992,#38993,#38994,#38995,#38996,#38997,
#38998,#38999,#39000,#39001,#39002,#39003,#39004,#39005,#39006),
 .UNSPECIFIED.,.F.,.F.,(4,3,3,3,3,3,3,3,4),(-141.928792249655,-141.908854966379,
-140.909496832813,-139.910138699247,-138.91078056568,-137.911422432114,
-136.912064298548,-135.912706164982,-135.645606942476),.UNSPECIFIED.);
#813=B_SPLINE_CURVE_WITH_KNOTS('',3,(#39007,#39008,#39009,#39010,#39011,
#39012,#39013,#39014,#39015,#39016,#39017,#39018,#39019,#39020,#39021,#39022,
#39023,#39024,#39025,#39026,#39027,#39028),.UNSPECIFIED.,.F.,.F.,(4,3,3,
3,3,3,3,4),(132.389952121326,132.914631764284,133.91398989785,134.913348031416,
135.912706164982,136.912064298549,137.911422432115,138.673137428505),
 .UNSPECIFIED.);
#814=B_SPLINE_CURVE_WITH_KNOTS('',3,(#39033,#39034,#39035,#39036,#39037,
#39038,#39039,#39040,#39041,#39042,#39043,#39044,#39045,#39046,#39047,#39048,
#39049,#39050,#39051,#39052,#39053,#39054),.UNSPECIFIED.,.F.,.F.,(4,3,3,
3,3,3,3,4),(-148.211977556835,-147.905003767775,-146.905645634209,-145.906287500643,
-144.906929367077,-143.907571233511,-142.908213099945,-141.928792249655),
 .UNSPECIFIED.);
#815=B_SPLINE_CURVE_WITH_KNOTS('',3,(#39055,#39056,#39057,#39058,#39059,
#39060,#39061,#39062,#39063,#39064,#39065,#39066,#39067,#39068,#39069,#39070,
#39071,#39072,#39073,#39074,#39075,#39076,#39077,#39078,#39079),
 .UNSPECIFIED.,.F.,.F.,(4,3,3,3,3,3,3,3,4),(138.673137428505,138.910780565681,
139.910138699247,140.909496832813,141.908854966379,142.908213099945,143.907571233511,
144.906929367077,144.956322735685),.UNSPECIFIED.);
#816=B_SPLINE_CURVE_WITH_KNOTS('',3,(#39084,#39085,#39086,#39087,#39088,
#39089,#39090,#39091,#39092,#39093,#39094,#39095,#39096,#39097,#39098,#39099,
#39100,#39101,#39102,#39103,#39104,#39105),.UNSPECIFIED.,.F.,.F.,(4,3,3,
3,3,3,3,4),(-154.495162864015,-153.901152569171,-152.901794435605,-151.902436302039,
-150.903078168473,-149.903720034907,-148.904361901341,-148.211977556835),
 .UNSPECIFIED.);
#817=B_SPLINE_CURVE_WITH_KNOTS('',3,(#39106,#39107,#39108,#39109,#39110,
#39111,#39112,#39113,#39114,#39115,#39116,#39117,#39118,#39119,#39120,#39121,
#39122,#39123,#39124,#39125,#39126,#39127),.UNSPECIFIED.,.F.,.F.,(4,3,3,
3,3,3,3,4),(144.956322735685,145.906287500643,146.905645634209,147.905003767775,
148.904361901341,149.903720034907,150.903078168473,151.239508042865),
 .UNSPECIFIED.);
#818=B_SPLINE_CURVE_WITH_KNOTS('',3,(#39132,#39133,#39134,#39135,#39136,
#39137,#39138,#39139,#39140,#39141,#39142,#39143,#39144,#39145,#39146,#39147,
#39148,#39149,#39150,#39151,#39152,#39153),.UNSPECIFIED.,.F.,.F.,(4,3,3,
3,3,3,3,4),(-160.778348171194,-159.897301370567,-158.897943237001,-157.898585103435,
-156.899226969869,-155.899868836303,-154.900510702737,-154.495162864015),
 .UNSPECIFIED.);
#819=B_SPLINE_CURVE_WITH_KNOTS('',3,(#39154,#39155,#39156,#39157,#39158,
#39159,#39160,#39161,#39162,#39163,#39164,#39165,#39166,#39167,#39168,#39169,
#39170,#39171,#39172,#39173,#39174,#39175),.UNSPECIFIED.,.F.,.F.,(4,3,3,
3,3,3,3,4),(151.239508042865,151.902436302039,152.901794435605,153.901152569171,
154.900510702737,155.899868836303,156.899226969869,157.522693350044),
 .UNSPECIFIED.);
#820=B_SPLINE_CURVE_WITH_KNOTS('',3,(#39180,#39181,#39182,#39183,#39184,
#39185,#39186,#39187,#39188,#39189,#39190,#39191,#39192,#39193,#39194,#39195,
#39196,#39197,#39198,#39199,#39200,#39201,#39202,#39203,#39204),
 .UNSPECIFIED.,.F.,.F.,(4,3,3,3,3,3,3,3,4),(-167.061533478374,-166.89280830553,
-165.893450171964,-164.894092038398,-163.894733904832,-162.895375771266,
-161.8960176377,-160.896659504134,-160.778348171194),.UNSPECIFIED.);
#821=B_SPLINE_CURVE_WITH_KNOTS('',3,(#39205,#39206,#39207,#39208,#39209,
#39210,#39211,#39212,#39213,#39214,#39215,#39216,#39217,#39218,#39219,#39220,
#39221,#39222,#39223,#39224,#39225,#39226),.UNSPECIFIED.,.F.,.F.,(4,3,3,
3,3,3,3,4),(157.522693350044,157.898585103435,158.897943237002,159.897301370568,
160.896659504134,161.8960176377,162.895375771266,163.805878657224),
 .UNSPECIFIED.);
#822=B_SPLINE_CURVE_WITH_KNOTS('',3,(#39231,#39232,#39233,#39234,#39235,
#39236,#39237,#39238,#39239,#39240,#39241,#39242,#39243,#39244,#39245,#39246,
#39247,#39248,#39249,#39250,#39251,#39252),.UNSPECIFIED.,.F.,.F.,(4,3,3,
3,3,3,3,4),(-173.344718785553,-172.888957106926,-171.88959897336,-170.890240839794,
-169.890882706228,-168.891524572662,-167.892166439096,-167.061533478374),
 .UNSPECIFIED.);
#823=B_SPLINE_CURVE_WITH_KNOTS('',3,(#39253,#39254,#39255,#39256,#39257,
#39258,#39259,#39260,#39261,#39262,#39263,#39264,#39265,#39266,#39267,#39268,
#39269,#39270,#39271,#39272,#39273,#39274,#39275,#39276,#39277),
 .UNSPECIFIED.,.F.,.F.,(4,3,3,3,3,3,3,3,4),(163.805878657224,163.894733904832,
164.894092038398,165.893450171964,166.89280830553,167.892166439096,168.891524572662,
169.890882706228,170.089063964403),.UNSPECIFIED.);
#824=B_SPLINE_CURVE_WITH_KNOTS('',3,(#39282,#39283,#39284,#39285,#39286,
#39287,#39288,#39289,#39290,#39291,#39292,#39293,#39294,#39295,#39296,#39297,
#39298,#39299,#39300,#39301,#39302,#39303),.UNSPECIFIED.,.F.,.F.,(4,3,3,
3,3,3,3,4),(-179.627904092733,-178.885105908322,-177.885747774756,-176.88638964119,
-175.887031507624,-174.887673374058,-173.888315240492,-173.344718785553),
 .UNSPECIFIED.);
#825=B_SPLINE_CURVE_WITH_KNOTS('',3,(#39304,#39305,#39306,#39307,#39308,
#39309,#39310,#39311,#39312,#39313,#39314,#39315,#39316,#39317,#39318,#39319,
#39320,#39321,#39322,#39323,#39324,#39325),.UNSPECIFIED.,.F.,.F.,(4,3,3,
3,3,3,3,4),(170.089063964403,170.890240839794,171.88959897336,172.888957106926,
173.888315240492,174.887673374058,175.887031507624,176.372249271583),
 .UNSPECIFIED.);
#826=B_SPLINE_CURVE_WITH_KNOTS('',3,(#39330,#39331,#39332,#39333,#39334,
#39335,#39336,#39337,#39338,#39339,#39340,#39341,#39342,#39343,#39344,#39345,
#39346,#39347,#39348,#39349,#39350,#39351,#39352,#39353,#39354),
 .UNSPECIFIED.,.F.,.F.,(4,3,3,3,3,3,3,3,4),(-185.911089399912,-185.880612843285,
-184.881254709719,-183.881896576153,-182.882538442587,-181.88318030902,
-180.883822175454,-179.884464041888,-179.627904092733),.UNSPECIFIED.);
#827=B_SPLINE_CURVE_WITH_KNOTS('',3,(#39355,#39356,#39357,#39358,#39359,
#39360,#39361,#39362,#39363,#39364,#39365,#39366,#39367,#39368,#39369,#39370,
#39371,#39372,#39373,#39374,#39375,#39376),.UNSPECIFIED.,.F.,.F.,(4,3,3,
3,3,3,3,4),(176.372249271583,176.88638964119,177.885747774756,178.885105908322,
179.884464041889,180.883822175455,181.883180309021,182.655434578762),
 .UNSPECIFIED.);
#828=B_SPLINE_CURVE_WITH_KNOTS('',3,(#39381,#39382,#39383,#39384,#39385,
#39386,#39387,#39388,#39389,#39390,#39391,#39392,#39393,#39394,#39395,#39396,
#39397,#39398,#39399,#39400,#39401,#39402),.UNSPECIFIED.,.F.,.F.,(4,3,3,
3,3,3,3,4),(-192.194274707092,-191.876761644681,-190.877403511115,-189.878045377549,
-188.878687243983,-187.879329110417,-186.879970976851,-185.911089399912),
 .UNSPECIFIED.);
#829=B_SPLINE_CURVE_WITH_KNOTS('',3,(#39403,#39404,#39405,#39406,#39407,
#39408,#39409,#39410,#39411,#39412,#39413,#39414,#39415,#39416,#39417,#39418,
#39419,#39420,#39421,#39422,#39423,#39424,#39425,#39426,#39427),
 .UNSPECIFIED.,.F.,.F.,(4,3,3,3,3,3,3,3,4),(182.655434578762,182.882538442587,
183.881896576153,184.881254709719,185.880612843285,186.879970976851,187.879329110417,
188.878687243983,188.938619885942),.UNSPECIFIED.);
#830=B_SPLINE_CURVE_WITH_KNOTS('',3,(#39432,#39433,#39434,#39435,#39436,
#39437,#39438,#39439,#39440,#39441,#39442,#39443,#39444,#39445,#39446,#39447,
#39448,#39449,#39450,#39451,#39452,#39453),.UNSPECIFIED.,.F.,.F.,(4,3,3,
3,3,3,3,4),(-198.477460014271,-197.872910446077,-196.873552312511,-195.874194178945,
-194.874836045379,-193.875477911813,-192.876119778247,-192.194274707092),
 .UNSPECIFIED.);
#831=B_SPLINE_CURVE_WITH_KNOTS('',3,(#39454,#39455,#39456,#39457,#39458,
#39459,#39460,#39461,#39462,#39463,#39464,#39465,#39466,#39467,#39468,#39469,
#39470,#39471,#39472,#39473,#39474,#39475),.UNSPECIFIED.,.F.,.F.,(4,3,3,
3,3,3,3,4),(188.938619885942,189.878045377549,190.877403511115,191.876761644681,
192.876119778247,193.875477911813,194.874836045379,195.221805193122),
 .UNSPECIFIED.);
#832=B_SPLINE_CURVE_WITH_KNOTS('',3,(#39480,#39481,#39482,#39483,#39484,
#39485,#39486,#39487,#39488,#39489,#39490,#39491,#39492,#39493,#39494,#39495,
#39496,#39497,#39498,#39499,#39500,#39501),.UNSPECIFIED.,.F.,.F.,(4,3,3,
3,3,3,3,4),(-204.760645321451,-203.869059247473,-202.869701113907,-201.870342980341,
-200.870984846775,-199.871626713209,-198.872268579643,-198.477460014271),
 .UNSPECIFIED.);
#833=B_SPLINE_CURVE_WITH_KNOTS('',3,(#39502,#39503,#39504,#39505,#39506,
#39507,#39508,#39509,#39510,#39511,#39512,#39513,#39514,#39515,#39516,#39517,
#39518,#39519,#39520,#39521,#39522,#39523),.UNSPECIFIED.,.F.,.F.,(4,3,3,
3,3,3,3,4),(195.221805193122,195.874194178945,196.873552312511,197.872910446077,
198.872268579643,199.871626713209,200.870984846776,201.504990500301),
 .UNSPECIFIED.);
#834=B_SPLINE_CURVE_WITH_KNOTS('',3,(#39528,#39529,#39530,#39531,#39532,
#39533,#39534,#39535,#39536,#39537,#39538,#39539,#39540,#39541,#39542,#39543,
#39544,#39545,#39546,#39547,#39548,#39549,#39550,#39551,#39552),
 .UNSPECIFIED.,.F.,.F.,(4,3,3,3,3,3,3,3,4),(-211.043830628631,-210.864566182436,
-209.86520804887,-208.865849915304,-207.866491781738,-206.867133648172,
-205.867775514606,-204.86841738104,-204.760645321451),.UNSPECIFIED.);
#835=B_SPLINE_CURVE_WITH_KNOTS('',3,(#39553,#39554,#39555,#39556,#39557,
#39558,#39559,#39560,#39561,#39562,#39563,#39564,#39565,#39566,#39567,#39568,
#39569,#39570,#39571,#39572,#39573,#39574),.UNSPECIFIED.,.F.,.F.,(4,3,3,
3,3,3,3,4),(201.504990500301,201.870342980342,202.869701113908,203.869059247474,
204.86841738104,205.867775514606,206.867133648172,207.788175807481),
 .UNSPECIFIED.);
#836=B_SPLINE_CURVE_WITH_KNOTS('',3,(#39579,#39580,#39581,#39582,#39583,
#39584,#39585,#39586,#39587,#39588,#39589,#39590,#39591,#39592,#39593,#39594,
#39595,#39596,#39597,#39598,#39599,#39600),.UNSPECIFIED.,.F.,.F.,(4,3,3,
3,3,3,3,4),(-217.32701593581,-216.860714983832,-215.861356850266,-214.8619987167,
-213.862640583134,-212.863282449568,-211.863924316002,-211.043830628631),
 .UNSPECIFIED.);
#837=B_SPLINE_CURVE_WITH_KNOTS('',3,(#39601,#39602,#39603,#39604,#39605,
#39606,#39607,#39608,#39609,#39610,#39611,#39612,#39613,#39614,#39615,#39616,
#39617,#39618,#39619,#39620,#39621,#39622,#39623,#39624,#39625),
 .UNSPECIFIED.,.F.,.F.,(4,3,3,3,3,3,3,3,4),(207.788175807481,207.866491781738,
208.865849915304,209.86520804887,210.864566182436,211.863924316002,212.863282449568,
213.862640583134,214.07136111466),.UNSPECIFIED.);
#838=B_SPLINE_CURVE_WITH_KNOTS('',3,(#39630,#39631,#39632,#39633,#39634,
#39635,#39636,#39637,#39638,#39639,#39640,#39641,#39642,#39643,#39644,#39645,
#39646,#39647,#39648,#39649,#39650,#39651),.UNSPECIFIED.,.F.,.F.,(4,3,3,
3,3,3,3,4),(-223.61020124299,-222.856863785228,-221.857505651662,-220.858147518096,
-219.85878938453,-218.859431250964,-217.860073117398,-217.32701593581),
 .UNSPECIFIED.);
#839=B_SPLINE_CURVE_WITH_KNOTS('',3,(#39652,#39653,#39654,#39655,#39656,
#39657,#39658,#39659,#39660,#39661,#39662,#39663,#39664,#39665,#39666,#39667,
#39668,#39669,#39670,#39671,#39672,#39673),.UNSPECIFIED.,.F.,.F.,(4,3,3,
3,3,3,3,4),(214.07136111466,214.8619987167,215.861356850266,216.860714983832,
217.860073117398,218.859431250964,219.85878938453,220.35454642184),
 .UNSPECIFIED.);
#840=B_SPLINE_CURVE_WITH_KNOTS('',3,(#39678,#39679,#39680,#39681,#39682,
#39683,#39684,#39685,#39686,#39687,#39688,#39689,#39690,#39691,#39692,#39693,
#39694,#39695,#39696,#39697,#39698,#39699,#39700,#39701,#39702),
 .UNSPECIFIED.,.F.,.F.,(4,3,3,3,3,3,3,3,4),(-229.893386550169,-229.852370720191,
-228.853012586625,-227.853654453059,-226.854296319493,-225.854938185927,
-224.85558005236,-223.856221918794,-223.61020124299),.UNSPECIFIED.);
#841=B_SPLINE_CURVE_WITH_KNOTS('',3,(#39703,#39704,#39705,#39706,#39707,
#39708,#39709,#39710,#39711,#39712,#39713,#39714,#39715,#39716,#39717,#39718,
#39719,#39720,#39721,#39722,#39723,#39724),.UNSPECIFIED.,.F.,.F.,(4,3,3,
3,3,3,3,4),(220.35454642184,220.858147518096,221.857505651663,222.856863785229,
223.856221918795,224.855580052361,225.854938185927,226.637731729019),
 .UNSPECIFIED.);
#842=B_SPLINE_CURVE_WITH_KNOTS('',3,(#39729,#39730,#39731,#39732,#39733,
#39734,#39735,#39736,#39737,#39738,#39739,#39740,#39741,#39742,#39743,#39744,
#39745,#39746,#39747,#39748,#39749,#39750),.UNSPECIFIED.,.F.,.F.,(4,3,3,
3,3,3,3,4),(-236.176571857349,-235.848519521587,-234.849161388021,-233.849803254455,
-232.850445120889,-231.851086987323,-230.851728853757,-229.893386550169),
 .UNSPECIFIED.);
#843=B_SPLINE_CURVE_WITH_KNOTS('',3,(#39751,#39752,#39753,#39754,#39755,
#39756,#39757,#39758,#39759,#39760,#39761,#39762,#39763,#39764,#39765,#39766,
#39767,#39768,#39769,#39770,#39771,#39772,#39773,#39774,#39775),
 .UNSPECIFIED.,.F.,.F.,(4,3,3,3,3,3,3,3,4),(226.637731729019,226.854296319493,
227.853654453059,228.853012586625,229.852370720191,230.851728853757,231.851086987323,
232.850445120889,232.920917036199),.UNSPECIFIED.);
#844=B_SPLINE_CURVE_WITH_KNOTS('',3,(#39780,#39781,#39782,#39783,#39784,
#39785,#39786,#39787,#39788,#39789,#39790,#39791,#39792,#39793,#39794,#39795,
#39796,#39797,#39798,#39799,#39800,#39801),.UNSPECIFIED.,.F.,.F.,(4,3,3,
3,3,3,3,4),(-242.459757164528,-241.844668322983,-240.845310189417,-239.845952055851,
-238.846593922285,-237.847235788719,-236.847877655153,-236.176571857349),
 .UNSPECIFIED.);
#845=B_SPLINE_CURVE_WITH_KNOTS('',3,(#39802,#39803,#39804,#39805,#39806,
#39807,#39808,#39809,#39810,#39811,#39812,#39813,#39814,#39815,#39816,#39817,
#39818,#39819,#39820,#39821,#39822,#39823),.UNSPECIFIED.,.F.,.F.,(4,3,3,
3,3,3,3,4),(232.920917036199,233.849803254455,234.849161388021,235.848519521587,
236.847877655153,237.847235788719,238.846593922285,239.204102343378),
 .UNSPECIFIED.);
#846=B_SPLINE_CURVE_WITH_KNOTS('',3,(#39828,#39829,#39830,#39831,#39832,
#39833,#39834,#39835,#39836,#39837,#39838,#39839,#39840,#39841,#39842,#39843,
#39844,#39845,#39846,#39847,#39848,#39849),.UNSPECIFIED.,.F.,.F.,(4,3,3,
3,3,3,3,4),(-248.742942471708,-247.84081712438,-246.841458990814,-245.842100857247,
-244.842742723681,-243.843384590115,-242.844026456549,-242.459757164528),
 .UNSPECIFIED.);
#847=B_SPLINE_CURVE_WITH_KNOTS('',3,(#39850,#39851,#39852,#39853,#39854,
#39855,#39856,#39857,#39858,#39859,#39860,#39861,#39862,#39863,#39864,#39865,
#39866,#39867,#39868,#39869,#39870,#39871),.UNSPECIFIED.,.F.,.F.,(4,3,3,
3,3,3,3,4),(239.204102343378,239.845952055851,240.845310189417,241.844668322983,
242.84402645655,243.843384590116,244.842742723682,245.487287650558),
 .UNSPECIFIED.);
#848=B_SPLINE_CURVE_WITH_KNOTS('',3,(#39876,#39877,#39878,#39879,#39880,
#39881,#39882,#39883,#39884,#39885,#39886,#39887,#39888,#39889,#39890,#39891,
#39892,#39893,#39894,#39895,#39896,#39897,#39898,#39899,#39900),
 .UNSPECIFIED.,.F.,.F.,(4,3,3,3,3,3,3,3,4),(-255.026127778888,-254.836324059342,
-253.836965925776,-252.83760779221,-251.838249658644,-250.838891525078,
-249.839533391512,-248.840175257946,-248.742942471708),.UNSPECIFIED.);
#849=B_SPLINE_CURVE_WITH_KNOTS('',3,(#39901,#39902,#39903,#39904,#39905,
#39906,#39907,#39908,#39909,#39910,#39911,#39912,#39913,#39914,#39915,#39916,
#39917,#39918,#39919,#39920,#39921,#39922),.UNSPECIFIED.,.F.,.F.,(4,3,3,
3,3,3,3,4),(245.487287650558,245.842100857248,246.841458990814,247.84081712438,
248.840175257946,249.839533391512,250.838891525078,251.770472957738),
 .UNSPECIFIED.);
#850=B_SPLINE_CURVE_WITH_KNOTS('',3,(#39927,#39928,#39929,#39930,#39931,
#39932,#39933,#39934,#39935,#39936,#39937,#39938,#39939,#39940,#39941,#39942,
#39943,#39944,#39945,#39946,#39947,#39948),.UNSPECIFIED.,.F.,.F.,(4,3,3,
3,3,3,3,4),(-261.309313086067,-260.832472860738,-259.833114727172,-258.833756593606,
-257.83439846004,-256.835040326474,-255.835682192908,-255.026127778888),
 .UNSPECIFIED.);
#851=B_SPLINE_CURVE_WITH_KNOTS('',3,(#39949,#39950,#39951,#39952,#39953,
#39954,#39955,#39956,#39957,#39958,#39959,#39960,#39961,#39962,#39963,#39964,
#39965,#39966,#39967,#39968,#39969,#39970,#39971,#39972,#39973),
 .UNSPECIFIED.,.F.,.F.,(4,3,3,3,3,3,3,3,4),(251.770472957738,251.838249658644,
252.83760779221,253.836965925776,254.836324059342,255.835682192908,256.835040326474,
257.83439846004,258.053658264917),.UNSPECIFIED.);
#852=B_SPLINE_CURVE_WITH_KNOTS('',3,(#39978,#39979,#39980,#39981,#39982,
#39983,#39984,#39985,#39986,#39987,#39988,#39989,#39990,#39991,#39992,#39993,
#39994,#39995,#39996,#39997,#39998,#39999),.UNSPECIFIED.,.F.,.F.,(4,3,3,
3,3,3,3,4),(-267.592498393247,-266.828621662134,-265.829263528568,-264.829905395002,
-263.830547261436,-262.83118912787,-261.831830994304,-261.309313086067),
 .UNSPECIFIED.);
#853=B_SPLINE_CURVE_WITH_KNOTS('',3,(#40000,#40001,#40002,#40003,#40004,
#40005,#40006,#40007,#40008,#40009,#40010,#40011,#40012,#40013,#40014,#40015,
#40016,#40017,#40018,#40019,#40020,#40021),.UNSPECIFIED.,.F.,.F.,(4,3,3,
3,3,3,3,4),(258.053658264917,258.833756593606,259.833114727172,260.832472860738,
261.831830994304,262.83118912787,263.830547261436,264.336843572097),
 .UNSPECIFIED.);
#854=B_SPLINE_CURVE_WITH_KNOTS('',3,(#40026,#40027,#40028,#40029,#40030,
#40031,#40032,#40033,#40034,#40035,#40036,#40037,#40038,#40039,#40040,#40041,
#40042,#40043,#40044,#40045,#40046,#40047,#40048,#40049,#40050),
 .UNSPECIFIED.,.F.,.F.,(4,3,3,3,3,3,3,3,4),(-273.875683700426,-273.824128597097,
-272.824770463531,-271.825412329965,-270.826054196399,-269.826696062833,
-268.827337929266,-267.8279797957,-267.592498393247),.UNSPECIFIED.);
#855=B_SPLINE_CURVE_WITH_KNOTS('',3,(#40051,#40052,#40053,#40054,#40055,
#40056,#40057,#40058,#40059,#40060,#40061,#40062,#40063,#40064,#40065,#40066,
#40067,#40068,#40069,#40070,#40071,#40072),.UNSPECIFIED.,.F.,.F.,(4,3,3,
3,3,3,3,4),(264.336843572097,264.829905395003,265.829263528569,266.828621662135,
267.827979795701,268.827337929267,269.826696062833,270.620028879276),
 .UNSPECIFIED.);
#856=B_SPLINE_CURVE_WITH_KNOTS('',3,(#40077,#40078,#40079,#40080,#40081,
#40082,#40083,#40084,#40085,#40086,#40087,#40088,#40089,#40090,#40091,#40092,
#40093,#40094,#40095,#40096,#40097,#40098),.UNSPECIFIED.,.F.,.F.,(4,3,3,
3,3,3,3,4),(-280.158869007606,-279.820277398493,-278.820919264927,-277.821561131361,
-276.822202997795,-275.822844864229,-274.823486730663,-273.875683700426),
 .UNSPECIFIED.);
#857=B_SPLINE_CURVE_WITH_KNOTS('',3,(#40099,#40100,#40101,#40102,#40103,
#40104,#40105,#40106,#40107,#40108,#40109,#40110,#40111,#40112,#40113,#40114,
#40115,#40116,#40117,#40118,#40119,#40120,#40121,#40122,#40123),
 .UNSPECIFIED.,.F.,.F.,(4,3,3,3,3,3,3,3,4),(270.620028879276,270.826054196399,
271.825412329965,272.824770463531,273.824128597097,274.823486730663,275.822844864229,
276.822202997795,276.903214186456),.UNSPECIFIED.);
#858=B_SPLINE_CURVE_WITH_KNOTS('',3,(#40128,#40129,#40130,#40131,#40132,
#40133,#40134,#40135,#40136,#40137,#40138,#40139,#40140,#40141,#40142,#40143,
#40144,#40145,#40146,#40147,#40148,#40149),.UNSPECIFIED.,.F.,.F.,(4,3,3,
3,3,3,3,4),(-286.442054314785,-285.816426199889,-284.817068066323,-283.817709932757,
-282.818351799191,-281.818993665625,-280.819635532059,-280.158869007606),
 .UNSPECIFIED.);
#859=B_SPLINE_CURVE_WITH_KNOTS('',3,(#40150,#40151,#40152,#40153,#40154,
#40155,#40156,#40157,#40158,#40159,#40160,#40161,#40162,#40163,#40164,#40165,
#40166,#40167,#40168,#40169,#40170,#40171),.UNSPECIFIED.,.F.,.F.,(4,3,3,
3,3,3,3,4),(276.903214186456,277.821561131361,278.820919264927,279.820277398493,
280.819635532059,281.818993665625,282.818351799191,283.186399493635),
 .UNSPECIFIED.);
#860=B_SPLINE_CURVE_WITH_KNOTS('',3,(#40176,#40177,#40178,#40179,#40180,
#40181,#40182,#40183,#40184,#40185,#40186,#40187,#40188,#40189,#40190,#40191,
#40192,#40193,#40194,#40195,#40196,#40197),.UNSPECIFIED.,.F.,.F.,(4,3,3,
3,3,3,3,4),(-292.725239621965,-291.812575001286,-290.81321686772,-289.813858734153,
-288.814500600587,-287.815142467021,-286.815784333455,-286.442054314785),
 .UNSPECIFIED.);
#861=B_SPLINE_CURVE_WITH_KNOTS('',3,(#40198,#40199,#40200,#40201,#40202,
#40203,#40204,#40205,#40206,#40207,#40208,#40209,#40210,#40211,#40212,#40213,
#40214,#40215,#40216,#40217,#40218,#40219),.UNSPECIFIED.,.F.,.F.,(4,3,3,
3,3,3,3,4),(283.186399493635,283.817709932757,284.817068066323,285.81642619989,
286.815784333456,287.815142467022,288.814500600588,289.469584800815),
 .UNSPECIFIED.);
#862=B_SPLINE_CURVE_WITH_KNOTS('',3,(#40224,#40225,#40226,#40227,#40228,
#40229,#40230,#40231,#40232,#40233,#40234,#40235,#40236,#40237,#40238,#40239,
#40240,#40241,#40242,#40243,#40244,#40245,#40246,#40247,#40248),
 .UNSPECIFIED.,.F.,.F.,(4,3,3,3,3,3,3,3,4),(-299.008424929145,-298.808081936248,
-297.808723802682,-296.809365669116,-295.81000753555,-294.810649401984,
-293.811291268418,-292.811933134852,-292.725239621965),.UNSPECIFIED.);
#863=B_SPLINE_CURVE_WITH_KNOTS('',3,(#40249,#40250,#40251,#40252,#40253,
#40254,#40255,#40256,#40257,#40258,#40259,#40260,#40261,#40262,#40263,#40264,
#40265,#40266,#40267,#40268,#40269,#40270),.UNSPECIFIED.,.F.,.F.,(4,3,3,
3,3,3,3,4),(289.469584800815,289.813858734154,290.81321686772,291.812575001286,
292.811933134852,293.811291268418,294.810649401984,295.752770107995),
 .UNSPECIFIED.);
#864=B_SPLINE_CURVE_WITH_KNOTS('',3,(#40275,#40276,#40277,#40278,#40279,
#40280,#40281,#40282,#40283,#40284,#40285,#40286,#40287,#40288,#40289,#40290,
#40291,#40292,#40293,#40294,#40295,#40296),.UNSPECIFIED.,.F.,.F.,(4,3,3,
3,3,3,3,4),(-305.291610236324,-304.804230737644,-303.804872604078,-302.805514470512,
-301.806156336946,-300.80679820338,-299.807440069814,-299.008424929145),
 .UNSPECIFIED.);
#865=B_SPLINE_CURVE_WITH_KNOTS('',3,(#40297,#40298,#40299,#40300,#40301,
#40302,#40303,#40304,#40305,#40306,#40307,#40308,#40309,#40310,#40311,#40312,
#40313,#40314,#40315,#40316,#40317,#40318,#40319,#40320,#40321),
 .UNSPECIFIED.,.F.,.F.,(4,3,3,3,3,3,3,3,4),(295.752770107995,295.81000753555,
296.809365669116,297.808723802682,298.808081936248,299.807440069814,300.80679820338,
301.806156336946,302.035955415174),.UNSPECIFIED.);
#866=B_SPLINE_CURVE_WITH_KNOTS('',3,(#40326,#40327,#40328,#40329,#40330,
#40331,#40332,#40333,#40334,#40335,#40336,#40337,#40338,#40339,#40340,#40341,
#40342,#40343,#40344,#40345,#40346,#40347),.UNSPECIFIED.,.F.,.F.,(4,3,3,
3,3,3,3,4),(-311.574795543504,-310.80037953904,-309.801021405475,-308.801663271908,
-307.802305138342,-306.802947004776,-305.80358887121,-305.291610236324),
 .UNSPECIFIED.);
#867=B_SPLINE_CURVE_WITH_KNOTS('',3,(#40348,#40349,#40350,#40351,#40352,
#40353,#40354,#40355,#40356,#40357,#40358,#40359,#40360,#40361,#40362,#40363,
#40364,#40365,#40366,#40367,#40368,#40369),.UNSPECIFIED.,.F.,.F.,(4,3,3,
3,3,3,3,4),(302.035955415174,302.805514470512,303.804872604078,304.804230737644,
305.80358887121,306.802947004777,307.802305138343,308.319140722354),
 .UNSPECIFIED.);
#868=B_SPLINE_CURVE_WITH_KNOTS('',3,(#40374,#40375,#40376,#40377,#40378,
#40379,#40380,#40381,#40382,#40383,#40384,#40385,#40386,#40387,#40388,#40389,
#40390,#40391,#40392,#40393,#40394,#40395,#40396,#40397,#40398),
 .UNSPECIFIED.,.F.,.F.,(4,3,3,3,3,3,3,3,4),(-317.857980850683,-317.795886474003,
-316.796528340437,-315.797170206871,-314.797812073305,-313.798453939739,
-312.799095806173,-311.799737672607,-311.574795543504),.UNSPECIFIED.);
#869=B_SPLINE_CURVE_WITH_KNOTS('',3,(#40399,#40400,#40401,#40402,#40403,
#40404,#40405,#40406,#40407,#40408,#40409,#40410,#40411,#40412,#40413,#40414,
#40415,#40416,#40417,#40418,#40419,#40420),.UNSPECIFIED.,.F.,.F.,(4,3,3,
3,3,3,3,4),(308.319140722354,308.801663271909,309.801021405475,310.800379539041,
311.799737672607,312.799095806173,313.798453939739,314.602326029533),
 .UNSPECIFIED.);
#870=B_SPLINE_CURVE_WITH_KNOTS('',3,(#40425,#40426,#40427,#40428,#40429,
#40430,#40431,#40432,#40433,#40434,#40435,#40436,#40437,#40438,#40439,#40440,
#40441,#40442,#40443,#40444,#40445,#40446),.UNSPECIFIED.,.F.,.F.,(4,3,3,
3,3,3,3,4),(-324.141166157863,-323.792035275399,-322.792677141833,-321.793319008267,
-320.793960874701,-319.794602741135,-318.795244607569,-317.857980850683),
 .UNSPECIFIED.);
#871=B_SPLINE_CURVE_WITH_KNOTS('',3,(#40447,#40448,#40449,#40450,#40451,
#40452,#40453,#40454,#40455,#40456,#40457,#40458,#40459,#40460,#40461,#40462,
#40463,#40464,#40465,#40466,#40467,#40468,#40469,#40470,#40471),
 .UNSPECIFIED.,.F.,.F.,(4,3,3,3,3,3,3,3,4),(314.602326029533,314.797812073305,
315.797170206871,316.796528340437,317.795886474003,318.795244607569,319.794602741135,
320.793960874701,320.885511336713),.UNSPECIFIED.);
#872=B_SPLINE_CURVE_WITH_KNOTS('',3,(#40476,#40477,#40478,#40479,#40480,
#40481,#40482,#40483,#40484,#40485,#40486,#40487,#40488,#40489,#40490,#40491,
#40492,#40493,#40494,#40495,#40496,#40497),.UNSPECIFIED.,.F.,.F.,(4,3,3,
3,3,3,3,4),(-330.424351465042,-329.788184076795,-328.788825943229,-327.789467809663,
-326.790109676097,-325.790751542531,-324.791393408965,-324.141166157863),
 .UNSPECIFIED.);
#873=B_SPLINE_CURVE_WITH_KNOTS('',3,(#40498,#40499,#40500,#40501,#40502,
#40503,#40504,#40505,#40506,#40507,#40508,#40509,#40510,#40511,#40512,#40513,
#40514,#40515,#40516,#40517,#40518,#40519),.UNSPECIFIED.,.F.,.F.,(4,3,3,
3,3,3,3,4),(320.885511336713,321.793319008267,322.792677141833,323.792035275399,
324.791393408965,325.790751542531,326.790109676097,327.168696643892),
 .UNSPECIFIED.);
#874=B_SPLINE_CURVE_WITH_KNOTS('',3,(#40524,#40525,#40526,#40527,#40528,
#40529,#40530,#40531,#40532,#40533,#40534,#40535,#40536,#40537,#40538,#40539,
#40540,#40541,#40542,#40543,#40544,#40545),.UNSPECIFIED.,.F.,.F.,(4,3,3,
3,3,3,3,4),(-336.707536772222,-335.784332878192,-334.784974744626,-333.78561661106,
-332.786258477494,-331.786900343927,-330.787542210361,-330.424351465042),
 .UNSPECIFIED.);
#875=B_SPLINE_CURVE_WITH_KNOTS('',3,(#40546,#40547,#40548,#40549,#40550,
#40551,#40552,#40553,#40554,#40555,#40556,#40557,#40558,#40559,#40560,#40561,
#40562,#40563,#40564,#40565,#40566,#40567),.UNSPECIFIED.,.F.,.F.,(4,3,3,
3,3,3,3,4),(327.168696643892,327.789467809663,328.78882594323,329.788184076796,
330.787542210362,331.786900343928,332.786258477494,333.451881951072),
 .UNSPECIFIED.);
#876=B_SPLINE_CURVE_WITH_KNOTS('',3,(#40572,#40573,#40574,#40575,#40576,
#40577,#40578,#40579,#40580,#40581,#40582,#40583,#40584,#40585,#40586,#40587,
#40588,#40589,#40590,#40591,#40592,#40593,#40594,#40595,#40596),
 .UNSPECIFIED.,.F.,.F.,(4,3,3,3,3,3,3,3,4),(-342.990722079402,-342.779839813154,
-341.780481679588,-340.781123546022,-339.781765412456,-338.78240727889,
-337.783049145324,-336.783691011758,-336.707536772222),.UNSPECIFIED.);
#877=B_SPLINE_CURVE_WITH_KNOTS('',3,(#40597,#40598,#40599,#40600,#40601,
#40602,#40603,#40604,#40605,#40606,#40607,#40608,#40609,#40610,#40611,#40612,
#40613,#40614,#40615,#40616,#40617,#40618),.UNSPECIFIED.,.F.,.F.,(4,3,3,
3,3,3,3,4),(333.451881951072,333.78561661106,334.784974744626,335.784332878192,
336.783691011758,337.783049145324,338.78240727889,339.735067258252),
 .UNSPECIFIED.);
#878=B_SPLINE_CURVE_WITH_KNOTS('',3,(#40623,#40624,#40625,#40626,#40627,
#40628,#40629,#40630,#40631,#40632,#40633,#40634,#40635,#40636,#40637,#40638,
#40639,#40640,#40641,#40642,#40643,#40644,#40645,#40646,#40647,#40648,#40649,
#40650,#40651,#40652,#40653,#40654,#40655,#40656),.UNSPECIFIED.,.F.,.F.,
(4,3,3,3,3,3,3,3,3,3,3,4),(-349.273907386581,-348.77598861455,-348.276309547767,
-347.776630480984,-347.276951414201,-346.777272347418,-346.277593280635,
-345.777914213852,-345.278235147069,-344.778556080286,-343.77919794672,
-342.990722079402),.UNSPECIFIED.);
#879=B_SPLINE_CURVE_WITH_KNOTS('',3,(#40657,#40658,#40659,#40660,#40661,
#40662,#40663,#40664,#40665,#40666,#40667,#40668,#40669,#40670,#40671,#40672,
#40673,#40674,#40675,#40676,#40677,#40678,#40679,#40680,#40681,#40682,#40683,
#40684),.UNSPECIFIED.,.F.,.F.,(4,3,3,3,3,3,3,3,3,4),(339.735067258252,339.781765412456,
340.781123546022,341.780481679588,342.779839813154,343.77919794672,344.778556080286,
345.278235147069,345.777914213852,346.018252565431),.UNSPECIFIED.);
#880=B_SPLINE_CURVE_WITH_KNOTS('',3,(#40689,#40690,#40691,#40692,#40693,
#40694,#40695,#40696,#40697,#40698,#40699,#40700,#40701,#40702,#40703,#40704,
#40705,#40706,#40707,#40708,#40709,#40710,#40711,#40712,#40713,#40714,#40715,
#40716,#40717,#40718,#40719,#40720,#40721,#40722,#40723,#40724,#40725,#40726,
#40727,#40728,#40729,#40730,#40731),.UNSPECIFIED.,.F.,.F.,(4,3,3,3,3,3,
3,3,3,3,3,3,3,3,4),(-355.557092693761,-355.27181648273,-354.772137415947,
-354.272458349164,-353.77277928238,-353.273100215597,-352.773421148814,
-352.273742082031,-351.774063015248,-351.274383948465,-350.774704881682,
-350.275025814899,-349.775346748116,-349.275667681333,-349.273907386581),
 .UNSPECIFIED.);
#881=B_SPLINE_CURVE_WITH_KNOTS('',3,(#40732,#40733,#40734,#40735,#40736,
#40737,#40738,#40739,#40740,#40741,#40742,#40743,#40744,#40745,#40746,#40747,
#40748,#40749,#40750,#40751,#40752,#40753,#40754,#40755,#40756,#40757,#40758,
#40759,#40760,#40761,#40762,#40763,#40764,#40765,#40766,#40767,#40768,#40769,
#40770,#40771,#40772,#40773,#40774),.UNSPECIFIED.,.F.,.F.,(4,3,3,3,3,3,
3,3,3,3,3,3,3,3,4),(346.018252565431,346.277593280635,346.777272347418,
347.276951414201,347.776630480984,348.276309547767,348.77598861455,349.275667681334,
349.775346748116,350.2750258149,350.774704881683,351.274383948466,351.774063015249,
352.273742082032,352.301437872611),.UNSPECIFIED.);
#882=B_SPLINE_CURVE_WITH_KNOTS('',3,(#40779,#40780,#40781,#40782,#40783,
#40784,#40785,#40786,#40787,#40788,#40789,#40790,#40791,#40792,#40793,#40794,
#40795,#40796,#40797,#40798,#40799,#40800,#40801,#40802,#40803,#40804,#40805,
#40806,#40807,#40808,#40809,#40810,#40811,#40812,#40813,#40814,#40815,#40816,
#40817,#40818,#40819,#40820,#40821),.UNSPECIFIED.,.F.,.F.,(4,3,3,3,3,3,
3,3,3,3,3,3,3,3,4),(-361.84027800094,-361.767644350909,-361.267965284126,
-360.768286217343,-360.26860715056,-359.768928083777,-359.269249016994,
-358.769569950211,-358.269890883428,-357.770211816645,-357.270532749862,
-356.770853683079,-356.271174616296,-355.771495549513,-355.557092693761),
 .UNSPECIFIED.);
#883=B_SPLINE_CURVE_WITH_KNOTS('',3,(#40822,#40823,#40824,#40825,#40826,
#40827,#40828,#40829,#40830,#40831,#40832,#40833,#40834,#40835,#40836,#40837,
#40838,#40839,#40840,#40841,#40842,#40843,#40844,#40845,#40846,#40847,#40848,
#40849,#40850,#40851,#40852,#40853,#40854,#40855,#40856,#40857,#40858,#40859,
#40860,#40861),.UNSPECIFIED.,.F.,.F.,(4,3,3,3,3,3,3,3,3,3,3,3,3,4),(352.301437872611,
352.773421148815,353.273100215598,353.772779282381,354.272458349164,354.772137415947,
355.27181648273,355.771495549513,356.271174616296,356.770853683079,357.270532749862,
357.770211816645,358.269890883428,358.58462317979),.UNSPECIFIED.);
#884=B_SPLINE_CURVE_WITH_KNOTS('',3,(#40866,#40867,#40868,#40869,#40870,
#40871,#40872,#40873,#40874,#40875,#40876,#40877,#40878,#40879,#40880,#40881,
#40882,#40883,#40884,#40885,#40886,#40887,#40888,#40889,#40890,#40891,#40892,
#40893,#40894,#40895,#40896,#40897,#40898,#40899,#40900,#40901,#40902,#40903,
#40904,#40905),.UNSPECIFIED.,.F.,.F.,(4,3,3,3,3,3,3,3,3,3,3,3,3,4),(-368.12346330812,
-367.763793152305,-367.264114085522,-366.764435018739,-366.264755951956,
-365.765076885173,-365.26539781839,-364.765718751607,-364.266039684824,
-363.766360618041,-363.266681551258,-362.767002484475,-362.267323417692,
-361.84027800094),.UNSPECIFIED.);
#885=B_SPLINE_CURVE_WITH_KNOTS('',3,(#40906,#40907,#40908,#40909,#40910,
#40911,#40912,#40913,#40914,#40915,#40916,#40917,#40918,#40919,#40920,#40921,
#40922,#40923,#40924,#40925,#40926,#40927,#40928,#40929,#40930,#40931,#40932,
#40933,#40934,#40935,#40936,#40937,#40938,#40939,#40940,#40941,#40942,#40943,
#40944,#40945,#40946,#40947,#40948),.UNSPECIFIED.,.F.,.F.,(4,3,3,3,3,3,
3,3,3,3,3,3,3,3,4),(358.58462317979,358.769569950211,359.269249016994,359.768928083777,
360.26860715056,360.768286217343,361.267965284126,361.767644350909,362.267323417692,
362.767002484475,363.266681551258,363.766360618041,364.266039684824,364.765718751607,
364.86780848697),.UNSPECIFIED.);
#886=B_SPLINE_CURVE_WITH_KNOTS('',3,(#40953,#40954,#40955,#40956,#40957,
#40958,#40959,#40960,#40961,#40962,#40963,#40964,#40965,#40966,#40967,#40968,
#40969,#40970,#40971,#40972,#40973,#40974,#40975,#40976,#40977,#40978,#40979,
#40980,#40981,#40982,#40983,#40984,#40985,#40986,#40987,#40988,#40989,#40990,
#40991,#40992,#40993,#40994,#40995),.UNSPECIFIED.,.F.,.F.,(4,3,3,3,3,3,
3,3,3,3,3,3,3,3,4),(-374.406648615299,-374.259621020484,-373.759941953701,
-373.260262886918,-372.760583820135,-372.260904753352,-371.761225686569,
-371.261546619786,-370.761867553003,-370.26218848622,-369.762509419437,
-369.262830352654,-368.763151285871,-368.263472219088,-368.12346330812),
 .UNSPECIFIED.);
#887=B_SPLINE_CURVE_WITH_KNOTS('',3,(#40996,#40997,#40998,#40999,#41000,
#41001,#41002,#41003,#41004,#41005,#41006,#41007,#41008,#41009,#41010,#41011,
#41012,#41013,#41014,#41015,#41016,#41017,#41018,#41019,#41020,#41021,#41022,
#41023,#41024,#41025,#41026,#41027,#41028,#41029,#41030,#41031,#41032,#41033,
#41034,#41035),.UNSPECIFIED.,.F.,.F.,(4,3,3,3,3,3,3,3,3,3,3,3,3,4),(364.86780848697,
365.26539781839,365.765076885173,366.264755951956,366.764435018739,367.264114085522,
367.763793152305,368.263472219088,368.763151285871,369.262830352654,369.762509419437,
370.26218848622,370.761867553004,371.150993794149),.UNSPECIFIED.);
#888=B_SPLINE_CURVE_WITH_KNOTS('',3,(#41040,#41041,#41042,#41043,#41044,
#41045,#41046,#41047,#41048,#41049,#41050,#41051,#41052,#41053,#41054,#41055,
#41056,#41057,#41058,#41059,#41060,#41061,#41062,#41063,#41064,#41065,#41066,
#41067,#41068,#41069,#41070,#41071,#41072,#41073,#41074,#41075,#41076,#41077,
#41078,#41079),.UNSPECIFIED.,.F.,.F.,(4,3,3,3,3,3,3,3,3,3,3,3,3,4),(-380.689833922479,
-380.255769821881,-379.756090755098,-379.256411688315,-378.756732621532,
-378.257053554749,-377.757374487966,-377.257695421183,-376.7580163544,-376.258337287616,
-375.758658220834,-375.25897915405,-374.759300087267,-374.406648615299),
 .UNSPECIFIED.);
#889=B_SPLINE_CURVE_WITH_KNOTS('',3,(#41080,#41081,#41082,#41083,#41084,
#41085,#41086,#41087,#41088,#41089,#41090,#41091,#41092,#41093,#41094,#41095,
#41096,#41097,#41098,#41099,#41100,#41101,#41102,#41103,#41104,#41105,#41106,
#41107,#41108,#41109,#41110,#41111,#41112,#41113,#41114,#41115,#41116,#41117,
#41118,#41119,#41120,#41121,#41122),.UNSPECIFIED.,.F.,.F.,(4,3,3,3,3,3,
3,3,3,3,3,3,3,3,4),(371.150993794149,371.261546619787,371.76122568657,372.260904753353,
372.760583820136,373.260262886919,373.759941953702,374.259621020485,374.759300087268,
375.258979154051,375.758658220834,376.258337287617,376.7580163544,377.257695421183,
377.434179101329),.UNSPECIFIED.);
#890=B_SPLINE_CURVE_WITH_KNOTS('',3,(#41127,#41128,#41129,#41130,#41131,
#41132,#41133,#41134,#41135,#41136,#41137,#41138,#41139,#41140,#41141,#41142,
#41143,#41144,#41145,#41146,#41147,#41148,#41149,#41150,#41151,#41152,#41153,
#41154,#41155,#41156,#41157,#41158,#41159,#41160,#41161,#41162,#41163,#41164,
#41165,#41166,#41167,#41168,#41169),.UNSPECIFIED.,.F.,.F.,(4,3,3,3,3,3,
3,3,3,3,3,3,3,3,4),(-386.973019229658,-386.75159769006,-386.251918623277,
-385.752239556494,-385.252560489711,-384.752881422928,-384.253202356145,
-383.753523289362,-383.253844222579,-382.754165155796,-382.254486089013,
-381.75480702223,-381.255127955447,-380.755448888664,-380.689833922479),
 .UNSPECIFIED.);
#891=B_SPLINE_CURVE_WITH_KNOTS('',3,(#41170,#41171,#41172,#41173,#41174,
#41175,#41176,#41177,#41178,#41179,#41180,#41181,#41182,#41183,#41184,#41185,
#41186,#41187,#41188,#41189,#41190,#41191,#41192,#41193,#41194,#41195,#41196,
#41197,#41198,#41199,#41200,#41201,#41202,#41203,#41204,#41205,#41206,#41207,
#41208,#41209),.UNSPECIFIED.,.F.,.F.,(4,3,3,3,3,3,3,3,3,3,3,3,3,4),(377.434179101329,
377.757374487966,378.257053554749,378.756732621532,379.256411688315,379.756090755098,
380.255769821881,380.755448888664,381.255127955447,381.75480702223,382.254486089013,
382.754165155796,383.253844222579,383.717364408508),.UNSPECIFIED.);
#892=B_SPLINE_CURVE_WITH_KNOTS('',3,(#41214,#41215,#41216,#41217,#41218,
#41219,#41220,#41221,#41222,#41223,#41224,#41225,#41226,#41227,#41228,#41229,
#41230,#41231,#41232,#41233,#41234,#41235,#41236,#41237,#41238,#41239,#41240,
#41241,#41242,#41243,#41244,#41245,#41246,#41247,#41248,#41249,#41250,#41251,
#41252,#41253,#41254,#41255,#41256),.UNSPECIFIED.,.F.,.F.,(4,3,3,3,3,3,
3,3,3,3,3,3,3,3,4),(-393.256204536838,-393.247425558239,-392.747746491456,
-392.248067424673,-391.74838835789,-391.248709291107,-390.749030224324,
-390.249351157541,-389.749672090758,-389.249993023975,-388.750313957192,
-388.250634890409,-387.750955823626,-387.251276756843,-386.973019229658),
 .UNSPECIFIED.);
#893=B_SPLINE_CURVE_WITH_KNOTS('',3,(#41257,#41258,#41259,#41260,#41261,
#41262,#41263,#41264,#41265,#41266,#41267,#41268,#41269,#41270,#41271,#41272,
#41273,#41274,#41275,#41276,#41277,#41278,#41279,#41280,#41281,#41282,#41283,
#41284,#41285,#41286,#41287,#41288,#41289,#41290,#41291,#41292,#41293,#41294,
#41295,#41296,#41297,#41298,#41299),.UNSPECIFIED.,.F.,.F.,(4,3,3,3,3,3,
3,3,3,3,3,3,3,3,4),(383.717364408508,383.753523289362,384.253202356145,
384.752881422928,385.252560489711,385.752239556494,386.251918623277,386.75159769006,
387.251276756843,387.750955823626,388.250634890409,388.750313957192,389.249993023975,
389.749672090758,390.000549715688),.UNSPECIFIED.);
#894=B_SPLINE_CURVE_WITH_KNOTS('',3,(#41305,#41306,#41307,#41308),
 .UNSPECIFIED.,.F.,.F.,(4,4),(405.265452313083,405.755527026166),
 .UNSPECIFIED.);
#895=B_SPLINE_CURVE_WITH_KNOTS('',3,(#41314,#41315,#41316,#41317,#41318,
#41319,#41320,#41321,#41322,#41323,#41324,#41325,#41326,#41327,#41328,#41329,
#41330),.UNSPECIFIED.,.F.,.F.,(4,1,1,1,1,1,1,1,1,1,1,1,1,1,4),(398.982267005903,
399.260524533088,399.760203599871,400.259882666654,400.759561733437,401.25924080022,
401.758919867003,402.258598933787,402.75827800057,403.257957067353,403.757636134136,
404.257315200919,404.756994267702,405.256673334485,405.265452313083),
 .UNSPECIFIED.);
#896=B_SPLINE_CURVE_WITH_KNOTS('',3,(#41333,#41334,#41335,#41336,#41337,
#41338,#41339,#41340,#41341,#41342,#41343,#41344,#41345),.UNSPECIFIED.,
 .F.,.F.,(4,1,1,1,1,1,1,1,1,1,4),(398.982267005904,399.231068447758,399.730747514541,
400.230426581324,400.730105648107,401.22978471489,401.729463781673,402.229142848456,
402.728821915239,403.228500982022,403.728180048805),.UNSPECIFIED.);
#897=B_SPLINE_CURVE_WITH_KNOTS('',3,(#41350,#41351,#41352,#41353,#41354,
#41355,#41356,#41357,#41358,#41359,#41360,#41361,#41362,#41363,#41364,#41365,
#41366),.UNSPECIFIED.,.F.,.F.,(4,1,1,1,1,1,1,1,1,1,1,1,1,1,4),(392.699081698724,
392.764696664909,393.264375731692,393.764054798475,394.263733865258,394.763412932041,
395.263091998824,395.762771065607,396.26245013239,396.762129199173,397.261808265956,
397.761487332739,398.261166399522,398.760845466305,398.982267005903),
 .UNSPECIFIED.);
#898=B_SPLINE_CURVE_WITH_KNOTS('',3,(#41367,#41368,#41369,#41370,#41371,
#41372,#41373,#41374,#41375,#41376,#41377,#41378,#41379,#41380,#41381,#41382,
#41383),.UNSPECIFIED.,.F.,.F.,(4,1,1,1,1,1,1,1,1,1,1,1,1,1,4),(392.699081698724,
392.735240579579,393.234919646362,393.734598713145,394.234277779928,394.733956846711,
395.233635913494,395.733314980277,396.23299404706,396.732673113843,397.232352180626,
397.732031247409,398.231710314192,398.731389380975,398.982267005904),
 .UNSPECIFIED.);
#899=B_SPLINE_CURVE_WITH_KNOTS('',3,(#41388,#41389,#41390,#41391,#41392,
#41393,#41394,#41395,#41396,#41397,#41398,#41399,#41400,#41401,#41402,#41403),
 .UNSPECIFIED.,.F.,.F.,(4,1,1,1,1,1,1,1,1,1,1,1,1,4),(386.415896391544,
386.768547863513,387.268226930296,387.767905997079,388.267585063862,388.767264130645,
389.266943197428,389.766622264211,390.266301330994,390.765980397777,391.26565946456,
391.765338531343,392.265017598126,392.699081698724),.UNSPECIFIED.);
#900=B_SPLINE_CURVE_WITH_KNOTS('',3,(#41404,#41405,#41406,#41407,#41408,
#41409,#41410,#41411,#41412,#41413,#41414,#41415,#41416,#41417,#41418,#41419),
 .UNSPECIFIED.,.F.,.F.,(4,1,1,1,1,1,1,1,1,1,1,1,1,4),(386.415896391545,
386.739091778183,387.238770844966,387.738449911749,388.238128978532,388.737808045315,
389.237487112098,389.737166178881,390.236845245664,390.736524312447,391.23620337923,
391.735882446013,392.235561512796,392.699081698724),.UNSPECIFIED.);
#901=B_SPLINE_CURVE_WITH_KNOTS('',3,(#41424,#41425,#41426,#41427,#41428,
#41429,#41430,#41431,#41432,#41433,#41434,#41435,#41436,#41437,#41438,#41439,
#41440),.UNSPECIFIED.,.F.,.F.,(4,1,1,1,1,1,1,1,1,1,1,1,1,1,4),(380.132711084365,
380.272719995333,380.772399062117,381.2720781289,381.771757195683,382.271436262466,
382.771115329249,383.270794396032,383.770473462815,384.270152529598,384.769831596381,
385.269510663164,385.769189729947,386.26886879673,386.415896391544),
 .UNSPECIFIED.);
#902=B_SPLINE_CURVE_WITH_KNOTS('',3,(#41441,#41442,#41443,#41444,#41445,
#41446,#41447,#41448,#41449,#41450,#41451,#41452,#41453,#41454,#41455,#41456,
#41457),.UNSPECIFIED.,.F.,.F.,(4,1,1,1,1,1,1,1,1,1,1,1,1,1,4),(380.132711084365,
380.243263910003,380.742942976786,381.242622043569,381.742301110352,382.241980177135,
382.741659243918,383.241338310702,383.741017377485,384.240696444268,384.740375511051,
385.240054577834,385.739733644617,386.2394127114,386.415896391545),
 .UNSPECIFIED.);
#903=B_SPLINE_CURVE_WITH_KNOTS('',3,(#41462,#41463,#41464,#41465,#41466,
#41467,#41468,#41469,#41470,#41471,#41472,#41473,#41474,#41475,#41476,#41477),
 .UNSPECIFIED.,.F.,.F.,(4,1,1,1,1,1,1,1,1,1,1,1,1,4),(373.849525777185,
374.276571193937,374.77625026072,375.275929327503,375.775608394286,376.275287461069,
376.774966527852,377.274645594635,377.774324661418,378.274003728201,378.773682794984,
379.273361861767,379.77304092855,380.132711084365),.UNSPECIFIED.);
#904=B_SPLINE_CURVE_WITH_KNOTS('',3,(#41478,#41479,#41480,#41481,#41482,
#41483,#41484,#41485,#41486,#41487,#41488,#41489,#41490,#41491,#41492,#41493),
 .UNSPECIFIED.,.F.,.F.,(4,1,1,1,1,1,1,1,1,1,1,1,1,4),(373.849525777185,
374.247115108607,374.74679417539,375.246473242173,375.746152308956,376.245831375739,
376.745510442522,377.245189509305,377.744868576088,378.244547642871,378.744226709654,
379.243905776437,379.74358484322,380.132711084365),.UNSPECIFIED.);
#905=B_SPLINE_CURVE_WITH_KNOTS('',3,(#41498,#41499,#41500,#41501,#41502,
#41503,#41504,#41505,#41506,#41507,#41508,#41509,#41510,#41511,#41512,#41513,
#41514),.UNSPECIFIED.,.F.,.F.,(4,1,1,1,1,1,1,1,1,1,1,1,1,1,4),(367.566340470006,
367.780743325758,368.280422392541,368.780101459324,369.279780526107,369.77945959289,
370.279138659673,370.778817726456,371.278496793239,371.778175860022,372.277854926805,
372.777533993588,373.277213060371,373.776892127154,373.849525777185),
 .UNSPECIFIED.);
#906=B_SPLINE_CURVE_WITH_KNOTS('',3,(#41515,#41516,#41517,#41518,#41519,
#41520,#41521,#41522,#41523,#41524,#41525,#41526,#41527,#41528,#41529,#41530,
#41531),.UNSPECIFIED.,.F.,.F.,(4,1,1,1,1,1,1,1,1,1,1,1,1,1,4),(367.566340470006,
367.751287240428,368.250966307211,368.750645373994,369.250324440777,369.75000350756,
370.249682574343,370.749361641126,371.249040707909,371.748719774692,372.248398841475,
372.748077908258,373.247756975041,373.747436041824,373.849525777185),
 .UNSPECIFIED.);
#907=B_SPLINE_CURVE_WITH_KNOTS('',3,(#41536,#41537,#41538,#41539,#41540,
#41541,#41542,#41543,#41544,#41545,#41546,#41547,#41548,#41549,#41550,#41551,
#41552),.UNSPECIFIED.,.F.,.F.,(4,1,1,1,1,1,1,1,1,1,1,1,1,1,4),(361.283155162826,
361.284915457579,361.784594524362,362.284273591145,362.783952657928,363.283631724711,
363.783310791494,364.282989858277,364.78266892506,365.282347991843,365.782027058626,
366.281706125409,366.781385192192,367.281064258975,367.566340470006),
 .UNSPECIFIED.);
#908=B_SPLINE_CURVE_WITH_KNOTS('',3,(#41553,#41554,#41555,#41556,#41557,
#41558,#41559,#41560,#41561,#41562,#41563,#41564,#41565,#41566,#41567,#41568),
 .UNSPECIFIED.,.F.,.F.,(4,1,1,1,1,1,1,1,1,1,1,1,1,4),(361.283155162826,
361.755138439031,362.254817505815,362.754496572598,363.254175639381,363.753854706164,
364.253533772947,364.75321283973,365.252891906513,365.752570973296,366.252250040079,
366.751929106862,367.251608173645,367.566340470006),.UNSPECIFIED.);
#909=B_SPLINE_CURVE_WITH_KNOTS('',3,(#41573,#41574,#41575,#41576,#41577,
#41578,#41579,#41580,#41581,#41582,#41583,#41584,#41585,#41586),
 .UNSPECIFIED.,.F.,.F.,(4,1,1,1,1,1,1,1,1,1,1,4),(354.999969855646,355.788445722965,
356.787803856531,357.287482923314,357.787161990097,358.28684105688,358.786520123663,
359.286199190446,359.78587825723,360.285557324013,360.785236390796,361.283155162826),
 .UNSPECIFIED.);
#910=B_SPLINE_CURVE_WITH_KNOTS('',3,(#41587,#41588,#41589,#41590,#41591,
#41592,#41593,#41594,#41595,#41596,#41597,#41598,#41599,#41600,#41601,#41602,
#41603),.UNSPECIFIED.,.F.,.F.,(4,1,1,1,1,1,1,1,1,1,1,1,1,1,4),(354.999969855647,
355.259310570852,355.758989637635,356.258668704418,356.758347771201,357.258026837984,
357.757705904767,358.25738497155,358.757064038333,359.256743105116,359.756422171899,
360.256101238682,360.755780305465,361.255459372248,361.283155162826),
 .UNSPECIFIED.);
#911=B_SPLINE_CURVE_WITH_KNOTS('',3,(#41608,#41609,#41610,#41611,#41612,
#41613,#41614,#41615,#41616,#41617,#41618),.UNSPECIFIED.,.F.,.F.,(4,1,1,
1,1,1,1,1,4),(348.716784548467,348.792938788003,349.792296921569,350.791655055135,
351.791013188701,352.790371322267,353.789729455833,354.789087589399,354.999969855646),
 .UNSPECIFIED.);
#912=B_SPLINE_CURVE_WITH_KNOTS('',3,(#41619,#41620,#41621,#41622,#41623,
#41624,#41625,#41626,#41627,#41628,#41629,#41630),.UNSPECIFIED.,.F.,.F.,
(4,1,1,1,1,1,1,1,1,4),(348.716784548467,348.763482702673,349.762840836239,
350.762198969805,351.761557103371,352.760915236937,353.760273370503,354.259952437286,
354.759631504069,354.999969855647),.UNSPECIFIED.);
#913=B_SPLINE_CURVE_WITH_KNOTS('',3,(#41635,#41636,#41637,#41638,#41639,
#41640,#41641,#41642,#41643,#41644),.UNSPECIFIED.,.F.,.F.,(4,1,1,1,1,1,
1,4),(342.433599241287,342.796789986607,343.796148120173,344.795506253739,
345.794864387305,346.794222520871,347.793580654437,348.716784548467),
 .UNSPECIFIED.);
#914=B_SPLINE_CURVE_WITH_KNOTS('',3,(#41645,#41646,#41647,#41648,#41649,
#41650,#41651,#41652,#41653,#41654),.UNSPECIFIED.,.F.,.F.,(4,1,1,1,1,1,
1,4),(342.433599241288,342.767333901277,343.766692034843,344.766050168409,
345.765408301975,346.764766435541,347.764124569107,348.716784548467),
 .UNSPECIFIED.);
#915=B_SPLINE_CURVE_WITH_KNOTS('',3,(#41659,#41660,#41661,#41662,#41663,
#41664,#41665,#41666,#41667,#41668),.UNSPECIFIED.,.F.,.F.,(4,1,1,1,1,1,
1,4),(336.150413934108,336.80064118521,337.799999318776,338.799357452343,
339.798715585909,340.798073719475,341.797431853041,342.433599241287),
 .UNSPECIFIED.);
#916=B_SPLINE_CURVE_WITH_KNOTS('',3,(#41669,#41670,#41671,#41672,#41673,
#41674,#41675,#41676,#41677,#41678),.UNSPECIFIED.,.F.,.F.,(4,1,1,1,1,1,
1,4),(336.150413934108,336.77118509988,337.770543233446,338.769901367012,
339.769259500578,340.768617634145,341.767975767711,342.433599241288),
 .UNSPECIFIED.);
#917=B_SPLINE_CURVE_WITH_KNOTS('',3,(#41683,#41684,#41685,#41686,#41687,
#41688,#41689,#41690,#41691,#41692),.UNSPECIFIED.,.F.,.F.,(4,1,1,1,1,1,
1,4),(329.867228626928,330.804492383814,331.80385051738,332.803208650946,
333.802566784512,334.801924918078,335.801283051644,336.150413934108),
 .UNSPECIFIED.);
#918=B_SPLINE_CURVE_WITH_KNOTS('',3,(#41693,#41694,#41695,#41696,#41697,
#41698,#41699,#41700,#41701,#41702),.UNSPECIFIED.,.F.,.F.,(4,1,1,1,1,1,
1,4),(329.867228626928,330.775036298484,331.77439443205,332.773752565616,
333.773110699182,334.772468832748,335.771826966314,336.150413934108),
 .UNSPECIFIED.);
#919=B_SPLINE_CURVE_WITH_KNOTS('',3,(#41707,#41708,#41709,#41710,#41711,
#41712,#41713,#41714,#41715,#41716,#41717),.UNSPECIFIED.,.F.,.F.,(4,1,1,
1,1,1,1,1,4),(323.584043319749,323.808985448852,324.808343582418,325.807701715984,
326.80705984955,327.806417983116,328.805776116682,329.805134250248,329.867228626928),
 .UNSPECIFIED.);
#920=B_SPLINE_CURVE_WITH_KNOTS('',3,(#41718,#41719,#41720,#41721,#41722,
#41723,#41724,#41725,#41726,#41727,#41728),.UNSPECIFIED.,.F.,.F.,(4,1,1,
1,1,1,1,1,4),(323.584043319749,323.779529363522,324.778887497088,325.778245630654,
326.77760376422,327.776961897786,328.776320031352,329.775678164918,329.867228626928),
 .UNSPECIFIED.);
#921=B_SPLINE_CURVE_WITH_KNOTS('',3,(#41733,#41734,#41735,#41736,#41737,
#41738,#41739,#41740,#41741,#41742),.UNSPECIFIED.,.F.,.F.,(4,1,1,1,1,1,
1,4),(317.300858012569,317.812836647456,318.812194781022,319.811552914588,
320.810911048154,321.81026918172,322.809627315286,323.584043319749),
 .UNSPECIFIED.);
#922=B_SPLINE_CURVE_WITH_KNOTS('',3,(#41743,#41744,#41745,#41746,#41747,
#41748,#41749,#41750,#41751,#41752),.UNSPECIFIED.,.F.,.F.,(4,1,1,1,1,1,
1,4),(317.300858012569,317.783380562125,318.782738695691,319.782096829258,
320.781454962824,321.78081309639,322.780171229956,323.584043319749),
 .UNSPECIFIED.);
#923=B_SPLINE_CURVE_WITH_KNOTS('',3,(#41757,#41758,#41759,#41760,#41761,
#41762,#41763,#41764,#41765,#41766),.UNSPECIFIED.,.F.,.F.,(4,1,1,1,1,1,
1,4),(311.017672705389,311.816687846059,312.816045979625,313.815404113191,
314.814762246757,315.814120380323,316.81347851389,317.300858012569),
 .UNSPECIFIED.);
#924=B_SPLINE_CURVE_WITH_KNOTS('',3,(#41767,#41768,#41769,#41770,#41771,
#41772,#41773,#41774,#41775,#41776),.UNSPECIFIED.,.F.,.F.,(4,1,1,1,1,1,
1,4),(311.01767270539,311.787231760729,312.786589894295,313.785948027861,
314.785306161427,315.784664294993,316.784022428559,317.300858012569),
 .UNSPECIFIED.);
#925=B_SPLINE_CURVE_WITH_KNOTS('',3,(#41781,#41782,#41783,#41784,#41785,
#41786,#41787,#41788,#41789,#41790,#41791),.UNSPECIFIED.,.F.,.F.,(4,1,1,
1,1,1,1,1,4),(304.73448739821,304.821180911097,305.820539044663,306.819897178229,
307.819255311795,308.818613445361,309.817971578927,310.817329712493,311.017672705389),
 .UNSPECIFIED.);
#926=B_SPLINE_CURVE_WITH_KNOTS('',3,(#41792,#41793,#41794,#41795,#41796,
#41797,#41798,#41799,#41800,#41801,#41802),.UNSPECIFIED.,.F.,.F.,(4,1,1,
1,1,1,1,1,4),(304.73448739821,304.791724825767,305.791082959333,306.790441092899,
307.789799226465,308.789157360031,309.788515493597,310.787873627163,311.01767270539),
 .UNSPECIFIED.);
#927=B_SPLINE_CURVE_WITH_KNOTS('',3,(#41807,#41808,#41809,#41810,#41811,
#41812,#41813,#41814,#41815,#41816),.UNSPECIFIED.,.F.,.F.,(4,1,1,1,1,1,
1,4),(298.45130209103,298.825032109701,299.824390243267,300.823748376833,
301.823106510399,302.822464643965,303.821822777531,304.73448739821),
 .UNSPECIFIED.);
#928=B_SPLINE_CURVE_WITH_KNOTS('',3,(#41817,#41818,#41819,#41820,#41821,
#41822,#41823,#41824,#41825,#41826),.UNSPECIFIED.,.F.,.F.,(4,1,1,1,1,1,
1,4),(298.451302091031,298.795576024371,299.794934157937,300.794292291503,
301.793650425069,302.793008558635,303.792366692201,304.73448739821),
 .UNSPECIFIED.);
#929=B_SPLINE_CURVE_WITH_KNOTS('',3,(#41831,#41832,#41833,#41834,#41835,
#41836,#41837,#41838,#41839,#41840),.UNSPECIFIED.,.F.,.F.,(4,1,1,1,1,1,
1,4),(292.168116783851,292.828883308304,293.82824144187,294.827599575437,
295.826957709003,296.826315842569,297.825673976135,298.45130209103),
 .UNSPECIFIED.);
#930=B_SPLINE_CURVE_WITH_KNOTS('',3,(#41841,#41842,#41843,#41844,#41845,
#41846,#41847,#41848,#41849,#41850),.UNSPECIFIED.,.F.,.F.,(4,1,1,1,1,1,
1,4),(292.168116783851,292.799427222974,293.79878535654,294.798143490106,
295.797501623672,296.796859757238,297.796217890804,298.451302091031),
 .UNSPECIFIED.);
#931=B_SPLINE_CURVE_WITH_KNOTS('',3,(#41855,#41856,#41857,#41858,#41859,
#41860,#41861,#41862,#41863,#41864),.UNSPECIFIED.,.F.,.F.,(4,1,1,1,1,1,
1,4),(285.884931476671,286.832734506908,287.832092640474,288.83145077404,
289.830808907606,290.830167041172,291.829525174738,292.168116783851),
 .UNSPECIFIED.);
#932=B_SPLINE_CURVE_WITH_KNOTS('',3,(#41865,#41866,#41867,#41868,#41869,
#41870,#41871,#41872,#41873,#41874),.UNSPECIFIED.,.F.,.F.,(4,1,1,1,1,1,
1,4),(285.884931476672,286.803278421578,287.802636555144,288.80199468871,
289.801352822276,290.800710955842,291.800069089408,292.168116783851),
 .UNSPECIFIED.);
#933=B_SPLINE_CURVE_WITH_KNOTS('',3,(#41879,#41880,#41881,#41882,#41883,
#41884,#41885,#41886,#41887,#41888,#41889),.UNSPECIFIED.,.F.,.F.,(4,1,1,
1,1,1,1,1,4),(279.601746169492,279.837227571946,280.836585705512,281.835943839078,
282.835301972644,283.83466010621,284.834018239776,285.833376373342,285.884931476671),
 .UNSPECIFIED.);
#934=B_SPLINE_CURVE_WITH_KNOTS('',3,(#41890,#41891,#41892,#41893,#41894,
#41895,#41896,#41897,#41898,#41899,#41900),.UNSPECIFIED.,.F.,.F.,(4,1,1,
1,1,1,1,1,4),(279.601746169492,279.807771486616,280.807129620182,281.806487753748,
282.805845887314,283.80520402088,284.804562154446,285.803920288012,285.884931476672),
 .UNSPECIFIED.);
#935=B_SPLINE_CURVE_WITH_KNOTS('',3,(#41905,#41906,#41907,#41908,#41909,
#41910,#41911,#41912,#41913,#41914),.UNSPECIFIED.,.F.,.F.,(4,1,1,1,1,1,
1,4),(273.318560862312,273.84107877055,274.840436904116,275.839795037682,
276.839153171248,277.838511304814,278.83786943838,279.601746169492),
 .UNSPECIFIED.);
#936=B_SPLINE_CURVE_WITH_KNOTS('',3,(#41915,#41916,#41917,#41918,#41919,
#41920,#41921,#41922,#41923,#41924),.UNSPECIFIED.,.F.,.F.,(4,1,1,1,1,1,
1,4),(273.318560862312,273.811622685219,274.810980818785,275.810338952351,
276.809697085917,277.809055219484,278.80841335305,279.601746169492),
 .UNSPECIFIED.);
#937=B_SPLINE_CURVE_WITH_KNOTS('',3,(#41929,#41930,#41931,#41932,#41933,
#41934,#41935,#41936,#41937,#41938),.UNSPECIFIED.,.F.,.F.,(4,1,1,1,1,1,
1,4),(267.035375555133,267.844929969153,268.844288102719,269.843646236285,
270.843004369851,271.842362503417,272.841720636983,273.318560862312),
 .UNSPECIFIED.);
#938=B_SPLINE_CURVE_WITH_KNOTS('',3,(#41939,#41940,#41941,#41942,#41943,
#41944,#41945,#41946,#41947,#41948),.UNSPECIFIED.,.F.,.F.,(4,1,1,1,1,1,
1,4),(267.035375555133,267.815473883823,268.814832017389,269.814190150955,
270.813548284521,271.812906418087,272.812264551653,273.318560862312),
 .UNSPECIFIED.);
#939=B_SPLINE_CURVE_WITH_KNOTS('',3,(#41953,#41954,#41955,#41956,#41957,
#41958,#41959,#41960,#41961,#41962,#41963),.UNSPECIFIED.,.F.,.F.,(4,1,1,
1,1,1,1,1,4),(260.752190247953,260.849423034191,261.848781167757,262.848139301323,
263.847497434889,264.846855568455,265.846213702021,266.845571835587,267.035375555133),
 .UNSPECIFIED.);
#940=B_SPLINE_CURVE_WITH_KNOTS('',3,(#41964,#41965,#41966,#41967,#41968,
#41969,#41970,#41971,#41972,#41973,#41974),.UNSPECIFIED.,.F.,.F.,(4,1,1,
1,1,1,1,1,4),(260.752190247953,260.819966948861,261.819325082427,262.818683215993,
263.818041349559,264.817399483125,265.816757616691,266.816115750257,267.035375555133),
 .UNSPECIFIED.);
#941=B_SPLINE_CURVE_WITH_KNOTS('',3,(#41979,#41980,#41981,#41982,#41983,
#41984,#41985,#41986,#41987,#41988),.UNSPECIFIED.,.F.,.F.,(4,1,1,1,1,1,
1,4),(254.469004940773,254.853274232795,255.852632366361,256.851990499927,
257.851348633493,258.850706767059,259.850064900625,260.752190247953),
 .UNSPECIFIED.);
#942=B_SPLINE_CURVE_WITH_KNOTS('',3,(#41989,#41990,#41991,#41992,#41993,
#41994,#41995,#41996,#41997,#41998),.UNSPECIFIED.,.F.,.F.,(4,1,1,1,1,1,
1,4),(254.469004940774,254.823818147464,255.82317628103,256.822534414597,
257.821892548163,258.821250681729,259.820608815295,260.752190247953),
 .UNSPECIFIED.);
#943=B_SPLINE_CURVE_WITH_KNOTS('',3,(#42003,#42004,#42005,#42006,#42007,
#42008,#42009,#42010,#42011,#42012),.UNSPECIFIED.,.F.,.F.,(4,1,1,1,1,1,
1,4),(248.185819633594,248.857125431398,249.856483564964,250.85584169853,
251.855199832097,252.854557965663,253.853916099229,254.469004940773),
 .UNSPECIFIED.);
#944=B_SPLINE_CURVE_WITH_KNOTS('',3,(#42013,#42014,#42015,#42016,#42017,
#42018,#42019,#42020,#42021,#42022),.UNSPECIFIED.,.F.,.F.,(4,1,1,1,1,1,
1,4),(248.185819633594,248.827669346068,249.827027479634,250.8263856132,
251.825743746766,252.825101880332,253.824460013898,254.469004940774),
 .UNSPECIFIED.);
#945=B_SPLINE_CURVE_WITH_KNOTS('',3,(#42027,#42028,#42029,#42030,#42031,
#42032,#42033,#42034,#42035,#42036),.UNSPECIFIED.,.F.,.F.,(4,1,1,1,1,1,
1,4),(241.902634326414,242.860976630002,243.860334763568,244.859692897134,
245.8590510307,246.858409164266,247.857767297832,248.185819633594),
 .UNSPECIFIED.);
#946=B_SPLINE_CURVE_WITH_KNOTS('',3,(#42037,#42038,#42039,#42040,#42041,
#42042,#42043,#42044,#42045,#42046),.UNSPECIFIED.,.F.,.F.,(4,1,1,1,1,1,
1,4),(241.902634326415,242.831520544672,243.830878678238,244.830236811804,
245.82959494537,246.828953078936,247.828311212502,248.185819633594),
 .UNSPECIFIED.);
#947=B_SPLINE_CURVE_WITH_KNOTS('',3,(#42051,#42052,#42053,#42054,#42055,
#42056,#42057,#42058,#42059,#42060,#42061),.UNSPECIFIED.,.F.,.F.,(4,1,1,
1,1,1,1,1,4),(235.619449019235,235.86546969504,236.864827828606,237.864185962172,
238.863544095738,239.862902229304,240.86226036287,241.861618496436,241.902634326414),
 .UNSPECIFIED.);
#948=B_SPLINE_CURVE_WITH_KNOTS('',3,(#42062,#42063,#42064,#42065,#42066,
#42067,#42068,#42069,#42070,#42071,#42072),.UNSPECIFIED.,.F.,.F.,(4,1,1,
1,1,1,1,1,4),(235.619449019235,235.83601360971,236.835371743276,237.834729876842,
238.834088010408,239.833446143974,240.83280427754,241.832162411106,241.902634326415),
 .UNSPECIFIED.);
#949=B_SPLINE_CURVE_WITH_KNOTS('',3,(#42077,#42078,#42079,#42080,#42081,
#42082,#42083,#42084,#42085,#42086),.UNSPECIFIED.,.F.,.F.,(4,1,1,1,1,1,
1,4),(229.336263712055,229.869320893643,230.86867902721,231.868037160776,
232.867395294342,233.866753427908,234.866111561474,235.619449019235),
 .UNSPECIFIED.);
#950=B_SPLINE_CURVE_WITH_KNOTS('',3,(#42087,#42088,#42089,#42090,#42091,
#42092,#42093,#42094,#42095,#42096),.UNSPECIFIED.,.F.,.F.,(4,1,1,1,1,1,
1,4),(229.336263712055,229.839864808313,230.839222941879,231.838581075445,
232.837939209011,233.837297342577,234.836655476144,235.619449019235),
 .UNSPECIFIED.);
#951=B_SPLINE_CURVE_WITH_KNOTS('',3,(#42101,#42102,#42103,#42104,#42105,
#42106,#42107,#42108,#42109,#42110),.UNSPECIFIED.,.F.,.F.,(4,1,1,1,1,1,
1,4),(223.053078404876,223.873172092247,224.872530225813,225.871888359379,
226.871246492945,227.870604626511,228.869962760077,229.336263712055),
 .UNSPECIFIED.);
#952=B_SPLINE_CURVE_WITH_KNOTS('',3,(#42111,#42112,#42113,#42114,#42115,
#42116,#42117,#42118,#42119,#42120),.UNSPECIFIED.,.F.,.F.,(4,1,1,1,1,1,
1,4),(223.053078404876,223.843716006917,224.843074140483,225.842432274049,
226.841790407615,227.841148541181,228.840506674747,229.336263712055),
 .UNSPECIFIED.);
#953=B_SPLINE_CURVE_WITH_KNOTS('',3,(#42125,#42126,#42127,#42128,#42129,
#42130,#42131,#42132,#42133,#42134,#42135),.UNSPECIFIED.,.F.,.F.,(4,1,1,
1,1,1,1,1,4),(216.769893097696,216.877665157285,217.877023290851,218.876381424417,
219.875739557983,220.875097691549,221.874455825115,222.873813958681,223.053078404876),
 .UNSPECIFIED.);
#954=B_SPLINE_CURVE_WITH_KNOTS('',3,(#42136,#42137,#42138,#42139,#42140,
#42141,#42142,#42143,#42144,#42145,#42146),.UNSPECIFIED.,.F.,.F.,(4,1,1,
1,1,1,1,1,4),(216.769893097696,216.848209071955,217.847567205521,218.846925339087,
219.846283472653,220.845641606219,221.844999739785,222.844357873351,223.053078404876),
 .UNSPECIFIED.);
#955=B_SPLINE_CURVE_WITH_KNOTS('',3,(#42151,#42152,#42153,#42154,#42155,
#42156,#42157,#42158,#42159,#42160),.UNSPECIFIED.,.F.,.F.,(4,1,1,1,1,1,
1,4),(210.486707790516,210.881516355889,211.880874489455,212.880232623021,
213.879590756587,214.878948890153,215.878307023719,216.769893097696),
 .UNSPECIFIED.);
#956=B_SPLINE_CURVE_WITH_KNOTS('',3,(#42161,#42162,#42163,#42164,#42165,
#42166,#42167,#42168,#42169,#42170),.UNSPECIFIED.,.F.,.F.,(4,1,1,1,1,1,
1,4),(210.486707790517,210.852060270558,211.851418404124,212.85077653769,
213.850134671257,214.849492804823,215.848850938389,216.769893097696),
 .UNSPECIFIED.);
#957=B_SPLINE_CURVE_WITH_KNOTS('',3,(#42175,#42176,#42177,#42178,#42179,
#42180,#42181,#42182,#42183,#42184),.UNSPECIFIED.,.F.,.F.,(4,1,1,1,1,1,
1,4),(204.203522483337,204.885367554492,205.884725688058,206.884083821624,
207.88344195519,208.882800088756,209.882158222323,210.486707790516),
 .UNSPECIFIED.);
#958=B_SPLINE_CURVE_WITH_KNOTS('',3,(#42185,#42186,#42187,#42188,#42189,
#42190,#42191,#42192,#42193,#42194),.UNSPECIFIED.,.F.,.F.,(4,1,1,1,1,1,
1,4),(204.203522483337,204.855911469162,205.855269602728,206.854627736294,
207.85398586986,208.853344003426,209.852702136992,210.486707790517),
 .UNSPECIFIED.);
#959=B_SPLINE_CURVE_WITH_KNOTS('',3,(#42199,#42200,#42201,#42202,#42203,
#42204,#42205,#42206,#42207,#42208),.UNSPECIFIED.,.F.,.F.,(4,1,1,1,1,1,
1,4),(197.920337176157,198.889218753096,199.888576886662,200.887935020228,
201.887293153794,202.88665128736,203.886009420926,204.203522483337),
 .UNSPECIFIED.);
#960=B_SPLINE_CURVE_WITH_KNOTS('',3,(#42209,#42210,#42211,#42212,#42213,
#42214,#42215,#42216,#42217,#42218),.UNSPECIFIED.,.F.,.F.,(4,1,1,1,1,1,
1,4),(197.920337176158,198.859762667766,199.859120801332,200.858478934898,
201.857837068464,202.85719520203,203.856553335596,204.203522483337),
 .UNSPECIFIED.);
#961=B_SPLINE_CURVE_WITH_KNOTS('',3,(#42223,#42224,#42225,#42226,#42227,
#42228,#42229,#42230,#42231,#42232,#42233),.UNSPECIFIED.,.F.,.F.,(4,1,1,
1,1,1,1,1,4),(191.637151868978,191.893711818134,192.8930699517,193.892428085266,
194.891786218832,195.891144352398,196.890502485964,197.88986061953,197.920337176157),
 .UNSPECIFIED.);
#962=B_SPLINE_CURVE_WITH_KNOTS('',3,(#42234,#42235,#42236,#42237,#42238,
#42239,#42240,#42241,#42242,#42243,#42244),.UNSPECIFIED.,.F.,.F.,(4,1,1,
1,1,1,1,1,4),(191.637151868978,191.864255732803,192.86361386637,193.862971999936,
194.862330133502,195.861688267068,196.861046400634,197.8604045342,197.920337176158),
 .UNSPECIFIED.);
#963=B_SPLINE_CURVE_WITH_KNOTS('',3,(#42249,#42250,#42251,#42252,#42253,
#42254,#42255,#42256,#42257,#42258),.UNSPECIFIED.,.F.,.F.,(4,1,1,1,1,1,
1,4),(185.353966561798,185.897563016737,186.896921150303,187.89627928387,
188.895637417436,189.894995551002,190.894353684568,191.637151868978),
 .UNSPECIFIED.);
#964=B_SPLINE_CURVE_WITH_KNOTS('',3,(#42259,#42260,#42261,#42262,#42263,
#42264,#42265,#42266,#42267,#42268),.UNSPECIFIED.,.F.,.F.,(4,1,1,1,1,1,
1,4),(185.353966561799,185.868106931407,186.867465064973,187.866823198539,
188.866181332105,189.865539465671,190.864897599237,191.637151868978),
 .UNSPECIFIED.);
#965=B_SPLINE_CURVE_WITH_KNOTS('',3,(#42273,#42274,#42275,#42276,#42277,
#42278,#42279,#42280,#42281,#42282),.UNSPECIFIED.,.F.,.F.,(4,1,1,1,1,1,
1,4),(179.070781254619,179.901414215341,180.900772348907,181.900130482473,
182.899488616039,183.898846749605,184.898204883171,185.353966561798),
 .UNSPECIFIED.);
#966=B_SPLINE_CURVE_WITH_KNOTS('',3,(#42283,#42284,#42285,#42286,#42287,
#42288,#42289,#42290,#42291,#42292),.UNSPECIFIED.,.F.,.F.,(4,1,1,1,1,1,
1,4),(179.070781254619,179.871958130011,180.871316263577,181.870674397143,
182.870032530709,183.869390664275,184.868748797841,185.353966561799),
 .UNSPECIFIED.);
#967=B_SPLINE_CURVE_WITH_KNOTS('',3,(#42297,#42298,#42299,#42300,#42301,
#42302,#42303,#42304,#42305,#42306,#42307),.UNSPECIFIED.,.F.,.F.,(4,1,1,
1,1,1,1,1,4),(172.787595947439,172.905907280379,173.905265413945,174.904623547511,
175.903981681077,176.903339814643,177.902697948209,178.902056081775,179.070781254619),
 .UNSPECIFIED.);
#968=B_SPLINE_CURVE_WITH_KNOTS('',3,(#42308,#42309,#42310,#42311,#42312,
#42313,#42314,#42315,#42316,#42317,#42318),.UNSPECIFIED.,.F.,.F.,(4,1,1,
1,1,1,1,1,4),(172.787595947439,172.876451195049,173.875809328615,174.875167462181,
175.874525595747,176.873883729313,177.873241862879,178.872599996445,179.070781254619),
 .UNSPECIFIED.);
#969=B_SPLINE_CURVE_WITH_KNOTS('',3,(#42323,#42324,#42325,#42326,#42327,
#42328,#42329,#42330,#42331,#42332),.UNSPECIFIED.,.F.,.F.,(4,1,1,1,1,1,
1,4),(166.504410640259,166.909758478983,167.909116612549,168.908474746115,
169.907832879681,170.907191013247,171.906549146813,172.787595947439),
 .UNSPECIFIED.);
#970=B_SPLINE_CURVE_WITH_KNOTS('',3,(#42333,#42334,#42335,#42336,#42337,
#42338,#42339,#42340,#42341,#42342),.UNSPECIFIED.,.F.,.F.,(4,1,1,1,1,1,
1,4),(166.50441064026,166.880302393652,167.879660527218,168.879018660784,
169.87837679435,170.877734927916,171.877093061483,172.787595947439),
 .UNSPECIFIED.);
#971=B_SPLINE_CURVE_WITH_KNOTS('',3,(#42347,#42348,#42349,#42350,#42351,
#42352,#42353,#42354,#42355,#42356),.UNSPECIFIED.,.F.,.F.,(4,1,1,1,1,1,
1,4),(160.22122533308,160.913609677586,161.912967811152,162.912325944718,
163.911684078284,164.91104221185,165.910400345416,166.504410640259),
 .UNSPECIFIED.);
#972=B_SPLINE_CURVE_WITH_KNOTS('',3,(#42357,#42358,#42359,#42360,#42361,
#42362,#42363,#42364,#42365,#42366),.UNSPECIFIED.,.F.,.F.,(4,1,1,1,1,1,
1,4),(160.22122533308,160.884153592256,161.883511725822,162.882869859388,
163.882227992954,164.88158612652,165.880944260086,166.50441064026),
 .UNSPECIFIED.);
#973=B_SPLINE_CURVE_WITH_KNOTS('',3,(#42371,#42372,#42373,#42374,#42375,
#42376,#42377,#42378,#42379,#42380),.UNSPECIFIED.,.F.,.F.,(4,1,1,1,1,1,
1,4),(153.9380400259,154.91746087619,155.916819009756,156.916177143322,
157.915535276888,158.914893410454,159.91425154402,160.22122533308),
 .UNSPECIFIED.);
#974=B_SPLINE_CURVE_WITH_KNOTS('',3,(#42381,#42382,#42383,#42384,#42385,
#42386,#42387,#42388,#42389,#42390),.UNSPECIFIED.,.F.,.F.,(4,1,1,1,1,1,
1,4),(153.938040025901,154.88800479086,155.887362924426,156.886721057992,
157.886079191558,158.885437325124,159.88479545869,160.22122533308),
 .UNSPECIFIED.);
#975=B_SPLINE_CURVE_WITH_KNOTS('',3,(#42395,#42396,#42397,#42398,#42399,
#42400,#42401,#42402,#42403,#42404,#42405),.UNSPECIFIED.,.F.,.F.,(4,1,1,
1,1,1,1,1,4),(147.654854718721,147.921953941228,148.921312074794,149.92067020836,
150.920028341926,151.919386475492,152.918744609058,153.918102742624,153.9380400259),
 .UNSPECIFIED.);
#976=B_SPLINE_CURVE_WITH_KNOTS('',3,(#42406,#42407,#42408,#42409,#42410,
#42411,#42412,#42413,#42414,#42415,#42416),.UNSPECIFIED.,.F.,.F.,(4,1,1,
1,1,1,1,1,4),(147.654854718721,147.892497855897,148.891855989463,149.891214123029,
150.890572256596,151.889930390162,152.889288523728,153.888646657294,153.938040025901),
 .UNSPECIFIED.);
#977=B_SPLINE_CURVE_WITH_KNOTS('',3,(#42421,#42422,#42423,#42424,#42425,
#42426,#42427,#42428,#42429,#42430),.UNSPECIFIED.,.F.,.F.,(4,1,1,1,1,1,
1,4),(141.371669411541,141.925805139831,142.925163273397,143.924521406963,
144.92387954053,145.923237674096,146.922595807662,147.654854718721),
 .UNSPECIFIED.);
#978=B_SPLINE_CURVE_WITH_KNOTS('',3,(#42431,#42432,#42433,#42434,#42435,
#42436,#42437,#42438,#42439,#42440),.UNSPECIFIED.,.F.,.F.,(4,1,1,1,1,1,
1,4),(141.371669411542,141.896349054501,142.895707188067,143.895065321633,
144.894423455199,145.893781588765,146.893139722331,147.654854718721),
 .UNSPECIFIED.);
#979=B_SPLINE_CURVE_WITH_KNOTS('',3,(#42445,#42446,#42447,#42448,#42449,
#42450,#42451,#42452,#42453,#42454),.UNSPECIFIED.,.F.,.F.,(4,1,1,1,1,1,
1,4),(135.088484104362,135.929656338435,136.929014472001,137.928372605567,
138.927730739133,139.927088872699,140.926447006265,141.371669411541),
 .UNSPECIFIED.);
#980=B_SPLINE_CURVE_WITH_KNOTS('',3,(#42455,#42456,#42457,#42458,#42459,
#42460,#42461,#42462,#42463,#42464),.UNSPECIFIED.,.F.,.F.,(4,1,1,1,1,1,
1,4),(135.088484104362,135.900200253105,136.899558386671,137.898916520237,
138.898274653803,139.897632787369,140.896990920935,141.371669411542),
 .UNSPECIFIED.);
#981=B_SPLINE_CURVE_WITH_KNOTS('',3,(#42469,#42470,#42471,#42472,#42473,
#42474,#42475,#42476,#42477,#42478,#42479),.UNSPECIFIED.,.F.,.F.,(4,1,1,
1,1,1,1,1,4),(128.805298797182,128.934149403473,129.933507537039,130.932865670605,
131.932223804171,132.931581937737,133.930940071303,134.930298204869,135.088484104362),
 .UNSPECIFIED.);
#982=B_SPLINE_CURVE_WITH_KNOTS('',3,(#42480,#42481,#42482,#42483,#42484,
#42485,#42486,#42487,#42488,#42489,#42490),.UNSPECIFIED.,.F.,.F.,(4,1,1,
1,1,1,1,1,4),(128.805298797182,128.904693318142,129.904051451709,130.903409585275,
131.902767718841,132.902125852407,133.901483985973,134.900842119539,135.088484104362),
 .UNSPECIFIED.);
#983=B_SPLINE_CURVE_WITH_KNOTS('',3,(#42495,#42496,#42497,#42498,#42499,
#42500,#42501,#42502,#42503,#42504),.UNSPECIFIED.,.F.,.F.,(4,1,1,1,1,1,
1,4),(122.522113490002,122.938000602077,123.937358735643,124.936716869209,
125.936075002775,126.935433136341,127.934791269907,128.805298797182),
 .UNSPECIFIED.);
#984=B_SPLINE_CURVE_WITH_KNOTS('',3,(#42505,#42506,#42507,#42508,#42509,
#42510,#42511,#42512,#42513,#42514),.UNSPECIFIED.,.F.,.F.,(4,1,1,1,1,1,
1,4),(122.522113490003,122.908544516746,123.907902650312,124.907260783878,
125.906618917444,126.90597705101,127.905335184576,128.805298797182),
 .UNSPECIFIED.);
#985=B_SPLINE_CURVE_WITH_KNOTS('',3,(#42519,#42520,#42521,#42522,#42523,
#42524,#42525,#42526,#42527,#42528),.UNSPECIFIED.,.F.,.F.,(4,1,1,1,1,1,
1,4),(116.238928182823,116.94185180068,117.941209934246,118.940568067812,
119.939926201378,120.939284334944,121.93864246851,122.522113490002),
 .UNSPECIFIED.);
#986=B_SPLINE_CURVE_WITH_KNOTS('',3,(#42529,#42530,#42531,#42532,#42533,
#42534,#42535,#42536,#42537,#42538),.UNSPECIFIED.,.F.,.F.,(4,1,1,1,1,1,
1,4),(116.238928182823,116.91239571535,117.911753848916,118.911111982482,
119.910470116048,120.909828249614,121.90918638318,122.522113490003),
 .UNSPECIFIED.);
#987=B_SPLINE_CURVE_WITH_KNOTS('',3,(#42543,#42544,#42545,#42546,#42547,
#42548,#42549,#42550,#42551,#42552),.UNSPECIFIED.,.F.,.F.,(4,1,1,1,1,1,
1,4),(109.955742875643,110.945702999284,111.94506113285,112.944419266416,
113.943777399982,114.943135533548,115.942493667114,116.238928182823),
 .UNSPECIFIED.);
#988=B_SPLINE_CURVE_WITH_KNOTS('',3,(#42553,#42554,#42555,#42556,#42557,
#42558,#42559,#42560,#42561,#42562),.UNSPECIFIED.,.F.,.F.,(4,1,1,1,1,1,
1,4),(109.955742875644,110.916246913954,111.91560504752,112.914963181086,
113.914321314652,114.913679448218,115.913037581784,116.238928182823),
 .UNSPECIFIED.);
#989=B_SPLINE_CURVE_WITH_KNOTS('',3,(#42567,#42568,#42569,#42570,#42571,
#42572,#42573,#42574,#42575,#42576,#42577),.UNSPECIFIED.,.F.,.F.,(4,1,1,
1,1,1,1,1,4),(103.672557568464,103.950196064322,104.949554197888,105.948912331454,
106.94827046502,107.947628598586,108.946986732152,109.946344865718,109.955742875643),
 .UNSPECIFIED.);
#990=B_SPLINE_CURVE_WITH_KNOTS('',3,(#42578,#42579,#42580,#42581,#42582,
#42583,#42584,#42585,#42586,#42587,#42588),.UNSPECIFIED.,.F.,.F.,(4,1,1,
1,1,1,1,1,4),(103.672557568464,103.920739978991,104.920098112557,105.919456246123,
106.918814379689,107.918172513255,108.917530646822,109.916888780388,109.955742875644),
 .UNSPECIFIED.);
#991=B_SPLINE_CURVE_WITH_KNOTS('',3,(#42593,#42594,#42595,#42596,#42597,
#42598,#42599,#42600,#42601,#42602),.UNSPECIFIED.,.F.,.F.,(4,1,1,1,1,1,
1,4),(97.3893722612841,97.9540472629253,98.9534053964914,99.9527635300574,
100.952121663623,101.95147979719,102.950837930756,103.672557568464),
 .UNSPECIFIED.);
#992=B_SPLINE_CURVE_WITH_KNOTS('',3,(#42603,#42604,#42605,#42606,#42607,
#42608,#42609,#42610,#42611,#42612),.UNSPECIFIED.,.F.,.F.,(4,1,1,1,1,1,
1,4),(97.3893722612845,97.924591177595,98.9239493111611,99.9233074447271,
100.922665578293,101.922023711859,102.921381845425,103.672557568464),
 .UNSPECIFIED.);
#993=B_SPLINE_CURVE_WITH_KNOTS('',3,(#42617,#42618,#42619,#42620,#42621,
#42622,#42623,#42624,#42625,#42626),.UNSPECIFIED.,.F.,.F.,(4,1,1,1,1,1,
1,4),(91.1061869541045,91.9578984615291,92.9572565950951,93.9566147286612,
94.9559728622272,95.9553309957932,96.9546891293593,97.3893722612841),
 .UNSPECIFIED.);
#994=B_SPLINE_CURVE_WITH_KNOTS('',3,(#42627,#42628,#42629,#42630,#42631,
#42632,#42633,#42634,#42635,#42636),.UNSPECIFIED.,.F.,.F.,(4,1,1,1,1,1,
1,4),(91.1061869541048,91.9284423761987,92.9278005097648,93.9271586433308,
94.9265167768969,95.9258749104629,96.925233044029,97.3893722612845),
 .UNSPECIFIED.);
#995=B_SPLINE_CURVE_WITH_KNOTS('',3,(#42641,#42642,#42643,#42644,#42645,
#42646,#42647,#42648,#42649,#42650,#42651),.UNSPECIFIED.,.F.,.F.,(4,1,1,
1,1,1,1,1,4),(84.8230016469249,84.9623915265667,85.9617496601328,86.9611077936988,
87.9604659272649,88.9598240608309,89.959182194397,90.958540327963,91.1061869541045),
 .UNSPECIFIED.);
#996=B_SPLINE_CURVE_WITH_KNOTS('',3,(#42652,#42653,#42654,#42655,#42656,
#42657,#42658,#42659,#42660,#42661,#42662),.UNSPECIFIED.,.F.,.F.,(4,1,1,
1,1,1,1,1,4),(84.8230016469253,84.9329354412364,85.9322935748025,86.9316517083685,
87.9310098419346,88.9303679755006,89.9297261090666,90.9290842426327,91.1061869541048),
 .UNSPECIFIED.);
#997=B_SPLINE_CURVE_WITH_KNOTS('',3,(#42667,#42668,#42669,#42670,#42671,
#42672,#42673,#42674,#42675,#42676),.UNSPECIFIED.,.F.,.F.,(4,1,1,1,1,1,
1,4),(78.5398163397454,78.9662427251705,79.9656008587365,80.9649589923026,
81.9643171258686,82.9636752594347,83.9630333930007,84.8230016469249),
 .UNSPECIFIED.);
#998=B_SPLINE_CURVE_WITH_KNOTS('',3,(#42677,#42678,#42679,#42680,#42681,
#42682,#42683,#42684,#42685,#42686),.UNSPECIFIED.,.F.,.F.,(4,1,1,1,1,1,
1,4),(78.5398163397457,78.9367866398401,79.9361447734062,80.9355029069722,
81.9348610405383,82.9342191741043,83.9335773076704,84.8230016469253),
 .UNSPECIFIED.);
#999=B_SPLINE_CURVE_WITH_KNOTS('',3,(#42691,#42692,#42693,#42694,#42695,
#42696,#42697,#42698,#42699,#42700),.UNSPECIFIED.,.F.,.F.,(4,1,1,1,1,1,
1,4),(72.2566310325658,72.9700939237742,73.9694520573402,74.9688101909063,
75.9681683244723,76.9675264580384,77.9668845916044,78.5398163397454),
 .UNSPECIFIED.);
#1000=B_SPLINE_CURVE_WITH_KNOTS('',3,(#42701,#42702,#42703,#42704,#42705,
#42706,#42707,#42708,#42709,#42710),.UNSPECIFIED.,.F.,.F.,(4,1,1,1,1,1,
1,4),(72.2566310325661,72.9406378384438,73.9399959720099,74.9393541055759,
75.938712239142,76.938070372708,77.9374285062741,78.5398163397457),
 .UNSPECIFIED.);
#1001=B_SPLINE_CURVE_WITH_KNOTS('',3,(#42715,#42716,#42717,#42718,#42719,
#42720,#42721,#42722,#42723,#42724,#42725),.UNSPECIFIED.,.F.,.F.,(4,1,1,
1,1,1,1,1,4),(65.9734457253862,65.9745869888119,66.9739451223779,67.9733032559439,
68.97266138951,69.972019523076,70.9713776566421,71.9707357902081,72.2566310325658),
 .UNSPECIFIED.);
#1002=B_SPLINE_CURVE_WITH_KNOTS('',3,(#42726,#42727,#42728,#42729,#42730,
#42731,#42732,#42733,#42734,#42735),.UNSPECIFIED.,.F.,.F.,(4,1,1,1,1,1,
1,4),(65.9734457253865,66.9444890370476,67.9438471706136,68.9432053041797,
69.9425634377457,70.9419215713118,71.9412797048778,72.2566310325661),
 .UNSPECIFIED.);
#1003=B_SPLINE_CURVE_WITH_KNOTS('',3,(#42740,#42741,#42742,#42743,#42744,
#42745,#42746,#42747,#42748,#42749,#42750,#42751),.UNSPECIFIED.,.F.,.F.,
(4,1,1,1,1,1,1,1,1,4),(59.6902604182066,59.9784381874156,60.4781172541986,
60.9777963209816,61.4774753877646,61.9771544545477,62.9765125881137,63.9758707216798,
64.9752288552458,65.9734457253862),.UNSPECIFIED.);
#1004=B_SPLINE_CURVE_WITH_KNOTS('',3,(#42752,#42753,#42754,#42755,#42756,
#42757,#42758,#42759,#42760,#42761,#42762),.UNSPECIFIED.,.F.,.F.,(4,1,1,
1,1,1,1,1,4),(59.6902604182069,59.9489821020852,60.9483402356513,61.9476983692173,
62.9470565027834,63.9464146363494,64.9457727699155,65.9451309034815,65.9734457253865),
 .UNSPECIFIED.);
#1005=B_SPLINE_CURVE_WITH_KNOTS('',3,(#42767,#42768,#42769,#42770,#42771,
#42772,#42773,#42774,#42775,#42776,#42777,#42778,#42779,#42780,#42781,#42782,
#42783),.UNSPECIFIED.,.F.,.F.,(4,1,1,1,1,1,1,1,1,1,1,1,1,1,4),(53.407075111027,
53.4826103192363,53.9822893860193,54.4819684528023,54.9816475195853,55.4813265863684,
55.9810056531514,56.4806847199344,56.9803637867174,57.4800428535005,57.9797219202835,
58.4794009870665,58.9790800538495,59.4787591206325,59.6902604182066),
 .UNSPECIFIED.);
#1006=B_SPLINE_CURVE_WITH_KNOTS('',3,(#42784,#42785,#42786,#42787,#42788,
#42789,#42790,#42791,#42792,#42793,#42794,#42795,#42796,#42797,#42798,#42799),
 .UNSPECIFIED.,.F.,.F.,(4,1,1,1,1,1,1,1,1,1,1,1,1,4),(53.4070751110273,
53.4531542339059,53.9528333006889,54.452512367472,54.952191434255,55.451870501038,
55.951549567821,56.4512286346041,56.9509077013871,57.4505867681701,57.9502658349531,
58.4499449017362,58.9496239685192,59.6902604182069),.UNSPECIFIED.);
#1007=B_SPLINE_CURVE_WITH_KNOTS('',3,(#42804,#42805,#42806,#42807,#42808,
#42809,#42810,#42811,#42812,#42813,#42814,#42815,#42816,#42817,#42818,#42819),
 .UNSPECIFIED.,.F.,.F.,(4,1,1,1,1,1,1,1,1,1,1,1,1,4),(47.1238898038474,
47.48646151784,47.986140584623,48.485819651406,48.9854987181891,49.4851777849721,
49.9848568517551,50.4845359185381,50.9842149853212,51.4838940521042,51.9835731188872,
52.4832521856702,52.9829312524532,53.407075111027),.UNSPECIFIED.);
#1008=B_SPLINE_CURVE_WITH_KNOTS('',3,(#42820,#42821,#42822,#42823,#42824,
#42825,#42826,#42827,#42828,#42829,#42830,#42831,#42832,#42833,#42834,#42835),
 .UNSPECIFIED.,.F.,.F.,(4,1,1,1,1,1,1,1,1,1,1,1,1,4),(47.1238898038477,
47.4570054325096,47.9566844992927,48.4563635660757,48.9560426328587,49.4557216996417,
49.9554007664248,50.4550798332078,50.9547588999908,51.4544379667738,51.9541170335568,
52.4537961003399,52.9534751671229,53.4070751110273),.UNSPECIFIED.);
#1009=B_SPLINE_CURVE_WITH_KNOTS('',3,(#42840,#42841,#42842,#42843,#42844,
#42845,#42846,#42847,#42848,#42849,#42850,#42851,#42852,#42853,#42854,#42855,
#42856),.UNSPECIFIED.,.F.,.F.,(4,1,1,1,1,1,1,1,1,1,1,1,1,1,4),(40.8407044966678,
40.9906336496607,41.4903127164437,41.9899917832267,42.4896708500098,42.9893499167928,
43.4890289835758,43.9887080503588,44.4883871171419,44.9880661839249,45.4877452507079,
45.9874243174909,46.4871033842739,46.986782451057,47.1238898038474),
 .UNSPECIFIED.);
#1010=B_SPLINE_CURVE_WITH_KNOTS('',3,(#42857,#42858,#42859,#42860,#42861,
#42862,#42863,#42864,#42865,#42866,#42867,#42868,#42869,#42870,#42871,#42872,
#42873),.UNSPECIFIED.,.F.,.F.,(4,1,1,1,1,1,1,1,1,1,1,1,1,1,4),(40.8407044966681,
40.9611775643303,41.4608566311134,41.9605356978964,42.4602147646794,42.9598938314624,
43.4595728982454,43.9592519650285,44.4589310318115,44.9586100985945,45.4582891653775,
45.9579682321606,46.4576472989436,46.9573263657266,47.1238898038477),
 .UNSPECIFIED.);
#1011=B_SPLINE_CURVE_WITH_KNOTS('',3,(#42878,#42879,#42880,#42881,#42882,
#42883,#42884,#42885,#42886,#42887,#42888,#42889,#42890,#42891,#42892,#42893),
 .UNSPECIFIED.,.F.,.F.,(4,1,1,1,1,1,1,1,1,1,1,1,1,4),(34.5575191894882,
34.9944848482644,35.4941639150474,35.9938429818305,36.4935220486135,36.9932011153965,
37.4928801821795,37.9925592489626,38.4922383157456,38.9919173825286,39.4915964493116,
39.9912755160946,40.4909545828777,40.8407044966678),.UNSPECIFIED.);
#1012=B_SPLINE_CURVE_WITH_KNOTS('',3,(#42894,#42895,#42896,#42897,#42898,
#42899,#42900,#42901,#42902,#42903,#42904,#42905,#42906,#42907,#42908,#42909),
 .UNSPECIFIED.,.F.,.F.,(4,1,1,1,1,1,1,1,1,1,1,1,1,4),(34.5575191894886,
34.965028762934,35.4647078297171,35.9643868965001,36.4640659632831,36.9637450300661,
37.4634240968492,37.9631031636322,38.4627822304152,38.9624612971982,39.4621403639813,
39.9618194307643,40.4614984975473,40.8407044966681),.UNSPECIFIED.);
#1013=B_SPLINE_CURVE_WITH_KNOTS('',3,(#42914,#42915,#42916,#42917,#42918,
#42919,#42920,#42921,#42922,#42923,#42924,#42925,#42926,#42927,#42928,#42929,
#42930),.UNSPECIFIED.,.F.,.F.,(4,1,1,1,1,1,1,1,1,1,1,1,1,1,4),(28.2743338823086,
28.4986569800851,28.9983360468681,29.4980151136512,29.9976941804342,30.4973732472172,
30.9970523140002,31.4967313807832,31.9964104475663,32.4960895143493,32.9957685811323,
33.4954476479153,33.9951267146984,34.4948057814814,34.5575191894882),
 .UNSPECIFIED.);
#1014=B_SPLINE_CURVE_WITH_KNOTS('',3,(#42931,#42932,#42933,#42934,#42935,
#42936,#42937,#42938,#42939,#42940,#42941,#42942,#42943,#42944,#42945,#42946,
#42947),.UNSPECIFIED.,.F.,.F.,(4,1,1,1,1,1,1,1,1,1,1,1,1,1,4),(28.2743338823089,
28.4692008947547,28.9688799615378,29.4685590283208,29.9682380951038,30.4679171618868,
30.9675962286699,31.4672752954529,31.9669543622359,32.4666334290189,32.966312495802,
33.465991562585,33.965670629368,34.465349696151,34.5575191894886),
 .UNSPECIFIED.);
#1015=B_SPLINE_CURVE_WITH_KNOTS('',3,(#42952,#42953,#42954,#42955,#42956,
#42957,#42958,#42959,#42960,#42961,#42962,#42963,#42964,#42965,#42966,#42967,
#42968),.UNSPECIFIED.,.F.,.F.,(4,1,1,1,1,1,1,1,1,1,1,1,1,1,4),(21.991148575129,
22.0028291119058,22.5025081786888,23.0021872454719,23.5018663122549,24.0015453790379,
24.5012244458209,25.0009035126039,25.500582579387,26.00026164617,26.499940712953,
26.999619779736,27.4992988465191,27.9989779133021,28.2743338823086),
 .UNSPECIFIED.);
#1016=B_SPLINE_CURVE_WITH_KNOTS('',3,(#42969,#42970,#42971,#42972,#42973,
#42974,#42975,#42976,#42977,#42978,#42979,#42980,#42981,#42982,#42983,#42984),
 .UNSPECIFIED.,.F.,.F.,(4,1,1,1,1,1,1,1,1,1,1,1,1,4),(21.9911485751294,
22.4730520933585,22.9727311601415,23.4724102269245,23.9720892937075,24.4717683604905,
24.9714474272736,25.4711264940566,25.9708055608396,26.4704846276226,26.9701636944057,
27.4698427611887,27.9695218279717,28.2743338823089),.UNSPECIFIED.);
#1017=B_SPLINE_CURVE_WITH_KNOTS('',3,(#42989,#42990,#42991,#42992,#42993,
#42994,#42995,#42996,#42997,#42998,#42999,#43000,#43001,#43002,#43003,#43004),
 .UNSPECIFIED.,.F.,.F.,(4,1,1,1,1,1,1,1,1,1,1,1,1,4),(15.7079632679495,
16.0066803105095,16.5063593772925,17.0060384440756,17.5057175108586,18.0053965776416,
18.5050756444246,19.0047547112077,19.5044337779907,20.0041128447737,20.5037919115567,
21.0034709783398,21.5031500451228,21.991148575129),.UNSPECIFIED.);
#1018=B_SPLINE_CURVE_WITH_KNOTS('',3,(#43005,#43006,#43007,#43008,#43009,
#43010,#43011,#43012,#43013,#43014,#43015,#43016,#43017,#43018,#43019,#43020,
#43021),.UNSPECIFIED.,.F.,.F.,(4,1,1,1,1,1,1,1,1,1,1,1,1,1,4),(15.7079632679498,
15.9772242251791,16.4769032919622,16.9765823587452,17.4762614255282,17.9759404923112,
18.4756195590943,18.9752986258773,19.4749776926603,19.9746567594433,20.4743358262264,
20.9740148930094,21.4736939597924,21.9733730265754,21.9911485751294),
 .UNSPECIFIED.);
#1019=B_SPLINE_CURVE_WITH_KNOTS('',3,(#43026,#43027,#43028,#43029,#43030,
#43031,#43032,#43033,#43034,#43035,#43036,#43037,#43038,#43039,#43040,#43041,
#43042,#43043,#43044,#43045,#43046,#43047,#43048,#43049,#43050,#43051,#43052,
#43053,#43054,#43055,#43056,#43057,#43058,#43059,#43060,#43061,#43062),
 .UNSPECIFIED.,.F.,.F.,(4,3,3,3,3,3,3,3,3,3,3,3,4),(0.,0.000373494560508806,
0.0620760815771024,0.112839239637108,0.153038169722591,0.175804963675793,
0.247183842626883,0.319084136954533,0.344742425233931,0.363606980156396,
0.439518700737557,0.51795432283266,0.534785019937482),.UNSPECIFIED.);
#1020=B_SPLINE_CURVE_WITH_KNOTS('',3,(#43064,#43065,#43066,#43067,#43068,
#43069,#43070,#43071,#43072,#43073,#43074,#43075,#43076,#43077,#43078,#43079,
#43080,#43081,#43082,#43083,#43084,#43085,#43086,#43087,#43088,#43089,#43090,
#43091,#43092,#43093,#43094,#43095,#43096,#43097,#43098,#43099,#43100),
 .UNSPECIFIED.,.F.,.F.,(4,3,3,3,3,3,3,3,3,3,3,3,4),(0.,0.000511892384038064,
0.078754853834616,0.155070466132989,0.20164291816609,0.227017770490094,
0.290460834304131,0.352619921814331,0.383703668213755,0.403796492255862,
0.466621120797767,0.52704524650008,0.539097184344933),.UNSPECIFIED.);
#1021=B_SPLINE_CURVE_WITH_KNOTS('',3,(#45100,#45101,#45102,#45103,#45104,
#45105,#45106,#45107,#45108,#45109,#45110,#45111,#45112,#45113,#45114,#45115,
#45116,#45117,#45118,#45119,#45120,#45121,#45122,#45123,#45124,#45125,#45126,
#45127,#45128,#45129,#45130,#45131,#45132,#45133,#45134,#45135,#45136,#45137,
#45138,#45139),.UNSPECIFIED.,.F.,.F.,(4,3,3,3,3,3,3,3,3,3,3,3,3,4),(-0.53478501993692,
-0.534277081309421,-0.456439695901019,-0.38064245929011,-0.348102919117109,
-0.328886681298388,-0.258595553176405,-0.246742105655551,-0.185056579241663,
-0.163339235199672,-0.143463957830519,-0.0808484674142256,-0.0206857924044652,
0.),.UNSPECIFIED.);
#1022=B_SPLINE_CURVE_WITH_KNOTS('',3,(#45140,#45141,#45142,#45143,#45144,
#45145,#45146,#45147,#45148,#45149,#45150,#45151,#45152,#45153,#45154,#45155,
#45156,#45157,#45158,#45159,#45160,#45161,#45162,#45163,#45164),
 .UNSPECIFIED.,.F.,.F.,(4,3,3,3,3,3,3,3,4),(390.000549715688,390.249351157541,
390.749030224325,391.248709291108,391.748388357891,392.248067424674,392.747746491457,
393.24742555824,393.746279249921),.UNSPECIFIED.);
#1023=B_SPLINE_CURVE_WITH_KNOTS('',3,(#45165,#45166,#45167,#45168,#45169,
#45170,#45171,#45172,#45173,#45174,#45175,#45176,#45177,#45178,#45179),
 .UNSPECIFIED.,.F.,.F.,(4,1,1,1,1,1,1,1,1,1,1,1,4),(9.98190079888485,10.4807544905659,
10.9804335573489,11.4801126241319,11.979791690915,12.479470757698,12.979149824481,
13.478828891264,13.9785079580471,14.4781870248301,14.9778660916131,15.4775451583961,
15.7079632679498),.UNSPECIFIED.);
#1024=B_SPLINE_CURVE_WITH_KNOTS('',3,(#45181,#45182,#45183,#45184,#45185,
#45186,#45187,#45188,#45189,#45190,#45191),.UNSPECIFIED.,.F.,.F.,(4,1,1,
1,1,1,1,1,4),(12.0092477762453,12.5089268430284,13.0086059098114,13.5082849765944,
14.0079640433774,14.5076431101605,15.0073221769435,15.5070012437265,15.7079632679495),
 .UNSPECIFIED.);
#1025=B_SPLINE_CURVE_WITH_KNOTS('',3,(#47185,#47186,#47187,#47188,#47189,
#47190,#47191,#47192,#47193,#47194,#47195,#47196,#47197,#47198,#47199,#47200,
#47201,#47202,#47203,#47204,#47205,#47206,#47207,#47208,#47209,#47210,#47211,
#47212,#47213,#47214,#47215,#47216,#47217,#47218,#47219,#47220,#47221,#47222,
#47223,#47224),.UNSPECIFIED.,.F.,.F.,(4,3,3,3,3,3,3,3,3,3,3,3,3,4),(-0.539097184344981,
-0.538720824057998,-0.476544551511477,-0.429912347101587,-0.401091234701428,
-0.381803774975435,-0.313681369269712,-0.290015733871917,-0.24230273417063,
-0.214804629165427,-0.192593514291413,-0.116696500404398,-0.0381316372362206,
0.),.UNSPECIFIED.);
#1026=B_SPLINE_CURVE_WITH_KNOTS('',3,(#47225,#47226,#47227,#47228,#47229,
#47230,#47231,#47232,#47233,#47234),.UNSPECIFIED.,.F.,.F.,(4,3,3,4),(-394.746462758588,
-394.246783691805,-393.747104625022,-393.256204536838),.UNSPECIFIED.);
#1536=SHAPE_REPRESENTATION_RELATIONSHIP('SRR','None',#63389,#1619);
#1619=ADVANCED_BREP_SHAPE_REPRESENTATION('',(#1827),#62926);
#1717=STYLED_ITEM('',(#63919),#1827);
#1827=MANIFOLD_SOLID_BREP('Body1',#23014);
#2061=FACE_BOUND('',#4909,.T.);
#2062=FACE_BOUND('',#4921,.T.);
#2063=FACE_BOUND('',#4924,.T.);
#2064=FACE_BOUND('',#4927,.T.);
#2517=PLANE('',#25000);
#2518=PLANE('',#25005);
#2519=PLANE('',#25007);
#2520=PLANE('',#25008);
#2521=PLANE('',#25010);
#2522=PLANE('',#25011);
#2523=PLANE('',#25012);
#2524=PLANE('',#25017);
#2525=PLANE('',#25018);
#2526=PLANE('',#25023);
#3294=FACE_OUTER_BOUND('',#4782,.T.);
#3295=FACE_OUTER_BOUND('',#4783,.T.);
#3296=FACE_OUTER_BOUND('',#4784,.T.);
#3297=FACE_OUTER_BOUND('',#4785,.T.);
#3298=FACE_OUTER_BOUND('',#4786,.T.);
#3299=FACE_OUTER_BOUND('',#4787,.T.);
#3300=FACE_OUTER_BOUND('',#4788,.T.);
#3301=FACE_OUTER_BOUND('',#4789,.T.);
#3302=FACE_OUTER_BOUND('',#4790,.T.);
#3303=FACE_OUTER_BOUND('',#4791,.T.);
#3304=FACE_OUTER_BOUND('',#4792,.T.);
#3305=FACE_OUTER_BOUND('',#4793,.T.);
#3306=FACE_OUTER_BOUND('',#4794,.T.);
#3307=FACE_OUTER_BOUND('',#4795,.T.);
#3308=FACE_OUTER_BOUND('',#4796,.T.);
#3309=FACE_OUTER_BOUND('',#4797,.T.);
#3310=FACE_OUTER_BOUND('',#4798,.T.);
#3311=FACE_OUTER_BOUND('',#4799,.T.);
#3312=FACE_OUTER_BOUND('',#4800,.T.);
#3313=FACE_OUTER_BOUND('',#4801,.T.);
#3314=FACE_OUTER_BOUND('',#4802,.T.);
#3315=FACE_OUTER_BOUND('',#4803,.T.);
#3316=FACE_OUTER_BOUND('',#4804,.T.);
#3317=FACE_OUTER_BOUND('',#4805,.T.);
#3318=FACE_OUTER_BOUND('',#4806,.T.);
#3319=FACE_OUTER_BOUND('',#4807,.T.);
#3320=FACE_OUTER_BOUND('',#4808,.T.);
#3321=FACE_OUTER_BOUND('',#4809,.T.);
#3322=FACE_OUTER_BOUND('',#4810,.T.);
#3323=FACE_OUTER_BOUND('',#4811,.T.);
#3324=FACE_OUTER_BOUND('',#4812,.T.);
#3325=FACE_OUTER_BOUND('',#4813,.T.);
#3326=FACE_OUTER_BOUND('',#4814,.T.);
#3327=FACE_OUTER_BOUND('',#4815,.T.);
#3328=FACE_OUTER_BOUND('',#4816,.T.);
#3329=FACE_OUTER_BOUND('',#4817,.T.);
#3330=FACE_OUTER_BOUND('',#4818,.T.);
#3331=FACE_OUTER_BOUND('',#4819,.T.);
#3332=FACE_OUTER_BOUND('',#4820,.T.);
#3333=FACE_OUTER_BOUND('',#4821,.T.);
#3334=FACE_OUTER_BOUND('',#4822,.T.);
#3335=FACE_OUTER_BOUND('',#4823,.T.);
#3336=FACE_OUTER_BOUND('',#4824,.T.);
#3337=FACE_OUTER_BOUND('',#4825,.T.);
#3338=FACE_OUTER_BOUND('',#4826,.T.);
#3339=FACE_OUTER_BOUND('',#4827,.T.);
#3340=FACE_OUTER_BOUND('',#4828,.T.);
#3341=FACE_OUTER_BOUND('',#4829,.T.);
#3342=FACE_OUTER_BOUND('',#4830,.T.);
#3343=FACE_OUTER_BOUND('',#4831,.T.);
#3344=FACE_OUTER_BOUND('',#4832,.T.);
#3345=FACE_OUTER_BOUND('',#4833,.T.);
#3346=FACE_OUTER_BOUND('',#4834,.T.);
#3347=FACE_OUTER_BOUND('',#4835,.T.);
#3348=FACE_OUTER_BOUND('',#4836,.T.);
#3349=FACE_OUTER_BOUND('',#4837,.T.);
#3350=FACE_OUTER_BOUND('',#4838,.T.);
#3351=FACE_OUTER_BOUND('',#4839,.T.);
#3352=FACE_OUTER_BOUND('',#4840,.T.);
#3353=FACE_OUTER_BOUND('',#4841,.T.);
#3354=FACE_OUTER_BOUND('',#4842,.T.);
#3355=FACE_OUTER_BOUND('',#4843,.T.);
#3356=FACE_OUTER_BOUND('',#4844,.T.);
#3357=FACE_OUTER_BOUND('',#4845,.T.);
#3358=FACE_OUTER_BOUND('',#4846,.T.);
#3359=FACE_OUTER_BOUND('',#4847,.T.);
#3360=FACE_OUTER_BOUND('',#4848,.T.);
#3361=FACE_OUTER_BOUND('',#4849,.T.);
#3362=FACE_OUTER_BOUND('',#4850,.T.);
#3363=FACE_OUTER_BOUND('',#4851,.T.);
#3364=FACE_OUTER_BOUND('',#4852,.T.);
#3365=FACE_OUTER_BOUND('',#4853,.T.);
#3366=FACE_OUTER_BOUND('',#4854,.T.);
#3367=FACE_OUTER_BOUND('',#4855,.T.);
#3368=FACE_OUTER_BOUND('',#4856,.T.);
#3369=FACE_OUTER_BOUND('',#4857,.T.);
#3370=FACE_OUTER_BOUND('',#4858,.T.);
#3371=FACE_OUTER_BOUND('',#4859,.T.);
#3372=FACE_OUTER_BOUND('',#4860,.T.);
#3373=FACE_OUTER_BOUND('',#4861,.T.);
#3374=FACE_OUTER_BOUND('',#4862,.T.);
#3375=FACE_OUTER_BOUND('',#4863,.T.);
#3376=FACE_OUTER_BOUND('',#4864,.T.);
#3377=FACE_OUTER_BOUND('',#4865,.T.);
#3378=FACE_OUTER_BOUND('',#4866,.T.);
#3379=FACE_OUTER_BOUND('',#4867,.T.);
#3380=FACE_OUTER_BOUND('',#4868,.T.);
#3381=FACE_OUTER_BOUND('',#4869,.T.);
#3382=FACE_OUTER_BOUND('',#4870,.T.);
#3383=FACE_OUTER_BOUND('',#4871,.T.);
#3384=FACE_OUTER_BOUND('',#4872,.T.);
#3385=FACE_OUTER_BOUND('',#4873,.T.);
#3386=FACE_OUTER_BOUND('',#4874,.T.);
#3387=FACE_OUTER_BOUND('',#4875,.T.);
#3388=FACE_OUTER_BOUND('',#4876,.T.);
#3389=FACE_OUTER_BOUND('',#4877,.T.);
#3390=FACE_OUTER_BOUND('',#4878,.T.);
#3391=FACE_OUTER_BOUND('',#4879,.T.);
#3392=FACE_OUTER_BOUND('',#4880,.T.);
#3393=FACE_OUTER_BOUND('',#4881,.T.);
#3394=FACE_OUTER_BOUND('',#4882,.T.);
#3395=FACE_OUTER_BOUND('',#4883,.T.);
#3396=FACE_OUTER_BOUND('',#4884,.T.);
#3397=FACE_OUTER_BOUND('',#4885,.T.);
#3398=FACE_OUTER_BOUND('',#4886,.T.);
#3399=FACE_OUTER_BOUND('',#4887,.T.);
#3400=FACE_OUTER_BOUND('',#4888,.T.);
#3401=FACE_OUTER_BOUND('',#4889,.T.);
#3402=FACE_OUTER_BOUND('',#4890,.T.);
#3403=FACE_OUTER_BOUND('',#4891,.T.);
#3404=FACE_OUTER_BOUND('',#4892,.T.);
#3405=FACE_OUTER_BOUND('',#4893,.T.);
#3406=FACE_OUTER_BOUND('',#4894,.T.);
#3407=FACE_OUTER_BOUND('',#4895,.T.);
#3408=FACE_OUTER_BOUND('',#4896,.T.);
#3409=FACE_OUTER_BOUND('',#4897,.T.);
#3410=FACE_OUTER_BOUND('',#4898,.T.);
#3411=FACE_OUTER_BOUND('',#4899,.T.);
#3412=FACE_OUTER_BOUND('',#4900,.T.);
#3413=FACE_OUTER_BOUND('',#4901,.T.);
#3414=FACE_OUTER_BOUND('',#4902,.T.);
#3415=FACE_OUTER_BOUND('',#4903,.T.);
#3416=FACE_OUTER_BOUND('',#4904,.T.);
#3417=FACE_OUTER_BOUND('',#4905,.T.);
#3418=FACE_OUTER_BOUND('',#4906,.T.);
#3419=FACE_OUTER_BOUND('',#4907,.T.);
#3420=FACE_OUTER_BOUND('',#4908,.T.);
#3421=FACE_OUTER_BOUND('',#4910,.T.);
#3422=FACE_OUTER_BOUND('',#4911,.T.);
#3423=FACE_OUTER_BOUND('',#4912,.T.);
#3424=FACE_OUTER_BOUND('',#4913,.T.);
#3425=FACE_OUTER_BOUND('',#4914,.T.);
#3426=FACE_OUTER_BOUND('',#4915,.T.);
#3427=FACE_OUTER_BOUND('',#4916,.T.);
#3428=FACE_OUTER_BOUND('',#4917,.T.);
#3429=FACE_OUTER_BOUND('',#4918,.T.);
#3430=FACE_OUTER_BOUND('',#4919,.T.);
#3431=FACE_OUTER_BOUND('',#4920,.T.);
#3432=FACE_OUTER_BOUND('',#4922,.T.);
#3433=FACE_OUTER_BOUND('',#4923,.T.);
#3434=FACE_OUTER_BOUND('',#4925,.T.);
#3435=FACE_OUTER_BOUND('',#4926,.T.);
#3436=FACE_OUTER_BOUND('',#4928,.T.);
#4782=EDGE_LOOP('',(#16798,#16799,#16800,#16801));
#4783=EDGE_LOOP('',(#16802,#16803,#16804,#16805));
#4784=EDGE_LOOP('',(#16806,#16807,#16808,#16809));
#4785=EDGE_LOOP('',(#16810,#16811,#16812,#16813));
#4786=EDGE_LOOP('',(#16814,#16815,#16816,#16817));
#4787=EDGE_LOOP('',(#16818,#16819,#16820,#16821));
#4788=EDGE_LOOP('',(#16822,#16823,#16824,#16825));
#4789=EDGE_LOOP('',(#16826,#16827,#16828,#16829));
#4790=EDGE_LOOP('',(#16830,#16831,#16832,#16833));
#4791=EDGE_LOOP('',(#16834,#16835,#16836,#16837));
#4792=EDGE_LOOP('',(#16838,#16839,#16840,#16841));
#4793=EDGE_LOOP('',(#16842,#16843,#16844,#16845));
#4794=EDGE_LOOP('',(#16846,#16847,#16848,#16849));
#4795=EDGE_LOOP('',(#16850,#16851,#16852,#16853));
#4796=EDGE_LOOP('',(#16854,#16855,#16856,#16857));
#4797=EDGE_LOOP('',(#16858,#16859,#16860,#16861));
#4798=EDGE_LOOP('',(#16862,#16863,#16864,#16865));
#4799=EDGE_LOOP('',(#16866,#16867,#16868,#16869));
#4800=EDGE_LOOP('',(#16870,#16871,#16872,#16873));
#4801=EDGE_LOOP('',(#16874,#16875,#16876,#16877));
#4802=EDGE_LOOP('',(#16878,#16879,#16880,#16881));
#4803=EDGE_LOOP('',(#16882,#16883,#16884,#16885));
#4804=EDGE_LOOP('',(#16886,#16887,#16888,#16889));
#4805=EDGE_LOOP('',(#16890,#16891,#16892,#16893));
#4806=EDGE_LOOP('',(#16894,#16895,#16896,#16897));
#4807=EDGE_LOOP('',(#16898,#16899,#16900,#16901));
#4808=EDGE_LOOP('',(#16902,#16903,#16904,#16905));
#4809=EDGE_LOOP('',(#16906,#16907,#16908,#16909));
#4810=EDGE_LOOP('',(#16910,#16911,#16912,#16913));
#4811=EDGE_LOOP('',(#16914,#16915,#16916,#16917));
#4812=EDGE_LOOP('',(#16918,#16919,#16920,#16921));
#4813=EDGE_LOOP('',(#16922,#16923,#16924,#16925));
#4814=EDGE_LOOP('',(#16926,#16927,#16928,#16929));
#4815=EDGE_LOOP('',(#16930,#16931,#16932,#16933));
#4816=EDGE_LOOP('',(#16934,#16935,#16936,#16937));
#4817=EDGE_LOOP('',(#16938,#16939,#16940,#16941));
#4818=EDGE_LOOP('',(#16942,#16943,#16944,#16945));
#4819=EDGE_LOOP('',(#16946,#16947,#16948,#16949));
#4820=EDGE_LOOP('',(#16950,#16951,#16952,#16953));
#4821=EDGE_LOOP('',(#16954,#16955,#16956,#16957));
#4822=EDGE_LOOP('',(#16958,#16959,#16960,#16961));
#4823=EDGE_LOOP('',(#16962,#16963,#16964,#16965));
#4824=EDGE_LOOP('',(#16966,#16967,#16968,#16969));
#4825=EDGE_LOOP('',(#16970,#16971,#16972,#16973));
#4826=EDGE_LOOP('',(#16974,#16975,#16976,#16977));
#4827=EDGE_LOOP('',(#16978,#16979,#16980,#16981));
#4828=EDGE_LOOP('',(#16982,#16983,#16984,#16985));
#4829=EDGE_LOOP('',(#16986,#16987,#16988,#16989));
#4830=EDGE_LOOP('',(#16990,#16991,#16992,#16993));
#4831=EDGE_LOOP('',(#16994,#16995,#16996,#16997));
#4832=EDGE_LOOP('',(#16998,#16999,#17000,#17001));
#4833=EDGE_LOOP('',(#17002,#17003,#17004,#17005));
#4834=EDGE_LOOP('',(#17006,#17007,#17008,#17009));
#4835=EDGE_LOOP('',(#17010,#17011,#17012,#17013));
#4836=EDGE_LOOP('',(#17014,#17015,#17016,#17017));
#4837=EDGE_LOOP('',(#17018,#17019,#17020,#17021));
#4838=EDGE_LOOP('',(#17022,#17023,#17024,#17025));
#4839=EDGE_LOOP('',(#17026,#17027,#17028,#17029));
#4840=EDGE_LOOP('',(#17030,#17031,#17032,#17033));
#4841=EDGE_LOOP('',(#17034,#17035,#17036,#17037));
#4842=EDGE_LOOP('',(#17038,#17039,#17040,#17041));
#4843=EDGE_LOOP('',(#17042,#17043,#17044,#17045));
#4844=EDGE_LOOP('',(#17046,#17047,#17048,#17049));
#4845=EDGE_LOOP('',(#17050,#17051,#17052));
#4846=EDGE_LOOP('',(#17053,#17054,#17055,#17056,#17057));
#4847=EDGE_LOOP('',(#17058,#17059,#17060,#17061));
#4848=EDGE_LOOP('',(#17062,#17063,#17064,#17065));
#4849=EDGE_LOOP('',(#17066,#17067,#17068,#17069));
#4850=EDGE_LOOP('',(#17070,#17071,#17072,#17073));
#4851=EDGE_LOOP('',(#17074,#17075,#17076,#17077));
#4852=EDGE_LOOP('',(#17078,#17079,#17080,#17081));
#4853=EDGE_LOOP('',(#17082,#17083,#17084,#17085));
#4854=EDGE_LOOP('',(#17086,#17087,#17088,#17089));
#4855=EDGE_LOOP('',(#17090,#17091,#17092,#17093));
#4856=EDGE_LOOP('',(#17094,#17095,#17096,#17097));
#4857=EDGE_LOOP('',(#17098,#17099,#17100,#17101));
#4858=EDGE_LOOP('',(#17102,#17103,#17104,#17105));
#4859=EDGE_LOOP('',(#17106,#17107,#17108,#17109));
#4860=EDGE_LOOP('',(#17110,#17111,#17112,#17113));
#4861=EDGE_LOOP('',(#17114,#17115,#17116,#17117));
#4862=EDGE_LOOP('',(#17118,#17119,#17120,#17121));
#4863=EDGE_LOOP('',(#17122,#17123,#17124,#17125));
#4864=EDGE_LOOP('',(#17126,#17127,#17128,#17129));
#4865=EDGE_LOOP('',(#17130,#17131,#17132,#17133));
#4866=EDGE_LOOP('',(#17134,#17135,#17136,#17137));
#4867=EDGE_LOOP('',(#17138,#17139,#17140,#17141));
#4868=EDGE_LOOP('',(#17142,#17143,#17144,#17145));
#4869=EDGE_LOOP('',(#17146,#17147,#17148,#17149));
#4870=EDGE_LOOP('',(#17150,#17151,#17152,#17153));
#4871=EDGE_LOOP('',(#17154,#17155,#17156,#17157));
#4872=EDGE_LOOP('',(#17158,#17159,#17160,#17161));
#4873=EDGE_LOOP('',(#17162,#17163,#17164,#17165));
#4874=EDGE_LOOP('',(#17166,#17167,#17168,#17169));
#4875=EDGE_LOOP('',(#17170,#17171,#17172,#17173));
#4876=EDGE_LOOP('',(#17174,#17175,#17176,#17177));
#4877=EDGE_LOOP('',(#17178,#17179,#17180,#17181));
#4878=EDGE_LOOP('',(#17182,#17183,#17184,#17185));
#4879=EDGE_LOOP('',(#17186,#17187,#17188,#17189));
#4880=EDGE_LOOP('',(#17190,#17191,#17192,#17193));
#4881=EDGE_LOOP('',(#17194,#17195,#17196,#17197));
#4882=EDGE_LOOP('',(#17198,#17199,#17200,#17201));
#4883=EDGE_LOOP('',(#17202,#17203,#17204,#17205));
#4884=EDGE_LOOP('',(#17206,#17207,#17208,#17209));
#4885=EDGE_LOOP('',(#17210,#17211,#17212,#17213));
#4886=EDGE_LOOP('',(#17214,#17215,#17216,#17217));
#4887=EDGE_LOOP('',(#17218,#17219,#17220,#17221));
#4888=EDGE_LOOP('',(#17222,#17223,#17224,#17225));
#4889=EDGE_LOOP('',(#17226,#17227,#17228,#17229));
#4890=EDGE_LOOP('',(#17230,#17231,#17232,#17233));
#4891=EDGE_LOOP('',(#17234,#17235,#17236,#17237));
#4892=EDGE_LOOP('',(#17238,#17239,#17240,#17241));
#4893=EDGE_LOOP('',(#17242,#17243,#17244,#17245));
#4894=EDGE_LOOP('',(#17246,#17247,#17248,#17249));
#4895=EDGE_LOOP('',(#17250,#17251,#17252,#17253));
#4896=EDGE_LOOP('',(#17254,#17255,#17256,#17257));
#4897=EDGE_LOOP('',(#17258,#17259,#17260,#17261));
#4898=EDGE_LOOP('',(#17262,#17263,#17264,#17265));
#4899=EDGE_LOOP('',(#17266,#17267,#17268,#17269));
#4900=EDGE_LOOP('',(#17270,#17271,#17272,#17273));
#4901=EDGE_LOOP('',(#17274,#17275,#17276,#17277));
#4902=EDGE_LOOP('',(#17278,#17279,#17280,#17281));
#4903=EDGE_LOOP('',(#17282,#17283,#17284,#17285));
#4904=EDGE_LOOP('',(#17286,#17287,#17288,#17289));
#4905=EDGE_LOOP('',(#17290,#17291,#17292,#17293));
#4906=EDGE_LOOP('',(#17294,#17295,#17296,#17297));
#4907=EDGE_LOOP('',(#17298,#17299,#17300,#17301));
#4908=EDGE_LOOP('',(#17302));
#4909=EDGE_LOOP('',(#17303,#17304,#17305,#17306));
#4910=EDGE_LOOP('',(#17307,#17308,#17309,#17310));
#4911=EDGE_LOOP('',(#17311));
#4912=EDGE_LOOP('',(#17312,#17313,#17314,#17315,#17316,#17317,#17318,#17319,
#17320,#17321,#17322,#17323,#17324,#17325,#17326,#17327,#17328,#17329,#17330,
#17331,#17332,#17333,#17334,#17335,#17336,#17337,#17338,#17339,#17340,#17341,
#17342,#17343,#17344,#17345,#17346,#17347,#17348,#17349,#17350,#17351,#17352,
#17353,#17354,#17355,#17356,#17357,#17358,#17359,#17360,#17361,#17362,#17363,
#17364,#17365,#17366,#17367,#17368,#17369,#17370,#17371,#17372,#17373,#17374,
#17375,#17376,#17377,#17378,#17379,#17380,#17381,#17382,#17383,#17384,#17385,
#17386,#17387,#17388,#17389,#17390,#17391,#17392,#17393,#17394,#17395,#17396,
#17397,#17398,#17399,#17400,#17401,#17402,#17403,#17404,#17405,#17406,#17407,
#17408,#17409,#17410,#17411,#17412,#17413,#17414,#17415,#17416,#17417,#17418,
#17419,#17420,#17421,#17422,#17423,#17424,#17425,#17426,#17427,#17428,#17429,
#17430,#17431,#17432,#17433,#17434,#17435,#17436,#17437,#17438,#17439,#17440));
#4913=EDGE_LOOP('',(#17441,#17442,#17443,#17444));
#4914=EDGE_LOOP('',(#17445,#17446,#17447,#17448,#17449,#17450,#17451,#17452,
#17453,#17454,#17455,#17456,#17457,#17458,#17459,#17460,#17461,#17462,#17463,
#17464,#17465,#17466,#17467,#17468,#17469,#17470,#17471,#17472,#17473,#17474,
#17475,#17476,#17477,#17478,#17479,#17480,#17481,#17482,#17483,#17484,#17485,
#17486,#17487,#17488,#17489,#17490,#17491,#17492,#17493,#17494,#17495,#17496,
#17497,#17498,#17499,#17500,#17501,#17502,#17503,#17504,#17505,#17506,#17507,
#17508,#17509,#17510,#17511,#17512,#17513,#17514,#17515,#17516,#17517,#17518,
#17519,#17520,#17521,#17522,#17523,#17524,#17525,#17526,#17527,#17528,#17529,
#17530,#17531,#17532,#17533,#17534,#17535,#17536,#17537,#17538,#17539,#17540,
#17541,#17542,#17543,#17544,#17545,#17546,#17547,#17548,#17549,#17550,#17551,
#17552,#17553,#17554,#17555,#17556,#17557,#17558,#17559,#17560,#17561,#17562,
#17563,#17564,#17565,#17566,#17567,#17568,#17569,#17570,#17571,#17572,#17573,
#17574));
#4915=EDGE_LOOP('',(#17575,#17576,#17577,#17578));
#4916=EDGE_LOOP('',(#17579,#17580,#17581,#17582));
#4917=EDGE_LOOP('',(#17583,#17584,#17585,#17586));
#4918=EDGE_LOOP('',(#17587,#17588,#17589,#17590));
#4919=EDGE_LOOP('',(#17591,#17592,#17593,#17594));
#4920=EDGE_LOOP('',(#17595,#17596,#17597,#17598));
#4921=EDGE_LOOP('',(#17599,#17600,#17601,#17602));
#4922=EDGE_LOOP('',(#17603));
#4923=EDGE_LOOP('',(#17604));
#4924=EDGE_LOOP('',(#17605,#17606,#17607,#17608,#17609));
#4925=EDGE_LOOP('',(#17610,#17611,#17612,#17613));
#4926=EDGE_LOOP('',(#17614));
#4927=EDGE_LOOP('',(#17615));
#4928=EDGE_LOOP('',(#17616,#17617,#17618,#17619));
#6404=LINE('',#37622,#7891);
#6405=LINE('',#37652,#7892);
#6406=LINE('',#37739,#7893);
#6407=LINE('',#37829,#7894);
#6408=LINE('',#37916,#7895);
#6409=LINE('',#38003,#7896);
#6410=LINE('',#38090,#7897);
#6411=LINE('',#38177,#7898);
#6412=LINE('',#38264,#7899);
#6413=LINE('',#38336,#7900);
#6414=LINE('',#38387,#7901);
#6415=LINE('',#38435,#7902);
#6416=LINE('',#38483,#7903);
#6417=LINE('',#38534,#7904);
#6418=LINE('',#38585,#7905);
#6419=LINE('',#38633,#7906);
#6420=LINE('',#38684,#7907);
#6421=LINE('',#38735,#7908);
#6422=LINE('',#38783,#7909);
#6423=LINE('',#38831,#7910);
#6424=LINE('',#38882,#7911);
#6425=LINE('',#38933,#7912);
#6426=LINE('',#38981,#7913);
#6427=LINE('',#39032,#7914);
#6428=LINE('',#39083,#7915);
#6429=LINE('',#39131,#7916);
#6430=LINE('',#39179,#7917);
#6431=LINE('',#39230,#7918);
#6432=LINE('',#39281,#7919);
#6433=LINE('',#39329,#7920);
#6434=LINE('',#39380,#7921);
#6435=LINE('',#39431,#7922);
#6436=LINE('',#39479,#7923);
#6437=LINE('',#39527,#7924);
#6438=LINE('',#39578,#7925);
#6439=LINE('',#39629,#7926);
#6440=LINE('',#39677,#7927);
#6441=LINE('',#39728,#7928);
#6442=LINE('',#39779,#7929);
#6443=LINE('',#39827,#7930);
#6444=LINE('',#39875,#7931);
#6445=LINE('',#39926,#7932);
#6446=LINE('',#39977,#7933);
#6447=LINE('',#40025,#7934);
#6448=LINE('',#40076,#7935);
#6449=LINE('',#40127,#7936);
#6450=LINE('',#40175,#7937);
#6451=LINE('',#40223,#7938);
#6452=LINE('',#40274,#7939);
#6453=LINE('',#40325,#7940);
#6454=LINE('',#40373,#7941);
#6455=LINE('',#40424,#7942);
#6456=LINE('',#40475,#7943);
#6457=LINE('',#40523,#7944);
#6458=LINE('',#40571,#7945);
#6459=LINE('',#40622,#7946);
#6460=LINE('',#40688,#7947);
#6461=LINE('',#40778,#7948);
#6462=LINE('',#40865,#7949);
#6463=LINE('',#40952,#7950);
#6464=LINE('',#41039,#7951);
#6465=LINE('',#41126,#7952);
#6466=LINE('',#41213,#7953);
#6467=LINE('',#41303,#7954);
#6468=LINE('',#41313,#7955);
#6469=LINE('',#41349,#7956);
#6470=LINE('',#41387,#7957);
#6471=LINE('',#41423,#7958);
#6472=LINE('',#41461,#7959);
#6473=LINE('',#41497,#7960);
#6474=LINE('',#41535,#7961);
#6475=LINE('',#41572,#7962);
#6476=LINE('',#41607,#7963);
#6477=LINE('',#41634,#7964);
#6478=LINE('',#41658,#7965);
#6479=LINE('',#41682,#7966);
#6480=LINE('',#41706,#7967);
#6481=LINE('',#41732,#7968);
#6482=LINE('',#41756,#7969);
#6483=LINE('',#41780,#7970);
#6484=LINE('',#41806,#7971);
#6485=LINE('',#41830,#7972);
#6486=LINE('',#41854,#7973);
#6487=LINE('',#41878,#7974);
#6488=LINE('',#41904,#7975);
#6489=LINE('',#41928,#7976);
#6490=LINE('',#41952,#7977);
#6491=LINE('',#41978,#7978);
#6492=LINE('',#42002,#7979);
#6493=LINE('',#42026,#7980);
#6494=LINE('',#42050,#7981);
#6495=LINE('',#42076,#7982);
#6496=LINE('',#42100,#7983);
#6497=LINE('',#42124,#7984);
#6498=LINE('',#42150,#7985);
#6499=LINE('',#42174,#7986);
#6500=LINE('',#42198,#7987);
#6501=LINE('',#42222,#7988);
#6502=LINE('',#42248,#7989);
#6503=LINE('',#42272,#7990);
#6504=LINE('',#42296,#7991);
#6505=LINE('',#42322,#7992);
#6506=LINE('',#42346,#7993);
#6507=LINE('',#42370,#7994);
#6508=LINE('',#42394,#7995);
#6509=LINE('',#42420,#7996);
#6510=LINE('',#42444,#7997);
#6511=LINE('',#42468,#7998);
#6512=LINE('',#42494,#7999);
#6513=LINE('',#42518,#8000);
#6514=LINE('',#42542,#8001);
#6515=LINE('',#42566,#8002);
#6516=LINE('',#42592,#8003);
#6517=LINE('',#42616,#8004);
#6518=LINE('',#42640,#8005);
#6519=LINE('',#42666,#8006);
#6520=LINE('',#42690,#8007);
#6521=LINE('',#42714,#8008);
#6522=LINE('',#42739,#8009);
#6523=LINE('',#42766,#8010);
#6524=LINE('',#42803,#8011);
#6525=LINE('',#42839,#8012);
#6526=LINE('',#42877,#8013);
#6527=LINE('',#42913,#8014);
#6528=LINE('',#42951,#8015);
#6529=LINE('',#42988,#8016);
#6530=LINE('',#43104,#8017);
#6531=LINE('',#47238,#8018);
#6532=LINE('',#47240,#8019);
#6533=LINE('',#47242,#8020);
#6534=LINE('',#47243,#8021);
#6535=LINE('',#47248,#8022);
#6536=LINE('',#47249,#8023);
#6537=LINE('',#47252,#8024);
#6538=LINE('',#47253,#8025);
#6539=LINE('',#47256,#8026);
#6540=LINE('',#47257,#8027);
#6541=LINE('',#47264,#8028);
#6542=LINE('',#47274,#8029);
#7891=VECTOR('',#28703,0.6);
#7892=VECTOR('',#28708,0.6);
#7893=VECTOR('',#28711,0.6);
#7894=VECTOR('',#28714,0.6);
#7895=VECTOR('',#28717,0.6);
#7896=VECTOR('',#28720,0.6);
#7897=VECTOR('',#28723,0.6);
#7898=VECTOR('',#28726,0.6);
#7899=VECTOR('',#28729,0.6);
#7900=VECTOR('',#28732,0.6);
#7901=VECTOR('',#28735,0.6);
#7902=VECTOR('',#28738,0.6);
#7903=VECTOR('',#28741,0.6);
#7904=VECTOR('',#28744,0.6);
#7905=VECTOR('',#28747,0.6);
#7906=VECTOR('',#28750,0.6);
#7907=VECTOR('',#28753,0.6);
#7908=VECTOR('',#28756,0.6);
#7909=VECTOR('',#28759,0.6);
#7910=VECTOR('',#28762,0.6);
#7911=VECTOR('',#28765,0.6);
#7912=VECTOR('',#28768,0.6);
#7913=VECTOR('',#28771,0.6);
#7914=VECTOR('',#28774,0.6);
#7915=VECTOR('',#28777,0.6);
#7916=VECTOR('',#28780,0.6);
#7917=VECTOR('',#28783,0.6);
#7918=VECTOR('',#28786,0.6);
#7919=VECTOR('',#28789,0.6);
#7920=VECTOR('',#28792,0.6);
#7921=VECTOR('',#28795,0.6);
#7922=VECTOR('',#28798,0.6);
#7923=VECTOR('',#28801,0.6);
#7924=VECTOR('',#28804,0.6);
#7925=VECTOR('',#28807,0.6);
#7926=VECTOR('',#28810,0.6);
#7927=VECTOR('',#28813,0.6);
#7928=VECTOR('',#28816,0.6);
#7929=VECTOR('',#28819,0.6);
#7930=VECTOR('',#28822,0.6);
#7931=VECTOR('',#28825,0.6);
#7932=VECTOR('',#28828,0.6);
#7933=VECTOR('',#28831,0.6);
#7934=VECTOR('',#28834,0.6);
#7935=VECTOR('',#28837,0.6);
#7936=VECTOR('',#28840,0.6);
#7937=VECTOR('',#28843,0.6);
#7938=VECTOR('',#28846,0.6);
#7939=VECTOR('',#28849,0.6);
#7940=VECTOR('',#28852,0.6);
#7941=VECTOR('',#28855,0.6);
#7942=VECTOR('',#28858,0.6);
#7943=VECTOR('',#28861,0.6);
#7944=VECTOR('',#28864,0.6);
#7945=VECTOR('',#28867,0.6);
#7946=VECTOR('',#28870,0.6);
#7947=VECTOR('',#28873,0.6);
#7948=VECTOR('',#28876,0.6);
#7949=VECTOR('',#28879,0.6);
#7950=VECTOR('',#28882,0.6);
#7951=VECTOR('',#28885,0.6);
#7952=VECTOR('',#28888,0.6);
#7953=VECTOR('',#28891,0.6);
#7954=VECTOR('',#28894,0.415875);
#7955=VECTOR('',#28899,0.415875);
#7956=VECTOR('',#28904,0.415875);
#7957=VECTOR('',#28907,0.415875);
#7958=VECTOR('',#28910,0.415875);
#7959=VECTOR('',#28913,0.415875);
#7960=VECTOR('',#28916,0.415875);
#7961=VECTOR('',#28919,0.415875);
#7962=VECTOR('',#28922,0.415875);
#7963=VECTOR('',#28925,0.415875);
#7964=VECTOR('',#28928,0.415875);
#7965=VECTOR('',#28931,0.415875);
#7966=VECTOR('',#28934,0.415875);
#7967=VECTOR('',#28937,0.415875);
#7968=VECTOR('',#28940,0.415875);
#7969=VECTOR('',#28943,0.415875);
#7970=VECTOR('',#28946,0.415875);
#7971=VECTOR('',#28949,0.415875);
#7972=VECTOR('',#28952,0.415875);
#7973=VECTOR('',#28955,0.415875);
#7974=VECTOR('',#28958,0.415875);
#7975=VECTOR('',#28961,0.415875);
#7976=VECTOR('',#28964,0.415875);
#7977=VECTOR('',#28967,0.415875);
#7978=VECTOR('',#28970,0.415875);
#7979=VECTOR('',#28973,0.415875);
#7980=VECTOR('',#28976,0.415875);
#7981=VECTOR('',#28979,0.415875);
#7982=VECTOR('',#28982,0.415875);
#7983=VECTOR('',#28985,0.415875);
#7984=VECTOR('',#28988,0.415875);
#7985=VECTOR('',#28991,0.415875);
#7986=VECTOR('',#28994,0.415875);
#7987=VECTOR('',#28997,0.415875);
#7988=VECTOR('',#29000,0.415875);
#7989=VECTOR('',#29003,0.415875);
#7990=VECTOR('',#29006,0.415875);
#7991=VECTOR('',#29009,0.415875);
#7992=VECTOR('',#29012,0.415875);
#7993=VECTOR('',#29015,0.415875);
#7994=VECTOR('',#29018,0.415875);
#7995=VECTOR('',#29021,0.415875);
#7996=VECTOR('',#29024,0.415875);
#7997=VECTOR('',#29027,0.415875);
#7998=VECTOR('',#29030,0.415875);
#7999=VECTOR('',#29033,0.415875);
#8000=VECTOR('',#29036,0.415875);
#8001=VECTOR('',#29039,0.415875);
#8002=VECTOR('',#29042,0.415875);
#8003=VECTOR('',#29045,0.415875);
#8004=VECTOR('',#29048,0.415875);
#8005=VECTOR('',#29051,0.415875);
#8006=VECTOR('',#29054,0.415875);
#8007=VECTOR('',#29057,0.415875);
#8008=VECTOR('',#29060,0.415875);
#8009=VECTOR('',#29063,0.415875);
#8010=VECTOR('',#29066,0.415875);
#8011=VECTOR('',#29069,0.415875);
#8012=VECTOR('',#29072,0.415875);
#8013=VECTOR('',#29075,0.415875);
#8014=VECTOR('',#29078,0.415875);
#8015=VECTOR('',#29081,0.415875);
#8016=VECTOR('',#29084,0.415875);
#8017=VECTOR('',#29093,0.6);
#8018=VECTOR('',#29102,1.);
#8019=VECTOR('',#29103,1.);
#8020=VECTOR('',#29104,1.);
#8021=VECTOR('',#29105,1.);
#8022=VECTOR('',#29110,1.);
#8023=VECTOR('',#29111,1.);
#8024=VECTOR('',#29114,1.);
#8025=VECTOR('',#29115,1.);
#8026=VECTOR('',#29118,1.);
#8027=VECTOR('',#29119,1.);
#8028=VECTOR('',#29128,1.);
#8029=VECTOR('',#29143,1.35);
#9254=CIRCLE('',#24872,0.5941);
#9255=CIRCLE('',#24936,0.415875);
#9256=CIRCLE('',#24938,0.415875);
#9257=CIRCLE('',#25001,0.6);
#9258=CIRCLE('',#25002,0.415875);
#9259=CIRCLE('',#25004,0.6);
#9260=CIRCLE('',#25009,1.);
#9261=CIRCLE('',#25013,1.);
#9262=CIRCLE('',#25015,1.);
#9263=CIRCLE('',#25016,1.);
#9264=CIRCLE('',#25019,1.35);
#9265=CIRCLE('',#25020,0.5941);
#9266=CIRCLE('',#25022,1.35);
#10415=VERTEX_POINT('',#37620);
#10416=VERTEX_POINT('',#37621);
#10417=VERTEX_POINT('',#37623);
#10418=VERTEX_POINT('',#37643);
#10419=VERTEX_POINT('',#37650);
#10420=VERTEX_POINT('',#37651);
#10421=VERTEX_POINT('',#37737);
#10422=VERTEX_POINT('',#37738);
#10423=VERTEX_POINT('',#37827);
#10424=VERTEX_POINT('',#37828);
#10425=VERTEX_POINT('',#37914);
#10426=VERTEX_POINT('',#37915);
#10427=VERTEX_POINT('',#38001);
#10428=VERTEX_POINT('',#38002);
#10429=VERTEX_POINT('',#38088);
#10430=VERTEX_POINT('',#38089);
#10431=VERTEX_POINT('',#38175);
#10432=VERTEX_POINT('',#38176);
#10433=VERTEX_POINT('',#38262);
#10434=VERTEX_POINT('',#38263);
#10435=VERTEX_POINT('',#38334);
#10436=VERTEX_POINT('',#38335);
#10437=VERTEX_POINT('',#38385);
#10438=VERTEX_POINT('',#38386);
#10439=VERTEX_POINT('',#38433);
#10440=VERTEX_POINT('',#38434);
#10441=VERTEX_POINT('',#38481);
#10442=VERTEX_POINT('',#38482);
#10443=VERTEX_POINT('',#38532);
#10444=VERTEX_POINT('',#38533);
#10445=VERTEX_POINT('',#38583);
#10446=VERTEX_POINT('',#38584);
#10447=VERTEX_POINT('',#38631);
#10448=VERTEX_POINT('',#38632);
#10449=VERTEX_POINT('',#38682);
#10450=VERTEX_POINT('',#38683);
#10451=VERTEX_POINT('',#38733);
#10452=VERTEX_POINT('',#38734);
#10453=VERTEX_POINT('',#38781);
#10454=VERTEX_POINT('',#38782);
#10455=VERTEX_POINT('',#38829);
#10456=VERTEX_POINT('',#38830);
#10457=VERTEX_POINT('',#38880);
#10458=VERTEX_POINT('',#38881);
#10459=VERTEX_POINT('',#38931);
#10460=VERTEX_POINT('',#38932);
#10461=VERTEX_POINT('',#38979);
#10462=VERTEX_POINT('',#38980);
#10463=VERTEX_POINT('',#39030);
#10464=VERTEX_POINT('',#39031);
#10465=VERTEX_POINT('',#39081);
#10466=VERTEX_POINT('',#39082);
#10467=VERTEX_POINT('',#39129);
#10468=VERTEX_POINT('',#39130);
#10469=VERTEX_POINT('',#39177);
#10470=VERTEX_POINT('',#39178);
#10471=VERTEX_POINT('',#39228);
#10472=VERTEX_POINT('',#39229);
#10473=VERTEX_POINT('',#39279);
#10474=VERTEX_POINT('',#39280);
#10475=VERTEX_POINT('',#39327);
#10476=VERTEX_POINT('',#39328);
#10477=VERTEX_POINT('',#39378);
#10478=VERTEX_POINT('',#39379);
#10479=VERTEX_POINT('',#39429);
#10480=VERTEX_POINT('',#39430);
#10481=VERTEX_POINT('',#39477);
#10482=VERTEX_POINT('',#39478);
#10483=VERTEX_POINT('',#39525);
#10484=VERTEX_POINT('',#39526);
#10485=VERTEX_POINT('',#39576);
#10486=VERTEX_POINT('',#39577);
#10487=VERTEX_POINT('',#39627);
#10488=VERTEX_POINT('',#39628);
#10489=VERTEX_POINT('',#39675);
#10490=VERTEX_POINT('',#39676);
#10491=VERTEX_POINT('',#39726);
#10492=VERTEX_POINT('',#39727);
#10493=VERTEX_POINT('',#39777);
#10494=VERTEX_POINT('',#39778);
#10495=VERTEX_POINT('',#39825);
#10496=VERTEX_POINT('',#39826);
#10497=VERTEX_POINT('',#39873);
#10498=VERTEX_POINT('',#39874);
#10499=VERTEX_POINT('',#39924);
#10500=VERTEX_POINT('',#39925);
#10501=VERTEX_POINT('',#39975);
#10502=VERTEX_POINT('',#39976);
#10503=VERTEX_POINT('',#40023);
#10504=VERTEX_POINT('',#40024);
#10505=VERTEX_POINT('',#40074);
#10506=VERTEX_POINT('',#40075);
#10507=VERTEX_POINT('',#40125);
#10508=VERTEX_POINT('',#40126);
#10509=VERTEX_POINT('',#40173);
#10510=VERTEX_POINT('',#40174);
#10511=VERTEX_POINT('',#40221);
#10512=VERTEX_POINT('',#40222);
#10513=VERTEX_POINT('',#40272);
#10514=VERTEX_POINT('',#40273);
#10515=VERTEX_POINT('',#40323);
#10516=VERTEX_POINT('',#40324);
#10517=VERTEX_POINT('',#40371);
#10518=VERTEX_POINT('',#40372);
#10519=VERTEX_POINT('',#40422);
#10520=VERTEX_POINT('',#40423);
#10521=VERTEX_POINT('',#40473);
#10522=VERTEX_POINT('',#40474);
#10523=VERTEX_POINT('',#40521);
#10524=VERTEX_POINT('',#40522);
#10525=VERTEX_POINT('',#40569);
#10526=VERTEX_POINT('',#40570);
#10527=VERTEX_POINT('',#40620);
#10528=VERTEX_POINT('',#40621);
#10529=VERTEX_POINT('',#40686);
#10530=VERTEX_POINT('',#40687);
#10531=VERTEX_POINT('',#40776);
#10532=VERTEX_POINT('',#40777);
#10533=VERTEX_POINT('',#40863);
#10534=VERTEX_POINT('',#40864);
#10535=VERTEX_POINT('',#40950);
#10536=VERTEX_POINT('',#40951);
#10537=VERTEX_POINT('',#41037);
#10538=VERTEX_POINT('',#41038);
#10539=VERTEX_POINT('',#41124);
#10540=VERTEX_POINT('',#41125);
#10541=VERTEX_POINT('',#41211);
#10542=VERTEX_POINT('',#41212);
#10543=VERTEX_POINT('',#41301);
#10544=VERTEX_POINT('',#41302);
#10545=VERTEX_POINT('',#41304);
#10546=VERTEX_POINT('',#41311);
#10547=VERTEX_POINT('',#41312);
#10548=VERTEX_POINT('',#41331);
#10549=VERTEX_POINT('',#41347);
#10550=VERTEX_POINT('',#41348);
#10551=VERTEX_POINT('',#41385);
#10552=VERTEX_POINT('',#41386);
#10553=VERTEX_POINT('',#41421);
#10554=VERTEX_POINT('',#41422);
#10555=VERTEX_POINT('',#41459);
#10556=VERTEX_POINT('',#41460);
#10557=VERTEX_POINT('',#41495);
#10558=VERTEX_POINT('',#41496);
#10559=VERTEX_POINT('',#41533);
#10560=VERTEX_POINT('',#41534);
#10561=VERTEX_POINT('',#41570);
#10562=VERTEX_POINT('',#41571);
#10563=VERTEX_POINT('',#41605);
#10564=VERTEX_POINT('',#41606);
#10565=VERTEX_POINT('',#41632);
#10566=VERTEX_POINT('',#41633);
#10567=VERTEX_POINT('',#41656);
#10568=VERTEX_POINT('',#41657);
#10569=VERTEX_POINT('',#41680);
#10570=VERTEX_POINT('',#41681);
#10571=VERTEX_POINT('',#41704);
#10572=VERTEX_POINT('',#41705);
#10573=VERTEX_POINT('',#41730);
#10574=VERTEX_POINT('',#41731);
#10575=VERTEX_POINT('',#41754);
#10576=VERTEX_POINT('',#41755);
#10577=VERTEX_POINT('',#41778);
#10578=VERTEX_POINT('',#41779);
#10579=VERTEX_POINT('',#41804);
#10580=VERTEX_POINT('',#41805);
#10581=VERTEX_POINT('',#41828);
#10582=VERTEX_POINT('',#41829);
#10583=VERTEX_POINT('',#41852);
#10584=VERTEX_POINT('',#41853);
#10585=VERTEX_POINT('',#41876);
#10586=VERTEX_POINT('',#41877);
#10587=VERTEX_POINT('',#41902);
#10588=VERTEX_POINT('',#41903);
#10589=VERTEX_POINT('',#41926);
#10590=VERTEX_POINT('',#41927);
#10591=VERTEX_POINT('',#41950);
#10592=VERTEX_POINT('',#41951);
#10593=VERTEX_POINT('',#41976);
#10594=VERTEX_POINT('',#41977);
#10595=VERTEX_POINT('',#42000);
#10596=VERTEX_POINT('',#42001);
#10597=VERTEX_POINT('',#42024);
#10598=VERTEX_POINT('',#42025);
#10599=VERTEX_POINT('',#42048);
#10600=VERTEX_POINT('',#42049);
#10601=VERTEX_POINT('',#42074);
#10602=VERTEX_POINT('',#42075);
#10603=VERTEX_POINT('',#42098);
#10604=VERTEX_POINT('',#42099);
#10605=VERTEX_POINT('',#42122);
#10606=VERTEX_POINT('',#42123);
#10607=VERTEX_POINT('',#42148);
#10608=VERTEX_POINT('',#42149);
#10609=VERTEX_POINT('',#42172);
#10610=VERTEX_POINT('',#42173);
#10611=VERTEX_POINT('',#42196);
#10612=VERTEX_POINT('',#42197);
#10613=VERTEX_POINT('',#42220);
#10614=VERTEX_POINT('',#42221);
#10615=VERTEX_POINT('',#42246);
#10616=VERTEX_POINT('',#42247);
#10617=VERTEX_POINT('',#42270);
#10618=VERTEX_POINT('',#42271);
#10619=VERTEX_POINT('',#42294);
#10620=VERTEX_POINT('',#42295);
#10621=VERTEX_POINT('',#42320);
#10622=VERTEX_POINT('',#42321);
#10623=VERTEX_POINT('',#42344);
#10624=VERTEX_POINT('',#42345);
#10625=VERTEX_POINT('',#42368);
#10626=VERTEX_POINT('',#42369);
#10627=VERTEX_POINT('',#42392);
#10628=VERTEX_POINT('',#42393);
#10629=VERTEX_POINT('',#42418);
#10630=VERTEX_POINT('',#42419);
#10631=VERTEX_POINT('',#42442);
#10632=VERTEX_POINT('',#42443);
#10633=VERTEX_POINT('',#42466);
#10634=VERTEX_POINT('',#42467);
#10635=VERTEX_POINT('',#42492);
#10636=VERTEX_POINT('',#42493);
#10637=VERTEX_POINT('',#42516);
#10638=VERTEX_POINT('',#42517);
#10639=VERTEX_POINT('',#42540);
#10640=VERTEX_POINT('',#42541);
#10641=VERTEX_POINT('',#42564);
#10642=VERTEX_POINT('',#42565);
#10643=VERTEX_POINT('',#42590);
#10644=VERTEX_POINT('',#42591);
#10645=VERTEX_POINT('',#42614);
#10646=VERTEX_POINT('',#42615);
#10647=VERTEX_POINT('',#42638);
#10648=VERTEX_POINT('',#42639);
#10649=VERTEX_POINT('',#42664);
#10650=VERTEX_POINT('',#42665);
#10651=VERTEX_POINT('',#42688);
#10652=VERTEX_POINT('',#42689);
#10653=VERTEX_POINT('',#42712);
#10654=VERTEX_POINT('',#42713);
#10655=VERTEX_POINT('',#42737);
#10656=VERTEX_POINT('',#42738);
#10657=VERTEX_POINT('',#42764);
#10658=VERTEX_POINT('',#42765);
#10659=VERTEX_POINT('',#42801);
#10660=VERTEX_POINT('',#42802);
#10661=VERTEX_POINT('',#42837);
#10662=VERTEX_POINT('',#42838);
#10663=VERTEX_POINT('',#42875);
#10664=VERTEX_POINT('',#42876);
#10665=VERTEX_POINT('',#42911);
#10666=VERTEX_POINT('',#42912);
#10667=VERTEX_POINT('',#42949);
#10668=VERTEX_POINT('',#42950);
#10669=VERTEX_POINT('',#42986);
#10670=VERTEX_POINT('',#42987);
#10671=VERTEX_POINT('',#43023);
#10672=VERTEX_POINT('',#43025);
#10673=VERTEX_POINT('',#43063);
#10674=VERTEX_POINT('',#43103);
#10675=VERTEX_POINT('',#45099);
#10676=VERTEX_POINT('',#47184);
#10677=VERTEX_POINT('',#47236);
#10678=VERTEX_POINT('',#47237);
#10679=VERTEX_POINT('',#47239);
#10680=VERTEX_POINT('',#47241);
#10681=VERTEX_POINT('',#47245);
#10682=VERTEX_POINT('',#47247);
#10683=VERTEX_POINT('',#47251);
#10684=VERTEX_POINT('',#47255);
#10685=VERTEX_POINT('',#47261);
#10686=VERTEX_POINT('',#47263);
#10687=VERTEX_POINT('',#47268);
#10688=VERTEX_POINT('',#47272);
#12783=EDGE_CURVE('',#10415,#10416,#6404,.T.);
#12784=EDGE_CURVE('',#10415,#10417,#768,.T.);
#12785=EDGE_CURVE('',#10417,#10418,#9254,.F.);
#12786=EDGE_CURVE('',#10418,#10416,#769,.T.);
#12787=EDGE_CURVE('',#10419,#10420,#6405,.T.);
#12788=EDGE_CURVE('',#10419,#10415,#770,.T.);
#12789=EDGE_CURVE('',#10416,#10420,#771,.T.);
#12790=EDGE_CURVE('',#10421,#10422,#6406,.T.);
#12791=EDGE_CURVE('',#10421,#10419,#772,.T.);
#12792=EDGE_CURVE('',#10420,#10422,#773,.T.);
#12793=EDGE_CURVE('',#10423,#10424,#6407,.T.);
#12794=EDGE_CURVE('',#10423,#10421,#774,.T.);
#12795=EDGE_CURVE('',#10422,#10424,#775,.T.);
#12796=EDGE_CURVE('',#10425,#10426,#6408,.T.);
#12797=EDGE_CURVE('',#10425,#10423,#776,.T.);
#12798=EDGE_CURVE('',#10424,#10426,#777,.T.);
#12799=EDGE_CURVE('',#10427,#10428,#6409,.T.);
#12800=EDGE_CURVE('',#10427,#10425,#778,.T.);
#12801=EDGE_CURVE('',#10426,#10428,#779,.T.);
#12802=EDGE_CURVE('',#10429,#10430,#6410,.T.);
#12803=EDGE_CURVE('',#10429,#10427,#780,.T.);
#12804=EDGE_CURVE('',#10428,#10430,#781,.T.);
#12805=EDGE_CURVE('',#10431,#10432,#6411,.T.);
#12806=EDGE_CURVE('',#10431,#10429,#782,.T.);
#12807=EDGE_CURVE('',#10430,#10432,#783,.T.);
#12808=EDGE_CURVE('',#10433,#10434,#6412,.T.);
#12809=EDGE_CURVE('',#10433,#10431,#784,.T.);
#12810=EDGE_CURVE('',#10432,#10434,#785,.T.);
#12811=EDGE_CURVE('',#10435,#10436,#6413,.T.);
#12812=EDGE_CURVE('',#10435,#10433,#786,.T.);
#12813=EDGE_CURVE('',#10434,#10436,#787,.T.);
#12814=EDGE_CURVE('',#10437,#10438,#6414,.T.);
#12815=EDGE_CURVE('',#10437,#10435,#788,.T.);
#12816=EDGE_CURVE('',#10436,#10438,#789,.T.);
#12817=EDGE_CURVE('',#10439,#10440,#6415,.T.);
#12818=EDGE_CURVE('',#10439,#10437,#790,.T.);
#12819=EDGE_CURVE('',#10438,#10440,#791,.T.);
#12820=EDGE_CURVE('',#10441,#10442,#6416,.T.);
#12821=EDGE_CURVE('',#10441,#10439,#792,.T.);
#12822=EDGE_CURVE('',#10440,#10442,#793,.T.);
#12823=EDGE_CURVE('',#10443,#10444,#6417,.T.);
#12824=EDGE_CURVE('',#10443,#10441,#794,.T.);
#12825=EDGE_CURVE('',#10442,#10444,#795,.T.);
#12826=EDGE_CURVE('',#10445,#10446,#6418,.T.);
#12827=EDGE_CURVE('',#10445,#10443,#796,.T.);
#12828=EDGE_CURVE('',#10444,#10446,#797,.T.);
#12829=EDGE_CURVE('',#10447,#10448,#6419,.T.);
#12830=EDGE_CURVE('',#10447,#10445,#798,.T.);
#12831=EDGE_CURVE('',#10446,#10448,#799,.T.);
#12832=EDGE_CURVE('',#10449,#10450,#6420,.T.);
#12833=EDGE_CURVE('',#10449,#10447,#800,.T.);
#12834=EDGE_CURVE('',#10448,#10450,#801,.T.);
#12835=EDGE_CURVE('',#10451,#10452,#6421,.T.);
#12836=EDGE_CURVE('',#10451,#10449,#802,.T.);
#12837=EDGE_CURVE('',#10450,#10452,#803,.T.);
#12838=EDGE_CURVE('',#10453,#10454,#6422,.T.);
#12839=EDGE_CURVE('',#10453,#10451,#804,.T.);
#12840=EDGE_CURVE('',#10452,#10454,#805,.T.);
#12841=EDGE_CURVE('',#10455,#10456,#6423,.T.);
#12842=EDGE_CURVE('',#10455,#10453,#806,.T.);
#12843=EDGE_CURVE('',#10454,#10456,#807,.T.);
#12844=EDGE_CURVE('',#10457,#10458,#6424,.T.);
#12845=EDGE_CURVE('',#10457,#10455,#808,.T.);
#12846=EDGE_CURVE('',#10456,#10458,#809,.T.);
#12847=EDGE_CURVE('',#10459,#10460,#6425,.T.);
#12848=EDGE_CURVE('',#10459,#10457,#810,.T.);
#12849=EDGE_CURVE('',#10458,#10460,#811,.T.);
#12850=EDGE_CURVE('',#10461,#10462,#6426,.T.);
#12851=EDGE_CURVE('',#10461,#10459,#812,.T.);
#12852=EDGE_CURVE('',#10460,#10462,#813,.T.);
#12853=EDGE_CURVE('',#10463,#10464,#6427,.T.);
#12854=EDGE_CURVE('',#10463,#10461,#814,.T.);
#12855=EDGE_CURVE('',#10462,#10464,#815,.T.);
#12856=EDGE_CURVE('',#10465,#10466,#6428,.T.);
#12857=EDGE_CURVE('',#10465,#10463,#816,.T.);
#12858=EDGE_CURVE('',#10464,#10466,#817,.T.);
#12859=EDGE_CURVE('',#10467,#10468,#6429,.T.);
#12860=EDGE_CURVE('',#10467,#10465,#818,.T.);
#12861=EDGE_CURVE('',#10466,#10468,#819,.T.);
#12862=EDGE_CURVE('',#10469,#10470,#6430,.T.);
#12863=EDGE_CURVE('',#10469,#10467,#820,.T.);
#12864=EDGE_CURVE('',#10468,#10470,#821,.T.);
#12865=EDGE_CURVE('',#10471,#10472,#6431,.T.);
#12866=EDGE_CURVE('',#10471,#10469,#822,.T.);
#12867=EDGE_CURVE('',#10470,#10472,#823,.T.);
#12868=EDGE_CURVE('',#10473,#10474,#6432,.T.);
#12869=EDGE_CURVE('',#10473,#10471,#824,.T.);
#12870=EDGE_CURVE('',#10472,#10474,#825,.T.);
#12871=EDGE_CURVE('',#10475,#10476,#6433,.T.);
#12872=EDGE_CURVE('',#10475,#10473,#826,.T.);
#12873=EDGE_CURVE('',#10474,#10476,#827,.T.);
#12874=EDGE_CURVE('',#10477,#10478,#6434,.T.);
#12875=EDGE_CURVE('',#10477,#10475,#828,.T.);
#12876=EDGE_CURVE('',#10476,#10478,#829,.T.);
#12877=EDGE_CURVE('',#10479,#10480,#6435,.T.);
#12878=EDGE_CURVE('',#10479,#10477,#830,.T.);
#12879=EDGE_CURVE('',#10478,#10480,#831,.T.);
#12880=EDGE_CURVE('',#10481,#10482,#6436,.T.);
#12881=EDGE_CURVE('',#10481,#10479,#832,.T.);
#12882=EDGE_CURVE('',#10480,#10482,#833,.T.);
#12883=EDGE_CURVE('',#10483,#10484,#6437,.T.);
#12884=EDGE_CURVE('',#10483,#10481,#834,.T.);
#12885=EDGE_CURVE('',#10482,#10484,#835,.T.);
#12886=EDGE_CURVE('',#10485,#10486,#6438,.T.);
#12887=EDGE_CURVE('',#10485,#10483,#836,.T.);
#12888=EDGE_CURVE('',#10484,#10486,#837,.T.);
#12889=EDGE_CURVE('',#10487,#10488,#6439,.T.);
#12890=EDGE_CURVE('',#10487,#10485,#838,.T.);
#12891=EDGE_CURVE('',#10486,#10488,#839,.T.);
#12892=EDGE_CURVE('',#10489,#10490,#6440,.T.);
#12893=EDGE_CURVE('',#10489,#10487,#840,.T.);
#12894=EDGE_CURVE('',#10488,#10490,#841,.T.);
#12895=EDGE_CURVE('',#10491,#10492,#6441,.T.);
#12896=EDGE_CURVE('',#10491,#10489,#842,.T.);
#12897=EDGE_CURVE('',#10490,#10492,#843,.T.);
#12898=EDGE_CURVE('',#10493,#10494,#6442,.T.);
#12899=EDGE_CURVE('',#10493,#10491,#844,.T.);
#12900=EDGE_CURVE('',#10492,#10494,#845,.T.);
#12901=EDGE_CURVE('',#10495,#10496,#6443,.T.);
#12902=EDGE_CURVE('',#10495,#10493,#846,.T.);
#12903=EDGE_CURVE('',#10494,#10496,#847,.T.);
#12904=EDGE_CURVE('',#10497,#10498,#6444,.T.);
#12905=EDGE_CURVE('',#10497,#10495,#848,.T.);
#12906=EDGE_CURVE('',#10496,#10498,#849,.T.);
#12907=EDGE_CURVE('',#10499,#10500,#6445,.T.);
#12908=EDGE_CURVE('',#10499,#10497,#850,.T.);
#12909=EDGE_CURVE('',#10498,#10500,#851,.T.);
#12910=EDGE_CURVE('',#10501,#10502,#6446,.T.);
#12911=EDGE_CURVE('',#10501,#10499,#852,.T.);
#12912=EDGE_CURVE('',#10500,#10502,#853,.T.);
#12913=EDGE_CURVE('',#10503,#10504,#6447,.T.);
#12914=EDGE_CURVE('',#10503,#10501,#854,.T.);
#12915=EDGE_CURVE('',#10502,#10504,#855,.T.);
#12916=EDGE_CURVE('',#10505,#10506,#6448,.T.);
#12917=EDGE_CURVE('',#10505,#10503,#856,.T.);
#12918=EDGE_CURVE('',#10504,#10506,#857,.T.);
#12919=EDGE_CURVE('',#10507,#10508,#6449,.T.);
#12920=EDGE_CURVE('',#10507,#10505,#858,.T.);
#12921=EDGE_CURVE('',#10506,#10508,#859,.T.);
#12922=EDGE_CURVE('',#10509,#10510,#6450,.T.);
#12923=EDGE_CURVE('',#10509,#10507,#860,.T.);
#12924=EDGE_CURVE('',#10508,#10510,#861,.T.);
#12925=EDGE_CURVE('',#10511,#10512,#6451,.T.);
#12926=EDGE_CURVE('',#10511,#10509,#862,.T.);
#12927=EDGE_CURVE('',#10510,#10512,#863,.T.);
#12928=EDGE_CURVE('',#10513,#10514,#6452,.T.);
#12929=EDGE_CURVE('',#10513,#10511,#864,.T.);
#12930=EDGE_CURVE('',#10512,#10514,#865,.T.);
#12931=EDGE_CURVE('',#10515,#10516,#6453,.T.);
#12932=EDGE_CURVE('',#10515,#10513,#866,.T.);
#12933=EDGE_CURVE('',#10514,#10516,#867,.T.);
#12934=EDGE_CURVE('',#10517,#10518,#6454,.T.);
#12935=EDGE_CURVE('',#10517,#10515,#868,.T.);
#12936=EDGE_CURVE('',#10516,#10518,#869,.T.);
#12937=EDGE_CURVE('',#10519,#10520,#6455,.T.);
#12938=EDGE_CURVE('',#10519,#10517,#870,.T.);
#12939=EDGE_CURVE('',#10518,#10520,#871,.T.);
#12940=EDGE_CURVE('',#10521,#10522,#6456,.T.);
#12941=EDGE_CURVE('',#10521,#10519,#872,.T.);
#12942=EDGE_CURVE('',#10520,#10522,#873,.T.);
#12943=EDGE_CURVE('',#10523,#10524,#6457,.T.);
#12944=EDGE_CURVE('',#10523,#10521,#874,.T.);
#12945=EDGE_CURVE('',#10522,#10524,#875,.T.);
#12946=EDGE_CURVE('',#10525,#10526,#6458,.T.);
#12947=EDGE_CURVE('',#10525,#10523,#876,.T.);
#12948=EDGE_CURVE('',#10524,#10526,#877,.T.);
#12949=EDGE_CURVE('',#10527,#10528,#6459,.T.);
#12950=EDGE_CURVE('',#10527,#10525,#878,.T.);
#12951=EDGE_CURVE('',#10526,#10528,#879,.T.);
#12952=EDGE_CURVE('',#10529,#10530,#6460,.T.);
#12953=EDGE_CURVE('',#10529,#10527,#880,.T.);
#12954=EDGE_CURVE('',#10528,#10530,#881,.T.);
#12955=EDGE_CURVE('',#10531,#10532,#6461,.T.);
#12956=EDGE_CURVE('',#10531,#10529,#882,.T.);
#12957=EDGE_CURVE('',#10530,#10532,#883,.T.);
#12958=EDGE_CURVE('',#10533,#10534,#6462,.T.);
#12959=EDGE_CURVE('',#10533,#10531,#884,.T.);
#12960=EDGE_CURVE('',#10532,#10534,#885,.T.);
#12961=EDGE_CURVE('',#10535,#10536,#6463,.T.);
#12962=EDGE_CURVE('',#10535,#10533,#886,.T.);
#12963=EDGE_CURVE('',#10534,#10536,#887,.T.);
#12964=EDGE_CURVE('',#10537,#10538,#6464,.T.);
#12965=EDGE_CURVE('',#10537,#10535,#888,.T.);
#12966=EDGE_CURVE('',#10536,#10538,#889,.T.);
#12967=EDGE_CURVE('',#10539,#10540,#6465,.T.);
#12968=EDGE_CURVE('',#10539,#10537,#890,.T.);
#12969=EDGE_CURVE('',#10538,#10540,#891,.T.);
#12970=EDGE_CURVE('',#10541,#10542,#6466,.T.);
#12971=EDGE_CURVE('',#10541,#10539,#892,.T.);
#12972=EDGE_CURVE('',#10540,#10542,#893,.T.);
#12973=EDGE_CURVE('',#10543,#10544,#6467,.T.);
#12974=EDGE_CURVE('',#10543,#10545,#894,.T.);
#12975=EDGE_CURVE('',#10544,#10545,#9255,.T.);
#12976=EDGE_CURVE('',#10546,#10547,#6468,.T.);
#12977=EDGE_CURVE('',#10546,#10543,#895,.T.);
#12978=EDGE_CURVE('',#10548,#10544,#9256,.T.);
#12979=EDGE_CURVE('',#10547,#10548,#896,.T.);
#12980=EDGE_CURVE('',#10549,#10550,#6469,.T.);
#12981=EDGE_CURVE('',#10549,#10546,#897,.T.);
#12982=EDGE_CURVE('',#10550,#10547,#898,.T.);
#12983=EDGE_CURVE('',#10551,#10552,#6470,.T.);
#12984=EDGE_CURVE('',#10551,#10549,#899,.T.);
#12985=EDGE_CURVE('',#10552,#10550,#900,.T.);
#12986=EDGE_CURVE('',#10553,#10554,#6471,.T.);
#12987=EDGE_CURVE('',#10553,#10551,#901,.T.);
#12988=EDGE_CURVE('',#10554,#10552,#902,.T.);
#12989=EDGE_CURVE('',#10555,#10556,#6472,.T.);
#12990=EDGE_CURVE('',#10555,#10553,#903,.T.);
#12991=EDGE_CURVE('',#10556,#10554,#904,.T.);
#12992=EDGE_CURVE('',#10557,#10558,#6473,.T.);
#12993=EDGE_CURVE('',#10557,#10555,#905,.T.);
#12994=EDGE_CURVE('',#10558,#10556,#906,.T.);
#12995=EDGE_CURVE('',#10559,#10560,#6474,.T.);
#12996=EDGE_CURVE('',#10559,#10557,#907,.T.);
#12997=EDGE_CURVE('',#10560,#10558,#908,.T.);
#12998=EDGE_CURVE('',#10561,#10562,#6475,.T.);
#12999=EDGE_CURVE('',#10561,#10559,#909,.T.);
#13000=EDGE_CURVE('',#10562,#10560,#910,.T.);
#13001=EDGE_CURVE('',#10563,#10564,#6476,.T.);
#13002=EDGE_CURVE('',#10563,#10561,#911,.T.);
#13003=EDGE_CURVE('',#10564,#10562,#912,.T.);
#13004=EDGE_CURVE('',#10565,#10566,#6477,.T.);
#13005=EDGE_CURVE('',#10565,#10563,#913,.T.);
#13006=EDGE_CURVE('',#10566,#10564,#914,.T.);
#13007=EDGE_CURVE('',#10567,#10568,#6478,.T.);
#13008=EDGE_CURVE('',#10567,#10565,#915,.T.);
#13009=EDGE_CURVE('',#10568,#10566,#916,.T.);
#13010=EDGE_CURVE('',#10569,#10570,#6479,.T.);
#13011=EDGE_CURVE('',#10569,#10567,#917,.T.);
#13012=EDGE_CURVE('',#10570,#10568,#918,.T.);
#13013=EDGE_CURVE('',#10571,#10572,#6480,.T.);
#13014=EDGE_CURVE('',#10571,#10569,#919,.T.);
#13015=EDGE_CURVE('',#10572,#10570,#920,.T.);
#13016=EDGE_CURVE('',#10573,#10574,#6481,.T.);
#13017=EDGE_CURVE('',#10573,#10571,#921,.T.);
#13018=EDGE_CURVE('',#10574,#10572,#922,.T.);
#13019=EDGE_CURVE('',#10575,#10576,#6482,.T.);
#13020=EDGE_CURVE('',#10575,#10573,#923,.T.);
#13021=EDGE_CURVE('',#10576,#10574,#924,.T.);
#13022=EDGE_CURVE('',#10577,#10578,#6483,.T.);
#13023=EDGE_CURVE('',#10577,#10575,#925,.T.);
#13024=EDGE_CURVE('',#10578,#10576,#926,.T.);
#13025=EDGE_CURVE('',#10579,#10580,#6484,.T.);
#13026=EDGE_CURVE('',#10579,#10577,#927,.T.);
#13027=EDGE_CURVE('',#10580,#10578,#928,.T.);
#13028=EDGE_CURVE('',#10581,#10582,#6485,.T.);
#13029=EDGE_CURVE('',#10581,#10579,#929,.T.);
#13030=EDGE_CURVE('',#10582,#10580,#930,.T.);
#13031=EDGE_CURVE('',#10583,#10584,#6486,.T.);
#13032=EDGE_CURVE('',#10583,#10581,#931,.T.);
#13033=EDGE_CURVE('',#10584,#10582,#932,.T.);
#13034=EDGE_CURVE('',#10585,#10586,#6487,.T.);
#13035=EDGE_CURVE('',#10585,#10583,#933,.T.);
#13036=EDGE_CURVE('',#10586,#10584,#934,.T.);
#13037=EDGE_CURVE('',#10587,#10588,#6488,.T.);
#13038=EDGE_CURVE('',#10587,#10585,#935,.T.);
#13039=EDGE_CURVE('',#10588,#10586,#936,.T.);
#13040=EDGE_CURVE('',#10589,#10590,#6489,.T.);
#13041=EDGE_CURVE('',#10589,#10587,#937,.T.);
#13042=EDGE_CURVE('',#10590,#10588,#938,.T.);
#13043=EDGE_CURVE('',#10591,#10592,#6490,.T.);
#13044=EDGE_CURVE('',#10591,#10589,#939,.T.);
#13045=EDGE_CURVE('',#10592,#10590,#940,.T.);
#13046=EDGE_CURVE('',#10593,#10594,#6491,.T.);
#13047=EDGE_CURVE('',#10593,#10591,#941,.T.);
#13048=EDGE_CURVE('',#10594,#10592,#942,.T.);
#13049=EDGE_CURVE('',#10595,#10596,#6492,.T.);
#13050=EDGE_CURVE('',#10595,#10593,#943,.T.);
#13051=EDGE_CURVE('',#10596,#10594,#944,.T.);
#13052=EDGE_CURVE('',#10597,#10598,#6493,.T.);
#13053=EDGE_CURVE('',#10597,#10595,#945,.T.);
#13054=EDGE_CURVE('',#10598,#10596,#946,.T.);
#13055=EDGE_CURVE('',#10599,#10600,#6494,.T.);
#13056=EDGE_CURVE('',#10599,#10597,#947,.T.);
#13057=EDGE_CURVE('',#10600,#10598,#948,.T.);
#13058=EDGE_CURVE('',#10601,#10602,#6495,.T.);
#13059=EDGE_CURVE('',#10601,#10599,#949,.T.);
#13060=EDGE_CURVE('',#10602,#10600,#950,.T.);
#13061=EDGE_CURVE('',#10603,#10604,#6496,.T.);
#13062=EDGE_CURVE('',#10603,#10601,#951,.T.);
#13063=EDGE_CURVE('',#10604,#10602,#952,.T.);
#13064=EDGE_CURVE('',#10605,#10606,#6497,.T.);
#13065=EDGE_CURVE('',#10605,#10603,#953,.T.);
#13066=EDGE_CURVE('',#10606,#10604,#954,.T.);
#13067=EDGE_CURVE('',#10607,#10608,#6498,.T.);
#13068=EDGE_CURVE('',#10607,#10605,#955,.T.);
#13069=EDGE_CURVE('',#10608,#10606,#956,.T.);
#13070=EDGE_CURVE('',#10609,#10610,#6499,.T.);
#13071=EDGE_CURVE('',#10609,#10607,#957,.T.);
#13072=EDGE_CURVE('',#10610,#10608,#958,.T.);
#13073=EDGE_CURVE('',#10611,#10612,#6500,.T.);
#13074=EDGE_CURVE('',#10611,#10609,#959,.T.);
#13075=EDGE_CURVE('',#10612,#10610,#960,.T.);
#13076=EDGE_CURVE('',#10613,#10614,#6501,.T.);
#13077=EDGE_CURVE('',#10613,#10611,#961,.T.);
#13078=EDGE_CURVE('',#10614,#10612,#962,.T.);
#13079=EDGE_CURVE('',#10615,#10616,#6502,.T.);
#13080=EDGE_CURVE('',#10615,#10613,#963,.T.);
#13081=EDGE_CURVE('',#10616,#10614,#964,.T.);
#13082=EDGE_CURVE('',#10617,#10618,#6503,.T.);
#13083=EDGE_CURVE('',#10617,#10615,#965,.T.);
#13084=EDGE_CURVE('',#10618,#10616,#966,.T.);
#13085=EDGE_CURVE('',#10619,#10620,#6504,.T.);
#13086=EDGE_CURVE('',#10619,#10617,#967,.T.);
#13087=EDGE_CURVE('',#10620,#10618,#968,.T.);
#13088=EDGE_CURVE('',#10621,#10622,#6505,.T.);
#13089=EDGE_CURVE('',#10621,#10619,#969,.T.);
#13090=EDGE_CURVE('',#10622,#10620,#970,.T.);
#13091=EDGE_CURVE('',#10623,#10624,#6506,.T.);
#13092=EDGE_CURVE('',#10623,#10621,#971,.T.);
#13093=EDGE_CURVE('',#10624,#10622,#972,.T.);
#13094=EDGE_CURVE('',#10625,#10626,#6507,.T.);
#13095=EDGE_CURVE('',#10625,#10623,#973,.T.);
#13096=EDGE_CURVE('',#10626,#10624,#974,.T.);
#13097=EDGE_CURVE('',#10627,#10628,#6508,.T.);
#13098=EDGE_CURVE('',#10627,#10625,#975,.T.);
#13099=EDGE_CURVE('',#10628,#10626,#976,.T.);
#13100=EDGE_CURVE('',#10629,#10630,#6509,.T.);
#13101=EDGE_CURVE('',#10629,#10627,#977,.T.);
#13102=EDGE_CURVE('',#10630,#10628,#978,.T.);
#13103=EDGE_CURVE('',#10631,#10632,#6510,.T.);
#13104=EDGE_CURVE('',#10631,#10629,#979,.T.);
#13105=EDGE_CURVE('',#10632,#10630,#980,.T.);
#13106=EDGE_CURVE('',#10633,#10634,#6511,.T.);
#13107=EDGE_CURVE('',#10633,#10631,#981,.T.);
#13108=EDGE_CURVE('',#10634,#10632,#982,.T.);
#13109=EDGE_CURVE('',#10635,#10636,#6512,.T.);
#13110=EDGE_CURVE('',#10635,#10633,#983,.T.);
#13111=EDGE_CURVE('',#10636,#10634,#984,.T.);
#13112=EDGE_CURVE('',#10637,#10638,#6513,.T.);
#13113=EDGE_CURVE('',#10637,#10635,#985,.T.);
#13114=EDGE_CURVE('',#10638,#10636,#986,.T.);
#13115=EDGE_CURVE('',#10639,#10640,#6514,.T.);
#13116=EDGE_CURVE('',#10639,#10637,#987,.T.);
#13117=EDGE_CURVE('',#10640,#10638,#988,.T.);
#13118=EDGE_CURVE('',#10641,#10642,#6515,.T.);
#13119=EDGE_CURVE('',#10641,#10639,#989,.T.);
#13120=EDGE_CURVE('',#10642,#10640,#990,.T.);
#13121=EDGE_CURVE('',#10643,#10644,#6516,.T.);
#13122=EDGE_CURVE('',#10643,#10641,#991,.T.);
#13123=EDGE_CURVE('',#10644,#10642,#992,.T.);
#13124=EDGE_CURVE('',#10645,#10646,#6517,.T.);
#13125=EDGE_CURVE('',#10645,#10643,#993,.T.);
#13126=EDGE_CURVE('',#10646,#10644,#994,.T.);
#13127=EDGE_CURVE('',#10647,#10648,#6518,.T.);
#13128=EDGE_CURVE('',#10647,#10645,#995,.T.);
#13129=EDGE_CURVE('',#10648,#10646,#996,.T.);
#13130=EDGE_CURVE('',#10649,#10650,#6519,.T.);
#13131=EDGE_CURVE('',#10649,#10647,#997,.T.);
#13132=EDGE_CURVE('',#10650,#10648,#998,.T.);
#13133=EDGE_CURVE('',#10651,#10652,#6520,.T.);
#13134=EDGE_CURVE('',#10651,#10649,#999,.T.);
#13135=EDGE_CURVE('',#10652,#10650,#1000,.T.);
#13136=EDGE_CURVE('',#10653,#10654,#6521,.T.);
#13137=EDGE_CURVE('',#10653,#10651,#1001,.T.);
#13138=EDGE_CURVE('',#10654,#10652,#1002,.T.);
#13139=EDGE_CURVE('',#10655,#10656,#6522,.T.);
#13140=EDGE_CURVE('',#10655,#10653,#1003,.T.);
#13141=EDGE_CURVE('',#10656,#10654,#1004,.T.);
#13142=EDGE_CURVE('',#10657,#10658,#6523,.T.);
#13143=EDGE_CURVE('',#10657,#10655,#1005,.T.);
#13144=EDGE_CURVE('',#10658,#10656,#1006,.T.);
#13145=EDGE_CURVE('',#10659,#10660,#6524,.T.);
#13146=EDGE_CURVE('',#10659,#10657,#1007,.T.);
#13147=EDGE_CURVE('',#10660,#10658,#1008,.T.);
#13148=EDGE_CURVE('',#10661,#10662,#6525,.T.);
#13149=EDGE_CURVE('',#10661,#10659,#1009,.T.);
#13150=EDGE_CURVE('',#10662,#10660,#1010,.T.);
#13151=EDGE_CURVE('',#10663,#10664,#6526,.T.);
#13152=EDGE_CURVE('',#10663,#10661,#1011,.T.);
#13153=EDGE_CURVE('',#10664,#10662,#1012,.T.);
#13154=EDGE_CURVE('',#10665,#10666,#6527,.T.);
#13155=EDGE_CURVE('',#10665,#10663,#1013,.T.);
#13156=EDGE_CURVE('',#10666,#10664,#1014,.T.);
#13157=EDGE_CURVE('',#10667,#10668,#6528,.T.);
#13158=EDGE_CURVE('',#10667,#10665,#1015,.T.);
#13159=EDGE_CURVE('',#10668,#10666,#1016,.T.);
#13160=EDGE_CURVE('',#10669,#10670,#6529,.T.);
#13161=EDGE_CURVE('',#10669,#10667,#1017,.T.);
#13162=EDGE_CURVE('',#10670,#10668,#1018,.T.);
#13163=EDGE_CURVE('',#10671,#10671,#9257,.T.);
#13164=EDGE_CURVE('',#10672,#10418,#1019,.T.);
#13165=EDGE_CURVE('',#10417,#10673,#1020,.T.);
#13166=EDGE_CURVE('',#10673,#10672,#9258,.T.);
#13167=EDGE_CURVE('',#10671,#10674,#6530,.T.);
#13168=EDGE_CURVE('',#10674,#10674,#9259,.T.);
#13169=EDGE_CURVE('',#10675,#10548,#1021,.T.);
#13170=EDGE_CURVE('',#10542,#10675,#1022,.T.);
#13171=EDGE_CURVE('',#10672,#10670,#1023,.T.);
#13172=EDGE_CURVE('',#10673,#10669,#1024,.T.);
#13173=EDGE_CURVE('',#10545,#10676,#1025,.T.);
#13174=EDGE_CURVE('',#10676,#10541,#1026,.T.);
#13175=EDGE_CURVE('',#10677,#10678,#6531,.T.);
#13176=EDGE_CURVE('',#10677,#10679,#6532,.T.);
#13177=EDGE_CURVE('',#10680,#10679,#6533,.T.);
#13178=EDGE_CURVE('',#10678,#10680,#6534,.T.);
#13179=EDGE_CURVE('',#10678,#10681,#9260,.T.);
#13180=EDGE_CURVE('',#10680,#10682,#6535,.T.);
#13181=EDGE_CURVE('',#10682,#10681,#6536,.T.);
#13182=EDGE_CURVE('',#10679,#10683,#6537,.T.);
#13183=EDGE_CURVE('',#10682,#10683,#6538,.T.);
#13184=EDGE_CURVE('',#10681,#10684,#6539,.T.);
#13185=EDGE_CURVE('',#10683,#10684,#6540,.T.);
#13186=EDGE_CURVE('',#10684,#10677,#9261,.T.);
#13187=EDGE_CURVE('',#10685,#10685,#9262,.T.);
#13188=EDGE_CURVE('',#10685,#10686,#6541,.T.);
#13189=EDGE_CURVE('',#10686,#10686,#9263,.T.);
#13190=EDGE_CURVE('',#10687,#10687,#9264,.T.);
#13191=EDGE_CURVE('',#10676,#10675,#9265,.F.);
#13192=EDGE_CURVE('',#10688,#10688,#9266,.T.);
#13193=EDGE_CURVE('',#10688,#10687,#6542,.T.);
#16798=ORIENTED_EDGE('',*,*,#12783,.F.);
#16799=ORIENTED_EDGE('',*,*,#12784,.T.);
#16800=ORIENTED_EDGE('',*,*,#12785,.T.);
#16801=ORIENTED_EDGE('',*,*,#12786,.T.);
#16802=ORIENTED_EDGE('',*,*,#12787,.F.);
#16803=ORIENTED_EDGE('',*,*,#12788,.T.);
#16804=ORIENTED_EDGE('',*,*,#12783,.T.);
#16805=ORIENTED_EDGE('',*,*,#12789,.T.);
#16806=ORIENTED_EDGE('',*,*,#12790,.F.);
#16807=ORIENTED_EDGE('',*,*,#12791,.T.);
#16808=ORIENTED_EDGE('',*,*,#12787,.T.);
#16809=ORIENTED_EDGE('',*,*,#12792,.T.);
#16810=ORIENTED_EDGE('',*,*,#12793,.F.);
#16811=ORIENTED_EDGE('',*,*,#12794,.T.);
#16812=ORIENTED_EDGE('',*,*,#12790,.T.);
#16813=ORIENTED_EDGE('',*,*,#12795,.T.);
#16814=ORIENTED_EDGE('',*,*,#12796,.F.);
#16815=ORIENTED_EDGE('',*,*,#12797,.T.);
#16816=ORIENTED_EDGE('',*,*,#12793,.T.);
#16817=ORIENTED_EDGE('',*,*,#12798,.T.);
#16818=ORIENTED_EDGE('',*,*,#12799,.F.);
#16819=ORIENTED_EDGE('',*,*,#12800,.T.);
#16820=ORIENTED_EDGE('',*,*,#12796,.T.);
#16821=ORIENTED_EDGE('',*,*,#12801,.T.);
#16822=ORIENTED_EDGE('',*,*,#12802,.F.);
#16823=ORIENTED_EDGE('',*,*,#12803,.T.);
#16824=ORIENTED_EDGE('',*,*,#12799,.T.);
#16825=ORIENTED_EDGE('',*,*,#12804,.T.);
#16826=ORIENTED_EDGE('',*,*,#12805,.F.);
#16827=ORIENTED_EDGE('',*,*,#12806,.T.);
#16828=ORIENTED_EDGE('',*,*,#12802,.T.);
#16829=ORIENTED_EDGE('',*,*,#12807,.T.);
#16830=ORIENTED_EDGE('',*,*,#12808,.F.);
#16831=ORIENTED_EDGE('',*,*,#12809,.T.);
#16832=ORIENTED_EDGE('',*,*,#12805,.T.);
#16833=ORIENTED_EDGE('',*,*,#12810,.T.);
#16834=ORIENTED_EDGE('',*,*,#12811,.F.);
#16835=ORIENTED_EDGE('',*,*,#12812,.T.);
#16836=ORIENTED_EDGE('',*,*,#12808,.T.);
#16837=ORIENTED_EDGE('',*,*,#12813,.T.);
#16838=ORIENTED_EDGE('',*,*,#12814,.F.);
#16839=ORIENTED_EDGE('',*,*,#12815,.T.);
#16840=ORIENTED_EDGE('',*,*,#12811,.T.);
#16841=ORIENTED_EDGE('',*,*,#12816,.T.);
#16842=ORIENTED_EDGE('',*,*,#12817,.F.);
#16843=ORIENTED_EDGE('',*,*,#12818,.T.);
#16844=ORIENTED_EDGE('',*,*,#12814,.T.);
#16845=ORIENTED_EDGE('',*,*,#12819,.T.);
#16846=ORIENTED_EDGE('',*,*,#12820,.F.);
#16847=ORIENTED_EDGE('',*,*,#12821,.T.);
#16848=ORIENTED_EDGE('',*,*,#12817,.T.);
#16849=ORIENTED_EDGE('',*,*,#12822,.T.);
#16850=ORIENTED_EDGE('',*,*,#12823,.F.);
#16851=ORIENTED_EDGE('',*,*,#12824,.T.);
#16852=ORIENTED_EDGE('',*,*,#12820,.T.);
#16853=ORIENTED_EDGE('',*,*,#12825,.T.);
#16854=ORIENTED_EDGE('',*,*,#12826,.F.);
#16855=ORIENTED_EDGE('',*,*,#12827,.T.);
#16856=ORIENTED_EDGE('',*,*,#12823,.T.);
#16857=ORIENTED_EDGE('',*,*,#12828,.T.);
#16858=ORIENTED_EDGE('',*,*,#12829,.F.);
#16859=ORIENTED_EDGE('',*,*,#12830,.T.);
#16860=ORIENTED_EDGE('',*,*,#12826,.T.);
#16861=ORIENTED_EDGE('',*,*,#12831,.T.);
#16862=ORIENTED_EDGE('',*,*,#12832,.F.);
#16863=ORIENTED_EDGE('',*,*,#12833,.T.);
#16864=ORIENTED_EDGE('',*,*,#12829,.T.);
#16865=ORIENTED_EDGE('',*,*,#12834,.T.);
#16866=ORIENTED_EDGE('',*,*,#12835,.F.);
#16867=ORIENTED_EDGE('',*,*,#12836,.T.);
#16868=ORIENTED_EDGE('',*,*,#12832,.T.);
#16869=ORIENTED_EDGE('',*,*,#12837,.T.);
#16870=ORIENTED_EDGE('',*,*,#12838,.F.);
#16871=ORIENTED_EDGE('',*,*,#12839,.T.);
#16872=ORIENTED_EDGE('',*,*,#12835,.T.);
#16873=ORIENTED_EDGE('',*,*,#12840,.T.);
#16874=ORIENTED_EDGE('',*,*,#12841,.F.);
#16875=ORIENTED_EDGE('',*,*,#12842,.T.);
#16876=ORIENTED_EDGE('',*,*,#12838,.T.);
#16877=ORIENTED_EDGE('',*,*,#12843,.T.);
#16878=ORIENTED_EDGE('',*,*,#12844,.F.);
#16879=ORIENTED_EDGE('',*,*,#12845,.T.);
#16880=ORIENTED_EDGE('',*,*,#12841,.T.);
#16881=ORIENTED_EDGE('',*,*,#12846,.T.);
#16882=ORIENTED_EDGE('',*,*,#12847,.F.);
#16883=ORIENTED_EDGE('',*,*,#12848,.T.);
#16884=ORIENTED_EDGE('',*,*,#12844,.T.);
#16885=ORIENTED_EDGE('',*,*,#12849,.T.);
#16886=ORIENTED_EDGE('',*,*,#12850,.F.);
#16887=ORIENTED_EDGE('',*,*,#12851,.T.);
#16888=ORIENTED_EDGE('',*,*,#12847,.T.);
#16889=ORIENTED_EDGE('',*,*,#12852,.T.);
#16890=ORIENTED_EDGE('',*,*,#12853,.F.);
#16891=ORIENTED_EDGE('',*,*,#12854,.T.);
#16892=ORIENTED_EDGE('',*,*,#12850,.T.);
#16893=ORIENTED_EDGE('',*,*,#12855,.T.);
#16894=ORIENTED_EDGE('',*,*,#12856,.F.);
#16895=ORIENTED_EDGE('',*,*,#12857,.T.);
#16896=ORIENTED_EDGE('',*,*,#12853,.T.);
#16897=ORIENTED_EDGE('',*,*,#12858,.T.);
#16898=ORIENTED_EDGE('',*,*,#12859,.F.);
#16899=ORIENTED_EDGE('',*,*,#12860,.T.);
#16900=ORIENTED_EDGE('',*,*,#12856,.T.);
#16901=ORIENTED_EDGE('',*,*,#12861,.T.);
#16902=ORIENTED_EDGE('',*,*,#12862,.F.);
#16903=ORIENTED_EDGE('',*,*,#12863,.T.);
#16904=ORIENTED_EDGE('',*,*,#12859,.T.);
#16905=ORIENTED_EDGE('',*,*,#12864,.T.);
#16906=ORIENTED_EDGE('',*,*,#12865,.F.);
#16907=ORIENTED_EDGE('',*,*,#12866,.T.);
#16908=ORIENTED_EDGE('',*,*,#12862,.T.);
#16909=ORIENTED_EDGE('',*,*,#12867,.T.);
#16910=ORIENTED_EDGE('',*,*,#12868,.F.);
#16911=ORIENTED_EDGE('',*,*,#12869,.T.);
#16912=ORIENTED_EDGE('',*,*,#12865,.T.);
#16913=ORIENTED_EDGE('',*,*,#12870,.T.);
#16914=ORIENTED_EDGE('',*,*,#12871,.F.);
#16915=ORIENTED_EDGE('',*,*,#12872,.T.);
#16916=ORIENTED_EDGE('',*,*,#12868,.T.);
#16917=ORIENTED_EDGE('',*,*,#12873,.T.);
#16918=ORIENTED_EDGE('',*,*,#12874,.F.);
#16919=ORIENTED_EDGE('',*,*,#12875,.T.);
#16920=ORIENTED_EDGE('',*,*,#12871,.T.);
#16921=ORIENTED_EDGE('',*,*,#12876,.T.);
#16922=ORIENTED_EDGE('',*,*,#12877,.F.);
#16923=ORIENTED_EDGE('',*,*,#12878,.T.);
#16924=ORIENTED_EDGE('',*,*,#12874,.T.);
#16925=ORIENTED_EDGE('',*,*,#12879,.T.);
#16926=ORIENTED_EDGE('',*,*,#12880,.F.);
#16927=ORIENTED_EDGE('',*,*,#12881,.T.);
#16928=ORIENTED_EDGE('',*,*,#12877,.T.);
#16929=ORIENTED_EDGE('',*,*,#12882,.T.);
#16930=ORIENTED_EDGE('',*,*,#12883,.F.);
#16931=ORIENTED_EDGE('',*,*,#12884,.T.);
#16932=ORIENTED_EDGE('',*,*,#12880,.T.);
#16933=ORIENTED_EDGE('',*,*,#12885,.T.);
#16934=ORIENTED_EDGE('',*,*,#12886,.F.);
#16935=ORIENTED_EDGE('',*,*,#12887,.T.);
#16936=ORIENTED_EDGE('',*,*,#12883,.T.);
#16937=ORIENTED_EDGE('',*,*,#12888,.T.);
#16938=ORIENTED_EDGE('',*,*,#12889,.F.);
#16939=ORIENTED_EDGE('',*,*,#12890,.T.);
#16940=ORIENTED_EDGE('',*,*,#12886,.T.);
#16941=ORIENTED_EDGE('',*,*,#12891,.T.);
#16942=ORIENTED_EDGE('',*,*,#12892,.F.);
#16943=ORIENTED_EDGE('',*,*,#12893,.T.);
#16944=ORIENTED_EDGE('',*,*,#12889,.T.);
#16945=ORIENTED_EDGE('',*,*,#12894,.T.);
#16946=ORIENTED_EDGE('',*,*,#12895,.F.);
#16947=ORIENTED_EDGE('',*,*,#12896,.T.);
#16948=ORIENTED_EDGE('',*,*,#12892,.T.);
#16949=ORIENTED_EDGE('',*,*,#12897,.T.);
#16950=ORIENTED_EDGE('',*,*,#12898,.F.);
#16951=ORIENTED_EDGE('',*,*,#12899,.T.);
#16952=ORIENTED_EDGE('',*,*,#12895,.T.);
#16953=ORIENTED_EDGE('',*,*,#12900,.T.);
#16954=ORIENTED_EDGE('',*,*,#12901,.F.);
#16955=ORIENTED_EDGE('',*,*,#12902,.T.);
#16956=ORIENTED_EDGE('',*,*,#12898,.T.);
#16957=ORIENTED_EDGE('',*,*,#12903,.T.);
#16958=ORIENTED_EDGE('',*,*,#12904,.F.);
#16959=ORIENTED_EDGE('',*,*,#12905,.T.);
#16960=ORIENTED_EDGE('',*,*,#12901,.T.);
#16961=ORIENTED_EDGE('',*,*,#12906,.T.);
#16962=ORIENTED_EDGE('',*,*,#12907,.F.);
#16963=ORIENTED_EDGE('',*,*,#12908,.T.);
#16964=ORIENTED_EDGE('',*,*,#12904,.T.);
#16965=ORIENTED_EDGE('',*,*,#12909,.T.);
#16966=ORIENTED_EDGE('',*,*,#12910,.F.);
#16967=ORIENTED_EDGE('',*,*,#12911,.T.);
#16968=ORIENTED_EDGE('',*,*,#12907,.T.);
#16969=ORIENTED_EDGE('',*,*,#12912,.T.);
#16970=ORIENTED_EDGE('',*,*,#12913,.F.);
#16971=ORIENTED_EDGE('',*,*,#12914,.T.);
#16972=ORIENTED_EDGE('',*,*,#12910,.T.);
#16973=ORIENTED_EDGE('',*,*,#12915,.T.);
#16974=ORIENTED_EDGE('',*,*,#12916,.F.);
#16975=ORIENTED_EDGE('',*,*,#12917,.T.);
#16976=ORIENTED_EDGE('',*,*,#12913,.T.);
#16977=ORIENTED_EDGE('',*,*,#12918,.T.);
#16978=ORIENTED_EDGE('',*,*,#12919,.F.);
#16979=ORIENTED_EDGE('',*,*,#12920,.T.);
#16980=ORIENTED_EDGE('',*,*,#12916,.T.);
#16981=ORIENTED_EDGE('',*,*,#12921,.T.);
#16982=ORIENTED_EDGE('',*,*,#12922,.F.);
#16983=ORIENTED_EDGE('',*,*,#12923,.T.);
#16984=ORIENTED_EDGE('',*,*,#12919,.T.);
#16985=ORIENTED_EDGE('',*,*,#12924,.T.);
#16986=ORIENTED_EDGE('',*,*,#12925,.F.);
#16987=ORIENTED_EDGE('',*,*,#12926,.T.);
#16988=ORIENTED_EDGE('',*,*,#12922,.T.);
#16989=ORIENTED_EDGE('',*,*,#12927,.T.);
#16990=ORIENTED_EDGE('',*,*,#12928,.F.);
#16991=ORIENTED_EDGE('',*,*,#12929,.T.);
#16992=ORIENTED_EDGE('',*,*,#12925,.T.);
#16993=ORIENTED_EDGE('',*,*,#12930,.T.);
#16994=ORIENTED_EDGE('',*,*,#12931,.F.);
#16995=ORIENTED_EDGE('',*,*,#12932,.T.);
#16996=ORIENTED_EDGE('',*,*,#12928,.T.);
#16997=ORIENTED_EDGE('',*,*,#12933,.T.);
#16998=ORIENTED_EDGE('',*,*,#12934,.F.);
#16999=ORIENTED_EDGE('',*,*,#12935,.T.);
#17000=ORIENTED_EDGE('',*,*,#12931,.T.);
#17001=ORIENTED_EDGE('',*,*,#12936,.T.);
#17002=ORIENTED_EDGE('',*,*,#12937,.F.);
#17003=ORIENTED_EDGE('',*,*,#12938,.T.);
#17004=ORIENTED_EDGE('',*,*,#12934,.T.);
#17005=ORIENTED_EDGE('',*,*,#12939,.T.);
#17006=ORIENTED_EDGE('',*,*,#12940,.F.);
#17007=ORIENTED_EDGE('',*,*,#12941,.T.);
#17008=ORIENTED_EDGE('',*,*,#12937,.T.);
#17009=ORIENTED_EDGE('',*,*,#12942,.T.);
#17010=ORIENTED_EDGE('',*,*,#12943,.F.);
#17011=ORIENTED_EDGE('',*,*,#12944,.T.);
#17012=ORIENTED_EDGE('',*,*,#12940,.T.);
#17013=ORIENTED_EDGE('',*,*,#12945,.T.);
#17014=ORIENTED_EDGE('',*,*,#12946,.F.);
#17015=ORIENTED_EDGE('',*,*,#12947,.T.);
#17016=ORIENTED_EDGE('',*,*,#12943,.T.);
#17017=ORIENTED_EDGE('',*,*,#12948,.T.);
#17018=ORIENTED_EDGE('',*,*,#12949,.F.);
#17019=ORIENTED_EDGE('',*,*,#12950,.T.);
#17020=ORIENTED_EDGE('',*,*,#12946,.T.);
#17021=ORIENTED_EDGE('',*,*,#12951,.T.);
#17022=ORIENTED_EDGE('',*,*,#12952,.F.);
#17023=ORIENTED_EDGE('',*,*,#12953,.T.);
#17024=ORIENTED_EDGE('',*,*,#12949,.T.);
#17025=ORIENTED_EDGE('',*,*,#12954,.T.);
#17026=ORIENTED_EDGE('',*,*,#12955,.F.);
#17027=ORIENTED_EDGE('',*,*,#12956,.T.);
#17028=ORIENTED_EDGE('',*,*,#12952,.T.);
#17029=ORIENTED_EDGE('',*,*,#12957,.T.);
#17030=ORIENTED_EDGE('',*,*,#12958,.F.);
#17031=ORIENTED_EDGE('',*,*,#12959,.T.);
#17032=ORIENTED_EDGE('',*,*,#12955,.T.);
#17033=ORIENTED_EDGE('',*,*,#12960,.T.);
#17034=ORIENTED_EDGE('',*,*,#12961,.F.);
#17035=ORIENTED_EDGE('',*,*,#12962,.T.);
#17036=ORIENTED_EDGE('',*,*,#12958,.T.);
#17037=ORIENTED_EDGE('',*,*,#12963,.T.);
#17038=ORIENTED_EDGE('',*,*,#12964,.F.);
#17039=ORIENTED_EDGE('',*,*,#12965,.T.);
#17040=ORIENTED_EDGE('',*,*,#12961,.T.);
#17041=ORIENTED_EDGE('',*,*,#12966,.T.);
#17042=ORIENTED_EDGE('',*,*,#12967,.F.);
#17043=ORIENTED_EDGE('',*,*,#12968,.T.);
#17044=ORIENTED_EDGE('',*,*,#12964,.T.);
#17045=ORIENTED_EDGE('',*,*,#12969,.T.);
#17046=ORIENTED_EDGE('',*,*,#12970,.F.);
#17047=ORIENTED_EDGE('',*,*,#12971,.T.);
#17048=ORIENTED_EDGE('',*,*,#12967,.T.);
#17049=ORIENTED_EDGE('',*,*,#12972,.T.);
#17050=ORIENTED_EDGE('',*,*,#12973,.F.);
#17051=ORIENTED_EDGE('',*,*,#12974,.T.);
#17052=ORIENTED_EDGE('',*,*,#12975,.F.);
#17053=ORIENTED_EDGE('',*,*,#12976,.F.);
#17054=ORIENTED_EDGE('',*,*,#12977,.T.);
#17055=ORIENTED_EDGE('',*,*,#12973,.T.);
#17056=ORIENTED_EDGE('',*,*,#12978,.F.);
#17057=ORIENTED_EDGE('',*,*,#12979,.F.);
#17058=ORIENTED_EDGE('',*,*,#12980,.F.);
#17059=ORIENTED_EDGE('',*,*,#12981,.T.);
#17060=ORIENTED_EDGE('',*,*,#12976,.T.);
#17061=ORIENTED_EDGE('',*,*,#12982,.F.);
#17062=ORIENTED_EDGE('',*,*,#12983,.F.);
#17063=ORIENTED_EDGE('',*,*,#12984,.T.);
#17064=ORIENTED_EDGE('',*,*,#12980,.T.);
#17065=ORIENTED_EDGE('',*,*,#12985,.F.);
#17066=ORIENTED_EDGE('',*,*,#12986,.F.);
#17067=ORIENTED_EDGE('',*,*,#12987,.T.);
#17068=ORIENTED_EDGE('',*,*,#12983,.T.);
#17069=ORIENTED_EDGE('',*,*,#12988,.F.);
#17070=ORIENTED_EDGE('',*,*,#12989,.F.);
#17071=ORIENTED_EDGE('',*,*,#12990,.T.);
#17072=ORIENTED_EDGE('',*,*,#12986,.T.);
#17073=ORIENTED_EDGE('',*,*,#12991,.F.);
#17074=ORIENTED_EDGE('',*,*,#12992,.F.);
#17075=ORIENTED_EDGE('',*,*,#12993,.T.);
#17076=ORIENTED_EDGE('',*,*,#12989,.T.);
#17077=ORIENTED_EDGE('',*,*,#12994,.F.);
#17078=ORIENTED_EDGE('',*,*,#12995,.F.);
#17079=ORIENTED_EDGE('',*,*,#12996,.T.);
#17080=ORIENTED_EDGE('',*,*,#12992,.T.);
#17081=ORIENTED_EDGE('',*,*,#12997,.F.);
#17082=ORIENTED_EDGE('',*,*,#12998,.F.);
#17083=ORIENTED_EDGE('',*,*,#12999,.T.);
#17084=ORIENTED_EDGE('',*,*,#12995,.T.);
#17085=ORIENTED_EDGE('',*,*,#13000,.F.);
#17086=ORIENTED_EDGE('',*,*,#13001,.F.);
#17087=ORIENTED_EDGE('',*,*,#13002,.T.);
#17088=ORIENTED_EDGE('',*,*,#12998,.T.);
#17089=ORIENTED_EDGE('',*,*,#13003,.F.);
#17090=ORIENTED_EDGE('',*,*,#13004,.F.);
#17091=ORIENTED_EDGE('',*,*,#13005,.T.);
#17092=ORIENTED_EDGE('',*,*,#13001,.T.);
#17093=ORIENTED_EDGE('',*,*,#13006,.F.);
#17094=ORIENTED_EDGE('',*,*,#13007,.F.);
#17095=ORIENTED_EDGE('',*,*,#13008,.T.);
#17096=ORIENTED_EDGE('',*,*,#13004,.T.);
#17097=ORIENTED_EDGE('',*,*,#13009,.F.);
#17098=ORIENTED_EDGE('',*,*,#13010,.F.);
#17099=ORIENTED_EDGE('',*,*,#13011,.T.);
#17100=ORIENTED_EDGE('',*,*,#13007,.T.);
#17101=ORIENTED_EDGE('',*,*,#13012,.F.);
#17102=ORIENTED_EDGE('',*,*,#13013,.F.);
#17103=ORIENTED_EDGE('',*,*,#13014,.T.);
#17104=ORIENTED_EDGE('',*,*,#13010,.T.);
#17105=ORIENTED_EDGE('',*,*,#13015,.F.);
#17106=ORIENTED_EDGE('',*,*,#13016,.F.);
#17107=ORIENTED_EDGE('',*,*,#13017,.T.);
#17108=ORIENTED_EDGE('',*,*,#13013,.T.);
#17109=ORIENTED_EDGE('',*,*,#13018,.F.);
#17110=ORIENTED_EDGE('',*,*,#13019,.F.);
#17111=ORIENTED_EDGE('',*,*,#13020,.T.);
#17112=ORIENTED_EDGE('',*,*,#13016,.T.);
#17113=ORIENTED_EDGE('',*,*,#13021,.F.);
#17114=ORIENTED_EDGE('',*,*,#13022,.F.);
#17115=ORIENTED_EDGE('',*,*,#13023,.T.);
#17116=ORIENTED_EDGE('',*,*,#13019,.T.);
#17117=ORIENTED_EDGE('',*,*,#13024,.F.);
#17118=ORIENTED_EDGE('',*,*,#13025,.F.);
#17119=ORIENTED_EDGE('',*,*,#13026,.T.);
#17120=ORIENTED_EDGE('',*,*,#13022,.T.);
#17121=ORIENTED_EDGE('',*,*,#13027,.F.);
#17122=ORIENTED_EDGE('',*,*,#13028,.F.);
#17123=ORIENTED_EDGE('',*,*,#13029,.T.);
#17124=ORIENTED_EDGE('',*,*,#13025,.T.);
#17125=ORIENTED_EDGE('',*,*,#13030,.F.);
#17126=ORIENTED_EDGE('',*,*,#13031,.F.);
#17127=ORIENTED_EDGE('',*,*,#13032,.T.);
#17128=ORIENTED_EDGE('',*,*,#13028,.T.);
#17129=ORIENTED_EDGE('',*,*,#13033,.F.);
#17130=ORIENTED_EDGE('',*,*,#13034,.F.);
#17131=ORIENTED_EDGE('',*,*,#13035,.T.);
#17132=ORIENTED_EDGE('',*,*,#13031,.T.);
#17133=ORIENTED_EDGE('',*,*,#13036,.F.);
#17134=ORIENTED_EDGE('',*,*,#13037,.F.);
#17135=ORIENTED_EDGE('',*,*,#13038,.T.);
#17136=ORIENTED_EDGE('',*,*,#13034,.T.);
#17137=ORIENTED_EDGE('',*,*,#13039,.F.);
#17138=ORIENTED_EDGE('',*,*,#13040,.F.);
#17139=ORIENTED_EDGE('',*,*,#13041,.T.);
#17140=ORIENTED_EDGE('',*,*,#13037,.T.);
#17141=ORIENTED_EDGE('',*,*,#13042,.F.);
#17142=ORIENTED_EDGE('',*,*,#13043,.F.);
#17143=ORIENTED_EDGE('',*,*,#13044,.T.);
#17144=ORIENTED_EDGE('',*,*,#13040,.T.);
#17145=ORIENTED_EDGE('',*,*,#13045,.F.);
#17146=ORIENTED_EDGE('',*,*,#13046,.F.);
#17147=ORIENTED_EDGE('',*,*,#13047,.T.);
#17148=ORIENTED_EDGE('',*,*,#13043,.T.);
#17149=ORIENTED_EDGE('',*,*,#13048,.F.);
#17150=ORIENTED_EDGE('',*,*,#13049,.F.);
#17151=ORIENTED_EDGE('',*,*,#13050,.T.);
#17152=ORIENTED_EDGE('',*,*,#13046,.T.);
#17153=ORIENTED_EDGE('',*,*,#13051,.F.);
#17154=ORIENTED_EDGE('',*,*,#13052,.F.);
#17155=ORIENTED_EDGE('',*,*,#13053,.T.);
#17156=ORIENTED_EDGE('',*,*,#13049,.T.);
#17157=ORIENTED_EDGE('',*,*,#13054,.F.);
#17158=ORIENTED_EDGE('',*,*,#13055,.F.);
#17159=ORIENTED_EDGE('',*,*,#13056,.T.);
#17160=ORIENTED_EDGE('',*,*,#13052,.T.);
#17161=ORIENTED_EDGE('',*,*,#13057,.F.);
#17162=ORIENTED_EDGE('',*,*,#13058,.F.);
#17163=ORIENTED_EDGE('',*,*,#13059,.T.);
#17164=ORIENTED_EDGE('',*,*,#13055,.T.);
#17165=ORIENTED_EDGE('',*,*,#13060,.F.);
#17166=ORIENTED_EDGE('',*,*,#13061,.F.);
#17167=ORIENTED_EDGE('',*,*,#13062,.T.);
#17168=ORIENTED_EDGE('',*,*,#13058,.T.);
#17169=ORIENTED_EDGE('',*,*,#13063,.F.);
#17170=ORIENTED_EDGE('',*,*,#13064,.F.);
#17171=ORIENTED_EDGE('',*,*,#13065,.T.);
#17172=ORIENTED_EDGE('',*,*,#13061,.T.);
#17173=ORIENTED_EDGE('',*,*,#13066,.F.);
#17174=ORIENTED_EDGE('',*,*,#13067,.F.);
#17175=ORIENTED_EDGE('',*,*,#13068,.T.);
#17176=ORIENTED_EDGE('',*,*,#13064,.T.);
#17177=ORIENTED_EDGE('',*,*,#13069,.F.);
#17178=ORIENTED_EDGE('',*,*,#13070,.F.);
#17179=ORIENTED_EDGE('',*,*,#13071,.T.);
#17180=ORIENTED_EDGE('',*,*,#13067,.T.);
#17181=ORIENTED_EDGE('',*,*,#13072,.F.);
#17182=ORIENTED_EDGE('',*,*,#13073,.F.);
#17183=ORIENTED_EDGE('',*,*,#13074,.T.);
#17184=ORIENTED_EDGE('',*,*,#13070,.T.);
#17185=ORIENTED_EDGE('',*,*,#13075,.F.);
#17186=ORIENTED_EDGE('',*,*,#13076,.F.);
#17187=ORIENTED_EDGE('',*,*,#13077,.T.);
#17188=ORIENTED_EDGE('',*,*,#13073,.T.);
#17189=ORIENTED_EDGE('',*,*,#13078,.F.);
#17190=ORIENTED_EDGE('',*,*,#13079,.F.);
#17191=ORIENTED_EDGE('',*,*,#13080,.T.);
#17192=ORIENTED_EDGE('',*,*,#13076,.T.);
#17193=ORIENTED_EDGE('',*,*,#13081,.F.);
#17194=ORIENTED_EDGE('',*,*,#13082,.F.);
#17195=ORIENTED_EDGE('',*,*,#13083,.T.);
#17196=ORIENTED_EDGE('',*,*,#13079,.T.);
#17197=ORIENTED_EDGE('',*,*,#13084,.F.);
#17198=ORIENTED_EDGE('',*,*,#13085,.F.);
#17199=ORIENTED_EDGE('',*,*,#13086,.T.);
#17200=ORIENTED_EDGE('',*,*,#13082,.T.);
#17201=ORIENTED_EDGE('',*,*,#13087,.F.);
#17202=ORIENTED_EDGE('',*,*,#13088,.F.);
#17203=ORIENTED_EDGE('',*,*,#13089,.T.);
#17204=ORIENTED_EDGE('',*,*,#13085,.T.);
#17205=ORIENTED_EDGE('',*,*,#13090,.F.);
#17206=ORIENTED_EDGE('',*,*,#13091,.F.);
#17207=ORIENTED_EDGE('',*,*,#13092,.T.);
#17208=ORIENTED_EDGE('',*,*,#13088,.T.);
#17209=ORIENTED_EDGE('',*,*,#13093,.F.);
#17210=ORIENTED_EDGE('',*,*,#13094,.F.);
#17211=ORIENTED_EDGE('',*,*,#13095,.T.);
#17212=ORIENTED_EDGE('',*,*,#13091,.T.);
#17213=ORIENTED_EDGE('',*,*,#13096,.F.);
#17214=ORIENTED_EDGE('',*,*,#13097,.F.);
#17215=ORIENTED_EDGE('',*,*,#13098,.T.);
#17216=ORIENTED_EDGE('',*,*,#13094,.T.);
#17217=ORIENTED_EDGE('',*,*,#13099,.F.);
#17218=ORIENTED_EDGE('',*,*,#13100,.F.);
#17219=ORIENTED_EDGE('',*,*,#13101,.T.);
#17220=ORIENTED_EDGE('',*,*,#13097,.T.);
#17221=ORIENTED_EDGE('',*,*,#13102,.F.);
#17222=ORIENTED_EDGE('',*,*,#13103,.F.);
#17223=ORIENTED_EDGE('',*,*,#13104,.T.);
#17224=ORIENTED_EDGE('',*,*,#13100,.T.);
#17225=ORIENTED_EDGE('',*,*,#13105,.F.);
#17226=ORIENTED_EDGE('',*,*,#13106,.F.);
#17227=ORIENTED_EDGE('',*,*,#13107,.T.);
#17228=ORIENTED_EDGE('',*,*,#13103,.T.);
#17229=ORIENTED_EDGE('',*,*,#13108,.F.);
#17230=ORIENTED_EDGE('',*,*,#13109,.F.);
#17231=ORIENTED_EDGE('',*,*,#13110,.T.);
#17232=ORIENTED_EDGE('',*,*,#13106,.T.);
#17233=ORIENTED_EDGE('',*,*,#13111,.F.);
#17234=ORIENTED_EDGE('',*,*,#13112,.F.);
#17235=ORIENTED_EDGE('',*,*,#13113,.T.);
#17236=ORIENTED_EDGE('',*,*,#13109,.T.);
#17237=ORIENTED_EDGE('',*,*,#13114,.F.);
#17238=ORIENTED_EDGE('',*,*,#13115,.F.);
#17239=ORIENTED_EDGE('',*,*,#13116,.T.);
#17240=ORIENTED_EDGE('',*,*,#13112,.T.);
#17241=ORIENTED_EDGE('',*,*,#13117,.F.);
#17242=ORIENTED_EDGE('',*,*,#13118,.F.);
#17243=ORIENTED_EDGE('',*,*,#13119,.T.);
#17244=ORIENTED_EDGE('',*,*,#13115,.T.);
#17245=ORIENTED_EDGE('',*,*,#13120,.F.);
#17246=ORIENTED_EDGE('',*,*,#13121,.F.);
#17247=ORIENTED_EDGE('',*,*,#13122,.T.);
#17248=ORIENTED_EDGE('',*,*,#13118,.T.);
#17249=ORIENTED_EDGE('',*,*,#13123,.F.);
#17250=ORIENTED_EDGE('',*,*,#13124,.F.);
#17251=ORIENTED_EDGE('',*,*,#13125,.T.);
#17252=ORIENTED_EDGE('',*,*,#13121,.T.);
#17253=ORIENTED_EDGE('',*,*,#13126,.F.);
#17254=ORIENTED_EDGE('',*,*,#13127,.F.);
#17255=ORIENTED_EDGE('',*,*,#13128,.T.);
#17256=ORIENTED_EDGE('',*,*,#13124,.T.);
#17257=ORIENTED_EDGE('',*,*,#13129,.F.);
#17258=ORIENTED_EDGE('',*,*,#13130,.F.);
#17259=ORIENTED_EDGE('',*,*,#13131,.T.);
#17260=ORIENTED_EDGE('',*,*,#13127,.T.);
#17261=ORIENTED_EDGE('',*,*,#13132,.F.);
#17262=ORIENTED_EDGE('',*,*,#13133,.F.);
#17263=ORIENTED_EDGE('',*,*,#13134,.T.);
#17264=ORIENTED_EDGE('',*,*,#13130,.T.);
#17265=ORIENTED_EDGE('',*,*,#13135,.F.);
#17266=ORIENTED_EDGE('',*,*,#13136,.F.);
#17267=ORIENTED_EDGE('',*,*,#13137,.T.);
#17268=ORIENTED_EDGE('',*,*,#13133,.T.);
#17269=ORIENTED_EDGE('',*,*,#13138,.F.);
#17270=ORIENTED_EDGE('',*,*,#13139,.F.);
#17271=ORIENTED_EDGE('',*,*,#13140,.T.);
#17272=ORIENTED_EDGE('',*,*,#13136,.T.);
#17273=ORIENTED_EDGE('',*,*,#13141,.F.);
#17274=ORIENTED_EDGE('',*,*,#13142,.F.);
#17275=ORIENTED_EDGE('',*,*,#13143,.T.);
#17276=ORIENTED_EDGE('',*,*,#13139,.T.);
#17277=ORIENTED_EDGE('',*,*,#13144,.F.);
#17278=ORIENTED_EDGE('',*,*,#13145,.F.);
#17279=ORIENTED_EDGE('',*,*,#13146,.T.);
#17280=ORIENTED_EDGE('',*,*,#13142,.T.);
#17281=ORIENTED_EDGE('',*,*,#13147,.F.);
#17282=ORIENTED_EDGE('',*,*,#13148,.F.);
#17283=ORIENTED_EDGE('',*,*,#13149,.T.);
#17284=ORIENTED_EDGE('',*,*,#13145,.T.);
#17285=ORIENTED_EDGE('',*,*,#13150,.F.);
#17286=ORIENTED_EDGE('',*,*,#13151,.F.);
#17287=ORIENTED_EDGE('',*,*,#13152,.T.);
#17288=ORIENTED_EDGE('',*,*,#13148,.T.);
#17289=ORIENTED_EDGE('',*,*,#13153,.F.);
#17290=ORIENTED_EDGE('',*,*,#13154,.F.);
#17291=ORIENTED_EDGE('',*,*,#13155,.T.);
#17292=ORIENTED_EDGE('',*,*,#13151,.T.);
#17293=ORIENTED_EDGE('',*,*,#13156,.F.);
#17294=ORIENTED_EDGE('',*,*,#13157,.F.);
#17295=ORIENTED_EDGE('',*,*,#13158,.T.);
#17296=ORIENTED_EDGE('',*,*,#13154,.T.);
#17297=ORIENTED_EDGE('',*,*,#13159,.F.);
#17298=ORIENTED_EDGE('',*,*,#13160,.F.);
#17299=ORIENTED_EDGE('',*,*,#13161,.T.);
#17300=ORIENTED_EDGE('',*,*,#13157,.T.);
#17301=ORIENTED_EDGE('',*,*,#13162,.F.);
#17302=ORIENTED_EDGE('',*,*,#13163,.T.);
#17303=ORIENTED_EDGE('',*,*,#13164,.T.);
#17304=ORIENTED_EDGE('',*,*,#12785,.F.);
#17305=ORIENTED_EDGE('',*,*,#13165,.T.);
#17306=ORIENTED_EDGE('',*,*,#13166,.T.);
#17307=ORIENTED_EDGE('',*,*,#13163,.F.);
#17308=ORIENTED_EDGE('',*,*,#13167,.T.);
#17309=ORIENTED_EDGE('',*,*,#13168,.T.);
#17310=ORIENTED_EDGE('',*,*,#13167,.F.);
#17311=ORIENTED_EDGE('',*,*,#13168,.F.);
#17312=ORIENTED_EDGE('',*,*,#13169,.F.);
#17313=ORIENTED_EDGE('',*,*,#13170,.F.);
#17314=ORIENTED_EDGE('',*,*,#12972,.F.);
#17315=ORIENTED_EDGE('',*,*,#12969,.F.);
#17316=ORIENTED_EDGE('',*,*,#12966,.F.);
#17317=ORIENTED_EDGE('',*,*,#12963,.F.);
#17318=ORIENTED_EDGE('',*,*,#12960,.F.);
#17319=ORIENTED_EDGE('',*,*,#12957,.F.);
#17320=ORIENTED_EDGE('',*,*,#12954,.F.);
#17321=ORIENTED_EDGE('',*,*,#12951,.F.);
#17322=ORIENTED_EDGE('',*,*,#12948,.F.);
#17323=ORIENTED_EDGE('',*,*,#12945,.F.);
#17324=ORIENTED_EDGE('',*,*,#12942,.F.);
#17325=ORIENTED_EDGE('',*,*,#12939,.F.);
#17326=ORIENTED_EDGE('',*,*,#12936,.F.);
#17327=ORIENTED_EDGE('',*,*,#12933,.F.);
#17328=ORIENTED_EDGE('',*,*,#12930,.F.);
#17329=ORIENTED_EDGE('',*,*,#12927,.F.);
#17330=ORIENTED_EDGE('',*,*,#12924,.F.);
#17331=ORIENTED_EDGE('',*,*,#12921,.F.);
#17332=ORIENTED_EDGE('',*,*,#12918,.F.);
#17333=ORIENTED_EDGE('',*,*,#12915,.F.);
#17334=ORIENTED_EDGE('',*,*,#12912,.F.);
#17335=ORIENTED_EDGE('',*,*,#12909,.F.);
#17336=ORIENTED_EDGE('',*,*,#12906,.F.);
#17337=ORIENTED_EDGE('',*,*,#12903,.F.);
#17338=ORIENTED_EDGE('',*,*,#12900,.F.);
#17339=ORIENTED_EDGE('',*,*,#12897,.F.);
#17340=ORIENTED_EDGE('',*,*,#12894,.F.);
#17341=ORIENTED_EDGE('',*,*,#12891,.F.);
#17342=ORIENTED_EDGE('',*,*,#12888,.F.);
#17343=ORIENTED_EDGE('',*,*,#12885,.F.);
#17344=ORIENTED_EDGE('',*,*,#12882,.F.);
#17345=ORIENTED_EDGE('',*,*,#12879,.F.);
#17346=ORIENTED_EDGE('',*,*,#12876,.F.);
#17347=ORIENTED_EDGE('',*,*,#12873,.F.);
#17348=ORIENTED_EDGE('',*,*,#12870,.F.);
#17349=ORIENTED_EDGE('',*,*,#12867,.F.);
#17350=ORIENTED_EDGE('',*,*,#12864,.F.);
#17351=ORIENTED_EDGE('',*,*,#12861,.F.);
#17352=ORIENTED_EDGE('',*,*,#12858,.F.);
#17353=ORIENTED_EDGE('',*,*,#12855,.F.);
#17354=ORIENTED_EDGE('',*,*,#12852,.F.);
#17355=ORIENTED_EDGE('',*,*,#12849,.F.);
#17356=ORIENTED_EDGE('',*,*,#12846,.F.);
#17357=ORIENTED_EDGE('',*,*,#12843,.F.);
#17358=ORIENTED_EDGE('',*,*,#12840,.F.);
#17359=ORIENTED_EDGE('',*,*,#12837,.F.);
#17360=ORIENTED_EDGE('',*,*,#12834,.F.);
#17361=ORIENTED_EDGE('',*,*,#12831,.F.);
#17362=ORIENTED_EDGE('',*,*,#12828,.F.);
#17363=ORIENTED_EDGE('',*,*,#12825,.F.);
#17364=ORIENTED_EDGE('',*,*,#12822,.F.);
#17365=ORIENTED_EDGE('',*,*,#12819,.F.);
#17366=ORIENTED_EDGE('',*,*,#12816,.F.);
#17367=ORIENTED_EDGE('',*,*,#12813,.F.);
#17368=ORIENTED_EDGE('',*,*,#12810,.F.);
#17369=ORIENTED_EDGE('',*,*,#12807,.F.);
#17370=ORIENTED_EDGE('',*,*,#12804,.F.);
#17371=ORIENTED_EDGE('',*,*,#12801,.F.);
#17372=ORIENTED_EDGE('',*,*,#12798,.F.);
#17373=ORIENTED_EDGE('',*,*,#12795,.F.);
#17374=ORIENTED_EDGE('',*,*,#12792,.F.);
#17375=ORIENTED_EDGE('',*,*,#12789,.F.);
#17376=ORIENTED_EDGE('',*,*,#12786,.F.);
#17377=ORIENTED_EDGE('',*,*,#13164,.F.);
#17378=ORIENTED_EDGE('',*,*,#13171,.T.);
#17379=ORIENTED_EDGE('',*,*,#13162,.T.);
#17380=ORIENTED_EDGE('',*,*,#13159,.T.);
#17381=ORIENTED_EDGE('',*,*,#13156,.T.);
#17382=ORIENTED_EDGE('',*,*,#13153,.T.);
#17383=ORIENTED_EDGE('',*,*,#13150,.T.);
#17384=ORIENTED_EDGE('',*,*,#13147,.T.);
#17385=ORIENTED_EDGE('',*,*,#13144,.T.);
#17386=ORIENTED_EDGE('',*,*,#13141,.T.);
#17387=ORIENTED_EDGE('',*,*,#13138,.T.);
#17388=ORIENTED_EDGE('',*,*,#13135,.T.);
#17389=ORIENTED_EDGE('',*,*,#13132,.T.);
#17390=ORIENTED_EDGE('',*,*,#13129,.T.);
#17391=ORIENTED_EDGE('',*,*,#13126,.T.);
#17392=ORIENTED_EDGE('',*,*,#13123,.T.);
#17393=ORIENTED_EDGE('',*,*,#13120,.T.);
#17394=ORIENTED_EDGE('',*,*,#13117,.T.);
#17395=ORIENTED_EDGE('',*,*,#13114,.T.);
#17396=ORIENTED_EDGE('',*,*,#13111,.T.);
#17397=ORIENTED_EDGE('',*,*,#13108,.T.);
#17398=ORIENTED_EDGE('',*,*,#13105,.T.);
#17399=ORIENTED_EDGE('',*,*,#13102,.T.);
#17400=ORIENTED_EDGE('',*,*,#13099,.T.);
#17401=ORIENTED_EDGE('',*,*,#13096,.T.);
#17402=ORIENTED_EDGE('',*,*,#13093,.T.);
#17403=ORIENTED_EDGE('',*,*,#13090,.T.);
#17404=ORIENTED_EDGE('',*,*,#13087,.T.);
#17405=ORIENTED_EDGE('',*,*,#13084,.T.);
#17406=ORIENTED_EDGE('',*,*,#13081,.T.);
#17407=ORIENTED_EDGE('',*,*,#13078,.T.);
#17408=ORIENTED_EDGE('',*,*,#13075,.T.);
#17409=ORIENTED_EDGE('',*,*,#13072,.T.);
#17410=ORIENTED_EDGE('',*,*,#13069,.T.);
#17411=ORIENTED_EDGE('',*,*,#13066,.T.);
#17412=ORIENTED_EDGE('',*,*,#13063,.T.);
#17413=ORIENTED_EDGE('',*,*,#13060,.T.);
#17414=ORIENTED_EDGE('',*,*,#13057,.T.);
#17415=ORIENTED_EDGE('',*,*,#13054,.T.);
#17416=ORIENTED_EDGE('',*,*,#13051,.T.);
#17417=ORIENTED_EDGE('',*,*,#13048,.T.);
#17418=ORIENTED_EDGE('',*,*,#13045,.T.);
#17419=ORIENTED_EDGE('',*,*,#13042,.T.);
#17420=ORIENTED_EDGE('',*,*,#13039,.T.);
#17421=ORIENTED_EDGE('',*,*,#13036,.T.);
#17422=ORIENTED_EDGE('',*,*,#13033,.T.);
#17423=ORIENTED_EDGE('',*,*,#13030,.T.);
#17424=ORIENTED_EDGE('',*,*,#13027,.T.);
#17425=ORIENTED_EDGE('',*,*,#13024,.T.);
#17426=ORIENTED_EDGE('',*,*,#13021,.T.);
#17427=ORIENTED_EDGE('',*,*,#13018,.T.);
#17428=ORIENTED_EDGE('',*,*,#13015,.T.);
#17429=ORIENTED_EDGE('',*,*,#13012,.T.);
#17430=ORIENTED_EDGE('',*,*,#13009,.T.);
#17431=ORIENTED_EDGE('',*,*,#13006,.T.);
#17432=ORIENTED_EDGE('',*,*,#13003,.T.);
#17433=ORIENTED_EDGE('',*,*,#13000,.T.);
#17434=ORIENTED_EDGE('',*,*,#12997,.T.);
#17435=ORIENTED_EDGE('',*,*,#12994,.T.);
#17436=ORIENTED_EDGE('',*,*,#12991,.T.);
#17437=ORIENTED_EDGE('',*,*,#12988,.T.);
#17438=ORIENTED_EDGE('',*,*,#12985,.T.);
#17439=ORIENTED_EDGE('',*,*,#12982,.T.);
#17440=ORIENTED_EDGE('',*,*,#12979,.T.);
#17441=ORIENTED_EDGE('',*,*,#13160,.T.);
#17442=ORIENTED_EDGE('',*,*,#13171,.F.);
#17443=ORIENTED_EDGE('',*,*,#13166,.F.);
#17444=ORIENTED_EDGE('',*,*,#13172,.T.);
#17445=ORIENTED_EDGE('',*,*,#13173,.F.);
#17446=ORIENTED_EDGE('',*,*,#12974,.F.);
#17447=ORIENTED_EDGE('',*,*,#12977,.F.);
#17448=ORIENTED_EDGE('',*,*,#12981,.F.);
#17449=ORIENTED_EDGE('',*,*,#12984,.F.);
#17450=ORIENTED_EDGE('',*,*,#12987,.F.);
#17451=ORIENTED_EDGE('',*,*,#12990,.F.);
#17452=ORIENTED_EDGE('',*,*,#12993,.F.);
#17453=ORIENTED_EDGE('',*,*,#12996,.F.);
#17454=ORIENTED_EDGE('',*,*,#12999,.F.);
#17455=ORIENTED_EDGE('',*,*,#13002,.F.);
#17456=ORIENTED_EDGE('',*,*,#13005,.F.);
#17457=ORIENTED_EDGE('',*,*,#13008,.F.);
#17458=ORIENTED_EDGE('',*,*,#13011,.F.);
#17459=ORIENTED_EDGE('',*,*,#13014,.F.);
#17460=ORIENTED_EDGE('',*,*,#13017,.F.);
#17461=ORIENTED_EDGE('',*,*,#13020,.F.);
#17462=ORIENTED_EDGE('',*,*,#13023,.F.);
#17463=ORIENTED_EDGE('',*,*,#13026,.F.);
#17464=ORIENTED_EDGE('',*,*,#13029,.F.);
#17465=ORIENTED_EDGE('',*,*,#13032,.F.);
#17466=ORIENTED_EDGE('',*,*,#13035,.F.);
#17467=ORIENTED_EDGE('',*,*,#13038,.F.);
#17468=ORIENTED_EDGE('',*,*,#13041,.F.);
#17469=ORIENTED_EDGE('',*,*,#13044,.F.);
#17470=ORIENTED_EDGE('',*,*,#13047,.F.);
#17471=ORIENTED_EDGE('',*,*,#13050,.F.);
#17472=ORIENTED_EDGE('',*,*,#13053,.F.);
#17473=ORIENTED_EDGE('',*,*,#13056,.F.);
#17474=ORIENTED_EDGE('',*,*,#13059,.F.);
#17475=ORIENTED_EDGE('',*,*,#13062,.F.);
#17476=ORIENTED_EDGE('',*,*,#13065,.F.);
#17477=ORIENTED_EDGE('',*,*,#13068,.F.);
#17478=ORIENTED_EDGE('',*,*,#13071,.F.);
#17479=ORIENTED_EDGE('',*,*,#13074,.F.);
#17480=ORIENTED_EDGE('',*,*,#13077,.F.);
#17481=ORIENTED_EDGE('',*,*,#13080,.F.);
#17482=ORIENTED_EDGE('',*,*,#13083,.F.);
#17483=ORIENTED_EDGE('',*,*,#13086,.F.);
#17484=ORIENTED_EDGE('',*,*,#13089,.F.);
#17485=ORIENTED_EDGE('',*,*,#13092,.F.);
#17486=ORIENTED_EDGE('',*,*,#13095,.F.);
#17487=ORIENTED_EDGE('',*,*,#13098,.F.);
#17488=ORIENTED_EDGE('',*,*,#13101,.F.);
#17489=ORIENTED_EDGE('',*,*,#13104,.F.);
#17490=ORIENTED_EDGE('',*,*,#13107,.F.);
#17491=ORIENTED_EDGE('',*,*,#13110,.F.);
#17492=ORIENTED_EDGE('',*,*,#13113,.F.);
#17493=ORIENTED_EDGE('',*,*,#13116,.F.);
#17494=ORIENTED_EDGE('',*,*,#13119,.F.);
#17495=ORIENTED_EDGE('',*,*,#13122,.F.);
#17496=ORIENTED_EDGE('',*,*,#13125,.F.);
#17497=ORIENTED_EDGE('',*,*,#13128,.F.);
#17498=ORIENTED_EDGE('',*,*,#13131,.F.);
#17499=ORIENTED_EDGE('',*,*,#13134,.F.);
#17500=ORIENTED_EDGE('',*,*,#13137,.F.);
#17501=ORIENTED_EDGE('',*,*,#13140,.F.);
#17502=ORIENTED_EDGE('',*,*,#13143,.F.);
#17503=ORIENTED_EDGE('',*,*,#13146,.F.);
#17504=ORIENTED_EDGE('',*,*,#13149,.F.);
#17505=ORIENTED_EDGE('',*,*,#13152,.F.);
#17506=ORIENTED_EDGE('',*,*,#13155,.F.);
#17507=ORIENTED_EDGE('',*,*,#13158,.F.);
#17508=ORIENTED_EDGE('',*,*,#13161,.F.);
#17509=ORIENTED_EDGE('',*,*,#13172,.F.);
#17510=ORIENTED_EDGE('',*,*,#13165,.F.);
#17511=ORIENTED_EDGE('',*,*,#12784,.F.);
#17512=ORIENTED_EDGE('',*,*,#12788,.F.);
#17513=ORIENTED_EDGE('',*,*,#12791,.F.);
#17514=ORIENTED_EDGE('',*,*,#12794,.F.);
#17515=ORIENTED_EDGE('',*,*,#12797,.F.);
#17516=ORIENTED_EDGE('',*,*,#12800,.F.);
#17517=ORIENTED_EDGE('',*,*,#12803,.F.);
#17518=ORIENTED_EDGE('',*,*,#12806,.F.);
#17519=ORIENTED_EDGE('',*,*,#12809,.F.);
#17520=ORIENTED_EDGE('',*,*,#12812,.F.);
#17521=ORIENTED_EDGE('',*,*,#12815,.F.);
#17522=ORIENTED_EDGE('',*,*,#12818,.F.);
#17523=ORIENTED_EDGE('',*,*,#12821,.F.);
#17524=ORIENTED_EDGE('',*,*,#12824,.F.);
#17525=ORIENTED_EDGE('',*,*,#12827,.F.);
#17526=ORIENTED_EDGE('',*,*,#12830,.F.);
#17527=ORIENTED_EDGE('',*,*,#12833,.F.);
#17528=ORIENTED_EDGE('',*,*,#12836,.F.);
#17529=ORIENTED_EDGE('',*,*,#12839,.F.);
#17530=ORIENTED_EDGE('',*,*,#12842,.F.);
#17531=ORIENTED_EDGE('',*,*,#12845,.F.);
#17532=ORIENTED_EDGE('',*,*,#12848,.F.);
#17533=ORIENTED_EDGE('',*,*,#12851,.F.);
#17534=ORIENTED_EDGE('',*,*,#12854,.F.);
#17535=ORIENTED_EDGE('',*,*,#12857,.F.);
#17536=ORIENTED_EDGE('',*,*,#12860,.F.);
#17537=ORIENTED_EDGE('',*,*,#12863,.F.);
#17538=ORIENTED_EDGE('',*,*,#12866,.F.);
#17539=ORIENTED_EDGE('',*,*,#12869,.F.);
#17540=ORIENTED_EDGE('',*,*,#12872,.F.);
#17541=ORIENTED_EDGE('',*,*,#12875,.F.);
#17542=ORIENTED_EDGE('',*,*,#12878,.F.);
#17543=ORIENTED_EDGE('',*,*,#12881,.F.);
#17544=ORIENTED_EDGE('',*,*,#12884,.F.);
#17545=ORIENTED_EDGE('',*,*,#12887,.F.);
#17546=ORIENTED_EDGE('',*,*,#12890,.F.);
#17547=ORIENTED_EDGE('',*,*,#12893,.F.);
#17548=ORIENTED_EDGE('',*,*,#12896,.F.);
#17549=ORIENTED_EDGE('',*,*,#12899,.F.);
#17550=ORIENTED_EDGE('',*,*,#12902,.F.);
#17551=ORIENTED_EDGE('',*,*,#12905,.F.);
#17552=ORIENTED_EDGE('',*,*,#12908,.F.);
#17553=ORIENTED_EDGE('',*,*,#12911,.F.);
#17554=ORIENTED_EDGE('',*,*,#12914,.F.);
#17555=ORIENTED_EDGE('',*,*,#12917,.F.);
#17556=ORIENTED_EDGE('',*,*,#12920,.F.);
#17557=ORIENTED_EDGE('',*,*,#12923,.F.);
#17558=ORIENTED_EDGE('',*,*,#12926,.F.);
#17559=ORIENTED_EDGE('',*,*,#12929,.F.);
#17560=ORIENTED_EDGE('',*,*,#12932,.F.);
#17561=ORIENTED_EDGE('',*,*,#12935,.F.);
#17562=ORIENTED_EDGE('',*,*,#12938,.F.);
#17563=ORIENTED_EDGE('',*,*,#12941,.F.);
#17564=ORIENTED_EDGE('',*,*,#12944,.F.);
#17565=ORIENTED_EDGE('',*,*,#12947,.F.);
#17566=ORIENTED_EDGE('',*,*,#12950,.F.);
#17567=ORIENTED_EDGE('',*,*,#12953,.F.);
#17568=ORIENTED_EDGE('',*,*,#12956,.F.);
#17569=ORIENTED_EDGE('',*,*,#12959,.F.);
#17570=ORIENTED_EDGE('',*,*,#12962,.F.);
#17571=ORIENTED_EDGE('',*,*,#12965,.F.);
#17572=ORIENTED_EDGE('',*,*,#12968,.F.);
#17573=ORIENTED_EDGE('',*,*,#12971,.F.);
#17574=ORIENTED_EDGE('',*,*,#13174,.F.);
#17575=ORIENTED_EDGE('',*,*,#13175,.F.);
#17576=ORIENTED_EDGE('',*,*,#13176,.T.);
#17577=ORIENTED_EDGE('',*,*,#13177,.F.);
#17578=ORIENTED_EDGE('',*,*,#13178,.F.);
#17579=ORIENTED_EDGE('',*,*,#13179,.F.);
#17580=ORIENTED_EDGE('',*,*,#13178,.T.);
#17581=ORIENTED_EDGE('',*,*,#13180,.T.);
#17582=ORIENTED_EDGE('',*,*,#13181,.T.);
#17583=ORIENTED_EDGE('',*,*,#13180,.F.);
#17584=ORIENTED_EDGE('',*,*,#13177,.T.);
#17585=ORIENTED_EDGE('',*,*,#13182,.T.);
#17586=ORIENTED_EDGE('',*,*,#13183,.F.);
#17587=ORIENTED_EDGE('',*,*,#13184,.F.);
#17588=ORIENTED_EDGE('',*,*,#13181,.F.);
#17589=ORIENTED_EDGE('',*,*,#13183,.T.);
#17590=ORIENTED_EDGE('',*,*,#13185,.T.);
#17591=ORIENTED_EDGE('',*,*,#13186,.F.);
#17592=ORIENTED_EDGE('',*,*,#13185,.F.);
#17593=ORIENTED_EDGE('',*,*,#13182,.F.);
#17594=ORIENTED_EDGE('',*,*,#13176,.F.);
#17595=ORIENTED_EDGE('',*,*,#13187,.F.);
#17596=ORIENTED_EDGE('',*,*,#13188,.T.);
#17597=ORIENTED_EDGE('',*,*,#13189,.F.);
#17598=ORIENTED_EDGE('',*,*,#13188,.F.);
#17599=ORIENTED_EDGE('',*,*,#13184,.T.);
#17600=ORIENTED_EDGE('',*,*,#13186,.T.);
#17601=ORIENTED_EDGE('',*,*,#13175,.T.);
#17602=ORIENTED_EDGE('',*,*,#13179,.T.);
#17603=ORIENTED_EDGE('',*,*,#13187,.T.);
#17604=ORIENTED_EDGE('',*,*,#13190,.F.);
#17605=ORIENTED_EDGE('',*,*,#13191,.T.);
#17606=ORIENTED_EDGE('',*,*,#13169,.T.);
#17607=ORIENTED_EDGE('',*,*,#12978,.T.);
#17608=ORIENTED_EDGE('',*,*,#12975,.T.);
#17609=ORIENTED_EDGE('',*,*,#13173,.T.);
#17610=ORIENTED_EDGE('',*,*,#13192,.F.);
#17611=ORIENTED_EDGE('',*,*,#13193,.T.);
#17612=ORIENTED_EDGE('',*,*,#13190,.T.);
#17613=ORIENTED_EDGE('',*,*,#13193,.F.);
#17614=ORIENTED_EDGE('',*,*,#13192,.T.);
#17615=ORIENTED_EDGE('',*,*,#13189,.T.);
#17616=ORIENTED_EDGE('',*,*,#12970,.T.);
#17617=ORIENTED_EDGE('',*,*,#13170,.T.);
#17618=ORIENTED_EDGE('',*,*,#13191,.F.);
#17619=ORIENTED_EDGE('',*,*,#13174,.T.);
#21188=CYLINDRICAL_SURFACE('',#24871,0.5941);
#21189=CYLINDRICAL_SURFACE('',#24873,0.5941);
#21190=CYLINDRICAL_SURFACE('',#24874,0.5941);
#21191=CYLINDRICAL_SURFACE('',#24875,0.5941);
#21192=CYLINDRICAL_SURFACE('',#24876,0.5941);
#21193=CYLINDRICAL_SURFACE('',#24877,0.5941);
#21194=CYLINDRICAL_SURFACE('',#24878,0.5941);
#21195=CYLINDRICAL_SURFACE('',#24879,0.5941);
#21196=CYLINDRICAL_SURFACE('',#24880,0.5941);
#21197=CYLINDRICAL_SURFACE('',#24881,0.5941);
#21198=CYLINDRICAL_SURFACE('',#24882,0.5941);
#21199=CYLINDRICAL_SURFACE('',#24883,0.5941);
#21200=CYLINDRICAL_SURFACE('',#24884,0.5941);
#21201=CYLINDRICAL_SURFACE('',#24885,0.5941);
#21202=CYLINDRICAL_SURFACE('',#24886,0.5941);
#21203=CYLINDRICAL_SURFACE('',#24887,0.5941);
#21204=CYLINDRICAL_SURFACE('',#24888,0.5941);
#21205=CYLINDRICAL_SURFACE('',#24889,0.5941);
#21206=CYLINDRICAL_SURFACE('',#24890,0.5941);
#21207=CYLINDRICAL_SURFACE('',#24891,0.5941);
#21208=CYLINDRICAL_SURFACE('',#24892,0.5941);
#21209=CYLINDRICAL_SURFACE('',#24893,0.5941);
#21210=CYLINDRICAL_SURFACE('',#24894,0.5941);
#21211=CYLINDRICAL_SURFACE('',#24895,0.5941);
#21212=CYLINDRICAL_SURFACE('',#24896,0.5941);
#21213=CYLINDRICAL_SURFACE('',#24897,0.5941);
#21214=CYLINDRICAL_SURFACE('',#24898,0.5941);
#21215=CYLINDRICAL_SURFACE('',#24899,0.5941);
#21216=CYLINDRICAL_SURFACE('',#24900,0.5941);
#21217=CYLINDRICAL_SURFACE('',#24901,0.5941);
#21218=CYLINDRICAL_SURFACE('',#24902,0.5941);
#21219=CYLINDRICAL_SURFACE('',#24903,0.5941);
#21220=CYLINDRICAL_SURFACE('',#24904,0.5941);
#21221=CYLINDRICAL_SURFACE('',#24905,0.5941);
#21222=CYLINDRICAL_SURFACE('',#24906,0.5941);
#21223=CYLINDRICAL_SURFACE('',#24907,0.5941);
#21224=CYLINDRICAL_SURFACE('',#24908,0.5941);
#21225=CYLINDRICAL_SURFACE('',#24909,0.5941);
#21226=CYLINDRICAL_SURFACE('',#24910,0.5941);
#21227=CYLINDRICAL_SURFACE('',#24911,0.5941);
#21228=CYLINDRICAL_SURFACE('',#24912,0.5941);
#21229=CYLINDRICAL_SURFACE('',#24913,0.5941);
#21230=CYLINDRICAL_SURFACE('',#24914,0.5941);
#21231=CYLINDRICAL_SURFACE('',#24915,0.5941);
#21232=CYLINDRICAL_SURFACE('',#24916,0.5941);
#21233=CYLINDRICAL_SURFACE('',#24917,0.5941);
#21234=CYLINDRICAL_SURFACE('',#24918,0.5941);
#21235=CYLINDRICAL_SURFACE('',#24919,0.5941);
#21236=CYLINDRICAL_SURFACE('',#24920,0.5941);
#21237=CYLINDRICAL_SURFACE('',#24921,0.5941);
#21238=CYLINDRICAL_SURFACE('',#24922,0.5941);
#21239=CYLINDRICAL_SURFACE('',#24923,0.5941);
#21240=CYLINDRICAL_SURFACE('',#24924,0.5941);
#21241=CYLINDRICAL_SURFACE('',#24925,0.5941);
#21242=CYLINDRICAL_SURFACE('',#24926,0.5941);
#21243=CYLINDRICAL_SURFACE('',#24927,0.5941);
#21244=CYLINDRICAL_SURFACE('',#24928,0.5941);
#21245=CYLINDRICAL_SURFACE('',#24929,0.5941);
#21246=CYLINDRICAL_SURFACE('',#24930,0.5941);
#21247=CYLINDRICAL_SURFACE('',#24931,0.5941);
#21248=CYLINDRICAL_SURFACE('',#24932,0.5941);
#21249=CYLINDRICAL_SURFACE('',#24933,0.5941);
#21250=CYLINDRICAL_SURFACE('',#24934,0.5941);
#21251=CYLINDRICAL_SURFACE('',#24935,0.415875);
#21252=CYLINDRICAL_SURFACE('',#24937,0.415875);
#21253=CYLINDRICAL_SURFACE('',#24939,0.415875);
#21254=CYLINDRICAL_SURFACE('',#24940,0.415875);
#21255=CYLINDRICAL_SURFACE('',#24941,0.415875);
#21256=CYLINDRICAL_SURFACE('',#24942,0.415875);
#21257=CYLINDRICAL_SURFACE('',#24943,0.415875);
#21258=CYLINDRICAL_SURFACE('',#24944,0.415875);
#21259=CYLINDRICAL_SURFACE('',#24945,0.415875);
#21260=CYLINDRICAL_SURFACE('',#24946,0.415875);
#21261=CYLINDRICAL_SURFACE('',#24947,0.415875);
#21262=CYLINDRICAL_SURFACE('',#24948,0.415875);
#21263=CYLINDRICAL_SURFACE('',#24949,0.415875);
#21264=CYLINDRICAL_SURFACE('',#24950,0.415875);
#21265=CYLINDRICAL_SURFACE('',#24951,0.415875);
#21266=CYLINDRICAL_SURFACE('',#24952,0.415875);
#21267=CYLINDRICAL_SURFACE('',#24953,0.415875);
#21268=CYLINDRICAL_SURFACE('',#24954,0.415875);
#21269=CYLINDRICAL_SURFACE('',#24955,0.415875);
#21270=CYLINDRICAL_SURFACE('',#24956,0.415875);
#21271=CYLINDRICAL_SURFACE('',#24957,0.415875);
#21272=CYLINDRICAL_SURFACE('',#24958,0.415875);
#21273=CYLINDRICAL_SURFACE('',#24959,0.415875);
#21274=CYLINDRICAL_SURFACE('',#24960,0.415875);
#21275=CYLINDRICAL_SURFACE('',#24961,0.415875);
#21276=CYLINDRICAL_SURFACE('',#24962,0.415875);
#21277=CYLINDRICAL_SURFACE('',#24963,0.415875);
#21278=CYLINDRICAL_SURFACE('',#24964,0.415875);
#21279=CYLINDRICAL_SURFACE('',#24965,0.415875);
#21280=CYLINDRICAL_SURFACE('',#24966,0.415875);
#21281=CYLINDRICAL_SURFACE('',#24967,0.415875);
#21282=CYLINDRICAL_SURFACE('',#24968,0.415875);
#21283=CYLINDRICAL_SURFACE('',#24969,0.415875);
#21284=CYLINDRICAL_SURFACE('',#24970,0.415875);
#21285=CYLINDRICAL_SURFACE('',#24971,0.415875);
#21286=CYLINDRICAL_SURFACE('',#24972,0.415875);
#21287=CYLINDRICAL_SURFACE('',#24973,0.415875);
#21288=CYLINDRICAL_SURFACE('',#24974,0.415875);
#21289=CYLINDRICAL_SURFACE('',#24975,0.415875);
#21290=CYLINDRICAL_SURFACE('',#24976,0.415875);
#21291=CYLINDRICAL_SURFACE('',#24977,0.415875);
#21292=CYLINDRICAL_SURFACE('',#24978,0.415875);
#21293=CYLINDRICAL_SURFACE('',#24979,0.415875);
#21294=CYLINDRICAL_SURFACE('',#24980,0.415875);
#21295=CYLINDRICAL_SURFACE('',#24981,0.415875);
#21296=CYLINDRICAL_SURFACE('',#24982,0.415875);
#21297=CYLINDRICAL_SURFACE('',#24983,0.415875);
#21298=CYLINDRICAL_SURFACE('',#24984,0.415875);
#21299=CYLINDRICAL_SURFACE('',#24985,0.415875);
#21300=CYLINDRICAL_SURFACE('',#24986,0.415875);
#21301=CYLINDRICAL_SURFACE('',#24987,0.415875);
#21302=CYLINDRICAL_SURFACE('',#24988,0.415875);
#21303=CYLINDRICAL_SURFACE('',#24989,0.415875);
#21304=CYLINDRICAL_SURFACE('',#24990,0.415875);
#21305=CYLINDRICAL_SURFACE('',#24991,0.415875);
#21306=CYLINDRICAL_SURFACE('',#24992,0.415875);
#21307=CYLINDRICAL_SURFACE('',#24993,0.415875);
#21308=CYLINDRICAL_SURFACE('',#24994,0.415875);
#21309=CYLINDRICAL_SURFACE('',#24995,0.415875);
#21310=CYLINDRICAL_SURFACE('',#24996,0.415875);
#21311=CYLINDRICAL_SURFACE('',#24997,0.415875);
#21312=CYLINDRICAL_SURFACE('',#24998,0.415875);
#21313=CYLINDRICAL_SURFACE('',#24999,0.415875);
#21314=CYLINDRICAL_SURFACE('',#25003,0.6);
#21315=CYLINDRICAL_SURFACE('',#25006,0.415875);
#21316=CYLINDRICAL_SURFACE('',#25014,1.);
#21317=CYLINDRICAL_SURFACE('',#25021,1.35);
#21318=CYLINDRICAL_SURFACE('',#25024,0.5941);
#22075=ADVANCED_FACE('',(#3294),#21188,.T.);
#22076=ADVANCED_FACE('',(#3295),#21189,.T.);
#22077=ADVANCED_FACE('',(#3296),#21190,.T.);
#22078=ADVANCED_FACE('',(#3297),#21191,.T.);
#22079=ADVANCED_FACE('',(#3298),#21192,.T.);
#22080=ADVANCED_FACE('',(#3299),#21193,.T.);
#22081=ADVANCED_FACE('',(#3300),#21194,.T.);
#22082=ADVANCED_FACE('',(#3301),#21195,.T.);
#22083=ADVANCED_FACE('',(#3302),#21196,.T.);
#22084=ADVANCED_FACE('',(#3303),#21197,.T.);
#22085=ADVANCED_FACE('',(#3304),#21198,.T.);
#22086=ADVANCED_FACE('',(#3305),#21199,.T.);
#22087=ADVANCED_FACE('',(#3306),#21200,.T.);
#22088=ADVANCED_FACE('',(#3307),#21201,.T.);
#22089=ADVANCED_FACE('',(#3308),#21202,.T.);
#22090=ADVANCED_FACE('',(#3309),#21203,.T.);
#22091=ADVANCED_FACE('',(#3310),#21204,.T.);
#22092=ADVANCED_FACE('',(#3311),#21205,.T.);
#22093=ADVANCED_FACE('',(#3312),#21206,.T.);
#22094=ADVANCED_FACE('',(#3313),#21207,.T.);
#22095=ADVANCED_FACE('',(#3314),#21208,.T.);
#22096=ADVANCED_FACE('',(#3315),#21209,.T.);
#22097=ADVANCED_FACE('',(#3316),#21210,.T.);
#22098=ADVANCED_FACE('',(#3317),#21211,.T.);
#22099=ADVANCED_FACE('',(#3318),#21212,.T.);
#22100=ADVANCED_FACE('',(#3319),#21213,.T.);
#22101=ADVANCED_FACE('',(#3320),#21214,.T.);
#22102=ADVANCED_FACE('',(#3321),#21215,.T.);
#22103=ADVANCED_FACE('',(#3322),#21216,.T.);
#22104=ADVANCED_FACE('',(#3323),#21217,.T.);
#22105=ADVANCED_FACE('',(#3324),#21218,.T.);
#22106=ADVANCED_FACE('',(#3325),#21219,.T.);
#22107=ADVANCED_FACE('',(#3326),#21220,.T.);
#22108=ADVANCED_FACE('',(#3327),#21221,.T.);
#22109=ADVANCED_FACE('',(#3328),#21222,.T.);
#22110=ADVANCED_FACE('',(#3329),#21223,.T.);
#22111=ADVANCED_FACE('',(#3330),#21224,.T.);
#22112=ADVANCED_FACE('',(#3331),#21225,.T.);
#22113=ADVANCED_FACE('',(#3332),#21226,.T.);
#22114=ADVANCED_FACE('',(#3333),#21227,.T.);
#22115=ADVANCED_FACE('',(#3334),#21228,.T.);
#22116=ADVANCED_FACE('',(#3335),#21229,.T.);
#22117=ADVANCED_FACE('',(#3336),#21230,.T.);
#22118=ADVANCED_FACE('',(#3337),#21231,.T.);
#22119=ADVANCED_FACE('',(#3338),#21232,.T.);
#22120=ADVANCED_FACE('',(#3339),#21233,.T.);
#22121=ADVANCED_FACE('',(#3340),#21234,.T.);
#22122=ADVANCED_FACE('',(#3341),#21235,.T.);
#22123=ADVANCED_FACE('',(#3342),#21236,.T.);
#22124=ADVANCED_FACE('',(#3343),#21237,.T.);
#22125=ADVANCED_FACE('',(#3344),#21238,.T.);
#22126=ADVANCED_FACE('',(#3345),#21239,.T.);
#22127=ADVANCED_FACE('',(#3346),#21240,.T.);
#22128=ADVANCED_FACE('',(#3347),#21241,.T.);
#22129=ADVANCED_FACE('',(#3348),#21242,.T.);
#22130=ADVANCED_FACE('',(#3349),#21243,.T.);
#22131=ADVANCED_FACE('',(#3350),#21244,.T.);
#22132=ADVANCED_FACE('',(#3351),#21245,.T.);
#22133=ADVANCED_FACE('',(#3352),#21246,.T.);
#22134=ADVANCED_FACE('',(#3353),#21247,.T.);
#22135=ADVANCED_FACE('',(#3354),#21248,.T.);
#22136=ADVANCED_FACE('',(#3355),#21249,.T.);
#22137=ADVANCED_FACE('',(#3356),#21250,.T.);
#22138=ADVANCED_FACE('',(#3357),#21251,.T.);
#22139=ADVANCED_FACE('',(#3358),#21252,.T.);
#22140=ADVANCED_FACE('',(#3359),#21253,.T.);
#22141=ADVANCED_FACE('',(#3360),#21254,.T.);
#22142=ADVANCED_FACE('',(#3361),#21255,.T.);
#22143=ADVANCED_FACE('',(#3362),#21256,.T.);
#22144=ADVANCED_FACE('',(#3363),#21257,.T.);
#22145=ADVANCED_FACE('',(#3364),#21258,.T.);
#22146=ADVANCED_FACE('',(#3365),#21259,.T.);
#22147=ADVANCED_FACE('',(#3366),#21260,.T.);
#22148=ADVANCED_FACE('',(#3367),#21261,.T.);
#22149=ADVANCED_FACE('',(#3368),#21262,.T.);
#22150=ADVANCED_FACE('',(#3369),#21263,.T.);
#22151=ADVANCED_FACE('',(#3370),#21264,.T.);
#22152=ADVANCED_FACE('',(#3371),#21265,.T.);
#22153=ADVANCED_FACE('',(#3372),#21266,.T.);
#22154=ADVANCED_FACE('',(#3373),#21267,.T.);
#22155=ADVANCED_FACE('',(#3374),#21268,.T.);
#22156=ADVANCED_FACE('',(#3375),#21269,.T.);
#22157=ADVANCED_FACE('',(#3376),#21270,.T.);
#22158=ADVANCED_FACE('',(#3377),#21271,.T.);
#22159=ADVANCED_FACE('',(#3378),#21272,.T.);
#22160=ADVANCED_FACE('',(#3379),#21273,.T.);
#22161=ADVANCED_FACE('',(#3380),#21274,.T.);
#22162=ADVANCED_FACE('',(#3381),#21275,.T.);
#22163=ADVANCED_FACE('',(#3382),#21276,.T.);
#22164=ADVANCED_FACE('',(#3383),#21277,.T.);
#22165=ADVANCED_FACE('',(#3384),#21278,.T.);
#22166=ADVANCED_FACE('',(#3385),#21279,.T.);
#22167=ADVANCED_FACE('',(#3386),#21280,.T.);
#22168=ADVANCED_FACE('',(#3387),#21281,.T.);
#22169=ADVANCED_FACE('',(#3388),#21282,.T.);
#22170=ADVANCED_FACE('',(#3389),#21283,.T.);
#22171=ADVANCED_FACE('',(#3390),#21284,.T.);
#22172=ADVANCED_FACE('',(#3391),#21285,.T.);
#22173=ADVANCED_FACE('',(#3392),#21286,.T.);
#22174=ADVANCED_FACE('',(#3393),#21287,.T.);
#22175=ADVANCED_FACE('',(#3394),#21288,.T.);
#22176=ADVANCED_FACE('',(#3395),#21289,.T.);
#22177=ADVANCED_FACE('',(#3396),#21290,.T.);
#22178=ADVANCED_FACE('',(#3397),#21291,.T.);
#22179=ADVANCED_FACE('',(#3398),#21292,.T.);
#22180=ADVANCED_FACE('',(#3399),#21293,.T.);
#22181=ADVANCED_FACE('',(#3400),#21294,.T.);
#22182=ADVANCED_FACE('',(#3401),#21295,.T.);
#22183=ADVANCED_FACE('',(#3402),#21296,.T.);
#22184=ADVANCED_FACE('',(#3403),#21297,.T.);
#22185=ADVANCED_FACE('',(#3404),#21298,.T.);
#22186=ADVANCED_FACE('',(#3405),#21299,.T.);
#22187=ADVANCED_FACE('',(#3406),#21300,.T.);
#22188=ADVANCED_FACE('',(#3407),#21301,.T.);
#22189=ADVANCED_FACE('',(#3408),#21302,.T.);
#22190=ADVANCED_FACE('',(#3409),#21303,.T.);
#22191=ADVANCED_FACE('',(#3410),#21304,.T.);
#22192=ADVANCED_FACE('',(#3411),#21305,.T.);
#22193=ADVANCED_FACE('',(#3412),#21306,.T.);
#22194=ADVANCED_FACE('',(#3413),#21307,.T.);
#22195=ADVANCED_FACE('',(#3414),#21308,.T.);
#22196=ADVANCED_FACE('',(#3415),#21309,.T.);
#22197=ADVANCED_FACE('',(#3416),#21310,.T.);
#22198=ADVANCED_FACE('',(#3417),#21311,.T.);
#22199=ADVANCED_FACE('',(#3418),#21312,.T.);
#22200=ADVANCED_FACE('',(#3419),#21313,.T.);
#22201=ADVANCED_FACE('',(#3420,#2061),#2517,.T.);
#22202=ADVANCED_FACE('',(#3421),#21314,.T.);
#22203=ADVANCED_FACE('',(#3422),#2518,.F.);
#22204=ADVANCED_FACE('',(#3423),#13,.F.);
#22205=ADVANCED_FACE('',(#3424),#21315,.T.);
#22206=ADVANCED_FACE('',(#3425),#14,.F.);
#22207=ADVANCED_FACE('',(#3426),#2519,.F.);
#22208=ADVANCED_FACE('',(#3427),#2520,.T.);
#22209=ADVANCED_FACE('',(#3428),#2521,.F.);
#22210=ADVANCED_FACE('',(#3429),#2522,.F.);
#22211=ADVANCED_FACE('',(#3430),#2523,.F.);
#22212=ADVANCED_FACE('',(#3431,#2062),#21316,.T.);
#22213=ADVANCED_FACE('',(#3432),#2524,.T.);
#22214=ADVANCED_FACE('',(#3433,#2063),#2525,.F.);
#22215=ADVANCED_FACE('',(#3434),#21317,.T.);
#22216=ADVANCED_FACE('',(#3435,#2064),#2526,.T.);
#22217=ADVANCED_FACE('',(#3436),#21318,.T.);
#23014=CLOSED_SHELL('',(#22075,#22076,#22077,#22078,#22079,#22080,#22081,
#22082,#22083,#22084,#22085,#22086,#22087,#22088,#22089,#22090,#22091,#22092,
#22093,#22094,#22095,#22096,#22097,#22098,#22099,#22100,#22101,#22102,#22103,
#22104,#22105,#22106,#22107,#22108,#22109,#22110,#22111,#22112,#22113,#22114,
#22115,#22116,#22117,#22118,#22119,#22120,#22121,#22122,#22123,#22124,#22125,
#22126,#22127,#22128,#22129,#22130,#22131,#22132,#22133,#22134,#22135,#22136,
#22137,#22138,#22139,#22140,#22141,#22142,#22143,#22144,#22145,#22146,#22147,
#22148,#22149,#22150,#22151,#22152,#22153,#22154,#22155,#22156,#22157,#22158,
#22159,#22160,#22161,#22162,#22163,#22164,#22165,#22166,#22167,#22168,#22169,
#22170,#22171,#22172,#22173,#22174,#22175,#22176,#22177,#22178,#22179,#22180,
#22181,#22182,#22183,#22184,#22185,#22186,#22187,#22188,#22189,#22190,#22191,
#22192,#22193,#22194,#22195,#22196,#22197,#22198,#22199,#22200,#22201,#22202,
#22203,#22204,#22205,#22206,#22207,#22208,#22209,#22210,#22211,#22212,#22213,
#22214,#22215,#22216,#22217));
#24870=AXIS2_PLACEMENT_3D('',#37618,#28699,#28700);
#24871=AXIS2_PLACEMENT_3D('',#37619,#28701,#28702);
#24872=AXIS2_PLACEMENT_3D('',#37644,#28704,#28705);
#24873=AXIS2_PLACEMENT_3D('',#37649,#28706,#28707);
#24874=AXIS2_PLACEMENT_3D('',#37736,#28709,#28710);
#24875=AXIS2_PLACEMENT_3D('',#37826,#28712,#28713);
#24876=AXIS2_PLACEMENT_3D('',#37913,#28715,#28716);
#24877=AXIS2_PLACEMENT_3D('',#38000,#28718,#28719);
#24878=AXIS2_PLACEMENT_3D('',#38087,#28721,#28722);
#24879=AXIS2_PLACEMENT_3D('',#38174,#28724,#28725);
#24880=AXIS2_PLACEMENT_3D('',#38261,#28727,#28728);
#24881=AXIS2_PLACEMENT_3D('',#38333,#28730,#28731);
#24882=AXIS2_PLACEMENT_3D('',#38384,#28733,#28734);
#24883=AXIS2_PLACEMENT_3D('',#38432,#28736,#28737);
#24884=AXIS2_PLACEMENT_3D('',#38480,#28739,#28740);
#24885=AXIS2_PLACEMENT_3D('',#38531,#28742,#28743);
#24886=AXIS2_PLACEMENT_3D('',#38582,#28745,#28746);
#24887=AXIS2_PLACEMENT_3D('',#38630,#28748,#28749);
#24888=AXIS2_PLACEMENT_3D('',#38681,#28751,#28752);
#24889=AXIS2_PLACEMENT_3D('',#38732,#28754,#28755);
#24890=AXIS2_PLACEMENT_3D('',#38780,#28757,#28758);
#24891=AXIS2_PLACEMENT_3D('',#38828,#28760,#28761);
#24892=AXIS2_PLACEMENT_3D('',#38879,#28763,#28764);
#24893=AXIS2_PLACEMENT_3D('',#38930,#28766,#28767);
#24894=AXIS2_PLACEMENT_3D('',#38978,#28769,#28770);
#24895=AXIS2_PLACEMENT_3D('',#39029,#28772,#28773);
#24896=AXIS2_PLACEMENT_3D('',#39080,#28775,#28776);
#24897=AXIS2_PLACEMENT_3D('',#39128,#28778,#28779);
#24898=AXIS2_PLACEMENT_3D('',#39176,#28781,#28782);
#24899=AXIS2_PLACEMENT_3D('',#39227,#28784,#28785);
#24900=AXIS2_PLACEMENT_3D('',#39278,#28787,#28788);
#24901=AXIS2_PLACEMENT_3D('',#39326,#28790,#28791);
#24902=AXIS2_PLACEMENT_3D('',#39377,#28793,#28794);
#24903=AXIS2_PLACEMENT_3D('',#39428,#28796,#28797);
#24904=AXIS2_PLACEMENT_3D('',#39476,#28799,#28800);
#24905=AXIS2_PLACEMENT_3D('',#39524,#28802,#28803);
#24906=AXIS2_PLACEMENT_3D('',#39575,#28805,#28806);
#24907=AXIS2_PLACEMENT_3D('',#39626,#28808,#28809);
#24908=AXIS2_PLACEMENT_3D('',#39674,#28811,#28812);
#24909=AXIS2_PLACEMENT_3D('',#39725,#28814,#28815);
#24910=AXIS2_PLACEMENT_3D('',#39776,#28817,#28818);
#24911=AXIS2_PLACEMENT_3D('',#39824,#28820,#28821);
#24912=AXIS2_PLACEMENT_3D('',#39872,#28823,#28824);
#24913=AXIS2_PLACEMENT_3D('',#39923,#28826,#28827);
#24914=AXIS2_PLACEMENT_3D('',#39974,#28829,#28830);
#24915=AXIS2_PLACEMENT_3D('',#40022,#28832,#28833);
#24916=AXIS2_PLACEMENT_3D('',#40073,#28835,#28836);
#24917=AXIS2_PLACEMENT_3D('',#40124,#28838,#28839);
#24918=AXIS2_PLACEMENT_3D('',#40172,#28841,#28842);
#24919=AXIS2_PLACEMENT_3D('',#40220,#28844,#28845);
#24920=AXIS2_PLACEMENT_3D('',#40271,#28847,#28848);
#24921=AXIS2_PLACEMENT_3D('',#40322,#28850,#28851);
#24922=AXIS2_PLACEMENT_3D('',#40370,#28853,#28854);
#24923=AXIS2_PLACEMENT_3D('',#40421,#28856,#28857);
#24924=AXIS2_PLACEMENT_3D('',#40472,#28859,#28860);
#24925=AXIS2_PLACEMENT_3D('',#40520,#28862,#28863);
#24926=AXIS2_PLACEMENT_3D('',#40568,#28865,#28866);
#24927=AXIS2_PLACEMENT_3D('',#40619,#28868,#28869);
#24928=AXIS2_PLACEMENT_3D('',#40685,#28871,#28872);
#24929=AXIS2_PLACEMENT_3D('',#40775,#28874,#28875);
#24930=AXIS2_PLACEMENT_3D('',#40862,#28877,#28878);
#24931=AXIS2_PLACEMENT_3D('',#40949,#28880,#28881);
#24932=AXIS2_PLACEMENT_3D('',#41036,#28883,#28884);
#24933=AXIS2_PLACEMENT_3D('',#41123,#28886,#28887);
#24934=AXIS2_PLACEMENT_3D('',#41210,#28889,#28890);
#24935=AXIS2_PLACEMENT_3D('',#41300,#28892,#28893);
#24936=AXIS2_PLACEMENT_3D('',#41309,#28895,#28896);
#24937=AXIS2_PLACEMENT_3D('',#41310,#28897,#28898);
#24938=AXIS2_PLACEMENT_3D('',#41332,#28900,#28901);
#24939=AXIS2_PLACEMENT_3D('',#41346,#28902,#28903);
#24940=AXIS2_PLACEMENT_3D('',#41384,#28905,#28906);
#24941=AXIS2_PLACEMENT_3D('',#41420,#28908,#28909);
#24942=AXIS2_PLACEMENT_3D('',#41458,#28911,#28912);
#24943=AXIS2_PLACEMENT_3D('',#41494,#28914,#28915);
#24944=AXIS2_PLACEMENT_3D('',#41532,#28917,#28918);
#24945=AXIS2_PLACEMENT_3D('',#41569,#28920,#28921);
#24946=AXIS2_PLACEMENT_3D('',#41604,#28923,#28924);
#24947=AXIS2_PLACEMENT_3D('',#41631,#28926,#28927);
#24948=AXIS2_PLACEMENT_3D('',#41655,#28929,#28930);
#24949=AXIS2_PLACEMENT_3D('',#41679,#28932,#28933);
#24950=AXIS2_PLACEMENT_3D('',#41703,#28935,#28936);
#24951=AXIS2_PLACEMENT_3D('',#41729,#28938,#28939);
#24952=AXIS2_PLACEMENT_3D('',#41753,#28941,#28942);
#24953=AXIS2_PLACEMENT_3D('',#41777,#28944,#28945);
#24954=AXIS2_PLACEMENT_3D('',#41803,#28947,#28948);
#24955=AXIS2_PLACEMENT_3D('',#41827,#28950,#28951);
#24956=AXIS2_PLACEMENT_3D('',#41851,#28953,#28954);
#24957=AXIS2_PLACEMENT_3D('',#41875,#28956,#28957);
#24958=AXIS2_PLACEMENT_3D('',#41901,#28959,#28960);
#24959=AXIS2_PLACEMENT_3D('',#41925,#28962,#28963);
#24960=AXIS2_PLACEMENT_3D('',#41949,#28965,#28966);
#24961=AXIS2_PLACEMENT_3D('',#41975,#28968,#28969);
#24962=AXIS2_PLACEMENT_3D('',#41999,#28971,#28972);
#24963=AXIS2_PLACEMENT_3D('',#42023,#28974,#28975);
#24964=AXIS2_PLACEMENT_3D('',#42047,#28977,#28978);
#24965=AXIS2_PLACEMENT_3D('',#42073,#28980,#28981);
#24966=AXIS2_PLACEMENT_3D('',#42097,#28983,#28984);
#24967=AXIS2_PLACEMENT_3D('',#42121,#28986,#28987);
#24968=AXIS2_PLACEMENT_3D('',#42147,#28989,#28990);
#24969=AXIS2_PLACEMENT_3D('',#42171,#28992,#28993);
#24970=AXIS2_PLACEMENT_3D('',#42195,#28995,#28996);
#24971=AXIS2_PLACEMENT_3D('',#42219,#28998,#28999);
#24972=AXIS2_PLACEMENT_3D('',#42245,#29001,#29002);
#24973=AXIS2_PLACEMENT_3D('',#42269,#29004,#29005);
#24974=AXIS2_PLACEMENT_3D('',#42293,#29007,#29008);
#24975=AXIS2_PLACEMENT_3D('',#42319,#29010,#29011);
#24976=AXIS2_PLACEMENT_3D('',#42343,#29013,#29014);
#24977=AXIS2_PLACEMENT_3D('',#42367,#29016,#29017);
#24978=AXIS2_PLACEMENT_3D('',#42391,#29019,#29020);
#24979=AXIS2_PLACEMENT_3D('',#42417,#29022,#29023);
#24980=AXIS2_PLACEMENT_3D('',#42441,#29025,#29026);
#24981=AXIS2_PLACEMENT_3D('',#42465,#29028,#29029);
#24982=AXIS2_PLACEMENT_3D('',#42491,#29031,#29032);
#24983=AXIS2_PLACEMENT_3D('',#42515,#29034,#29035);
#24984=AXIS2_PLACEMENT_3D('',#42539,#29037,#29038);
#24985=AXIS2_PLACEMENT_3D('',#42563,#29040,#29041);
#24986=AXIS2_PLACEMENT_3D('',#42589,#29043,#29044);
#24987=AXIS2_PLACEMENT_3D('',#42613,#29046,#29047);
#24988=AXIS2_PLACEMENT_3D('',#42637,#29049,#29050);
#24989=AXIS2_PLACEMENT_3D('',#42663,#29052,#29053);
#24990=AXIS2_PLACEMENT_3D('',#42687,#29055,#29056);
#24991=AXIS2_PLACEMENT_3D('',#42711,#29058,#29059);
#24992=AXIS2_PLACEMENT_3D('',#42736,#29061,#29062);
#24993=AXIS2_PLACEMENT_3D('',#42763,#29064,#29065);
#24994=AXIS2_PLACEMENT_3D('',#42800,#29067,#29068);
#24995=AXIS2_PLACEMENT_3D('',#42836,#29070,#29071);
#24996=AXIS2_PLACEMENT_3D('',#42874,#29073,#29074);
#24997=AXIS2_PLACEMENT_3D('',#42910,#29076,#29077);
#24998=AXIS2_PLACEMENT_3D('',#42948,#29079,#29080);
#24999=AXIS2_PLACEMENT_3D('',#42985,#29082,#29083);
#25000=AXIS2_PLACEMENT_3D('',#43022,#29085,#29086);
#25001=AXIS2_PLACEMENT_3D('',#43024,#29087,#29088);
#25002=AXIS2_PLACEMENT_3D('',#43101,#29089,#29090);
#25003=AXIS2_PLACEMENT_3D('',#43102,#29091,#29092);
#25004=AXIS2_PLACEMENT_3D('',#43105,#29094,#29095);
#25005=AXIS2_PLACEMENT_3D('',#43106,#29096,#29097);
#25006=AXIS2_PLACEMENT_3D('',#45180,#29098,#29099);
#25007=AXIS2_PLACEMENT_3D('',#47235,#29100,#29101);
#25008=AXIS2_PLACEMENT_3D('',#47244,#29106,#29107);
#25009=AXIS2_PLACEMENT_3D('',#47246,#29108,#29109);
#25010=AXIS2_PLACEMENT_3D('',#47250,#29112,#29113);
#25011=AXIS2_PLACEMENT_3D('',#47254,#29116,#29117);
#25012=AXIS2_PLACEMENT_3D('',#47258,#29120,#29121);
#25013=AXIS2_PLACEMENT_3D('',#47259,#29122,#29123);
#25014=AXIS2_PLACEMENT_3D('',#47260,#29124,#29125);
#25015=AXIS2_PLACEMENT_3D('',#47262,#29126,#29127);
#25016=AXIS2_PLACEMENT_3D('',#47265,#29129,#29130);
#25017=AXIS2_PLACEMENT_3D('',#47266,#29131,#29132);
#25018=AXIS2_PLACEMENT_3D('',#47267,#29133,#29134);
#25019=AXIS2_PLACEMENT_3D('',#47269,#29135,#29136);
#25020=AXIS2_PLACEMENT_3D('',#47270,#29137,#29138);
#25021=AXIS2_PLACEMENT_3D('',#47271,#29139,#29140);
#25022=AXIS2_PLACEMENT_3D('',#47273,#29141,#29142);
#25023=AXIS2_PLACEMENT_3D('',#47275,#29144,#29145);
#25024=AXIS2_PLACEMENT_3D('',#47276,#29146,#29147);
#28699=DIRECTION('axis',(0.,0.,1.));
#28700=DIRECTION('refdir',(1.,0.,0.));
#28701=DIRECTION('center_axis',(1.,0.,0.));
#28702=DIRECTION('ref_axis',(0.,0.975560628713931,0.219730425074181));
#28703=DIRECTION('',(-1.,0.,0.));
#28704=DIRECTION('center_axis',(-1.,0.,0.));
#28705=DIRECTION('ref_axis',(0.,0.,-1.));
#28706=DIRECTION('center_axis',(1.,0.,0.));
#28707=DIRECTION('ref_axis',(0.,0.,-1.));
#28708=DIRECTION('',(-1.,0.,0.));
#28709=DIRECTION('center_axis',(1.,0.,0.));
#28710=DIRECTION('ref_axis',(0.,0.,-1.));
#28711=DIRECTION('',(-1.,0.,0.));
#28712=DIRECTION('center_axis',(1.,0.,0.));
#28713=DIRECTION('ref_axis',(0.,0.,-1.));
#28714=DIRECTION('',(-1.,0.,0.));
#28715=DIRECTION('center_axis',(1.,0.,0.));
#28716=DIRECTION('ref_axis',(0.,0.,-1.));
#28717=DIRECTION('',(-1.,0.,0.));
#28718=DIRECTION('center_axis',(1.,0.,0.));
#28719=DIRECTION('ref_axis',(0.,0.,-1.));
#28720=DIRECTION('',(-1.,0.,0.));
#28721=DIRECTION('center_axis',(1.,0.,0.));
#28722=DIRECTION('ref_axis',(0.,0.,-1.));
#28723=DIRECTION('',(-1.,0.,0.));
#28724=DIRECTION('center_axis',(1.,0.,0.));
#28725=DIRECTION('ref_axis',(0.,0.,-1.));
#28726=DIRECTION('',(-1.,0.,0.));
#28727=DIRECTION('center_axis',(1.,0.,0.));
#28728=DIRECTION('ref_axis',(0.,0.,-1.));
#28729=DIRECTION('',(-1.,0.,0.));
#28730=DIRECTION('center_axis',(1.,0.,0.));
#28731=DIRECTION('ref_axis',(0.,0.,-1.));
#28732=DIRECTION('',(-1.,0.,0.));
#28733=DIRECTION('center_axis',(1.,0.,0.));
#28734=DIRECTION('ref_axis',(0.,0.,-1.));
#28735=DIRECTION('',(-1.,0.,0.));
#28736=DIRECTION('center_axis',(1.,0.,0.));
#28737=DIRECTION('ref_axis',(0.,0.,-1.));
#28738=DIRECTION('',(-1.,0.,0.));
#28739=DIRECTION('center_axis',(1.,0.,0.));
#28740=DIRECTION('ref_axis',(0.,0.,-1.));
#28741=DIRECTION('',(-1.,0.,0.));
#28742=DIRECTION('center_axis',(1.,0.,0.));
#28743=DIRECTION('ref_axis',(0.,0.,-1.));
#28744=DIRECTION('',(-1.,0.,0.));
#28745=DIRECTION('center_axis',(1.,0.,0.));
#28746=DIRECTION('ref_axis',(0.,0.,-1.));
#28747=DIRECTION('',(-1.,0.,0.));
#28748=DIRECTION('center_axis',(1.,0.,0.));
#28749=DIRECTION('ref_axis',(0.,0.,-1.));
#28750=DIRECTION('',(-1.,0.,0.));
#28751=DIRECTION('center_axis',(1.,0.,0.));
#28752=DIRECTION('ref_axis',(0.,0.,-1.));
#28753=DIRECTION('',(-1.,0.,0.));
#28754=DIRECTION('center_axis',(1.,0.,0.));
#28755=DIRECTION('ref_axis',(0.,0.,-1.));
#28756=DIRECTION('',(-1.,0.,0.));
#28757=DIRECTION('center_axis',(1.,0.,0.));
#28758=DIRECTION('ref_axis',(0.,0.,-1.));
#28759=DIRECTION('',(-1.,0.,0.));
#28760=DIRECTION('center_axis',(1.,0.,0.));
#28761=DIRECTION('ref_axis',(0.,0.,-1.));
#28762=DIRECTION('',(-1.,0.,0.));
#28763=DIRECTION('center_axis',(1.,0.,0.));
#28764=DIRECTION('ref_axis',(0.,0.,-1.));
#28765=DIRECTION('',(-1.,0.,0.));
#28766=DIRECTION('center_axis',(1.,0.,0.));
#28767=DIRECTION('ref_axis',(0.,0.,-1.));
#28768=DIRECTION('',(-1.,0.,0.));
#28769=DIRECTION('center_axis',(1.,0.,0.));
#28770=DIRECTION('ref_axis',(0.,0.,-1.));
#28771=DIRECTION('',(-1.,0.,0.));
#28772=DIRECTION('center_axis',(1.,0.,0.));
#28773=DIRECTION('ref_axis',(0.,0.,-1.));
#28774=DIRECTION('',(-1.,0.,0.));
#28775=DIRECTION('center_axis',(1.,0.,0.));
#28776=DIRECTION('ref_axis',(0.,0.,-1.));
#28777=DIRECTION('',(-1.,0.,0.));
#28778=DIRECTION('center_axis',(1.,0.,0.));
#28779=DIRECTION('ref_axis',(0.,0.,-1.));
#28780=DIRECTION('',(-1.,0.,0.));
#28781=DIRECTION('center_axis',(1.,0.,0.));
#28782=DIRECTION('ref_axis',(0.,0.,-1.));
#28783=DIRECTION('',(-1.,0.,0.));
#28784=DIRECTION('center_axis',(1.,0.,0.));
#28785=DIRECTION('ref_axis',(0.,0.,-1.));
#28786=DIRECTION('',(-1.,0.,0.));
#28787=DIRECTION('center_axis',(1.,0.,0.));
#28788=DIRECTION('ref_axis',(0.,0.,-1.));
#28789=DIRECTION('',(-1.,0.,0.));
#28790=DIRECTION('center_axis',(1.,0.,0.));
#28791=DIRECTION('ref_axis',(0.,0.,-1.));
#28792=DIRECTION('',(-1.,0.,0.));
#28793=DIRECTION('center_axis',(1.,0.,0.));
#28794=DIRECTION('ref_axis',(0.,0.,-1.));
#28795=DIRECTION('',(-1.,0.,0.));
#28796=DIRECTION('center_axis',(1.,0.,0.));
#28797=DIRECTION('ref_axis',(0.,0.,-1.));
#28798=DIRECTION('',(-1.,0.,0.));
#28799=DIRECTION('center_axis',(1.,0.,0.));
#28800=DIRECTION('ref_axis',(0.,0.,-1.));
#28801=DIRECTION('',(-1.,0.,0.));
#28802=DIRECTION('center_axis',(1.,0.,0.));
#28803=DIRECTION('ref_axis',(0.,0.,-1.));
#28804=DIRECTION('',(-1.,0.,0.));
#28805=DIRECTION('center_axis',(1.,0.,0.));
#28806=DIRECTION('ref_axis',(0.,0.,-1.));
#28807=DIRECTION('',(-1.,0.,0.));
#28808=DIRECTION('center_axis',(1.,0.,0.));
#28809=DIRECTION('ref_axis',(0.,0.,-1.));
#28810=DIRECTION('',(-1.,0.,0.));
#28811=DIRECTION('center_axis',(1.,0.,0.));
#28812=DIRECTION('ref_axis',(0.,0.,-1.));
#28813=DIRECTION('',(-1.,0.,0.));
#28814=DIRECTION('center_axis',(1.,0.,0.));
#28815=DIRECTION('ref_axis',(0.,0.,-1.));
#28816=DIRECTION('',(-1.,0.,0.));
#28817=DIRECTION('center_axis',(1.,0.,0.));
#28818=DIRECTION('ref_axis',(0.,0.,-1.));
#28819=DIRECTION('',(-1.,0.,0.));
#28820=DIRECTION('center_axis',(1.,0.,0.));
#28821=DIRECTION('ref_axis',(0.,0.,-1.));
#28822=DIRECTION('',(-1.,0.,0.));
#28823=DIRECTION('center_axis',(1.,0.,0.));
#28824=DIRECTION('ref_axis',(0.,0.,-1.));
#28825=DIRECTION('',(-1.,0.,0.));
#28826=DIRECTION('center_axis',(1.,0.,0.));
#28827=DIRECTION('ref_axis',(0.,0.,-1.));
#28828=DIRECTION('',(-1.,0.,0.));
#28829=DIRECTION('center_axis',(1.,0.,0.));
#28830=DIRECTION('ref_axis',(0.,0.,-1.));
#28831=DIRECTION('',(-1.,0.,0.));
#28832=DIRECTION('center_axis',(1.,0.,0.));
#28833=DIRECTION('ref_axis',(0.,0.,-1.));
#28834=DIRECTION('',(-1.,0.,0.));
#28835=DIRECTION('center_axis',(1.,0.,0.));
#28836=DIRECTION('ref_axis',(0.,0.,-1.));
#28837=DIRECTION('',(-1.,0.,0.));
#28838=DIRECTION('center_axis',(1.,0.,0.));
#28839=DIRECTION('ref_axis',(0.,0.,-1.));
#28840=DIRECTION('',(-1.,0.,0.));
#28841=DIRECTION('center_axis',(1.,0.,0.));
#28842=DIRECTION('ref_axis',(0.,0.,-1.));
#28843=DIRECTION('',(-1.,0.,0.));
#28844=DIRECTION('center_axis',(1.,0.,0.));
#28845=DIRECTION('ref_axis',(0.,0.,-1.));
#28846=DIRECTION('',(-1.,0.,0.));
#28847=DIRECTION('center_axis',(1.,0.,0.));
#28848=DIRECTION('ref_axis',(0.,0.,-1.));
#28849=DIRECTION('',(-1.,0.,0.));
#28850=DIRECTION('center_axis',(1.,0.,0.));
#28851=DIRECTION('ref_axis',(0.,0.,-1.));
#28852=DIRECTION('',(-1.,0.,0.));
#28853=DIRECTION('center_axis',(1.,0.,0.));
#28854=DIRECTION('ref_axis',(0.,0.,-1.));
#28855=DIRECTION('',(-1.,0.,0.));
#28856=DIRECTION('center_axis',(1.,0.,0.));
#28857=DIRECTION('ref_axis',(0.,0.,-1.));
#28858=DIRECTION('',(-1.,0.,0.));
#28859=DIRECTION('center_axis',(1.,0.,0.));
#28860=DIRECTION('ref_axis',(0.,0.,-1.));
#28861=DIRECTION('',(-1.,0.,0.));
#28862=DIRECTION('center_axis',(1.,0.,0.));
#28863=DIRECTION('ref_axis',(0.,0.,-1.));
#28864=DIRECTION('',(-1.,0.,0.));
#28865=DIRECTION('center_axis',(1.,0.,0.));
#28866=DIRECTION('ref_axis',(0.,0.,-1.));
#28867=DIRECTION('',(-1.,0.,0.));
#28868=DIRECTION('center_axis',(1.,0.,0.));
#28869=DIRECTION('ref_axis',(0.,0.,-1.));
#28870=DIRECTION('',(-1.,0.,0.));
#28871=DIRECTION('center_axis',(1.,0.,0.));
#28872=DIRECTION('ref_axis',(0.,0.,-1.));
#28873=DIRECTION('',(-1.,0.,0.));
#28874=DIRECTION('center_axis',(1.,0.,0.));
#28875=DIRECTION('ref_axis',(0.,0.,-1.));
#28876=DIRECTION('',(-1.,0.,0.));
#28877=DIRECTION('center_axis',(1.,0.,0.));
#28878=DIRECTION('ref_axis',(0.,0.,-1.));
#28879=DIRECTION('',(-1.,0.,0.));
#28880=DIRECTION('center_axis',(1.,0.,0.));
#28881=DIRECTION('ref_axis',(0.,0.,-1.));
#28882=DIRECTION('',(-1.,0.,0.));
#28883=DIRECTION('center_axis',(1.,0.,0.));
#28884=DIRECTION('ref_axis',(0.,0.,-1.));
#28885=DIRECTION('',(-1.,0.,0.));
#28886=DIRECTION('center_axis',(1.,0.,0.));
#28887=DIRECTION('ref_axis',(0.,0.,-1.));
#28888=DIRECTION('',(-1.,0.,0.));
#28889=DIRECTION('center_axis',(1.,0.,0.));
#28890=DIRECTION('ref_axis',(0.,0.,-1.));
#28891=DIRECTION('',(-1.,0.,0.));
#28892=DIRECTION('center_axis',(1.,0.,0.));
#28893=DIRECTION('ref_axis',(0.,-1.17203152359781E-12,-1.));
#28894=DIRECTION('',(1.,0.,0.));
#28895=DIRECTION('center_axis',(1.,0.,0.));
#28896=DIRECTION('ref_axis',(0.,-1.17203152359781E-12,-1.));
#28897=DIRECTION('center_axis',(1.,0.,0.));
#28898=DIRECTION('ref_axis',(0.,-1.17203152359781E-12,-1.));
#28899=DIRECTION('',(1.,0.,0.));
#28900=DIRECTION('center_axis',(1.,0.,0.));
#28901=DIRECTION('ref_axis',(0.,-1.17203152359781E-12,-1.));
#28902=DIRECTION('center_axis',(1.,0.,0.));
#28903=DIRECTION('ref_axis',(0.,-1.17203152359781E-12,-1.));
#28904=DIRECTION('',(1.,0.,0.));
#28905=DIRECTION('center_axis',(1.,0.,0.));
#28906=DIRECTION('ref_axis',(0.,-1.17203152359781E-12,-1.));
#28907=DIRECTION('',(1.,0.,0.));
#28908=DIRECTION('center_axis',(1.,0.,0.));
#28909=DIRECTION('ref_axis',(0.,-1.17203152359781E-12,-1.));
#28910=DIRECTION('',(1.,0.,0.));
#28911=DIRECTION('center_axis',(1.,0.,0.));
#28912=DIRECTION('ref_axis',(0.,-1.17203152359781E-12,-1.));
#28913=DIRECTION('',(1.,0.,0.));
#28914=DIRECTION('center_axis',(1.,0.,0.));
#28915=DIRECTION('ref_axis',(0.,-1.17203152359781E-12,-1.));
#28916=DIRECTION('',(1.,0.,0.));
#28917=DIRECTION('center_axis',(1.,0.,0.));
#28918=DIRECTION('ref_axis',(0.,-1.17203152359781E-12,-1.));
#28919=DIRECTION('',(1.,0.,0.));
#28920=DIRECTION('center_axis',(1.,0.,0.));
#28921=DIRECTION('ref_axis',(0.,-1.17203152359781E-12,-1.));
#28922=DIRECTION('',(1.,0.,0.));
#28923=DIRECTION('center_axis',(1.,0.,0.));
#28924=DIRECTION('ref_axis',(0.,-1.17203152359781E-12,-1.));
#28925=DIRECTION('',(1.,0.,0.));
#28926=DIRECTION('center_axis',(1.,0.,0.));
#28927=DIRECTION('ref_axis',(0.,-1.17203152359781E-12,-1.));
#28928=DIRECTION('',(1.,0.,0.));
#28929=DIRECTION('center_axis',(1.,0.,0.));
#28930=DIRECTION('ref_axis',(0.,-1.17203152359781E-12,-1.));
#28931=DIRECTION('',(1.,0.,0.));
#28932=DIRECTION('center_axis',(1.,0.,0.));
#28933=DIRECTION('ref_axis',(0.,-1.17203152359781E-12,-1.));
#28934=DIRECTION('',(1.,0.,0.));
#28935=DIRECTION('center_axis',(1.,0.,0.));
#28936=DIRECTION('ref_axis',(0.,-1.17203152359781E-12,-1.));
#28937=DIRECTION('',(1.,0.,0.));
#28938=DIRECTION('center_axis',(1.,0.,0.));
#28939=DIRECTION('ref_axis',(0.,-1.17203152359781E-12,-1.));
#28940=DIRECTION('',(1.,0.,0.));
#28941=DIRECTION('center_axis',(1.,0.,0.));
#28942=DIRECTION('ref_axis',(0.,-1.17203152359781E-12,-1.));
#28943=DIRECTION('',(1.,0.,0.));
#28944=DIRECTION('center_axis',(1.,0.,0.));
#28945=DIRECTION('ref_axis',(0.,-1.17203152359781E-12,-1.));
#28946=DIRECTION('',(1.,0.,0.));
#28947=DIRECTION('center_axis',(1.,0.,0.));
#28948=DIRECTION('ref_axis',(0.,-1.17203152359781E-12,-1.));
#28949=DIRECTION('',(1.,0.,0.));
#28950=DIRECTION('center_axis',(1.,0.,0.));
#28951=DIRECTION('ref_axis',(0.,-1.17203152359781E-12,-1.));
#28952=DIRECTION('',(1.,0.,0.));
#28953=DIRECTION('center_axis',(1.,0.,0.));
#28954=DIRECTION('ref_axis',(0.,-1.17203152359781E-12,-1.));
#28955=DIRECTION('',(1.,0.,0.));
#28956=DIRECTION('center_axis',(1.,0.,0.));
#28957=DIRECTION('ref_axis',(0.,-1.17203152359781E-12,-1.));
#28958=DIRECTION('',(1.,0.,0.));
#28959=DIRECTION('center_axis',(1.,0.,0.));
#28960=DIRECTION('ref_axis',(0.,-1.17203152359781E-12,-1.));
#28961=DIRECTION('',(1.,0.,0.));
#28962=DIRECTION('center_axis',(1.,0.,0.));
#28963=DIRECTION('ref_axis',(0.,-1.17203152359781E-12,-1.));
#28964=DIRECTION('',(1.,0.,0.));
#28965=DIRECTION('center_axis',(1.,0.,0.));
#28966=DIRECTION('ref_axis',(0.,-1.17203152359781E-12,-1.));
#28967=DIRECTION('',(1.,0.,0.));
#28968=DIRECTION('center_axis',(1.,0.,0.));
#28969=DIRECTION('ref_axis',(0.,-1.17203152359781E-12,-1.));
#28970=DIRECTION('',(1.,0.,0.));
#28971=DIRECTION('center_axis',(1.,0.,0.));
#28972=DIRECTION('ref_axis',(0.,-1.17203152359781E-12,-1.));
#28973=DIRECTION('',(1.,0.,0.));
#28974=DIRECTION('center_axis',(1.,0.,0.));
#28975=DIRECTION('ref_axis',(0.,-1.17203152359781E-12,-1.));
#28976=DIRECTION('',(1.,0.,0.));
#28977=DIRECTION('center_axis',(1.,0.,0.));
#28978=DIRECTION('ref_axis',(0.,-1.17203152359781E-12,-1.));
#28979=DIRECTION('',(1.,0.,0.));
#28980=DIRECTION('center_axis',(1.,0.,0.));
#28981=DIRECTION('ref_axis',(0.,-1.17203152359781E-12,-1.));
#28982=DIRECTION('',(1.,0.,0.));
#28983=DIRECTION('center_axis',(1.,0.,0.));
#28984=DIRECTION('ref_axis',(0.,-1.17203152359781E-12,-1.));
#28985=DIRECTION('',(1.,0.,0.));
#28986=DIRECTION('center_axis',(1.,0.,0.));
#28987=DIRECTION('ref_axis',(0.,-1.17203152359781E-12,-1.));
#28988=DIRECTION('',(1.,0.,0.));
#28989=DIRECTION('center_axis',(1.,0.,0.));
#28990=DIRECTION('ref_axis',(0.,-1.17203152359781E-12,-1.));
#28991=DIRECTION('',(1.,0.,0.));
#28992=DIRECTION('center_axis',(1.,0.,0.));
#28993=DIRECTION('ref_axis',(0.,-1.17203152359781E-12,-1.));
#28994=DIRECTION('',(1.,0.,0.));
#28995=DIRECTION('center_axis',(1.,0.,0.));
#28996=DIRECTION('ref_axis',(0.,-1.17203152359781E-12,-1.));
#28997=DIRECTION('',(1.,0.,0.));
#28998=DIRECTION('center_axis',(1.,0.,0.));
#28999=DIRECTION('ref_axis',(0.,-1.17203152359781E-12,-1.));
#29000=DIRECTION('',(1.,0.,0.));
#29001=DIRECTION('center_axis',(1.,0.,0.));
#29002=DIRECTION('ref_axis',(0.,-1.17203152359781E-12,-1.));
#29003=DIRECTION('',(1.,0.,0.));
#29004=DIRECTION('center_axis',(1.,0.,0.));
#29005=DIRECTION('ref_axis',(0.,-1.17203152359781E-12,-1.));
#29006=DIRECTION('',(1.,0.,0.));
#29007=DIRECTION('center_axis',(1.,0.,0.));
#29008=DIRECTION('ref_axis',(0.,-1.17203152359781E-12,-1.));
#29009=DIRECTION('',(1.,0.,0.));
#29010=DIRECTION('center_axis',(1.,0.,0.));
#29011=DIRECTION('ref_axis',(0.,-1.17203152359781E-12,-1.));
#29012=DIRECTION('',(1.,0.,0.));
#29013=DIRECTION('center_axis',(1.,0.,0.));
#29014=DIRECTION('ref_axis',(0.,-1.17203152359781E-12,-1.));
#29015=DIRECTION('',(1.,0.,0.));
#29016=DIRECTION('center_axis',(1.,0.,0.));
#29017=DIRECTION('ref_axis',(0.,-1.17203152359781E-12,-1.));
#29018=DIRECTION('',(1.,0.,0.));
#29019=DIRECTION('center_axis',(1.,0.,0.));
#29020=DIRECTION('ref_axis',(0.,-1.17203152359781E-12,-1.));
#29021=DIRECTION('',(1.,0.,0.));
#29022=DIRECTION('center_axis',(1.,0.,0.));
#29023=DIRECTION('ref_axis',(0.,-1.17203152359781E-12,-1.));
#29024=DIRECTION('',(1.,0.,0.));
#29025=DIRECTION('center_axis',(1.,0.,0.));
#29026=DIRECTION('ref_axis',(0.,-1.17203152359781E-12,-1.));
#29027=DIRECTION('',(1.,0.,0.));
#29028=DIRECTION('center_axis',(1.,0.,0.));
#29029=DIRECTION('ref_axis',(0.,-1.17203152359781E-12,-1.));
#29030=DIRECTION('',(1.,0.,0.));
#29031=DIRECTION('center_axis',(1.,0.,0.));
#29032=DIRECTION('ref_axis',(0.,-1.17203152359781E-12,-1.));
#29033=DIRECTION('',(1.,0.,0.));
#29034=DIRECTION('center_axis',(1.,0.,0.));
#29035=DIRECTION('ref_axis',(0.,-1.17203152359781E-12,-1.));
#29036=DIRECTION('',(1.,0.,0.));
#29037=DIRECTION('center_axis',(1.,0.,0.));
#29038=DIRECTION('ref_axis',(0.,-1.17203152359781E-12,-1.));
#29039=DIRECTION('',(1.,0.,0.));
#29040=DIRECTION('center_axis',(1.,0.,0.));
#29041=DIRECTION('ref_axis',(0.,-1.17203152359781E-12,-1.));
#29042=DIRECTION('',(1.,0.,0.));
#29043=DIRECTION('center_axis',(1.,0.,0.));
#29044=DIRECTION('ref_axis',(0.,-1.17203152359781E-12,-1.));
#29045=DIRECTION('',(1.,0.,0.));
#29046=DIRECTION('center_axis',(1.,0.,0.));
#29047=DIRECTION('ref_axis',(0.,-1.17203152359781E-12,-1.));
#29048=DIRECTION('',(1.,0.,0.));
#29049=DIRECTION('center_axis',(1.,0.,0.));
#29050=DIRECTION('ref_axis',(0.,-1.17203152359781E-12,-1.));
#29051=DIRECTION('',(1.,0.,0.));
#29052=DIRECTION('center_axis',(1.,0.,0.));
#29053=DIRECTION('ref_axis',(0.,-1.17203152359781E-12,-1.));
#29054=DIRECTION('',(1.,0.,0.));
#29055=DIRECTION('center_axis',(1.,0.,0.));
#29056=DIRECTION('ref_axis',(0.,-1.17203152359781E-12,-1.));
#29057=DIRECTION('',(1.,0.,0.));
#29058=DIRECTION('center_axis',(1.,0.,0.));
#29059=DIRECTION('ref_axis',(0.,-1.17203152359781E-12,-1.));
#29060=DIRECTION('',(1.,0.,0.));
#29061=DIRECTION('center_axis',(1.,0.,0.));
#29062=DIRECTION('ref_axis',(0.,-1.17203152359781E-12,-1.));
#29063=DIRECTION('',(1.,0.,0.));
#29064=DIRECTION('center_axis',(1.,0.,0.));
#29065=DIRECTION('ref_axis',(0.,-1.17203152359781E-12,-1.));
#29066=DIRECTION('',(1.,0.,0.));
#29067=DIRECTION('center_axis',(1.,0.,0.));
#29068=DIRECTION('ref_axis',(0.,-1.17203152359781E-12,-1.));
#29069=DIRECTION('',(1.,0.,0.));
#29070=DIRECTION('center_axis',(1.,0.,0.));
#29071=DIRECTION('ref_axis',(0.,-1.17203152359781E-12,-1.));
#29072=DIRECTION('',(1.,0.,0.));
#29073=DIRECTION('center_axis',(1.,0.,0.));
#29074=DIRECTION('ref_axis',(0.,-1.17203152359781E-12,-1.));
#29075=DIRECTION('',(1.,0.,0.));
#29076=DIRECTION('center_axis',(1.,0.,0.));
#29077=DIRECTION('ref_axis',(0.,-1.17203152359781E-12,-1.));
#29078=DIRECTION('',(1.,0.,0.));
#29079=DIRECTION('center_axis',(1.,0.,0.));
#29080=DIRECTION('ref_axis',(0.,-1.17203152359781E-12,-1.));
#29081=DIRECTION('',(1.,0.,0.));
#29082=DIRECTION('center_axis',(1.,0.,0.));
#29083=DIRECTION('ref_axis',(0.,-1.17203152359781E-12,-1.));
#29084=DIRECTION('',(1.,0.,0.));
#29085=DIRECTION('center_axis',(1.,0.,0.));
#29086=DIRECTION('ref_axis',(0.,0.,-1.));
#29087=DIRECTION('center_axis',(1.,0.,0.));
#29088=DIRECTION('ref_axis',(0.,0.,-1.));
#29089=DIRECTION('center_axis',(-1.,0.,0.));
#29090=DIRECTION('ref_axis',(0.,-1.17203152359781E-12,-1.));
#29091=DIRECTION('center_axis',(1.,0.,0.));
#29092=DIRECTION('ref_axis',(0.,0.,-1.));
#29093=DIRECTION('',(-1.,0.,0.));
#29094=DIRECTION('center_axis',(1.,0.,0.));
#29095=DIRECTION('ref_axis',(0.,0.,-1.));
#29096=DIRECTION('center_axis',(1.,0.,0.));
#29097=DIRECTION('ref_axis',(0.,0.,-1.));
#29098=DIRECTION('center_axis',(1.,0.,0.));
#29099=DIRECTION('ref_axis',(0.,-1.17203152359781E-12,-1.));
#29100=DIRECTION('center_axis',(0.,1.,0.));
#29101=DIRECTION('ref_axis',(0.,0.,1.));
#29102=DIRECTION('',(-1.,0.,0.));
#29103=DIRECTION('',(0.,0.,1.));
#29104=DIRECTION('',(1.,0.,0.));
#29105=DIRECTION('',(0.,0.,1.));
#29106=DIRECTION('center_axis',(1.,0.,0.));
#29107=DIRECTION('ref_axis',(0.,0.,-1.));
#29108=DIRECTION('center_axis',(-1.,0.,0.));
#29109=DIRECTION('ref_axis',(0.,0.,-1.));
#29110=DIRECTION('',(0.,-1.,0.));
#29111=DIRECTION('',(0.,0.,-1.));
#29112=DIRECTION('center_axis',(0.,0.,1.));
#29113=DIRECTION('ref_axis',(0.,-1.,0.));
#29114=DIRECTION('',(0.,-1.,0.));
#29115=DIRECTION('',(1.,0.,0.));
#29116=DIRECTION('center_axis',(0.,-1.,0.));
#29117=DIRECTION('ref_axis',(0.,0.,-1.));
#29118=DIRECTION('',(1.,0.,0.));
#29119=DIRECTION('',(0.,0.,-1.));
#29120=DIRECTION('center_axis',(1.,0.,0.));
#29121=DIRECTION('ref_axis',(0.,0.,-1.));
#29122=DIRECTION('center_axis',(1.,0.,0.));
#29123=DIRECTION('ref_axis',(0.,0.,-1.));
#29124=DIRECTION('center_axis',(1.,0.,0.));
#29125=DIRECTION('ref_axis',(0.,0.,-1.));
#29126=DIRECTION('center_axis',(1.,0.,0.));
#29127=DIRECTION('ref_axis',(0.,0.,-1.));
#29128=DIRECTION('',(-1.,0.,0.));
#29129=DIRECTION('center_axis',(-1.,0.,0.));
#29130=DIRECTION('ref_axis',(0.,0.,-1.));
#29131=DIRECTION('center_axis',(1.,0.,0.));
#29132=DIRECTION('ref_axis',(0.,0.,-1.));
#29133=DIRECTION('center_axis',(1.,0.,0.));
#29134=DIRECTION('ref_axis',(0.,0.,-1.));
#29135=DIRECTION('center_axis',(1.,0.,0.));
#29136=DIRECTION('ref_axis',(0.,0.,-1.));
#29137=DIRECTION('center_axis',(-1.,0.,0.));
#29138=DIRECTION('ref_axis',(0.,0.,-1.));
#29139=DIRECTION('center_axis',(1.,0.,0.));
#29140=DIRECTION('ref_axis',(0.,0.,-1.));
#29141=DIRECTION('center_axis',(1.,0.,0.));
#29142=DIRECTION('ref_axis',(0.,0.,-1.));
#29143=DIRECTION('',(-1.,0.,0.));
#29144=DIRECTION('center_axis',(1.,0.,0.));
#29145=DIRECTION('ref_axis',(0.,0.,-1.));
#29146=DIRECTION('center_axis',(1.,0.,0.));
#29147=DIRECTION('ref_axis',(0.,0.,-1.));
#37618=CARTESIAN_POINT('',(0.,0.,0.));
#37619=CARTESIAN_POINT('Origin',(4.,0.,4.));
#37620=CARTESIAN_POINT('',(4.12884541125756,8.40637486662632E-6,4.59405635738975));
#37621=CARTESIAN_POINT('',(4.02115458874249,-9.26662433349265E-6,4.59413599269206));
#37622=CARTESIAN_POINT('',(4.,-7.27562663373442E-17,4.5941));
#37623=CARTESIAN_POINT('',(4.,0.254721014554615,3.46322028700965));
#37624=CARTESIAN_POINT('Ctrl Pts',(4.12884541125756,8.40637486662632E-6,
4.59405635738975));
#37625=CARTESIAN_POINT('Ctrl Pts',(4.12564700130467,0.0398130654959074,
4.59407663624518));
#37626=CARTESIAN_POINT('Ctrl Pts',(4.12244859135178,0.079613792300143,4.59013569217808));
#37627=CARTESIAN_POINT('Ctrl Pts',(4.11925018139889,0.118599576779877,4.58219388355888));
#37628=CARTESIAN_POINT('Ctrl Pts',(4.11129754205509,0.215535206692688,4.56244709042845));
#37629=CARTESIAN_POINT('Ctrl Pts',(4.10334490271129,0.30743256945264,4.51796551073728));
#37630=CARTESIAN_POINT('Ctrl Pts',(4.09539226336748,0.383054411795556,4.45418672179759));
#37631=CARTESIAN_POINT('Ctrl Pts',(4.08743962402367,0.458676254138472,4.3904079328579));
#37632=CARTESIAN_POINT('Ctrl Pts',(4.07948698467986,0.518022576064352,4.30733193466969));
#37633=CARTESIAN_POINT('Ctrl Pts',(4.07153434533606,0.553840407547632,4.21511760274296));
#37634=CARTESIAN_POINT('Ctrl Pts',(4.06358170599225,0.589658239030912,4.12290327081622));
#37635=CARTESIAN_POINT('Ctrl Pts',(4.05562906664845,0.601947580071592,4.02155060515096));
#37636=CARTESIAN_POINT('Ctrl Pts',(4.04767642730464,0.589200356533535,3.92344812692479));
#37637=CARTESIAN_POINT('Ctrl Pts',(4.03972378796084,0.576453132995478,3.82534564869861));
#37638=CARTESIAN_POINT('Ctrl Pts',(4.03177114861703,0.538669344878685,3.73049335791153));
#37639=CARTESIAN_POINT('Ctrl Pts',(4.02381850927322,0.480479105222089,3.65049437695417));
#37640=CARTESIAN_POINT('Ctrl Pts',(4.01587900618215,0.422384984811151,3.57062753914914));
#37641=CARTESIAN_POINT('Ctrl Pts',(4.00793950309107,0.343951772361455,3.50556498199611));
#37642=CARTESIAN_POINT('Ctrl Pts',(4.,0.254721014554615,3.46322028700965));
#37643=CARTESIAN_POINT('',(4.,0.254694598474614,4.53673594206822));
#37644=CARTESIAN_POINT('Origin',(4.,0.,4.));
#37645=CARTESIAN_POINT('Ctrl Pts',(3.99999999999998,0.254694598474614,4.53673594206822));
#37646=CARTESIAN_POINT('Ctrl Pts',(4.00705152958082,0.175425736340139,4.5743509952638));
#37647=CARTESIAN_POINT('Ctrl Pts',(4.01410305916165,0.0876996967667308,
4.59405101338575));
#37648=CARTESIAN_POINT('Ctrl Pts',(4.02115458874249,-9.26662433349265E-6,
4.59413599269206));
#37649=CARTESIAN_POINT('Origin',(4.,0.,4.));
#37650=CARTESIAN_POINT('',(4.42884541125756,-2.46302091461148E-6,4.59415045696459));
#37651=CARTESIAN_POINT('',(4.32115458874249,3.58587963140688E-6,4.59404994535016));
#37652=CARTESIAN_POINT('',(4.,-7.27562663373442E-17,4.5941));
#37653=CARTESIAN_POINT('Ctrl Pts',(4.42884541125756,-2.46302091461148E-6,
4.59415045696459));
#37654=CARTESIAN_POINT('Ctrl Pts',(4.42107867343035,0.0966117732708647,
4.59412799973471));
#37655=CARTESIAN_POINT('Ctrl Pts',(4.41331193560314,0.193236775309615,4.57009608476161));
#37656=CARTESIAN_POINT('Ctrl Pts',(4.40554519777592,0.278573173318151,4.52479781884576));
#37657=CARTESIAN_POINT('Ctrl Pts',(4.39759255843212,0.36595214906825,4.47841531183407));
#37658=CARTESIAN_POINT('Ctrl Pts',(4.38963991908831,0.441495654419193,4.40973622444741));
#37659=CARTESIAN_POINT('Ctrl Pts',(4.3816872797445,0.495967466205845,4.32715751007026));
#37660=CARTESIAN_POINT('Ctrl Pts',(4.3737346404007,0.550439277992498,4.24457879569311));
#37661=CARTESIAN_POINT('Ctrl Pts',(4.36578200105689,0.58383939621486,4.14810045432546));
#37662=CARTESIAN_POINT('Ctrl Pts',(4.35782936171309,0.59208420294366,4.04951827803692));
#37663=CARTESIAN_POINT('Ctrl Pts',(4.34987672236928,0.600329009672459,3.95093610174838));
#37664=CARTESIAN_POINT('Ctrl Pts',(4.34192408302547,0.583418504907695,3.85025009053894));
#37665=CARTESIAN_POINT('Ctrl Pts',(4.33397144368167,0.54342022548472,3.75977047903001));
#37666=CARTESIAN_POINT('Ctrl Pts',(4.32601880433786,0.503421946061746,3.66929086752108));
#37667=CARTESIAN_POINT('Ctrl Pts',(4.31806616499406,0.440335891980562,3.58901765571266));
#37668=CARTESIAN_POINT('Ctrl Pts',(4.31011352565025,0.361875197644003,3.52876534000234));
#37669=CARTESIAN_POINT('Ctrl Pts',(4.30216088630644,0.283414503307443,3.46851302429202));
#37670=CARTESIAN_POINT('Ctrl Pts',(4.29420824696263,0.189579168715509,3.4282816046798));
#37671=CARTESIAN_POINT('Ctrl Pts',(4.28625560761883,0.0918418319479975,
3.41298991457491));
#37672=CARTESIAN_POINT('Ctrl Pts',(4.27830296827502,-0.00589550481951406,
3.39769822447003));
#37673=CARTESIAN_POINT('Ctrl Pts',(4.27035032893122,-0.107534843762603,
3.4073462638725));
#37674=CARTESIAN_POINT('Ctrl Pts',(4.26239768958741,-0.200649373295791,
3.44075443909651));
#37675=CARTESIAN_POINT('Ctrl Pts',(4.25444505024361,-0.293763902828979,
3.47416261432052));
#37676=CARTESIAN_POINT('Ctrl Pts',(4.24649241089979,-0.378353622952266,
3.53133092536608));
#37677=CARTESIAN_POINT('Ctrl Pts',(4.23853977155599,-0.444076322467606,
3.60526974769923));
#37678=CARTESIAN_POINT('Ctrl Pts',(4.23058713221218,-0.509799021982947,
3.67920857003239));
#37679=CARTESIAN_POINT('Ctrl Pts',(4.22263449286838,-0.556654700890342,
3.76991790365313));
#37680=CARTESIAN_POINT('Ctrl Pts',(4.21468185352458,-0.578914549750806,
3.86630733464992));
#37681=CARTESIAN_POINT('Ctrl Pts',(4.20672921418077,-0.601174398611269,
3.96269676564671));
#37682=CARTESIAN_POINT('Ctrl Pts',(4.19877657483696,-0.598838417424802,
4.06476629401955));
#37683=CARTESIAN_POINT('Ctrl Pts',(4.19082393549315,-0.5721923335546,4.16003645884502));
#37684=CARTESIAN_POINT('Ctrl Pts',(4.18287129614934,-0.545546249684398,
4.25530662367048));
#37685=CARTESIAN_POINT('Ctrl Pts',(4.17491865680554,-0.494590063130461,
4.34377742494856));
#37686=CARTESIAN_POINT('Ctrl Pts',(4.16696601746173,-0.425553631634784,
4.41463223618795));
#37687=CARTESIAN_POINT('Ctrl Pts',(4.15901337811793,-0.356517200139107,
4.48548704742733));
#37688=CARTESIAN_POINT('Ctrl Pts',(4.15106073877413,-0.269400523701689,
4.53872586862801));
#37689=CARTESIAN_POINT('Ctrl Pts',(4.14310809943032,-0.174855236950146,
4.56783927594351));
#37690=CARTESIAN_POINT('Ctrl Pts',(4.1383538700394,-0.118334381217266,4.5852437891806));
#37691=CARTESIAN_POINT('Ctrl Pts',(4.13359964064848,-0.0591586432141876,
4.59402621418361));
#37692=CARTESIAN_POINT('Ctrl Pts',(4.12884541125756,8.40637486662632E-6,
4.59405635738975));
#37693=CARTESIAN_POINT('Ctrl Pts',(4.02115458874249,-9.26662433349265E-6,
4.59413599269206));
#37694=CARTESIAN_POINT('Ctrl Pts',(4.02205569850546,-0.0112175303500608,
4.59414685213492));
#37695=CARTESIAN_POINT('Ctrl Pts',(4.02295680826843,-0.0224255152200988,
4.5938373961197));
#37696=CARTESIAN_POINT('Ctrl Pts',(4.0238579180314,-0.0336155370699344,
4.59320407706013));
#37697=CARTESIAN_POINT('Ctrl Pts',(4.03181055737521,-0.132371772633995,
4.58761479340425));
#37698=CARTESIAN_POINT('Ctrl Pts',(4.03976319671902,-0.229728915328813,
4.55680066053817));
#37699=CARTESIAN_POINT('Ctrl Pts',(4.04771583606282,-0.31374319278985,4.50455967689729));
#37700=CARTESIAN_POINT('Ctrl Pts',(4.05566847540663,-0.397757470250888,
4.4523186932564));
#37701=CARTESIAN_POINT('Ctrl Pts',(4.06362111475043,-0.468428882478145,
4.37865085884071));
#37702=CARTESIAN_POINT('Ctrl Pts',(4.07157375409424,-0.517135915630147,
4.29254879227412));
#37703=CARTESIAN_POINT('Ctrl Pts',(4.07952639343804,-0.565842948782149,
4.20644672570752));
#37704=CARTESIAN_POINT('Ctrl Pts',(4.08747903278185,-0.592585602858896,
4.10791042699003));
#37705=CARTESIAN_POINT('Ctrl Pts',(4.09543167212566,-0.594084460855775,
4.00899459728238));
#37706=CARTESIAN_POINT('Ctrl Pts',(4.10338431146947,-0.595583318852653,
3.91007876757474));
#37707=CARTESIAN_POINT('Ctrl Pts',(4.11133695081327,-0.571838380769662,
3.81078340687695));
#37708=CARTESIAN_POINT('Ctrl Pts',(4.11928959015708,-0.525757920758293,
3.72324489380985));
#37709=CARTESIAN_POINT('Ctrl Pts',(4.12724222950088,-0.479677460746923,
3.63570638074275));
#37710=CARTESIAN_POINT('Ctrl Pts',(4.13519486884469,-0.411261478807175,
3.55992471530633));
#37711=CARTESIAN_POINT('Ctrl Pts',(4.1431475081885,-0.328872047298013,3.50516726345229));
#37712=CARTESIAN_POINT('Ctrl Pts',(4.1511001475323,-0.246482615788851,3.45040981159825));
#37713=CARTESIAN_POINT('Ctrl Pts',(4.15905278687611,-0.150119734710276,
3.41667657332659));
#37714=CARTESIAN_POINT('Ctrl Pts',(4.16700542621992,-0.0515665150750243,
3.40809082437526));
#37715=CARTESIAN_POINT('Ctrl Pts',(4.17495806556372,0.0469867045602276,
3.39950507542393));
#37716=CARTESIAN_POINT('Ctrl Pts',(4.18291070490753,0.147730262752155,3.41606681579293));
#37717=CARTESIAN_POINT('Ctrl Pts',(4.19086334425134,0.238347648045887,3.45575171487277));
#37718=CARTESIAN_POINT('Ctrl Pts',(4.19881598359514,0.32896503333962,3.49543661395261));
#37719=CARTESIAN_POINT('Ctrl Pts',(4.20676862293895,0.409456245735157,3.55824467174328));
#37720=CARTESIAN_POINT('Ctrl Pts',(4.21472126228276,0.469979735422806,3.63649644709345));
#37721=CARTESIAN_POINT('Ctrl Pts',(4.22267390162656,0.530503225110456,3.71474822244363));
#37722=CARTESIAN_POINT('Ctrl Pts',(4.23062654097037,0.571058992090217,3.80844371535332));
#37723=CARTESIAN_POINT('Ctrl Pts',(4.23857918031417,0.586688754827568,3.90612753493601));
#37724=CARTESIAN_POINT('Ctrl Pts',(4.24653181965798,0.602318517564919,4.0038113545187));
#37725=CARTESIAN_POINT('Ctrl Pts',(4.25448445900178,0.593022276059861,4.10548350077438));
#37726=CARTESIAN_POINT('Ctrl Pts',(4.26243709834559,0.559936509464549,4.19871308474845));
#37727=CARTESIAN_POINT('Ctrl Pts',(4.2703897376894,0.526850742869238,4.29194266872251));
#37728=CARTESIAN_POINT('Ctrl Pts',(4.27834237703321,0.469975451183674,4.37672969041494));
#37729=CARTESIAN_POINT('Ctrl Pts',(4.28629501637701,0.396264473279151,4.44270782630825));
#37730=CARTESIAN_POINT('Ctrl Pts',(4.29424765572082,0.322553495374627,4.50868596220156));
#37731=CARTESIAN_POINT('Ctrl Pts',(4.30220029506462,0.232006831251144,4.55585521229574));
#37732=CARTESIAN_POINT('Ctrl Pts',(4.31015293440843,0.135695012128791,4.57844846968215));
#37733=CARTESIAN_POINT('Ctrl Pts',(4.31382015251978,0.0912825306677821,
4.58886694826517));
#37734=CARTESIAN_POINT('Ctrl Pts',(4.31748737063114,0.0456441298716245,
4.59405951624442));
#37735=CARTESIAN_POINT('Ctrl Pts',(4.32115458874249,3.58587963140688E-6,
4.59404994535016));
#37736=CARTESIAN_POINT('Origin',(4.,0.,4.));
#37737=CARTESIAN_POINT('',(4.72884541125756,-4.67700812217808E-6,4.59405084457266));
#37738=CARTESIAN_POINT('',(4.62115458874249,3.7232086238465E-6,4.59414939806979));
#37739=CARTESIAN_POINT('',(4.,-7.27562663373442E-17,4.5941));
#37740=CARTESIAN_POINT('Ctrl Pts',(4.72884541125756,-4.67700812217808E-6,
4.59405084457266));
#37741=CARTESIAN_POINT('Ctrl Pts',(4.72446298489983,0.0545367878429411,
4.59403588702548));
#37742=CARTESIAN_POINT('Ctrl Pts',(4.7200805585421,0.10908225468116,4.58659074407712));
#37743=CARTESIAN_POINT('Ctrl Pts',(4.71569813218437,0.16154350694756,4.57176871113812));
#37744=CARTESIAN_POINT('Ctrl Pts',(4.70774549284056,0.256743148594298,4.54487167450041));
#37745=CARTESIAN_POINT('Ctrl Pts',(4.69979285349676,0.345079446524661,4.4936824501733));
#37746=CARTESIAN_POINT('Ctrl Pts',(4.69184021415295,0.415752085200636,4.42445961801412));
#37747=CARTESIAN_POINT('Ctrl Pts',(4.68388757480915,0.486424723876611,4.35523678585494));
#37748=CARTESIAN_POINT('Ctrl Pts',(4.67593493546534,0.539433703298198,4.26798034586369));
#37749=CARTESIAN_POINT('Ctrl Pts',(4.66798229612153,0.568297953762936,4.17335858623793));
#37750=CARTESIAN_POINT('Ctrl Pts',(4.66002965677773,0.597162204227674,4.07873682661218));
#37751=CARTESIAN_POINT('Ctrl Pts',(4.65207701743392,0.601881725735563,3.97674974735193));
#37752=CARTESIAN_POINT('Ctrl Pts',(4.64412437809011,0.581879492504365,3.87986665793328));
#37753=CARTESIAN_POINT('Ctrl Pts',(4.63617173874631,0.561877259273167,3.78298356851463));
#37754=CARTESIAN_POINT('Ctrl Pts',(4.6282190994025,0.517153271302883,3.69120446893757));
#37755=CARTESIAN_POINT('Ctrl Pts',(4.6202664600587,0.453175645250056,3.61575060413089));
#37756=CARTESIAN_POINT('Ctrl Pts',(4.61231382071489,0.389198019197228,3.5402967393242));
#37757=CARTESIAN_POINT('Ctrl Pts',(4.60436118137108,0.305966755061857,3.48116810928789));
#37758=CARTESIAN_POINT('Ctrl Pts',(4.59640854202727,0.213658008474022,3.4455939943611));
#37759=CARTESIAN_POINT('Ctrl Pts',(4.58845590268347,0.121349261886187,3.41001987943431));
#37760=CARTESIAN_POINT('Ctrl Pts',(4.58050326333966,0.0199630328458878,
3.39800027961704));
#37761=CARTESIAN_POINT('Ctrl Pts',(4.57255062399586,-0.0781048312986516,
3.41100475468789));
#37762=CARTESIAN_POINT('Ctrl Pts',(4.56459798465205,-0.17617269544319,3.42400922975875));
#37763=CARTESIAN_POINT('Ctrl Pts',(4.55664534530825,-0.270922194691968,
3.46203777971774));
#37764=CARTESIAN_POINT('Ctrl Pts',(4.54869270596444,-0.350768912290741,
3.52044089639904));
#37765=CARTESIAN_POINT('Ctrl Pts',(4.54074006662063,-0.430615629889515,
3.57884401308035));
#37766=CARTESIAN_POINT('Ctrl Pts',(4.53278742727683,-0.495559565838284,
3.65762169648397));
#37767=CARTESIAN_POINT('Ctrl Pts',(4.52483478793302,-0.537660439465301,
3.74714230187364));
#37768=CARTESIAN_POINT('Ctrl Pts',(4.51688214858921,-0.579761313092318,
3.8366629072633));
#37769=CARTESIAN_POINT('Ctrl Pts',(4.50892950924541,-0.599019124397585,
3.936926434639));
#37770=CARTESIAN_POINT('Ctrl Pts',(4.5009768699016,-0.593079343631488,4.03567430223551));
#37771=CARTESIAN_POINT('Ctrl Pts',(4.49302423055779,-0.587139562865391,
4.13442216983203));
#37772=CARTESIAN_POINT('Ctrl Pts',(4.48507159121399,-0.556002190027932,
4.23165437764937));
#37773=CARTESIAN_POINT('Ctrl Pts',(4.47711895187018,-0.503474193090318,
4.31548296397124));
#37774=CARTESIAN_POINT('Ctrl Pts',(4.46916631252638,-0.450946196152703,
4.39931155029312));
#37775=CARTESIAN_POINT('Ctrl Pts',(4.46121367318257,-0.377027575114933,
4.46973651511953));
#37776=CARTESIAN_POINT('Ctrl Pts',(4.45326103383876,-0.290755888038263,
4.51814744739689));
#37777=CARTESIAN_POINT('Ctrl Pts',(4.44530839449495,-0.204484200961595,
4.56655837967425));
#37778=CARTESIAN_POINT('Ctrl Pts',(4.43735575515115,-0.105859447846027,
4.59295527940255));
#37779=CARTESIAN_POINT('Ctrl Pts',(4.42940311580734,-0.00693984821361558,
4.59411076594835));
#37780=CARTESIAN_POINT('Ctrl Pts',(4.42921721429075,-0.0046274959494805,
4.59413777669183));
#37781=CARTESIAN_POINT('Ctrl Pts',(4.42903131277416,-0.00231498256911503,
4.59415099449182));
#37782=CARTESIAN_POINT('Ctrl Pts',(4.42884541125756,-2.46302091461148E-6,
4.59415045696459));
#37783=CARTESIAN_POINT('Ctrl Pts',(4.32115458874249,3.58587963140688E-6,
4.59404994535016));
#37784=CARTESIAN_POINT('Ctrl Pts',(4.32544000997495,-0.0533308355660028,
4.59403876103764));
#37785=CARTESIAN_POINT('Ctrl Pts',(4.3297254312074,-0.106668183692779,4.58692369872924));
#37786=CARTESIAN_POINT('Ctrl Pts',(4.33401085243985,-0.158055593105036,
4.57274269264177));
#37787=CARTESIAN_POINT('Ctrl Pts',(4.34196349178366,-0.253417405095285,
4.54642639353635));
#37788=CARTESIAN_POINT('Ctrl Pts',(4.34991613112746,-0.342064054954561,
4.49577653064689));
#37789=CARTESIAN_POINT('Ctrl Pts',(4.35786877047127,-0.413157291282808,
4.42698573291487));
#37790=CARTESIAN_POINT('Ctrl Pts',(4.36582140981507,-0.484250527611055,
4.35819493518285));
#37791=CARTESIAN_POINT('Ctrl Pts',(4.37377404915888,-0.537790350408272,
4.27126320260829));
#37792=CARTESIAN_POINT('Ctrl Pts',(4.38172668850269,-0.567230782432438,
4.17681912699824));
#37793=CARTESIAN_POINT('Ctrl Pts',(4.3896793278465,-0.596671214456604,4.0823750513882));
#37794=CARTESIAN_POINT('Ctrl Pts',(4.3976319671903,-0.602012255707717,3.98041863274268));
#37795=CARTESIAN_POINT('Ctrl Pts',(4.40558460653411,-0.582600893642323,
3.88341542999892));
#37796=CARTESIAN_POINT('Ctrl Pts',(4.41353724587791,-0.563189531576929,
3.78641222725516));
#37797=CARTESIAN_POINT('Ctrl Pts',(4.42148988522172,-0.519025766195027,
3.69436224041317));
#37798=CARTESIAN_POINT('Ctrl Pts',(4.42944252456553,-0.455509217992651,
3.61851983504546));
#37799=CARTESIAN_POINT('Ctrl Pts',(4.43739516390933,-0.391992669790276,
3.54267742967776));
#37800=CARTESIAN_POINT('Ctrl Pts',(4.44534780325314,-0.309123338767427,
3.48304260578434));
#37801=CARTESIAN_POINT('Ctrl Pts',(4.45330044259694,-0.217033129998519,
3.44690653227429));
#37802=CARTESIAN_POINT('Ctrl Pts',(4.46125308194075,-0.12494292122961,3.41077045876423));
#37803=CARTESIAN_POINT('Ctrl Pts',(4.46920572128456,-0.0236318347146405,
3.39813313563753));
#37804=CARTESIAN_POINT('Ctrl Pts',(4.47715836062837,0.074513469760962,3.41053964803971));
#37805=CARTESIAN_POINT('Ctrl Pts',(4.48511099997217,0.172658774236564,3.42294616044189));
#37806=CARTESIAN_POINT('Ctrl Pts',(4.49306363931598,0.2676382966728,3.46039650837296));
#37807=CARTESIAN_POINT('Ctrl Pts',(4.50101627865978,0.34783949666059,3.51831187658845));
#37808=CARTESIAN_POINT('Ctrl Pts',(4.50896891800359,0.428040696648381,3.57622724480394));
#37809=CARTESIAN_POINT('Ctrl Pts',(4.51692155734739,0.493463574187728,3.65460763330386));
#37810=CARTESIAN_POINT('Ctrl Pts',(4.5248741966912,0.536109291561612,3.74386997215216));
#37811=CARTESIAN_POINT('Ctrl Pts',(4.53282683603501,0.578755008935497,3.83313231100046));
#37812=CARTESIAN_POINT('Ctrl Pts',(4.54077947537881,0.598623566143919,3.93327660019715));
#37813=CARTESIAN_POINT('Ctrl Pts',(4.54873211472262,0.593285761408823,4.03205883640902));
#37814=CARTESIAN_POINT('Ctrl Pts',(4.55668475406643,0.587947956673727,4.1308410726209));
#37815=CARTESIAN_POINT('Ctrl Pts',(4.56463739341024,0.557403789995114,4.22826125584796));
#37816=CARTESIAN_POINT('Ctrl Pts',(4.57259003275404,0.505387701781775,4.31240844187621));
#37817=CARTESIAN_POINT('Ctrl Pts',(4.58054267209785,0.453371613568435,4.39655562790445));
#37818=CARTESIAN_POINT('Ctrl Pts',(4.58849531144165,0.37988360382037,4.46742981673387));
#37819=CARTESIAN_POINT('Ctrl Pts',(4.59644795078546,0.293908582600447,4.51636567348148));
#37820=CARTESIAN_POINT('Ctrl Pts',(4.60440059012926,0.207933561380525,4.56530153022909));
#37821=CARTESIAN_POINT('Ctrl Pts',(4.61235322947307,0.109471528688745,4.59229905489488));
#37822=CARTESIAN_POINT('Ctrl Pts',(4.62030586881688,0.01056080905581,4.59405743239568));
#37823=CARTESIAN_POINT('Ctrl Pts',(4.62058877545875,0.00704216595801619,
4.59411998479525));
#37824=CARTESIAN_POINT('Ctrl Pts',(4.62087168210062,0.00352295504485493,
4.59415059693914));
#37825=CARTESIAN_POINT('Ctrl Pts',(4.62115458874249,3.7232086238465E-6,
4.59414939806979));
#37826=CARTESIAN_POINT('Origin',(4.,0.,4.));
#37827=CARTESIAN_POINT('',(5.02884541125756,1.1583539301252E-5,4.59413174414479));
#37828=CARTESIAN_POINT('',(4.92115458874249,-9.52916733652962E-6,4.59405847898621));
#37829=CARTESIAN_POINT('',(4.,-7.27562663373442E-17,4.5941));
#37830=CARTESIAN_POINT('Ctrl Pts',(5.02884541125756,1.1583539301252E-5,
4.59413174414479));
#37831=CARTESIAN_POINT('Ctrl Pts',(5.02784729636931,0.0124287555737821,
4.59414271605904));
#37832=CARTESIAN_POINT('Ctrl Pts',(5.02684918148107,0.024845254523583,4.59376142828251));
#37833=CARTESIAN_POINT('Ctrl Pts',(5.02585106659282,0.0372368329321061,
4.59298328977014));
#37834=CARTESIAN_POINT('Ctrl Pts',(5.01789842724901,0.135968707532707,4.58678334723719));
#37835=CARTESIAN_POINT('Ctrl Pts',(5.00994578790521,0.233118536601742,4.55538989360237));
#37836=CARTESIAN_POINT('Ctrl Pts',(5.0019931485614,0.316808430381418,4.50264120614281));
#37837=CARTESIAN_POINT('Ctrl Pts',(4.9940405092176,0.400498324161095,4.44989251868324));
#37838=CARTESIAN_POINT('Ctrl Pts',(4.98608786987379,0.470728282651411,4.37578859739892));
#37839=CARTESIAN_POINT('Ctrl Pts',(4.97813523052998,0.518911736914097,4.289389655942));
#37840=CARTESIAN_POINT('Ctrl Pts',(4.97018259118617,0.567095191176782,4.20299071448508));
#37841=CARTESIAN_POINT('Ctrl Pts',(4.96222995184237,0.593232141211837,4.10429675285556));
#37842=CARTESIAN_POINT('Ctrl Pts',(4.95427731249856,0.594126988899363,4.00537445204741));
#37843=CARTESIAN_POINT('Ctrl Pts',(4.94632467315476,0.595021836586889,3.90645215123927));
#37844=CARTESIAN_POINT('Ctrl Pts',(4.93837203381095,0.570674581926886,3.80730151125251));
#37845=CARTESIAN_POINT('Ctrl Pts',(4.93041939446714,0.524062008404491,3.72004504823011));
#37846=CARTESIAN_POINT('Ctrl Pts',(4.92246675512334,0.477449434882097,3.6327885852077));
#37847=CARTESIAN_POINT('Ctrl Pts',(4.91451411577953,0.408571542497308,3.55742629914966));
#37848=CARTESIAN_POINT('Ctrl Pts',(4.90656147643572,0.325849591692228,3.50317225594031));
#37849=CARTESIAN_POINT('Ctrl Pts',(4.89860883709192,0.243127640887147,3.44891821273095));
#37850=CARTESIAN_POINT('Ctrl Pts',(4.89065619774811,0.146561631661773,3.41577241237029));
#37851=CARTESIAN_POINT('Ctrl Pts',(4.88270355840431,0.0479580738465473,
3.40778738038914));
#37852=CARTESIAN_POINT('Ctrl Pts',(4.8747509190605,-0.0506454839686783,
3.39980234840799));
#37853=CARTESIAN_POINT('Ctrl Pts',(4.86679827971669,-0.151286590373755,
3.41697808480634));
#37854=CARTESIAN_POINT('Ctrl Pts',(4.85884564037289,-0.241660499406316,
3.45721462188069));
#37855=CARTESIAN_POINT('Ctrl Pts',(4.85089300102908,-0.332034408438876,
3.49745115895503));
#37856=CARTESIAN_POINT('Ctrl Pts',(4.84294036168527,-0.41214112009892,3.56074849670536));
#37857=CARTESIAN_POINT('Ctrl Pts',(4.83498772234147,-0.472186497854497,
3.63936767349926));
#37858=CARTESIAN_POINT('Ctrl Pts',(4.82703508299766,-0.532231875610076,
3.71798685029316));
#37859=CARTESIAN_POINT('Ctrl Pts',(4.81908244365386,-0.572215919461187,
3.81192786613063));
#37860=CARTESIAN_POINT('Ctrl Pts',(4.81112980431005,-0.587250035475296,
3.9097051523746));
#37861=CARTESIAN_POINT('Ctrl Pts',(4.80317716496624,-0.602284151489406,
4.00748243861856));
#37862=CARTESIAN_POINT('Ctrl Pts',(4.79522452562244,-0.592368339666514,
4.10909599526903));
#37863=CARTESIAN_POINT('Ctrl Pts',(4.78727188627863,-0.558714943052599,
4.20212218107662));
#37864=CARTESIAN_POINT('Ctrl Pts',(4.77931924693482,-0.525061546438685,
4.2951483668842));
#37865=CARTESIAN_POINT('Ctrl Pts',(4.77136660759101,-0.467670565033749,
4.37958718184891));
#37866=CARTESIAN_POINT('Ctrl Pts',(4.76341396824721,-0.393558827964045,
4.44511483080773));
#37867=CARTESIAN_POINT('Ctrl Pts',(4.7554613289034,-0.319447090894342,4.51064247976655));
#37868=CARTESIAN_POINT('Ctrl Pts',(4.7475086895596,-0.228614598159871,4.55725896271948));
#37869=CARTESIAN_POINT('Ctrl Pts',(4.73955605021579,-0.13216685911108,4.5792647797218));
#37870=CARTESIAN_POINT('Ctrl Pts',(4.73598583722972,-0.0888681559330128,
4.58914394690572));
#37871=CARTESIAN_POINT('Ctrl Pts',(4.73241562424364,-0.0444377444908,4.59406302997518));
#37872=CARTESIAN_POINT('Ctrl Pts',(4.72884541125756,-4.67700812217808E-6,
4.59405084457266));
#37873=CARTESIAN_POINT('Ctrl Pts',(4.62115458874249,3.7232086238465E-6,
4.59414939806979));
#37874=CARTESIAN_POINT('Ctrl Pts',(4.62882432144443,-0.0954043143036648,
4.59411689615543));
#37875=CARTESIAN_POINT('Ctrl Pts',(4.63649405414636,-0.190827729806029,
4.57070400848325));
#37876=CARTESIAN_POINT('Ctrl Pts',(4.6441637868483,-0.275369369969159,4.52648596729292));
#37877=CARTESIAN_POINT('Ctrl Pts',(4.65211642619211,-0.363029422787103,
4.48063689435358));
#37878=CARTESIAN_POINT('Ctrl Pts',(4.66006906553591,-0.438990121848901,
4.4124195181391));
#37879=CARTESIAN_POINT('Ctrl Pts',(4.66802170487971,-0.493964237128006,
4.33017434199545));
#37880=CARTESIAN_POINT('Ctrl Pts',(4.67597434422352,-0.548938352407109,
4.24792916585179));
#37881=CARTESIAN_POINT('Ctrl Pts',(4.68392698356733,-0.582925883903521,
4.15165618977896));
#37882=CARTESIAN_POINT('Ctrl Pts',(4.69187962291114,-0.591771392992132,
4.05312609631255));
#37883=CARTESIAN_POINT('Ctrl Pts',(4.69983226225494,-0.600616902080743,
3.95459600284613));
#37884=CARTESIAN_POINT('Ctrl Pts',(4.70778490159875,-0.584320388761555,
3.85380879198612));
#37885=CARTESIAN_POINT('Ctrl Pts',(4.71573754094256,-0.544874323741249,
3.76308707295491));
#37886=CARTESIAN_POINT('Ctrl Pts',(4.72369018028636,-0.505428258720944,
3.6723653539237));
#37887=CARTESIAN_POINT('Ctrl Pts',(4.73164281963017,-0.442832641999522,
3.59170912672127));
#37888=CARTESIAN_POINT('Ctrl Pts',(4.73959545897397,-0.364740640256699,
3.53097971363863));
#37889=CARTESIAN_POINT('Ctrl Pts',(4.74754809831778,-0.286648638513876,
3.47025030055599));
#37890=CARTESIAN_POINT('Ctrl Pts',(4.75550073766158,-0.193060251749651,
3.42944770159313));
#37891=CARTESIAN_POINT('Ctrl Pts',(4.76345337700539,-0.095417934894009,
3.41356059019365));
#37892=CARTESIAN_POINT('Ctrl Pts',(4.7714060163492,0.00222438196163176,
3.39767347879416));
#37893=CARTESIAN_POINT('Ctrl Pts',(4.77935865569301,0.10392062890869,3.40670185495805));
#37894=CARTESIAN_POINT('Ctrl Pts',(4.78731129503681,0.19723705468272,3.43954187673519));
#37895=CARTESIAN_POINT('Ctrl Pts',(4.79526393438062,0.290553480456751,3.47238189851233));
#37896=CARTESIAN_POINT('Ctrl Pts',(4.80321657372443,0.375490085057754,3.52903356590271));
#37897=CARTESIAN_POINT('Ctrl Pts',(4.81116921306823,0.441662211759978,3.60257044098769));
#37898=CARTESIAN_POINT('Ctrl Pts',(4.81912185241204,0.507834338462201,3.67610731607267));
#37899=CARTESIAN_POINT('Ctrl Pts',(4.82707449175584,0.555241987265645,3.76652939885225));
#37900=CARTESIAN_POINT('Ctrl Pts',(4.83502713109965,0.57808892742485,3.86278135818256));
#37901=CARTESIAN_POINT('Ctrl Pts',(4.84297977044346,0.600935867584054,3.95903331751286));
#37902=CARTESIAN_POINT('Ctrl Pts',(4.85093240978726,0.599222099099018,4.0611151533939));
#37903=CARTESIAN_POINT('Ctrl Pts',(4.85888504913107,0.573157153508111,4.15654597106253));
#37904=CARTESIAN_POINT('Ctrl Pts',(4.86683768847488,0.547092207917203,4.25197678873116));
#37905=CARTESIAN_POINT('Ctrl Pts',(4.87479032781868,0.496676085220424,4.34075658818739));
#37906=CARTESIAN_POINT('Ctrl Pts',(4.88274296716249,0.428072843071251,4.41203082979109));
#37907=CARTESIAN_POINT('Ctrl Pts',(4.89069560650629,0.359469600922078,4.48330507139479));
#37908=CARTESIAN_POINT('Ctrl Pts',(4.8986482458501,0.272679239320511,4.53707375514596));
#37909=CARTESIAN_POINT('Ctrl Pts',(4.90660088519391,0.178313062033339,4.56676292714126));
#37910=CARTESIAN_POINT('Ctrl Pts',(4.9114521197101,0.120748216373203,4.58487378690922));
#37911=CARTESIAN_POINT('Ctrl Pts',(4.9163033542263,0.0603642649825261,4.59402420038378));
#37912=CARTESIAN_POINT('Ctrl Pts',(4.92115458874249,-9.52916733652962E-6,
4.59405847898621));
#37913=CARTESIAN_POINT('Origin',(4.,0.,4.));
#37914=CARTESIAN_POINT('',(5.32884541125756,-1.45357002139801E-5,4.59407911932661));
#37915=CARTESIAN_POINT('',(5.22115458874249,1.46139895546772E-5,4.59411444380891));
#37916=CARTESIAN_POINT('',(4.,-7.27562663373442E-17,4.5941));
#37917=CARTESIAN_POINT('Ctrl Pts',(5.32884541125756,-1.45357002139801E-5,
4.59407911932661));
#37918=CARTESIAN_POINT('Ctrl Pts',(5.32327896849499,0.0692531541268509,
4.59401614001471));
#37919=CARTESIAN_POINT('Ctrl Pts',(5.31771252573242,0.138542285837495,4.5819075943171));
#37920=CARTESIAN_POINT('Ctrl Pts',(5.31214608296985,0.203593590158122,4.55818044906639));
#37921=CARTESIAN_POINT('Ctrl Pts',(5.30419344362604,0.296530782575621,4.5242820624512));
#37922=CARTESIAN_POINT('Ctrl Pts',(5.29624080428224,0.380818089806801,4.46666879957728));
#37923=CARTESIAN_POINT('Ctrl Pts',(5.28828816493843,0.446150240572578,4.39238466650784));
#37924=CARTESIAN_POINT('Ctrl Pts',(5.28033552559462,0.511482391338355,4.3181005334384));
#37925=CARTESIAN_POINT('Ctrl Pts',(5.27238288625081,0.557859385638729,4.22714553017344));
#37926=CARTESIAN_POINT('Ctrl Pts',(5.26443024690701,0.579611004278495,4.13064014464439));
#37927=CARTESIAN_POINT('Ctrl Pts',(5.2564776075632,0.601362622918262,4.03413475911534));
#37928=CARTESIAN_POINT('Ctrl Pts',(5.2485249682194,0.598488865897423,3.93207899132219));
#37929=CARTESIAN_POINT('Ctrl Pts',(5.24057232887559,0.571341089151559,3.8369505488493));
#37930=CARTESIAN_POINT('Ctrl Pts',(5.23261968953179,0.544193312405696,3.74182210637642));
#37931=CARTESIAN_POINT('Ctrl Pts',(5.22466705018798,0.492771515934809,3.65362098922379));
#37932=CARTESIAN_POINT('Ctrl Pts',(5.21671441084417,0.423362714708271,3.58313098523844));
#37933=CARTESIAN_POINT('Ctrl Pts',(5.20876177150037,0.353953913481732,3.51264098125308));
#37934=CARTESIAN_POINT('Ctrl Pts',(5.20080913215656,0.266558107499543,3.45986209043499));
#37935=CARTESIAN_POINT('Ctrl Pts',(5.19285649281275,0.171860624350003,3.43124725102074));
#37936=CARTESIAN_POINT('Ctrl Pts',(5.18490385346895,0.0771631412004631,
3.40263241160649));
#37937=CARTESIAN_POINT('Ctrl Pts',(5.17695121412514,-0.0248360191164267,
3.39818162359609));
#37938=CARTESIAN_POINT('Ctrl Pts',(5.16899857478133,-0.121666070051256,
3.41843905644231));
#37939=CARTESIAN_POINT('Ctrl Pts',(5.16104593543753,-0.218496120986084,
3.43869648928852));
#37940=CARTESIAN_POINT('Ctrl Pts',(5.15309329609372,-0.310157062538852,
3.48366214299137));
#37941=CARTESIAN_POINT('Ctrl Pts',(5.14514065674991,-0.385442096207774,
3.54783835396576));
#37942=CARTESIAN_POINT('Ctrl Pts',(5.13718801740611,-0.460727129876697,
3.61201456494015));
#37943=CARTESIAN_POINT('Ctrl Pts',(5.1292353780623,-0.519636255661773,3.6954013331861));
#37944=CARTESIAN_POINT('Ctrl Pts',(5.1212827387185,-0.554967030609594,3.78780349058054));
#37945=CARTESIAN_POINT('Ctrl Pts',(5.11333009937469,-0.590297805557415,
3.88020564797498));
#37946=CARTESIAN_POINT('Ctrl Pts',(5.10537746003088,-0.60205022966798,3.98162319451792));
#37947=CARTESIAN_POINT('Ctrl Pts',(5.09742482068708,-0.588787409028971,
4.07965645386523));
#37948=CARTESIAN_POINT('Ctrl Pts',(5.08947218134327,-0.575524588389962,
4.17768971321255));
#37949=CARTESIAN_POINT('Ctrl Pts',(5.08151954199946,-0.537246523001379,
4.27233868536424));
#37950=CARTESIAN_POINT('Ctrl Pts',(5.07356690265566,-0.47863322769376,4.35203124438164));
#37951=CARTESIAN_POINT('Ctrl Pts',(5.06561426331185,-0.42001993238614,4.43172380339905));
#37952=CARTESIAN_POINT('Ctrl Pts',(5.05766162396805,-0.341071407159484,
4.49645994928216));
#37953=CARTESIAN_POINT('Ctrl Pts',(5.04970898462424,-0.251440184480074,
4.53832480650817));
#37954=CARTESIAN_POINT('Ctrl Pts',(5.04275446016868,-0.1730583412759,4.5749353153996));
#37955=CARTESIAN_POINT('Ctrl Pts',(5.03579993571312,-0.0865070403179845,
4.59405529558476));
#37956=CARTESIAN_POINT('Ctrl Pts',(5.02884541125756,1.1583539301252E-5,
4.59413174414479));
#37957=CARTESIAN_POINT('Ctrl Pts',(4.92115458874249,-9.52916733652962E-6,
4.59405847898621));
#37958=CARTESIAN_POINT('Ctrl Pts',(4.9242559935701,-0.0386066277022544,
4.59408039337166));
#37959=CARTESIAN_POINT('Ctrl Pts',(4.92735739839772,-0.0771995748988638,
4.59037647703175));
#37960=CARTESIAN_POINT('Ctrl Pts',(4.93045880322533,-0.115049119822012,
4.58290605049323));
#37961=CARTESIAN_POINT('Ctrl Pts',(4.93841144256913,-0.212103131417409,
4.56375034161047));
#37962=CARTESIAN_POINT('Ctrl Pts',(4.94636408191294,-0.304269161635426,
4.51982926360553));
#37963=CARTESIAN_POINT('Ctrl Pts',(4.95431672125675,-0.380278658005779,
4.45651276645759));
#37964=CARTESIAN_POINT('Ctrl Pts',(4.96226936060055,-0.456288154376132,
4.39319626930964));
#37965=CARTESIAN_POINT('Ctrl Pts',(4.97022199994436,-0.516141116898821,
4.31048435301868));
#37966=CARTESIAN_POINT('Ctrl Pts',(4.97817463928816,-0.552519705724467,
4.21848967586497));
#37967=CARTESIAN_POINT('Ctrl Pts',(4.98612727863197,-0.588898294550112,
4.12649499871126));
#37968=CARTESIAN_POINT('Ctrl Pts',(4.99407991797578,-0.601802509678713,
4.0252175606948));
#37969=CARTESIAN_POINT('Ctrl Pts',(5.00203255731958,-0.589654635058918,
3.92703990798411));
#37970=CARTESIAN_POINT('Ctrl Pts',(5.00998519666339,-0.577506760439122,
3.82886225527341));
#37971=CARTESIAN_POINT('Ctrl Pts',(5.0179378360072,-0.540306796070929,3.73378438786847));
#37972=CARTESIAN_POINT('Ctrl Pts',(5.025890475351,-0.482602944251693,3.65343086999412));
#37973=CARTESIAN_POINT('Ctrl Pts',(5.03384311469481,-0.424899092432456,
3.57307735211977));
#37974=CARTESIAN_POINT('Ctrl Pts',(5.04179575403862,-0.346691353162178,
3.50744818377599));
#37975=CARTESIAN_POINT('Ctrl Pts',(5.04974839338242,-0.257541687734669,
3.46456742464414));
#37976=CARTESIAN_POINT('Ctrl Pts',(5.05770103272623,-0.16839202230716,3.42168666551229));
#37977=CARTESIAN_POINT('Ctrl Pts',(5.06565367207003,-0.0683004307224215,
3.40155431559236));
#37978=CARTESIAN_POINT('Ctrl Pts',(5.07360631141384,0.0304955267282049,
3.40663182885918));
#37979=CARTESIAN_POINT('Ctrl Pts',(5.08155895075765,0.129291484178831,3.41170934212599));
#37980=CARTESIAN_POINT('Ctrl Pts',(5.08951159010146,0.226791807495345,3.44199671857955));
#37981=CARTESIAN_POINT('Ctrl Pts',(5.09746422944526,0.311075754224562,3.49379091394262));
#37982=CARTESIAN_POINT('Ctrl Pts',(5.10541686878907,0.395359700953779,3.54558510930568));
#37983=CARTESIAN_POINT('Ctrl Pts',(5.11336950813287,0.466427271095698,3.61888612357825));
#37984=CARTESIAN_POINT('Ctrl Pts',(5.12132214747668,0.515589486279599,3.70473190942573));
#37985=CARTESIAN_POINT('Ctrl Pts',(5.12927478682048,0.564751701463499,3.79057769527322));
#37986=CARTESIAN_POINT('Ctrl Pts',(5.13722742616429,0.592008561689381,3.88896825269562));
#37987=CARTESIAN_POINT('Ctrl Pts',(5.1451800655081,0.594027544563649,3.98787399599556));
#37988=CARTESIAN_POINT('Ctrl Pts',(5.1531327048519,0.596046527437917,4.0867797392955));
#37989=CARTESIAN_POINT('Ctrl Pts',(5.16108534419571,0.572827632960568,4.18620066847299));
#37990=CARTESIAN_POINT('Ctrl Pts',(5.16903798353952,0.527209687216453,4.2739812208502));
#37991=CARTESIAN_POINT('Ctrl Pts',(5.17699062288332,0.481591741472338,4.3617617732274));
#37992=CARTESIAN_POINT('Ctrl Pts',(5.18494326222713,0.413574744461461,4.43790194880433));
#37993=CARTESIAN_POINT('Ctrl Pts',(5.19289590157094,0.331474700441294,4.49309257410834));
#37994=CARTESIAN_POINT('Ctrl Pts',(5.20084854091474,0.24937465642113,4.54828319941234));
#37995=CARTESIAN_POINT('Ctrl Pts',(5.20880118025855,0.153191565391677,4.58252427444343));
#37996=CARTESIAN_POINT('Ctrl Pts',(5.21675381960235,0.0546851202186884,
4.59162936142496));
#37997=CARTESIAN_POINT('Ctrl Pts',(5.21822074264906,0.0365148790664279,
4.59330886194775));
#37998=CARTESIAN_POINT('Ctrl Pts',(5.21968766569578,0.018265586889787,4.59413312238171));
#37999=CARTESIAN_POINT('Ctrl Pts',(5.22115458874249,1.46139895546772E-5,
4.59411444380891));
#38000=CARTESIAN_POINT('Origin',(4.,0.,4.));
#38001=CARTESIAN_POINT('',(5.62884541125756,1.52328526200479E-5,4.59408648697874));
#38002=CARTESIAN_POINT('',(5.52115458874249,-1.55733839743342E-5,4.59409663347568));
#38003=CARTESIAN_POINT('',(4.,-7.27562663373442E-17,4.5941));
#38004=CARTESIAN_POINT('Ctrl Pts',(5.62884541125756,1.52328526200479E-5,
4.59408648697874));
#38005=CARTESIAN_POINT('Ctrl Pts',(5.62666327996447,0.0271682673899915,
4.59411287463303));
#38006=CARTESIAN_POINT('Ctrl Pts',(5.62448114867138,0.054317778225707,4.59228554395034));
#38007=CARTESIAN_POINT('Ctrl Pts',(5.62229901737829,0.0812075234320336,
4.58857548522516));
#38008=CARTESIAN_POINT('Ctrl Pts',(5.61434637803449,0.179205497408217,4.57505441109036));
#38009=CARTESIAN_POINT('Ctrl Pts',(5.60639373869068,0.273753285393806,4.53652709601604));
#38010=CARTESIAN_POINT('Ctrl Pts',(5.59844109934688,0.353291132582354,4.47770402899113));
#38011=CARTESIAN_POINT('Ctrl Pts',(5.59048846000307,0.432828979770902,4.41888096196622));
#38012=CARTESIAN_POINT('Ctrl Pts',(5.58253582065927,0.497356886162411,4.33976214299073));
#38013=CARTESIAN_POINT('Ctrl Pts',(5.57458318131546,0.538985436353474,4.25002092526659));
#38014=CARTESIAN_POINT('Ctrl Pts',(5.56663054197165,0.580613986544537,4.16027970754245));
#38015=CARTESIAN_POINT('Ctrl Pts',(5.55867790262784,0.599343180535155,4.05991609106967));
#38016=CARTESIAN_POINT('Ctrl Pts',(5.55072526328404,0.592883119270616,3.96120089488413));
#38017=CARTESIAN_POINT('Ctrl Pts',(5.54277262394023,0.586423058006077,3.86248569869858));
#38018=CARTESIAN_POINT('Ctrl Pts',(5.53481998459642,0.554773741486382,3.76541892280029));
#38019=CARTESIAN_POINT('Ctrl Pts',(5.52686734525262,0.501804729712613,3.68186830256729));
#38020=CARTESIAN_POINT('Ctrl Pts',(5.51891470590881,0.448835717938844,3.5983176823343));
#38021=CARTESIAN_POINT('Ctrl Pts',(5.51096206656501,0.374547010911001,3.52828321776661));
#38022=CARTESIAN_POINT('Ctrl Pts',(5.5030094272212,0.288021414854312,3.48032757600706));
#38023=CARTESIAN_POINT('Ctrl Pts',(5.4950567878774,0.201495818797622,3.4323719342475));
#38024=CARTESIAN_POINT('Ctrl Pts',(5.48710414853359,0.102733333712086,3.40649511529609));
#38025=CARTESIAN_POINT('Ctrl Pts',(5.47915150918978,0.00380901851787326,
3.40586091270526));
#38026=CARTESIAN_POINT('Ctrl Pts',(5.47119886984597,-0.0951152966763399,
3.40522671011442));
#38027=CARTESIAN_POINT('Ctrl Pts',(5.46324623050217,-0.194201441979227,
3.42983512388417));
#38028=CARTESIAN_POINT('Ctrl Pts',(5.45529359115836,-0.281334786601535,
3.47667744027106));
#38029=CARTESIAN_POINT('Ctrl Pts',(5.44734095181456,-0.368468131223842,
3.52351975665794));
#38030=CARTESIAN_POINT('Ctrl Pts',(5.43938831247075,-0.443648675165568,
3.59259597566196));
#38031=CARTESIAN_POINT('Ctrl Pts',(5.43143567312694,-0.497684572991269,
3.67546058871077));
#38032=CARTESIAN_POINT('Ctrl Pts',(5.42348303378314,-0.551720470816969,
3.75832520175959));
#38033=CARTESIAN_POINT('Ctrl Pts',(5.41553039443933,-0.584611722526643,
3.85497820885321));
#38034=CARTESIAN_POINT('Ctrl Pts',(5.40757775509553,-0.592336924628993,
3.95360246348684));
#38035=CARTESIAN_POINT('Ctrl Pts',(5.39962511575172,-0.600062126731343,
4.05222671812048));
#38036=CARTESIAN_POINT('Ctrl Pts',(5.39167247640791,-0.582621279226368,
4.15282222029412));
#38037=CARTESIAN_POINT('Ctrl Pts',(5.3837198370641,-0.542146763261091,4.24308979978386));
#38038=CARTESIAN_POINT('Ctrl Pts',(5.3757671977203,-0.501672247295815,4.3333573792736));
#38039=CARTESIAN_POINT('Ctrl Pts',(5.36781455837649,-0.438164062870237,
4.41329703607943));
#38040=CARTESIAN_POINT('Ctrl Pts',(5.35986191903269,-0.359386950494509,
4.47313505840055));
#38041=CARTESIAN_POINT('Ctrl Pts',(5.35190927968888,-0.28060983811878,4.53297308072167));
#38042=CARTESIAN_POINT('Ctrl Pts',(5.34395664034507,-0.1865637977929,4.57270946855809));
#38043=CARTESIAN_POINT('Ctrl Pts',(5.33600400100126,-0.0887472388280498,
4.58748590729807));
#38044=CARTESIAN_POINT('Ctrl Pts',(5.33361780442003,-0.0593972924141157,
4.59191959101989));
#38045=CARTESIAN_POINT('Ctrl Pts',(5.3312316078388,-0.0297078841644672,
4.59410611700271));
#38046=CARTESIAN_POINT('Ctrl Pts',(5.32884541125756,-1.45357002139801E-5,
4.59407911932661));
#38047=CARTESIAN_POINT('Ctrl Pts',(5.22115458874249,1.46139895546772E-5,
4.59411444380891));
#38048=CARTESIAN_POINT('Ctrl Pts',(5.22764030503958,-0.0806785298274998,
4.59403186011492));
#38049=CARTESIAN_POINT('Ctrl Pts',(5.23412602133668,-0.161404528346198,
4.57747154641029));
#38050=CARTESIAN_POINT('Ctrl Pts',(5.24061173763377,-0.235476461490165,
4.54549665421293));
#38051=CARTESIAN_POINT('Ctrl Pts',(5.24856437697758,-0.32630179870949,4.50628976108741));
#38052=CARTESIAN_POINT('Ctrl Pts',(5.25651701632139,-0.407122673831612,
4.44390687590439));
#38053=CARTESIAN_POINT('Ctrl Pts',(5.26446965566519,-0.468057634114636,
4.36597515601533));
#38054=CARTESIAN_POINT('Ctrl Pts',(5.272422295009,-0.52899259439766,4.28804343612627));
#38055=CARTESIAN_POINT('Ctrl Pts',(5.28037493435281,-0.570041639841584,
4.19456288153117));
#38056=CARTESIAN_POINT('Ctrl Pts',(5.28832757369661,-0.586185965564114,
4.09696276320888));
#38057=CARTESIAN_POINT('Ctrl Pts',(5.29628021304042,-0.602330291286644,
3.99936264488659));
#38058=CARTESIAN_POINT('Ctrl Pts',(5.30423285238423,-0.59356989728778,3.89764296283709));
#38059=CARTESIAN_POINT('Ctrl Pts',(5.31218549172803,-0.560975861048054,
3.80424033358521));
#38060=CARTESIAN_POINT('Ctrl Pts',(5.32013813107184,-0.528381824808328,
3.71083770433334));
#38061=CARTESIAN_POINT('Ctrl Pts',(5.32809077041564,-0.471954146327742,
3.62575212787907));
#38062=CARTESIAN_POINT('Ctrl Pts',(5.33604340975945,-0.398591877830097,
3.55938647478623));
#38063=CARTESIAN_POINT('Ctrl Pts',(5.34399604910326,-0.325229609332449,
3.49302082169338));
#38064=CARTESIAN_POINT('Ctrl Pts',(5.35194868844707,-0.234932750817741,
3.44537509196196));
#38065=CARTESIAN_POINT('Ctrl Pts',(5.35990132779087,-0.138741323057917,
3.42227462497344));
#38066=CARTESIAN_POINT('Ctrl Pts',(5.36785396713468,-0.042549895298095,
3.39917415798493));
#38067=CARTESIAN_POINT('Ctrl Pts',(5.37580660647848,0.059536101706843,3.40061895373932));
#38068=CARTESIAN_POINT('Ctrl Pts',(5.38375924582229,0.155035264439678,3.42643236627792));
#38069=CARTESIAN_POINT('Ctrl Pts',(5.39171188516609,0.250534427172515,3.45224577881651));
#38070=CARTESIAN_POINT('Ctrl Pts',(5.3996645245099,0.339446755633248,3.5024278081393));
#38071=CARTESIAN_POINT('Ctrl Pts',(5.40761716385371,0.41090150670596,3.57084301769608));
#38072=CARTESIAN_POINT('Ctrl Pts',(5.41556980319751,0.482356257778672,3.63925822725286));
#38073=CARTESIAN_POINT('Ctrl Pts',(5.42352244254132,0.536353431463363,3.72590661704362));
#38074=CARTESIAN_POINT('Ctrl Pts',(5.43147508188513,0.566291137850326,3.82019424128906));
#38075=CARTESIAN_POINT('Ctrl Pts',(5.43942772122893,0.596228844237288,3.91448186553449));
#38076=CARTESIAN_POINT('Ctrl Pts',(5.44738036057274,0.602107083326521,4.01640872423458));
#38077=CARTESIAN_POINT('Ctrl Pts',(5.45533299991655,0.583207160329387,4.11351287069736));
#38078=CARTESIAN_POINT('Ctrl Pts',(5.46328563926035,0.564307237332252,4.21061701716013));
#38079=CARTESIAN_POINT('Ctrl Pts',(5.47123827860416,0.520629152248751,4.30289845138559));
#38080=CARTESIAN_POINT('Ctrl Pts',(5.47919091794796,0.457513145863858,4.37907451119169));
#38081=CARTESIAN_POINT('Ctrl Pts',(5.48714355729177,0.394397139478966,4.45525057099779));
#38082=CARTESIAN_POINT('Ctrl Pts',(5.49509619663558,0.311843211792683,4.51532125638452));
#38083=CARTESIAN_POINT('Ctrl Pts',(5.50304883597938,0.219944704826683,4.5519421079172));
#38084=CARTESIAN_POINT('Ctrl Pts',(5.50908408690042,0.150203009669811,4.5797336395568));
#38085=CARTESIAN_POINT('Ctrl Pts',(5.51511933782146,0.0750795109720808,
4.59401975858331));
#38086=CARTESIAN_POINT('Ctrl Pts',(5.52115458874249,-1.55733839743342E-5,
4.59409663347568));
#38087=CARTESIAN_POINT('Origin',(4.,0.,4.));
#38088=CARTESIAN_POINT('',(5.92884541125757,-1.3134308860685E-5,4.59412454375027));
#38089=CARTESIAN_POINT('',(5.82115458874249,1.31105368646138E-5,4.59407040741879));
#38090=CARTESIAN_POINT('',(4.,-7.27562663373442E-17,4.5941));
#38091=CARTESIAN_POINT('Ctrl Pts',(5.92884541125757,-1.3134308860685E-5,
4.59412454375027));
#38092=CARTESIAN_POINT('Ctrl Pts',(5.92209495209015,0.0839697382976411,
4.5940436242297));
#38093=CARTESIAN_POINT('Ctrl Pts',(5.91534449292274,0.16798613900316,4.57606223573506));
#38094=CARTESIAN_POINT('Ctrl Pts',(5.90859403375532,0.244517407380453,4.54150437939301));
#38095=CARTESIAN_POINT('Ctrl Pts',(5.90064139441152,0.334678026211646,4.50079216098422));
#38096=CARTESIAN_POINT('Ctrl Pts',(5.89268875506771,0.41445008323119,4.43707358099086));
#38097=CARTESIAN_POINT('Ctrl Pts',(5.8847361157239,0.474080337065587,4.35813908232779));
#38098=CARTESIAN_POINT('Ctrl Pts',(5.8767834763801,0.533710590899983,4.27920458366471));
#38099=CARTESIAN_POINT('Ctrl Pts',(5.86883083703629,0.573199041549232,4.18505416633191));
#38100=CARTESIAN_POINT('Ctrl Pts',(5.86087819769249,0.587717699183782,4.08719901244189));
#38101=CARTESIAN_POINT('Ctrl Pts',(5.85292555834868,0.602236356818331,3.98934385855186));
#38102=CARTESIAN_POINT('Ctrl Pts',(5.84497291900487,0.591785221438181,3.88778396810461));
#38103=CARTESIAN_POINT('Ctrl Pts',(5.83702027966107,0.557642080814915,3.79493641494568));
#38104=CARTESIAN_POINT('Ctrl Pts',(5.82906764031726,0.523498940191649,3.70208886178675));
#38105=CARTESIAN_POINT('Ctrl Pts',(5.82111500097346,0.465663794325265,3.61795364591614));
#38106=CARTESIAN_POINT('Ctrl Pts',(5.81316236162965,0.391207780605707,3.55281744653948));
#38107=CARTESIAN_POINT('Ctrl Pts',(5.80520972228584,0.31675176688615,3.48768124716281));
#38108=CARTESIAN_POINT('Ctrl Pts',(5.79725708294203,0.225674885313418,3.44154406428009));
#38109=CARTESIAN_POINT('Ctrl Pts',(5.78930444359823,0.129112523455512,3.42004679519738));
#38110=CARTESIAN_POINT('Ctrl Pts',(5.78135180425442,0.0325501615976049,
3.39854952611466));
#38111=CARTESIAN_POINT('Ctrl Pts',(5.77339916491062,-0.0694976805454773,
3.40169217083197));
#38112=CARTESIAN_POINT('Ctrl Pts',(5.76544652556681,-0.164554263536051,
3.42909049911887));
#38113=CARTESIAN_POINT('Ctrl Pts',(5.75749388622301,-0.259610846526622,
3.45648882740576));
#38114=CARTESIAN_POINT('Ctrl Pts',(5.7495412468792,-0.347676170364685,3.50814283926225));
#38115=CARTESIAN_POINT('Ctrl Pts',(5.74158860753539,-0.417983050247216,
3.57773712775495));
#38116=CARTESIAN_POINT('Ctrl Pts',(5.73363596819158,-0.488289930129746,
3.64733141624764));
#38117=CARTESIAN_POINT('Ctrl Pts',(5.72568332884778,-0.540838366056745,
3.73486598137654));
#38118=CARTESIAN_POINT('Ctrl Pts',(5.71773068950397,-0.569203595796233,
3.82963853060694));
#38119=CARTESIAN_POINT('Ctrl Pts',(5.70977805016017,-0.597568825535722,
3.92441107983734));
#38120=CARTESIAN_POINT('Ctrl Pts',(5.70182541081636,-0.6017508490877,4.02642161316923));
#38121=CARTESIAN_POINT('Ctrl Pts',(5.69387277147255,-0.581238357244447,
4.12319795341528));
#38122=CARTESIAN_POINT('Ctrl Pts',(5.68592013212875,-0.560725865401195,
4.21997429366132));
#38123=CARTESIAN_POINT('Ctrl Pts',(5.67796749278494,-0.515518858162713,
4.31151644082153));
#38124=CARTESIAN_POINT('Ctrl Pts',(5.67001485344113,-0.451144507802385,
4.38663212069642));
#38125=CARTESIAN_POINT('Ctrl Pts',(5.66206221409732,-0.386770157442057,
4.46174780057131));
#38126=CARTESIAN_POINT('Ctrl Pts',(5.65410957475352,-0.303228463959881,
4.52043701316089));
#38127=CARTESIAN_POINT('Ctrl Pts',(5.64615693540972,-0.210733537235404,
4.55552420285805));
#38128=CARTESIAN_POINT('Ctrl Pts',(5.640386427359,-0.143618370026196,4.5809837895275));
#38129=CARTESIAN_POINT('Ctrl Pts',(5.63461591930828,-0.07178924788396,4.59401670649762));
#38130=CARTESIAN_POINT('Ctrl Pts',(5.62884541125756,1.52328526200479E-5,
4.59408648697874));
#38131=CARTESIAN_POINT('Ctrl Pts',(5.52115458874249,-1.55733839743342E-5,
4.59409663347568));
#38132=CARTESIAN_POINT('Ctrl Pts',(5.52307197716526,-0.0238731473664388,
4.59412105649149));
#38133=CARTESIAN_POINT('Ctrl Pts',(5.52498936558803,-0.0477278534282068,
4.59271130989713));
#38134=CARTESIAN_POINT('Ctrl Pts',(5.5269067540108,-0.0714062077139717,
4.58984482465595));
#38135=CARTESIAN_POINT('Ctrl Pts',(5.53485939335461,-0.169615527042917,
4.57795567218339));
#38136=CARTESIAN_POINT('Ctrl Pts',(5.54281203269841,-0.264791079455087,
4.54100634955965));
#38137=CARTESIAN_POINT('Ctrl Pts',(5.55076467204222,-0.345296357402727,
4.48351441471562));
#38138=CARTESIAN_POINT('Ctrl Pts',(5.55871731138603,-0.425801635350366,
4.4260224798716));
#38139=CARTESIAN_POINT('Ctrl Pts',(5.56666995072984,-0.491636638833473,
4.34798793280729));
#38140=CARTESIAN_POINT('Ctrl Pts',(5.57462259007364,-0.534752142022197,
4.2589515597096));
#38141=CARTESIAN_POINT('Ctrl Pts',(5.58257522941745,-0.577867645210921,
4.16991518661191));
#38142=CARTESIAN_POINT('Ctrl Pts',(5.59052786876125,-0.598263648105263,
4.06987698748084));
#38143=CARTESIAN_POINT('Ctrl Pts',(5.59848050810506,-0.59344646156208,3.97106799465478));
#38144=CARTESIAN_POINT('Ctrl Pts',(5.60643314744886,-0.588629275018896,
3.87225900182873));
#38145=CARTESIAN_POINT('Ctrl Pts',(5.61438578679267,-0.558598899038186,
3.77467921530768));
#38146=CARTESIAN_POINT('Ctrl Pts',(5.62233842613648,-0.50702695609161,3.69025909300064));
#38147=CARTESIAN_POINT('Ctrl Pts',(5.63029106548029,-0.455455013145033,
3.6058389706936));
#38148=CARTESIAN_POINT('Ctrl Pts',(5.63824370482409,-0.382341503232591,
3.53457851260056));
#38149=CARTESIAN_POINT('Ctrl Pts',(5.6461963441679,-0.296625548722353,3.48519028027742));
#38150=CARTESIAN_POINT('Ctrl Pts',(5.6541489835117,-0.210909594212113,3.43580204795428));
#38151=CARTESIAN_POINT('Ctrl Pts',(5.66210162285551,-0.112591195104077,
3.40828604140104));
#38152=CARTESIAN_POINT('Ctrl Pts',(5.67005426219932,-0.0136911147678568,
3.40600646716786));
#38153=CARTESIAN_POINT('Ctrl Pts',(5.67800690154312,0.0852089655683624,
3.40372689293467));
#38154=CARTESIAN_POINT('Ctrl Pts',(5.68595954088693,0.184690727132768,3.42668375102154));
#38155=CARTESIAN_POINT('Ctrl Pts',(5.69391218023074,0.272591169676606,3.47207025288287));
#38156=CARTESIAN_POINT('Ctrl Pts',(5.70186481957454,0.360491612220445,3.51745675474419));
#38157=CARTESIAN_POINT('Ctrl Pts',(5.70981745891835,0.436810735743714,3.58527290037998));
#38158=CARTESIAN_POINT('Ctrl Pts',(5.71777009826216,0.492217487918224,3.667227242308));
#38159=CARTESIAN_POINT('Ctrl Pts',(5.72572273760596,0.547624240092733,3.74918158423602));
#38160=CARTESIAN_POINT('Ctrl Pts',(5.73367537694977,0.582118620918482,3.84527412245626));
#38161=CARTESIAN_POINT('Ctrl Pts',(5.74162801629357,0.591483222595687,3.94375623549444));
#38162=CARTESIAN_POINT('Ctrl Pts',(5.74958065563738,0.600847824272892,4.04223834853263));
#38163=CARTESIAN_POINT('Ctrl Pts',(5.75753329498119,0.585082646801554,4.14311003638875));
#38164=CARTESIAN_POINT('Ctrl Pts',(5.76548593432499,0.546115197731279,4.23403836123177));
#38165=CARTESIAN_POINT('Ctrl Pts',(5.7734385736688,0.507147748661005,4.32496668607478));
#38166=CARTESIAN_POINT('Ctrl Pts',(5.78139121301261,0.444978027991796,4.4059516479047));
#38167=CARTESIAN_POINT('Ctrl Pts',(5.78934385235641,0.367207131024688,4.46709173242012));
#38168=CARTESIAN_POINT('Ctrl Pts',(5.79729649170022,0.28943623405758,4.52823181693554));
#38169=CARTESIAN_POINT('Ctrl Pts',(5.80524913104403,0.196064160792572,4.56952702413646));
#38170=CARTESIAN_POINT('Ctrl Pts',(5.81320177038783,0.0985069184831505,
4.58592845199323));
#38171=CARTESIAN_POINT('Ctrl Pts',(5.81585270983939,0.0659871057213339,
4.59139571767544));
#38172=CARTESIAN_POINT('Ctrl Pts',(5.81850364929094,0.0330022532417819,
4.59409688335147));
#38173=CARTESIAN_POINT('Ctrl Pts',(5.82115458874249,1.31105368646138E-5,
4.59407040741879));
#38174=CARTESIAN_POINT('Origin',(4.,0.,4.));
#38175=CARTESIAN_POINT('',(6.22884541125756,-1.27841859475647E-5,4.5940334609955));
#38176=CARTESIAN_POINT('',(6.12115458874249,-9.50793186244619E-6,4.59413936148612));
#38177=CARTESIAN_POINT('',(4.,-7.27562663373442E-17,4.5941));
#38178=CARTESIAN_POINT('Ctrl Pts',(6.22884541125756,-1.27841859475647E-5,
4.5940334609955));
#38179=CARTESIAN_POINT('Ctrl Pts',(6.22547926355963,0.0418951881409122,
4.59406590912705));
#38180=CARTESIAN_POINT('Ctrl Pts',(6.2221131158617,0.0838018877146867,4.58971510200585));
#38181=CARTESIAN_POINT('Ctrl Pts',(6.21874696816377,0.124749109322564,4.58093223526196));
#38182=CARTESIAN_POINT('Ctrl Pts',(6.21079432881996,0.22148832423537,4.56018241146135));
#38183=CARTESIAN_POINT('Ctrl Pts',(6.20284168947616,0.31287214740051,4.51469474440412));
#38184=CARTESIAN_POINT('Ctrl Pts',(6.19488905013236,0.387808805213989,4.4501133836823));
#38185=CARTESIAN_POINT('Ctrl Pts',(6.18693641078855,0.462745463027469,4.38553202296047));
#38186=CARTESIAN_POINT('Ctrl Pts',(6.17898377144474,0.521234955489287,4.30185696857405));
#38187=CARTESIAN_POINT('Ctrl Pts',(6.17103113210093,0.556083161424236,4.20927485003939));
#38188=CARTESIAN_POINT('Ctrl Pts',(6.16307849275713,0.590931367359184,4.11669273150472));
#38189=CARTESIAN_POINT('Ctrl Pts',(6.15512585341332,0.602138286767263,4.0152035488218));
#38190=CARTESIAN_POINT('Ctrl Pts',(6.14717321406952,0.588356486924291,3.9172389266648));
#38191=CARTESIAN_POINT('Ctrl Pts',(6.13922057472571,0.574574687081318,3.81927430450779));
#38192=CARTESIAN_POINT('Ctrl Pts',(6.1312679353819,0.535804167987293,3.7248342428767));
#38193=CARTESIAN_POINT('Ctrl Pts',(6.12331529603809,0.476773096629474,3.64545304401991));
#38194=CARTESIAN_POINT('Ctrl Pts',(6.11536265669429,0.417742025271657,3.56607184516312));
#38195=CARTESIAN_POINT('Ctrl Pts',(6.10741001735048,0.338450401650047,3.50174950908064));
#38196=CARTESIAN_POINT('Ctrl Pts',(6.09945737800668,0.248599092144812,3.46035682177302));
#38197=CARTESIAN_POINT('Ctrl Pts',(6.09150473866287,0.158747782639575,3.41896413446539));
#38198=CARTESIAN_POINT('Ctrl Pts',(6.08355209931906,0.0583367872507115,
3.40050109593262));
#38199=CARTESIAN_POINT('Ctrl Pts',(6.07559945997526,-0.0403606640336046,
3.40722161935946));
#38200=CARTESIAN_POINT('Ctrl Pts',(6.06764682063145,-0.139058115317921,
3.4139421427863));
#38201=CARTESIAN_POINT('Ctrl Pts',(6.05969418128764,-0.23604202249769,3.44584622817275));
#38202=CARTESIAN_POINT('Ctrl Pts',(6.05174154194384,-0.319452991027635,
3.49903499090221));
#38203=CARTESIAN_POINT('Ctrl Pts',(6.04378890260003,-0.40286395955758,3.55222375363166));
#38204=CARTESIAN_POINT('Ctrl Pts',(6.03583626325623,-0.472701989437702,
3.62669719370411));
#38205=CARTESIAN_POINT('Ctrl Pts',(6.02788362391242,-0.520429378860104,
3.71334895258148));
#38206=CARTESIAN_POINT('Ctrl Pts',(6.01993098456861,-0.568156768282506,
3.80000071145885));
#38207=CARTESIAN_POINT('Ctrl Pts',(6.0119783452248,-0.593773517247188,3.89883078914114));
#38208=CARTESIAN_POINT('Ctrl Pts',(6.004025705881,-0.594147126960238,3.99775637428654));
#38209=CARTESIAN_POINT('Ctrl Pts',(5.99607306653719,-0.594520736673288,
4.09668195943193));
#38210=CARTESIAN_POINT('Ctrl Pts',(5.98812042719339,-0.569651207134705,
4.19570305204043));
#38211=CARTESIAN_POINT('Ctrl Pts',(5.98016778784958,-0.52257944308796,4.28271270390554));
#38212=CARTESIAN_POINT('Ctrl Pts',(5.97221514850578,-0.475507679041215,
4.36972235577065));
#38213=CARTESIAN_POINT('Ctrl Pts',(5.96426250916196,-0.406233680486307,
4.44472056689237));
#38214=CARTESIAN_POINT('Ctrl Pts',(5.95630986981816,-0.323226996343023,
4.49853792802592));
#38215=CARTESIAN_POINT('Ctrl Pts',(5.94835723047435,-0.240220312199739,
4.55235528915947));
#38216=CARTESIAN_POINT('Ctrl Pts',(5.94040459113055,-0.143480942468078,
4.58499180030486));
#38217=CARTESIAN_POINT('Ctrl Pts',(5.93245195178675,-0.0448366672808267,
4.59245712746544));
#38218=CARTESIAN_POINT('Ctrl Pts',(5.93124977161035,-0.0299248641651563,
4.59358564190382));
#38219=CARTESIAN_POINT('Ctrl Pts',(5.93004759143396,-0.0149695309183627,
4.59413895459864));
#38220=CARTESIAN_POINT('Ctrl Pts',(5.92884541125757,-1.3134308860685E-5,
4.59412454375027));
#38221=CARTESIAN_POINT('Ctrl Pts',(5.82115458874249,1.31105368646138E-5,
4.59407040741879));
#38222=CARTESIAN_POINT('Ctrl Pts',(5.82645628863475,-0.0659629472043463,
4.59401745734129));
#38223=CARTESIAN_POINT('Ctrl Pts',(5.831757988527,-0.131956164688202,4.58305467757793));
#38224=CARTESIAN_POINT('Ctrl Pts',(5.83705968841925,-0.194280919321303,
4.56148970414564));
#38225=CARTESIAN_POINT('Ctrl Pts',(5.84501232776306,-0.287769103462499,
4.52914187992864));
#38226=CARTESIAN_POINT('Ctrl Pts',(5.85296496710686,-0.373003060391055,
4.47293858298203));
#38227=CARTESIAN_POINT('Ctrl Pts',(5.86091760645067,-0.439561779454174,
4.39975142997742));
#38228=CARTESIAN_POINT('Ctrl Pts',(5.86887024579447,-0.506120498517293,
4.32656427697281));
#38229=CARTESIAN_POINT('Ctrl Pts',(5.87682288513828,-0.554003979714975,
4.2363932679102));
#38230=CARTESIAN_POINT('Ctrl Pts',(5.88477552448209,-0.577357812582609,
4.14026304025204));
#38231=CARTESIAN_POINT('Ctrl Pts',(5.8927281638259,-0.600711645450243,4.04413281259387));
#38232=CARTESIAN_POINT('Ctrl Pts',(5.9006808031697,-0.59953582998783,3.94204336634015));
#38233=CARTESIAN_POINT('Ctrl Pts',(5.90863344251351,-0.573974130801472,
3.84647652011691));
#38234=CARTESIAN_POINT('Ctrl Pts',(5.91658608185731,-0.548412431615114,
3.75090967389367));
#38235=CARTESIAN_POINT('Ctrl Pts',(5.92453872120112,-0.498464848704808,
3.66186542770092));
#38236=CARTESIAN_POINT('Ctrl Pts',(5.93249136054493,-0.430238144626613,
3.59023066587279));
#38237=CARTESIAN_POINT('Ctrl Pts',(5.94044399988873,-0.362011440548417,
3.51859590404466));
#38238=CARTESIAN_POINT('Ctrl Pts',(5.94839663923254,-0.275505615302329,
3.46437062658116));
#38239=CARTESIAN_POINT('Ctrl Pts',(5.95634927857635,-0.181297202577209,
3.43418458862315));
#38240=CARTESIAN_POINT('Ctrl Pts',(5.96430191792015,-0.087088789852092,
3.40399855066514));
#38241=CARTESIAN_POINT('Ctrl Pts',(5.97225455726396,0.0148222103520573,
3.39785175221263));
#38242=CARTESIAN_POINT('Ctrl Pts',(5.98020719660777,0.111975824940657,3.41649576758492));
#38243=CARTESIAN_POINT('Ctrl Pts',(5.98815983595157,0.209129439529257,3.43513978295721));
#38244=CARTESIAN_POINT('Ctrl Pts',(5.99611247529537,0.301525668502307,3.47857461215431));
#38245=CARTESIAN_POINT('Ctrl Pts',(6.00406511463918,0.377867748972965,3.54148967172874));
#38246=CARTESIAN_POINT('Ctrl Pts',(6.01201775398299,0.454209829443624,3.60440473130317));
#38247=CARTESIAN_POINT('Ctrl Pts',(6.0199703933268,0.514497761411887,3.68680002125492));
#38248=CARTESIAN_POINT('Ctrl Pts',(6.02792303267061,0.551360647735685,3.77860175380959));
#38249=CARTESIAN_POINT('Ctrl Pts',(6.03587567201441,0.588223534059482,3.87040348636426));
#38250=CARTESIAN_POINT('Ctrl Pts',(6.04382831135821,0.601661374738811,3.97161166152184));
#38251=CARTESIAN_POINT('Ctrl Pts',(6.05178095070202,0.590030977261751,4.06985190192822));
#38252=CARTESIAN_POINT('Ctrl Pts',(6.05973359004583,0.578400579784692,4.16809214233459));
#38253=CARTESIAN_POINT('Ctrl Pts',(6.06768622938964,0.541701944151245,4.26336444798975));
#38254=CARTESIAN_POINT('Ctrl Pts',(6.07563886873345,0.484422419230229,4.3440210474869));
#38255=CARTESIAN_POINT('Ctrl Pts',(6.08359150807725,0.427142894309213,4.42467764698404));
#38256=CARTESIAN_POINT('Ctrl Pts',(6.09154414742105,0.349282480100627,4.49071854032316));
#38257=CARTESIAN_POINT('Ctrl Pts',(6.09949678676486,0.26035984028865,4.53406826097581));
#38258=CARTESIAN_POINT('Ctrl Pts',(6.10671605409073,0.179637418414302,4.5734203814938));
#38259=CARTESIAN_POINT('Ctrl Pts',(6.11393532141662,0.0897989573399868,
4.59407340590587));
#38260=CARTESIAN_POINT('Ctrl Pts',(6.12115458874249,-9.50793186244619E-6,
4.59413936148612));
#38261=CARTESIAN_POINT('Origin',(4.,0.,4.));
#38262=CARTESIAN_POINT('',(6.52884541125757,2.61457539729726E-5,4.59508370962656));
#38263=CARTESIAN_POINT('',(6.42115458874249,-0.000630941829811112,4.59394485456974));
#38264=CARTESIAN_POINT('',(4.,-7.27562663373442E-17,4.5941));
#38265=CARTESIAN_POINT('Ctrl Pts',(6.52884541125757,2.61457539729726E-5,
4.59508370962656));
#38266=CARTESIAN_POINT('Ctrl Pts',(6.5129582963415,0.196771080344787,4.59506033873941));
#38267=CARTESIAN_POINT('Ctrl Pts',(6.49707118142544,0.393450480974957,4.48779253427891));
#38268=CARTESIAN_POINT('Ctrl Pts',(6.48118406650938,0.500111739713094,4.32240987211318));
#38269=CARTESIAN_POINT('Ctrl Pts',(6.46527878782176,0.606894944490356,4.15683812760557));
#38270=CARTESIAN_POINT('Ctrl Pts',(6.44937350913416,0.623454053851315,3.93301856375293));
#38271=CARTESIAN_POINT('Ctrl Pts',(6.43346823044654,0.541809843535619,3.75368369989414));
#38272=CARTESIAN_POINT('Ctrl Pts',(6.41756295175893,0.460165633219924,3.57434883603535));
#38273=CARTESIAN_POINT('Ctrl Pts',(6.40165767307132,0.280318103227576,3.43949867217041));
#38274=CARTESIAN_POINT('Ctrl Pts',(6.3857523943837,0.085604811340831,3.41110814665827));
#38275=CARTESIAN_POINT('Ctrl Pts',(6.36984711569609,-0.109108480545914,
3.38271762114613));
#38276=CARTESIAN_POINT('Ctrl Pts',(6.35394183700848,-0.318687534327053,
3.46078673398678));
#38277=CARTESIAN_POINT('Ctrl Pts',(6.33803655832087,-0.448733343985475,
3.60951691634857));
#38278=CARTESIAN_POINT('Ctrl Pts',(6.33008391897706,-0.513756248814686,
3.68388200752946));
#38279=CARTESIAN_POINT('Ctrl Pts',(6.32213127963325,-0.558895842613217,
3.77591236609064));
#38280=CARTESIAN_POINT('Ctrl Pts',(6.31417864028945,-0.579995970841135,
3.87270290659392));
#38281=CARTESIAN_POINT('Ctrl Pts',(6.30622600094564,-0.601096099069052,
3.9694934470972));
#38282=CARTESIAN_POINT('Ctrl Pts',(6.29827336160184,-0.598156761726356,
4.07104416954258));
#38283=CARTESIAN_POINT('Ctrl Pts',(6.29032072225803,-0.570614590620327,
4.16591643177432));
#38284=CARTESIAN_POINT('Ctrl Pts',(6.28236808291422,-0.543072419514299,
4.26078869400605));
#38285=CARTESIAN_POINT('Ctrl Pts',(6.27441544357042,-0.490927414644939,
4.34898249602413));
#38286=CARTESIAN_POINT('Ctrl Pts',(6.26646280422661,-0.421087730399527,
4.41916768405122));
#38287=CARTESIAN_POINT('Ctrl Pts',(6.2585101648828,-0.351248046154114,4.48935287207832));
#38288=CARTESIAN_POINT('Ctrl Pts',(6.250557525539,-0.263713682532649,4.54152944611444));
#38289=CARTESIAN_POINT('Ctrl Pts',(6.24260488619519,-0.168899197391682,
4.5696117428605));
#38290=CARTESIAN_POINT('Ctrl Pts',(6.23801839454932,-0.114217245248871,
4.58580752565092));
#38291=CARTESIAN_POINT('Ctrl Pts',(6.23343190290344,-0.0571138332845632,
4.59398924930378));
#38292=CARTESIAN_POINT('Ctrl Pts',(6.22884541125756,-1.27841859475647E-5,
4.5940334609955));
#38293=CARTESIAN_POINT('Ctrl Pts',(6.12115458874249,-9.50793186244619E-6,
4.59413936148612));
#38294=CARTESIAN_POINT('Ctrl Pts',(6.12188796076042,-0.00913273504488762,
4.59414606160884));
#38295=CARTESIAN_POINT('Ctrl Pts',(6.12262133277835,-0.0182556526135436,
4.59394031163173));
#38296=CARTESIAN_POINT('Ctrl Pts',(6.12335470479628,-0.0273686726716501,
4.59352013235631));
#38297=CARTESIAN_POINT('Ctrl Pts',(6.13130734414009,-0.126189680404606,
4.58896373511797));
#38298=CARTESIAN_POINT('Ctrl Pts',(6.13925998348389,-0.223846830455152,
4.55919239267511));
#38299=CARTESIAN_POINT('Ctrl Pts',(6.14721262282769,-0.308403173896691,
4.50784224986958));
#38300=CARTESIAN_POINT('Ctrl Pts',(6.1551652621715,-0.392959517338232,4.45649210706404));
#38301=CARTESIAN_POINT('Ctrl Pts',(6.16311790151532,-0.464415054170765,
4.38356316389581));
#38302=CARTESIAN_POINT('Ctrl Pts',(6.17107054085912,-0.514027768136376,
4.29797916579711));
#38303=CARTESIAN_POINT('Ctrl Pts',(6.17902318020293,-0.563640482101988,
4.2123951676984));
#38304=CARTESIAN_POINT('Ctrl Pts',(6.18697581954673,-0.591410373200678,
4.11415611466921));
#38305=CARTESIAN_POINT('Ctrl Pts',(6.19492845889053,-0.593952774873424,
4.0152594949342));
#38306=CARTESIAN_POINT('Ctrl Pts',(6.20288109823434,-0.59649517654617,3.9163628751992));
#38307=CARTESIAN_POINT('Ctrl Pts',(6.21083373757815,-0.573810088792972,
3.81680868875837));
#38308=CARTESIAN_POINT('Ctrl Pts',(6.21878637692196,-0.528651094032059,
3.72879442104321));
#38309=CARTESIAN_POINT('Ctrl Pts',(6.22673901626577,-0.483492099271145,
3.64078015332805));
#38310=CARTESIAN_POINT('Ctrl Pts',(6.23469165560957,-0.415859197502516,
3.56430580433857));
#38311=CARTESIAN_POINT('Ctrl Pts',(6.24264429495337,-0.334059153459168,
3.50867301156809));
#38312=CARTESIAN_POINT('Ctrl Pts',(6.25059693429718,-0.252259109415819,
3.45304021879761));
#38313=CARTESIAN_POINT('Ctrl Pts',(6.25854957364099,-0.156291923097747,
3.41824898224614));
#38314=CARTESIAN_POINT('Ctrl Pts',(6.2665022129848,-0.057819682214149,3.40864436538418));
#38315=CARTESIAN_POINT('Ctrl Pts',(6.2744548523286,0.0406525586694487,3.39903974852221));
#38316=CARTESIAN_POINT('Ctrl Pts',(6.28240749167241,0.141629854118573,3.41462175134974));
#38317=CARTESIAN_POINT('Ctrl Pts',(6.29036013101621,0.232632044389671,3.453312878872));
#38318=CARTESIAN_POINT('Ctrl Pts',(6.29831277036002,0.323634234660771,3.49200400639426));
#38319=CARTESIAN_POINT('Ctrl Pts',(6.30626540970382,0.404661319753841,3.55380425861124));
#38320=CARTESIAN_POINT('Ctrl Pts',(6.31421804904763,0.466059055789261,3.63148218419904));
#38321=CARTESIAN_POINT('Ctrl Pts',(6.32217068839144,0.527456791824679,3.70916010978684));
#38322=CARTESIAN_POINT('Ctrl Pts',(6.33012332773525,0.569225178802449,3.80271570874544));
#38323=CARTESIAN_POINT('Ctrl Pts',(6.33807596707905,0.585790493249255,3.90010619949006));
#38324=CARTESIAN_POINT('Ctrl Pts',(6.34602860642286,0.602355807696062,3.99749669023468));
#38325=CARTESIAN_POINT('Ctrl Pts',(6.35398124576666,0.593718049611903,4.09872207276531));
#38326=CARTESIAN_POINT('Ctrl Pts',(6.36193388511047,0.56173881546021,4.19248215342453));
#38327=CARTESIAN_POINT('Ctrl Pts',(6.36988652445427,0.529759581308516,4.28624223408375));
#38328=CARTESIAN_POINT('Ctrl Pts',(6.37783916379808,0.474438871089287,4.37253701287156));
#38329=CARTESIAN_POINT('Ctrl Pts',(6.38579180314189,0.401374624788453,4.4390182948332));
#38330=CARTESIAN_POINT('Ctrl Pts',(6.39757939834209,0.293077024234899,4.53755846574697));
#38331=CARTESIAN_POINT('Ctrl Pts',(6.40936699354229,0.145797072855576,4.59256860517148));
#38332=CARTESIAN_POINT('Ctrl Pts',(6.42115458874249,-0.000630941829811112,
4.59394485456974));
#38333=CARTESIAN_POINT('Origin',(4.,0.,4.));
#38334=CARTESIAN_POINT('',(6.82884541125756,0.000528213615369061,4.5937871332276));
#38335=CARTESIAN_POINT('',(6.72115458874249,0.000109070110168276,4.59505938903171));
#38336=CARTESIAN_POINT('',(4.,-7.27562663373442E-17,4.5941));
#38337=CARTESIAN_POINT('Ctrl Pts',(6.82884541125756,0.000528213615369061,
4.5937871332276));
#38338=CARTESIAN_POINT('Ctrl Pts',(6.82429524715479,0.0572034606387535,
4.59426930340541));
#38339=CARTESIAN_POINT('Ctrl Pts',(6.81974508305202,0.113754426020979,4.58681959872387));
#38340=CARTESIAN_POINT('Ctrl Pts',(6.81519491894924,0.167823213394864,4.57092612439125));
#38341=CARTESIAN_POINT('Ctrl Pts',(6.79928964026163,0.356822799356826,4.51536985589957));
#38342=CARTESIAN_POINT('Ctrl Pts',(6.78338436157403,0.515493156338912,4.35664088088147));
#38343=CARTESIAN_POINT('Ctrl Pts',(6.76747908288642,0.570983871223461,4.16762126762428));
#38344=CARTESIAN_POINT('Ctrl Pts',(6.7515738041988,0.626474586108011,3.97860165436708));
#38345=CARTESIAN_POINT('Ctrl Pts',(6.73566852551118,0.578785658895023,3.75929140287077));
#38346=CARTESIAN_POINT('Ctrl Pts',(6.71976324682357,0.449805704301045,3.61038767491097));
#38347=CARTESIAN_POINT('Ctrl Pts',(6.70385796813595,0.320825749707067,3.46148394695116));
#38348=CARTESIAN_POINT('Ctrl Pts',(6.68795268944834,0.110554767732096,3.38298674252784));
#38349=CARTESIAN_POINT('Ctrl Pts',(6.67204741076073,-0.0844443642884844,
3.4109402193496));
#38350=CARTESIAN_POINT('Ctrl Pts',(6.65614213207312,-0.279443496309066,
3.43889369617135));
#38351=CARTESIAN_POINT('Ctrl Pts',(6.64023685338551,-0.459170778375258,
3.57329785423817));
#38352=CARTESIAN_POINT('Ctrl Pts',(6.6243315746979,-0.541132009270427,3.75243704050979));
#38353=CARTESIAN_POINT('Ctrl Pts',(6.60842629601029,-0.623093240165596,
3.9315762267814));
#38354=CARTESIAN_POINT('Ctrl Pts',(6.59252101732267,-0.60728841988974,4.15545044125781));
#38355=CARTESIAN_POINT('Ctrl Pts',(6.57661573863506,-0.500919754058047,
4.32127168369798));
#38356=CARTESIAN_POINT('Ctrl Pts',(6.56069229617589,-0.394429615589227,
4.48728229340579));
#38357=CARTESIAN_POINT('Ctrl Pts',(6.54476885371673,-0.197168666623305,
4.59510713395368));
#38358=CARTESIAN_POINT('Ctrl Pts',(6.52884541125757,2.61457539729726E-5,
4.59508370962656));
#38359=CARTESIAN_POINT('Ctrl Pts',(6.42115458874249,-0.000630941829811112,
4.59394485456974));
#38360=CARTESIAN_POINT('Ctrl Pts',(6.4252722722299,-0.0517816819022344,
4.59442561076518));
#38361=CARTESIAN_POINT('Ctrl Pts',(6.42938995571731,-0.102828462800867,
4.58836159088269));
#38362=CARTESIAN_POINT('Ctrl Pts',(6.43350763920472,-0.152073274319339,
4.5753220992581));
#38363=CARTESIAN_POINT('Ctrl Pts',(6.44941291789233,-0.342290043897387,
4.52495476314113));
#38364=CARTESIAN_POINT('Ctrl Pts',(6.46531819657995,-0.5056209461254,4.37051151428857));
#38365=CARTESIAN_POINT('Ctrl Pts',(6.48122347526756,-0.56632363157735,4.18304963962536));
#38366=CARTESIAN_POINT('Ctrl Pts',(6.49712875395518,-0.627026317029301,
3.99558776496215));
#38367=CARTESIAN_POINT('Ctrl Pts',(6.51303403264279,-0.58510078570519,3.77510726448829));
#38368=CARTESIAN_POINT('Ctrl Pts',(6.5289393113304,-0.460166914262479,3.62276494217392));
#38369=CARTESIAN_POINT('Ctrl Pts',(6.54484459001801,-0.335233042819767,
3.47042261985956));
#38370=CARTESIAN_POINT('Ctrl Pts',(6.56074986870563,-0.127290831258456,
3.38621847570468));
#38371=CARTESIAN_POINT('Ctrl Pts',(6.57665514739324,0.068373869747762,3.4088573345089));
#38372=CARTESIAN_POINT('Ctrl Pts',(6.59256042608085,0.26403857075398,3.43149619331313));
#38373=CARTESIAN_POINT('Ctrl Pts',(6.60846570476847,0.447425761205104,3.56097805507645));
#38374=CARTESIAN_POINT('Ctrl Pts',(6.62437098345608,0.534230294511761,3.73782813427527));
#38375=CARTESIAN_POINT('Ctrl Pts',(6.64027626214369,0.621034827818418,3.91467821347409));
#38376=CARTESIAN_POINT('Ctrl Pts',(6.65618154083131,0.611256703980608,4.1388965101084));
#38377=CARTESIAN_POINT('Ctrl Pts',(6.67208681951892,0.509439333868548,4.30754322537844));
#38378=CARTESIAN_POINT('Ctrl Pts',(6.68799209820653,0.40762196375649,4.47618994064847));
#38379=CARTESIAN_POINT('Ctrl Pts',(6.70389737689414,0.213765347370184,4.58926507455422));
#38380=CARTESIAN_POINT('Ctrl Pts',(6.71980265558175,0.016851802420978,4.59484308232941));
#38381=CARTESIAN_POINT('Ctrl Pts',(6.72025329996867,0.0112726493937942,
4.59500112406784));
#38382=CARTESIAN_POINT('Ctrl Pts',(6.72070394435558,0.00569104238866241,
4.59507287148453));
#38383=CARTESIAN_POINT('Ctrl Pts',(6.72115458874249,0.000109070110168276,
4.59505938903171));
#38384=CARTESIAN_POINT('Origin',(4.,0.,4.));
#38385=CARTESIAN_POINT('',(7.12884541125757,-0.000233413975479213,4.59320261234329));
#38386=CARTESIAN_POINT('',(7.02115458874249,0.000491936389841303,4.5936290357477));
#38387=CARTESIAN_POINT('',(4.,-7.27562663373442E-17,4.5941));
#38388=CARTESIAN_POINT('Ctrl Pts',(7.12884541125757,-0.000233413975479213,
4.59320261234329));
#38389=CARTESIAN_POINT('Ctrl Pts',(7.11972691928047,0.113624805666132,4.59280158872514));
#38390=CARTESIAN_POINT('Ctrl Pts',(7.11060842730338,0.227688545642871,4.56127879346404));
#38391=CARTESIAN_POINT('Ctrl Pts',(7.10148993532628,0.322592019514134,4.50005536307953));
#38392=CARTESIAN_POINT('Ctrl Pts',(7.08558465663867,0.488131036726243,4.39326405099382));
#38393=CARTESIAN_POINT('Ctrl Pts',(7.06967937795105,0.595374147168556,4.19610732087965));
#38394=CARTESIAN_POINT('Ctrl Pts',(7.05377409926343,0.595079946532544,3.99911121186167));
#38395=CARTESIAN_POINT('Ctrl Pts',(7.03786882057582,0.594785745896532,3.80211510284369));
#38396=CARTESIAN_POINT('Ctrl Pts',(7.02196354188821,0.486954234182196,3.60527961492189));
#38397=CARTESIAN_POINT('Ctrl Pts',(7.0060582632006,0.321096900356496,3.49898325846904));
#38398=CARTESIAN_POINT('Ctrl Pts',(6.99015298451299,0.155239566530797,3.3926869020162));
#38399=CARTESIAN_POINT('Ctrl Pts',(6.97424770582538,-0.0686435894062663,
3.37692967703231));
#38400=CARTESIAN_POINT('Ctrl Pts',(6.95834242713776,-0.247754555527299,
3.45894666907189));
#38401=CARTESIAN_POINT('Ctrl Pts',(6.94243714845015,-0.426865521648332,
3.54096366111146));
#38402=CARTESIAN_POINT('Ctrl Pts',(6.92653186976253,-0.561204297953336,
3.72075487017451));
#38403=CARTESIAN_POINT('Ctrl Pts',(6.91062659107492,-0.589088840804576,
3.91576771430201));
#38404=CARTESIAN_POINT('Ctrl Pts',(6.89472131238731,-0.616973383655816,
4.11078055842951));
#38405=CARTESIAN_POINT('Ctrl Pts',(6.8788160336997,-0.538403693053295,4.32101503762147));
#38406=CARTESIAN_POINT('Ctrl Pts',(6.86291075501209,-0.389454440281117,
4.44994049623482));
#38407=CARTESIAN_POINT('Ctrl Pts',(6.85155564042725,-0.283116420949728,
4.54198310574898));
#38408=CARTESIAN_POINT('Ctrl Pts',(6.8402005258424,-0.140907108175025,4.59258385846765));
#38409=CARTESIAN_POINT('Ctrl Pts',(6.82884541125756,0.000528213615369061,
4.5937871332276));
#38410=CARTESIAN_POINT('Ctrl Pts',(6.72115458874249,0.000109070110168276,
4.59505938903171));
#38411=CARTESIAN_POINT('Ctrl Pts',(6.73660922304319,-0.191322006690816,
4.59459701474307));
#38412=CARTESIAN_POINT('Ctrl Pts',(6.75206385734389,-0.38318268672033,4.49389457135631));
#38413=CARTESIAN_POINT('Ctrl Pts',(6.76751849164459,-0.49122657597837,4.33588597251985));
#38414=CARTESIAN_POINT('Ctrl Pts',(6.78342377033221,-0.60242093591639,4.17326997329048));
#38415=CARTESIAN_POINT('Ctrl Pts',(6.79932904901982,-0.624839182280325,
3.94995709318712));
#38416=CARTESIAN_POINT('Ctrl Pts',(6.81523432770743,-0.548195780923551,
3.76848141254984));
#38417=CARTESIAN_POINT('Ctrl Pts',(6.83113960639504,-0.471552379566775,
3.58700573191256));
#38418=CARTESIAN_POINT('Ctrl Pts',(6.84704488508266,-0.295847330489284,
3.44736725074137));
#38419=CARTESIAN_POINT('Ctrl Pts',(6.86295016377027,-0.101752734572189,
3.41368297698799));
#38420=CARTESIAN_POINT('Ctrl Pts',(6.87885544245788,0.0923418613449005,
3.37999870323461));
#38421=CARTESIAN_POINT('Ctrl Pts',(6.8947607211455,0.304826004101594,3.45226863689903));
#38422=CARTESIAN_POINT('Ctrl Pts',(6.91066599983311,0.438133727661537,3.59730899203965));
#38423=CARTESIAN_POINT('Ctrl Pts',(6.92657127852072,0.571441451221483,3.74234934718029));
#38424=CARTESIAN_POINT('Ctrl Pts',(6.94247655720833,0.625572755584675,3.96016012379713));
#38425=CARTESIAN_POINT('Ctrl Pts',(6.95838183589594,0.57567402069499,4.15073208753033));
#38426=CARTESIAN_POINT('Ctrl Pts',(6.97428711458356,0.525775285805305,4.34130405126353));
#38427=CARTESIAN_POINT('Ctrl Pts',(6.99019239327118,0.371846511662747,4.5046372021131));
#38428=CARTESIAN_POINT('Ctrl Pts',(7.00609767195879,0.184564651688987,4.56573572985967));
#38429=CARTESIAN_POINT('Ctrl Pts',(7.01111664422002,0.125467135782336,4.58501560681028));
#38430=CARTESIAN_POINT('Ctrl Pts',(7.01613561648126,0.0630485115161635,
4.59411554829291));
#38431=CARTESIAN_POINT('Ctrl Pts',(7.02115458874249,0.000491936389841303,
4.5936290357477));
#38432=CARTESIAN_POINT('Origin',(4.,0.,4.));
#38433=CARTESIAN_POINT('',(7.42884541125756,-0.000438237927964824,4.59464495791636));
#38434=CARTESIAN_POINT('',(7.32115458874249,-0.000317338366111653,4.59328419319629));
#38435=CARTESIAN_POINT('',(4.,-7.27562663373442E-17,4.5941));
#38436=CARTESIAN_POINT('Ctrl Pts',(7.42884541125756,-0.000438237927964824,
4.59464495791636));
#38437=CARTESIAN_POINT('Ctrl Pts',(7.41515859140615,0.169409178821721,4.5932420274804));
#38438=CARTESIAN_POINT('Ctrl Pts',(7.40147177155473,0.340360224580004,4.51673272682389));
#38439=CARTESIAN_POINT('Ctrl Pts',(7.38778495170331,0.450965110664874,4.38826722161738));
#38440=CARTESIAN_POINT('Ctrl Pts',(7.37187967301569,0.579497637321094,4.23897909740477));
#38441=CARTESIAN_POINT('Ctrl Pts',(7.35597439432808,0.626535888751401,4.01952688559808));
#38442=CARTESIAN_POINT('Ctrl Pts',(7.34006911564046,0.570481892017836,3.83067375781486));
#38443=CARTESIAN_POINT('Ctrl Pts',(7.32416383695285,0.51442789528427,3.64182063003164));
#38444=CARTESIAN_POINT('Ctrl Pts',(7.30825855826524,0.355281650386831,3.48356658627189));
#38445=CARTESIAN_POINT('Ctrl Pts',(7.29235327957763,0.166116376105148,3.42857518785077));
#38446=CARTESIAN_POINT('Ctrl Pts',(7.27644800089002,-0.023048898176535,
3.37358378942964));
#38447=CARTESIAN_POINT('Ctrl Pts',(7.2605427222024,-0.242233201842457,3.42185503634715));
#38448=CARTESIAN_POINT('Ctrl Pts',(7.24463744351479,-0.390796368104757,
3.5512248149675));
#38449=CARTESIAN_POINT('Ctrl Pts',(7.22873216482718,-0.539359534367058,
3.68059459358785));
#38450=CARTESIAN_POINT('Ctrl Pts',(7.21282688613957,-0.617301563225728,
3.89106290391106));
#38451=CARTESIAN_POINT('Ctrl Pts',(7.19692160745195,-0.588834786584626,
4.08599160058025));
#38452=CARTESIAN_POINT('Ctrl Pts',(7.18101632876434,-0.560368009943526,
4.28092029724944));
#38453=CARTESIAN_POINT('Ctrl Pts',(7.16511105007672,-0.425492427802657,
4.46030938026461));
#38454=CARTESIAN_POINT('Ctrl Pts',(7.14920577138911,-0.24613717474127,4.54179097474357));
#38455=CARTESIAN_POINT('Ctrl Pts',(7.1424189846786,-0.169606239833077,4.57655919310821));
#38456=CARTESIAN_POINT('Ctrl Pts',(7.13563219796808,-0.0849767524450092,
4.59350108952231));
#38457=CARTESIAN_POINT('Ctrl Pts',(7.12884541125757,-0.000233413975479213,
4.59320261234329));
#38458=CARTESIAN_POINT('Ctrl Pts',(7.02115458874249,0.000491936389841303,
4.5936290357477));
#38459=CARTESIAN_POINT('Ctrl Pts',(7.03204089516887,-0.135195214358064,
4.59257377495492));
#38460=CARTESIAN_POINT('Ctrl Pts',(7.04292720159524,-0.271531381894462,
4.54641716720817));
#38461=CARTESIAN_POINT('Ctrl Pts',(7.05381350802162,-0.376033620593693,
4.46121547122365));
#38462=CARTESIAN_POINT('Ctrl Pts',(7.06971878670923,-0.528715087097646,
4.33673278019746));
#38463=CARTESIAN_POINT('Ctrl Pts',(7.08562406539685,-0.613443074300594,
4.1289034935015));
#38464=CARTESIAN_POINT('Ctrl Pts',(7.10152934408446,-0.591314251018945,
3.93315398851514));
#38465=CARTESIAN_POINT('Ctrl Pts',(7.11743462277207,-0.569185427737295,
3.73740448352876));
#38466=CARTESIAN_POINT('Ctrl Pts',(7.13333990145968,-0.440199793971044,
3.55373476025198));
#38467=CARTESIAN_POINT('Ctrl Pts',(7.14924518014729,-0.263582002606135,
3.46647820559892));
#38468=CARTESIAN_POINT('Ctrl Pts',(7.16515045883491,-0.0869642112412332,
3.37922165094586));
#38469=CARTESIAN_POINT('Ctrl Pts',(7.18105573752253,0.137285737722324,3.38837826491652));
#38470=CARTESIAN_POINT('Ctrl Pts',(7.19696101621014,0.306201705590428,3.48974370695041));
#38471=CARTESIAN_POINT('Ctrl Pts',(7.21286629489775,0.47511767345854,3.59110914898431));
#38472=CARTESIAN_POINT('Ctrl Pts',(7.22877157358536,0.588699660231196,3.78468341908144));
#38473=CARTESIAN_POINT('Ctrl Pts',(7.24467685227297,0.594795648982816,3.98158540759));
#38474=CARTESIAN_POINT('Ctrl Pts',(7.26058213096058,0.600891637734436,4.17848739609855));
#38475=CARTESIAN_POINT('Ctrl Pts',(7.2764874096482,0.499501628465021,4.37871710301853));
#38476=CARTESIAN_POINT('Ctrl Pts',(7.29239268833581,0.337179610128186,4.49033751492072));
#38477=CARTESIAN_POINT('Ctrl Pts',(7.30197998847137,0.239335998647354,4.5576194790522));
#38478=CARTESIAN_POINT('Ctrl Pts',(7.31156728860693,0.119353510611835,4.59270637405629));
#38479=CARTESIAN_POINT('Ctrl Pts',(7.32115458874249,-0.000317338366111653,
4.59328419319629));
#38480=CARTESIAN_POINT('Origin',(4.,0.,4.));
#38481=CARTESIAN_POINT('',(7.72884541125757,0.000455182276646732,4.59460030787683));
#38482=CARTESIAN_POINT('',(7.62115458874249,-0.000367422317862595,4.59479267874092));
#38483=CARTESIAN_POINT('',(4.,-7.27562663373442E-17,4.5941));
#38484=CARTESIAN_POINT('Ctrl Pts',(7.72884541125757,0.000455182276646732,
4.59460030787683));
#38485=CARTESIAN_POINT('Ctrl Pts',(7.72649554221944,0.0296217258780686,
4.59484761241511));
#38486=CARTESIAN_POINT('Ctrl Pts',(7.72414567318131,0.0587549042441869,
4.59288776399295));
#38487=CARTESIAN_POINT('Ctrl Pts',(7.72179580414318,0.0875427725731367,
4.58860617484604));
#38488=CARTESIAN_POINT('Ctrl Pts',(7.70589052545556,0.282395788279217,4.55962589232715));
#38489=CARTESIAN_POINT('Ctrl Pts',(7.68998524676794,0.461428877889185,4.42427810603975));
#38490=CARTESIAN_POINT('Ctrl Pts',(7.67407996808033,0.542437620895056,4.24470879335187));
#38491=CARTESIAN_POINT('Ctrl Pts',(7.65817468939272,0.623446363900926,4.065139480664));
#38492=CARTESIAN_POINT('Ctrl Pts',(7.64226941070511,0.606430760302702,3.84134864157567));
#38493=CARTESIAN_POINT('Ctrl Pts',(7.6263641320175,0.499203655448083,3.67609156159133));
#38494=CARTESIAN_POINT('Ctrl Pts',(7.61045885332988,0.391976550593464,3.51083448160699));
#38495=CARTESIAN_POINT('Ctrl Pts',(7.59455357464227,0.19453794448245,3.40411116072664));
#38496=CARTESIAN_POINT('Ctrl Pts',(7.57864829595466,-0.00245670798462758,
3.40492443279829));
#38497=CARTESIAN_POINT('Ctrl Pts',(7.56274301726704,-0.199451360451705,
3.40573770486994));
#38498=CARTESIAN_POINT('Ctrl Pts',(7.54683773857943,-0.396002059274846,
3.5140875698936));
#38499=CARTESIAN_POINT('Ctrl Pts',(7.53093245989182,-0.50186103876401,3.68022435377194));
#38500=CARTESIAN_POINT('Ctrl Pts',(7.51502718120421,-0.607720018253171,
3.84636113765028));
#38501=CARTESIAN_POINT('Ctrl Pts',(7.4991219025166,-0.622887278408357,4.07028484038331));
#38502=CARTESIAN_POINT('Ctrl Pts',(7.48321662382898,-0.540398655351294,
4.24917917107494));
#38503=CARTESIAN_POINT('Ctrl Pts',(7.46731134514137,-0.45791003229423,4.42807350176658));
#38504=CARTESIAN_POINT('Ctrl Pts',(7.45140606645375,-0.277765526024924,
4.56193846041682));
#38505=CARTESIAN_POINT('Ctrl Pts',(7.43550078776614,-0.0826798719492015,
4.58930892143267));
#38506=CARTESIAN_POINT('Ctrl Pts',(7.43328232892995,-0.0554694406452989,
4.59312653709876));
#38507=CARTESIAN_POINT('Ctrl Pts',(7.43106387009376,-0.0279683367079049,
4.5948723550368));
#38508=CARTESIAN_POINT('Ctrl Pts',(7.42884541125756,-0.000438237927964824,
4.59464495791636));
#38509=CARTESIAN_POINT('Ctrl Pts',(7.32115458874249,-0.000317338366111653,
4.59328419319629));
#38510=CARTESIAN_POINT('Ctrl Pts',(7.32747256729455,-0.0791797758050172,
4.59366497286126));
#38511=CARTESIAN_POINT('Ctrl Pts',(7.3337905458466,-0.157906876560309,4.57905936436794));
#38512=CARTESIAN_POINT('Ctrl Pts',(7.34010852439865,-0.230073660466993,
4.54880513582638));
#38513=CARTESIAN_POINT('Ctrl Pts',(7.35601380308626,-0.411750885321067,
4.47264122794544));
#38514=CARTESIAN_POINT('Ctrl Pts',(7.37191908177388,-0.551851307624962,
4.29730229529918));
#38515=CARTESIAN_POINT('Ctrl Pts',(7.38782436046149,-0.586046744500155,
4.10329655692985));
#38516=CARTESIAN_POINT('Ctrl Pts',(7.4037296391491,-0.620242181375348,3.90929081856053));
#38517=CARTESIAN_POINT('Ctrl Pts',(7.41963491783671,-0.548532632821828,
3.69661827446815));
#38518=CARTESIAN_POINT('Ctrl Pts',(7.43554019652432,-0.403844087697925,
3.56292915991696));
#38519=CARTESIAN_POINT('Ctrl Pts',(7.45144547521194,-0.259155542574025,
3.42924004536577));
#38520=CARTESIAN_POINT('Ctrl Pts',(7.46735075389955,-0.0414880008797467,
3.37453436035576));
#38521=CARTESIAN_POINT('Ctrl Pts',(7.48325603258717,0.149214809903968,3.42393064079835));
#38522=CARTESIAN_POINT('Ctrl Pts',(7.49916131127478,0.339917620687686,3.47332692124094));
#38523=CARTESIAN_POINT('Ctrl Pts',(7.51506658996239,0.50365570056084,3.62682516713614));
#38524=CARTESIAN_POINT('Ctrl Pts',(7.53097186865001,0.56524745100941,3.81394547807041));
#38525=CARTESIAN_POINT('Ctrl Pts',(7.54687714733762,0.626839201457978,4.00106578900469));
#38526=CARTESIAN_POINT('Ctrl Pts',(7.56278242602523,0.58628462248197,4.22180816497804));
#38527=CARTESIAN_POINT('Ctrl Pts',(7.57868770471284,0.462204660718925,4.3748170457164));
#38528=CARTESIAN_POINT('Ctrl Pts',(7.59284333272272,0.351774041004839,4.51099427596058));
#38529=CARTESIAN_POINT('Ctrl Pts',(7.60699896073261,0.175183620117616,4.59352033541115));
#38530=CARTESIAN_POINT('Ctrl Pts',(7.62115458874249,-0.000367422317862596,
4.59479267874092));
#38531=CARTESIAN_POINT('Origin',(4.,0.,4.));
#38532=CARTESIAN_POINT('',(8.02884541125756,0.000208508845897126,4.59318438507865));
#38533=CARTESIAN_POINT('',(7.92115458874249,0.000504499356536197,4.59443266285439));
#38534=CARTESIAN_POINT('',(4.,-7.27562663373442E-17,4.5941));
#38535=CARTESIAN_POINT('Ctrl Pts',(8.02884541125756,0.000208508845897126,
4.59318438507865));
#38536=CARTESIAN_POINT('Ctrl Pts',(8.02192721434511,0.0865993248636432,
4.5934556945658));
#38537=CARTESIAN_POINT('Ctrl Pts',(8.01500901743265,0.17288466952141,4.57582457789876));
#38538=CARTESIAN_POINT('Ctrl Pts',(8.0080908205202,0.250602156771344,4.53974023855861));
#38539=CARTESIAN_POINT('Ctrl Pts',(7.99218554183259,0.42927852421987,4.4567805482338));
#38540=CARTESIAN_POINT('Ctrl Pts',(7.97628026314498,0.562668370741438,4.27628395749428));
#38541=CARTESIAN_POINT('Ctrl Pts',(7.96037498445736,0.589524722071826,4.08112686462655));
#38542=CARTESIAN_POINT('Ctrl Pts',(7.94446970576975,0.616381073402214,3.88596977175883));
#38543=CARTESIAN_POINT('Ctrl Pts',(7.92856442708213,0.536703929541425,3.67615217676291));
#38544=CARTESIAN_POINT('Ctrl Pts',(7.91265914839452,0.387077664089382,3.54801344261061));
#38545=CARTESIAN_POINT('Ctrl Pts',(7.89675386970691,0.237451398637336,3.41987470845831));
#38546=CARTESIAN_POINT('Ctrl Pts',(7.88084859101929,0.0178760115940344,
3.37341483514963));
#38547=CARTESIAN_POINT('Ctrl Pts',(7.86494331233168,-0.170828768780714,
3.42996623095257));
#38548=CARTESIAN_POINT('Ctrl Pts',(7.84903803364407,-0.359533549155462,
3.48651762675552));
#38549=CARTESIAN_POINT('Ctrl Pts',(7.83313275495647,-0.517367722861657,
3.64608029167009));
#38550=CARTESIAN_POINT('Ctrl Pts',(7.81722747626885,-0.571860514742998,
3.83538980050754));
#38551=CARTESIAN_POINT('Ctrl Pts',(7.80132219758124,-0.626353306624339,
4.02469930934499));
#38552=CARTESIAN_POINT('Ctrl Pts',(7.78541691889362,-0.577504716680827,
4.24375566210532));
#38553=CARTESIAN_POINT('Ctrl Pts',(7.769511640206,-0.447743950807975,4.3919774491103));
#38554=CARTESIAN_POINT('Ctrl Pts',(7.75595623055652,-0.337154229471824,
4.51830073342946));
#38555=CARTESIAN_POINT('Ctrl Pts',(7.74240082090705,-0.16779438404434,4.593173711641));
#38556=CARTESIAN_POINT('Ctrl Pts',(7.72884541125757,0.000455182276646732,
4.59460030787683));
#38557=CARTESIAN_POINT('Ctrl Pts',(7.62115458874249,-0.000367422317862596,
4.59479267874092));
#38558=CARTESIAN_POINT('Ctrl Pts',(7.62290423942022,-0.022065717876263,
4.59494994172972));
#38559=CARTESIAN_POINT('Ctrl Pts',(7.62465389009795,-0.043748134618359,
4.59386587358433));
#38560=CARTESIAN_POINT('Ctrl Pts',(7.62640354077568,-0.0652877816099521,
4.59148835294282));
#38561=CARTESIAN_POINT('Ctrl Pts',(7.64230881946329,-0.261094917625702,
4.56987539392751));
#38562=CARTESIAN_POINT('Ctrl Pts',(7.6582140981509,-0.445103845107109,4.44137409039354));
#38563=CARTESIAN_POINT('Ctrl Pts',(7.67411937683852,-0.532825449416136,
4.2649868044631));
#38564=CARTESIAN_POINT('Ctrl Pts',(7.69002465552613,-0.620547053725161,
4.08859951853267));
#38565=CARTESIAN_POINT('Ctrl Pts',(7.70592993421374,-0.611981334861803,
3.86432625020577));
#38566=CARTESIAN_POINT('Ctrl Pts',(7.72183521290136,-0.511061308497056,
3.69514379608856));
#38567=CARTESIAN_POINT('Ctrl Pts',(7.73774049158897,-0.410141282132307,
3.52596134197134));
#38568=CARTESIAN_POINT('Ctrl Pts',(7.75364577027658,-0.216866948266163,
3.4118697020638));
#38569=CARTESIAN_POINT('Ctrl Pts',(7.76955104896419,-0.0199817042712483,
3.40525493058698));
#38570=CARTESIAN_POINT('Ctrl Pts',(7.78545632765181,0.176903539723664,3.39864015911017));
#38571=CARTESIAN_POINT('Ctrl Pts',(7.80136160633942,0.377399693847348,3.49950225606407));
#38572=CARTESIAN_POINT('Ctrl Pts',(7.81726688502703,0.489447406431712,3.66152961365368));
#38573=CARTESIAN_POINT('Ctrl Pts',(7.83317216371464,0.601495119016078,3.82355697124329));
#38574=CARTESIAN_POINT('Ctrl Pts',(7.84907744240226,0.625094390061116,4.04674958946861));
#38575=CARTESIAN_POINT('Ctrl Pts',(7.86498272108987,0.549409432699027,4.22862686054007));
#38576=CARTESIAN_POINT('Ctrl Pts',(7.88088799977748,0.473724475336938,4.41050413161152));
#38577=CARTESIAN_POINT('Ctrl Pts',(7.89679327846509,0.298755289567731,4.55106605552911));
#38578=CARTESIAN_POINT('Ctrl Pts',(7.91269855715271,0.104840323164387,4.58577254351526));
#38579=CARTESIAN_POINT('Ctrl Pts',(7.9155172343493,0.0704753991278659,4.59192310448195));
#38580=CARTESIAN_POINT('Ctrl Pts',(7.91833591154589,0.0355154700816755,
4.59474920414003));
#38581=CARTESIAN_POINT('Ctrl Pts',(7.92115458874249,0.000504499356536197,
4.59443266285439));
#38582=CARTESIAN_POINT('Origin',(4.,0.,4.));
#38583=CARTESIAN_POINT('',(8.32884541125757,-0.000534402448739424,4.5938336238991));
#38584=CARTESIAN_POINT('',(8.2211545887425,0.000116005647334215,4.59313666129657));
#38585=CARTESIAN_POINT('',(4.,-7.27562663373442E-17,4.5941));
#38586=CARTESIAN_POINT('Ctrl Pts',(8.32884541125757,-0.000534402448739424,
4.5938336238991));
#38587=CARTESIAN_POINT('Ctrl Pts',(8.31735888647079,0.142509087977489,4.59259298046846));
#38588=CARTESIAN_POINT('Ctrl Pts',(8.30587236168401,0.286359812054371,4.54070236535691));
#38589=CARTESIAN_POINT('Ctrl Pts',(8.29438583689723,0.393155811111917,4.44670960845581));
#38590=CARTESIAN_POINT('Ctrl Pts',(8.27848055820962,0.541035187969857,4.31655875596735));
#38591=CARTESIAN_POINT('Ctrl Pts',(8.262575279522,0.617867056310918,4.10568264439756));
#38592=CARTESIAN_POINT('Ctrl Pts',(8.24667000083439,0.588373472681163,3.91090666274675));
#38593=CARTESIAN_POINT('Ctrl Pts',(8.23076472214677,0.558879889051408,3.71613068109593));
#38594=CARTESIAN_POINT('Ctrl Pts',(8.21485944345917,0.423060853450833,3.53745482936408));
#38595=CARTESIAN_POINT('Ctrl Pts',(8.19895416477155,0.243278720997716,3.45691949951456));
#38596=CARTESIAN_POINT('Ctrl Pts',(8.18304888608394,0.0634965885445972,
3.37638416966503));
#38597=CARTESIAN_POINT('Ctrl Pts',(8.16714360739632,-0.160248640761069,
3.39398936169784));
#38598=CARTESIAN_POINT('Ctrl Pts',(8.15123832870871,-0.325222623502191,
3.50165151624576));
#38599=CARTESIAN_POINT('Ctrl Pts',(8.1353330500211,-0.490196606243315,3.60931367079368));
#38600=CARTESIAN_POINT('Ctrl Pts',(8.11942777133349,-0.59639934241989,3.80703278785672));
#38601=CARTESIAN_POINT('Ctrl Pts',(8.10352249264588,-0.595067028646789,
4.00402461368555));
#38602=CARTESIAN_POINT('Ctrl Pts',(8.08761721395827,-0.593734714873688,
4.20101643951437));
#38603=CARTESIAN_POINT('Ctrl Pts',(8.07171193527065,-0.484867351150922,
4.39728097410898));
#38604=CARTESIAN_POINT('Ctrl Pts',(8.05580665658303,-0.3184522251018,4.50270184645125));
#38605=CARTESIAN_POINT('Ctrl Pts',(8.04681957480788,-0.224421408301879,
4.56226861162124));
#38606=CARTESIAN_POINT('Ctrl Pts',(8.03783249303272,-0.112017456676448,
4.59283194056482));
#38607=CARTESIAN_POINT('Ctrl Pts',(8.02884541125756,0.000208508845897126,
4.59318438507865));
#38608=CARTESIAN_POINT('Ctrl Pts',(7.92115458874249,0.000504499356536197,
4.59443266285439));
#38609=CARTESIAN_POINT('Ctrl Pts',(7.93424119023351,-0.162045019349314,
4.59296301969496));
#38610=CARTESIAN_POINT('Ctrl Pts',(7.94732779172453,-0.325694779556815,
4.52375140444135));
#38611=CARTESIAN_POINT('Ctrl Pts',(7.96041439321555,-0.436005268305889,
4.40499428651169));
#38612=CARTESIAN_POINT('Ctrl Pts',(7.97631967190316,-0.570075146335334,
4.26065848946726));
#38613=CARTESIAN_POINT('Ctrl Pts',(7.99222495059077,-0.625354155356748,
4.04313584332371));
#38614=CARTESIAN_POINT('Ctrl Pts',(8.00813022927838,-0.576460513088508,
3.85230354456612));
#38615=CARTESIAN_POINT('Ctrl Pts',(8.024035507966,-0.527566870820267,3.66147124580852));
#38616=CARTESIAN_POINT('Ctrl Pts',(8.03994078665361,-0.374500577262366,
3.49732929443689));
#38617=CARTESIAN_POINT('Ctrl Pts',(8.05584606534123,-0.187543198716277,
3.43524473024767));
#38618=CARTESIAN_POINT('Ctrl Pts',(8.07175134402884,-0.000585820170193818,
3.37316016605846));
#38619=CARTESIAN_POINT('Ctrl Pts',(8.08765662271645,0.220262643364076,3.41313298905166));
#38620=CARTESIAN_POINT('Ctrl Pts',(8.10356190140406,0.37359792075985,3.53680937001953));
#38621=CARTESIAN_POINT('Ctrl Pts',(8.11946718009167,0.526933198155627,3.66048575098741));
#38622=CARTESIAN_POINT('Ctrl Pts',(8.13537245877928,0.612755289412907,3.86786568992997));
#38623=CARTESIAN_POINT('Ctrl Pts',(8.1512777374669,0.591658321059451,4.06372909240644));
#38624=CARTESIAN_POINT('Ctrl Pts',(8.16718301615451,0.570561352705995,4.2595924948829));
#38625=CARTESIAN_POINT('Ctrl Pts',(8.18308829484212,0.44254532474181,4.44393936089328));
#38626=CARTESIAN_POINT('Ctrl Pts',(8.19899357352974,0.266389781296621,4.53212540863836));
#38627=CARTESIAN_POINT('Ctrl Pts',(8.20638057860065,0.184576572093718,4.57308230066594));
#38628=CARTESIAN_POINT('Ctrl Pts',(8.21376758367158,0.0923795717789203,
4.59329710918813));
#38629=CARTESIAN_POINT('Ctrl Pts',(8.2211545887425,0.000116005647334215,
4.59313666129657));
#38630=CARTESIAN_POINT('Origin',(4.,0.,4.));
#38631=CARTESIAN_POINT('',(8.62884541125757,3.48566139269993E-5,4.59507810043999));
#38632=CARTESIAN_POINT('',(8.5211545887425,-0.000547905086566465,4.594005652201));
#38633=CARTESIAN_POINT('',(4.,-7.27562663373442E-17,4.5941));
#38634=CARTESIAN_POINT('Ctrl Pts',(8.62884541125757,3.48566139269993E-5,
4.59507810043999));
#38635=CARTESIAN_POINT('Ctrl Pts',(8.62869583728408,0.00188744051982823,
4.59507966949126));
#38636=CARTESIAN_POINT('Ctrl Pts',(8.62854626331059,0.00374001065808006,
4.59507176912216));
#38637=CARTESIAN_POINT('Ctrl Pts',(8.6283966893371,0.00559249142073073,
4.59505435897699));
#38638=CARTESIAN_POINT('Ctrl Pts',(8.61249141064948,0.202580123064263,4.59320301275402));
#38639=CARTESIAN_POINT('Ctrl Pts',(8.59658613196187,0.398557131004382,4.48381890612783));
#38640=CARTESIAN_POINT('Ctrl Pts',(8.58068085327426,0.503539164298441,4.31712659320126));
#38641=CARTESIAN_POINT('Ctrl Pts',(8.56477557458664,0.608521197592498,4.15043428027469));
#38642=CARTESIAN_POINT('Ctrl Pts',(8.54887029589904,0.622508256240502,3.92643376104774));
#38643=CARTESIAN_POINT('Ctrl Pts',(8.53296501721142,0.539078074654942,3.74797659726896));
#38644=CARTESIAN_POINT('Ctrl Pts',(8.51705973852381,0.455647893069379,3.56951943349019));
#38645=CARTESIAN_POINT('Ctrl Pts',(8.50115445983619,0.274800471250253,3.43660562515959));
#38646=CARTESIAN_POINT('Ctrl Pts',(8.48524918114857,0.0795732942734406,
3.41026356994308));
#38647=CARTESIAN_POINT('Ctrl Pts',(8.46934390246096,-0.115653882703369,
3.38392151472657));
#38648=CARTESIAN_POINT('Ctrl Pts',(8.45343862377335,-0.32526081483786,3.46415121262414));
#38649=CARTESIAN_POINT('Ctrl Pts',(8.43753334508574,-0.453004866631874,
3.61411458059983));
#38650=CARTESIAN_POINT('Ctrl Pts',(8.42162806639813,-0.580748918425883,
3.76407794857552));
#38651=CARTESIAN_POINT('Ctrl Pts',(8.40572278771052,-0.626630089879422,
3.98377498662932));
#38652=CARTESIAN_POINT('Ctrl Pts',(8.3898175090229,-0.569581688133314,4.17233010950212));
#38653=CARTESIAN_POINT('Ctrl Pts',(8.37391223033529,-0.512533286387202,
4.36088523237493));
#38654=CARTESIAN_POINT('Ctrl Pts',(8.35800695164768,-0.352555311441432,
4.51829844006673));
#38655=CARTESIAN_POINT('Ctrl Pts',(8.34210167296007,-0.163102881281137,
4.57229224720906));
#38656=CARTESIAN_POINT('Ctrl Pts',(8.33768291905923,-0.110469810133188,
4.58729263485501));
#38657=CARTESIAN_POINT('Ctrl Pts',(8.3332641651584,-0.0555618361628184,
4.59431088730997));
#38658=CARTESIAN_POINT('Ctrl Pts',(8.32884541125757,-0.000534402448739424,
4.5938336238991));
#38659=CARTESIAN_POINT('Ctrl Pts',(8.2211545887425,0.000116005647334215,
4.59313666129657));
#38660=CARTESIAN_POINT('Ctrl Pts',(8.22967286235919,-0.106277085140544,
4.59295164192424));
#38661=CARTESIAN_POINT('Ctrl Pts',(8.23819113597589,-0.212758691085218,
4.56567285125378));
#38662=CARTESIAN_POINT('Ctrl Pts',(8.24670940959258,-0.303508593564514,
4.51186277431583));
#38663=CARTESIAN_POINT('Ctrl Pts',(8.26261468828019,-0.472956366054245,
4.41138886276846));
#38664=CARTESIAN_POINT('Ctrl Pts',(8.2785199669678,-0.587556852107514,4.21841581019395));
#38665=CARTESIAN_POINT('Ctrl Pts',(8.29442524565541,-0.594690356875377,
4.02154867831793));
#38666=CARTESIAN_POINT('Ctrl Pts',(8.31033052434302,-0.60182386164324,3.82468154644191));
#38667=CARTESIAN_POINT('Ctrl Pts',(8.32623580303064,-0.501490385125681,
3.62392033526436));
#38668=CARTESIAN_POINT('Ctrl Pts',(8.34214108171825,-0.339758814980244,
3.51144609945163));
#38669=CARTESIAN_POINT('Ctrl Pts',(8.35804636040587,-0.178027244834812,
3.3989718636389));
#38670=CARTESIAN_POINT('Ctrl Pts',(8.37395163909348,0.0451024189384938,
3.37478460319097));
#38671=CARTESIAN_POINT('Ctrl Pts',(8.38985691778109,0.227178474572579,3.44999008482693));
#38672=CARTESIAN_POINT('Ctrl Pts',(8.4057621964687,0.40925453020667,3.5251955664629));
#38673=CARTESIAN_POINT('Ctrl Pts',(8.42166747515631,0.550276977701535,3.69979379018275));
#38674=CARTESIAN_POINT('Ctrl Pts',(8.43757275384392,0.585494275335268,3.89361663829603));
#38675=CARTESIAN_POINT('Ctrl Pts',(8.45347803253154,0.620711572969,4.0874394864093));
#38676=CARTESIAN_POINT('Ctrl Pts',(8.46938331121915,0.550123720741606,4.30048695891599));
#38677=CARTESIAN_POINT('Ctrl Pts',(8.48528858990677,0.406141674070155,4.4349366697363));
#38678=CARTESIAN_POINT('Ctrl Pts',(8.49724392285201,0.297916389879728,4.53599689564107));
#38679=CARTESIAN_POINT('Ctrl Pts',(8.50919925579725,0.148224117540273,4.59265016978245));
#38680=CARTESIAN_POINT('Ctrl Pts',(8.5211545887425,-0.000547905086566465,
4.594005652201));
#38681=CARTESIAN_POINT('Origin',(4.,0.,4.));
#38682=CARTESIAN_POINT('',(8.92884541125757,0.000516595407308196,4.59372894893997));
#38683=CARTESIAN_POINT('',(8.82115458874249,0.000142235148737217,4.59503945166131));
#38684=CARTESIAN_POINT('',(4.,-7.27562663373442E-17,4.5941));
#38685=CARTESIAN_POINT('Ctrl Pts',(8.92884541125757,0.000516595407308196,
4.59372894893997));
#38686=CARTESIAN_POINT('Ctrl Pts',(8.92412750940976,0.0592956068199462,
4.59421507565108));
#38687=CARTESIAN_POINT('Ctrl Pts',(8.91940960756194,0.117944888069788,4.58619493689145));
#38688=CARTESIAN_POINT('Ctrl Pts',(8.91469170571413,0.17383025386194,4.56912565303288));
#38689=CARTESIAN_POINT('Ctrl Pts',(8.89878642702651,0.362234410233906,4.51158064138869));
#38690=CARTESIAN_POINT('Ctrl Pts',(8.8828811483389,0.519225559109383,4.35118846702123));
#38691=CARTESIAN_POINT('Ctrl Pts',(8.86697586965128,0.572720006672535,4.16159443076672));
#38692=CARTESIAN_POINT('Ctrl Pts',(8.85107059096367,0.626214454235688,3.97200039451221));
#38693=CARTESIAN_POINT('Ctrl Pts',(8.83516531227606,0.576212200486512,3.75320449637065));
#38694=CARTESIAN_POINT('Ctrl Pts',(8.81926003358845,0.445672164925724,3.60566855627755));
#38695=CARTESIAN_POINT('Ctrl Pts',(8.80335475490084,0.315132129364936,3.45813261618446));
#38696=CARTESIAN_POINT('Ctrl Pts',(8.78744947621322,0.104054311992536,3.38185663413984));
#38697=CARTESIAN_POINT('Ctrl Pts',(8.77154419752561,-0.0906432834200916,
3.41186331412789));
#38698=CARTESIAN_POINT('Ctrl Pts',(8.755638918838,-0.285340878832719,3.44186999411594));
#38699=CARTESIAN_POINT('Ctrl Pts',(8.73973364015038,-0.463658252285575,
3.57815933613666));
#38700=CARTESIAN_POINT('Ctrl Pts',(8.72382836146277,-0.543719609875046,
3.75815304026071));
#38701=CARTESIAN_POINT('Ctrl Pts',(8.70792308277515,-0.623780967464517,
3.93814674438476));
#38702=CARTESIAN_POINT('Ctrl Pts',(8.69201780408754,-0.605586309190603,
4.16184481061213));
#38703=CARTESIAN_POINT('Ctrl Pts',(8.67611252539993,-0.497489852380174,
4.32653455081593));
#38704=CARTESIAN_POINT('Ctrl Pts',(8.66035682068581,-0.390409939629295,
4.48967554111606));
#38705=CARTESIAN_POINT('Ctrl Pts',(8.64460111597169,-0.195111159088962,
4.59491282095998));
#38706=CARTESIAN_POINT('Ctrl Pts',(8.62884541125757,3.48566139269993E-5,
4.59507810043999));
#38707=CARTESIAN_POINT('Ctrl Pts',(8.5211545887425,-0.000547905086566465,
4.594005652201));
#38708=CARTESIAN_POINT('Ctrl Pts',(8.52510453448487,-0.0497009834700827,
4.59445349267793));
#38709=CARTESIAN_POINT('Ctrl Pts',(8.52905448022724,-0.0987536084630192,
4.58886509038946));
#38710=CARTESIAN_POINT('Ctrl Pts',(8.53300442596961,-0.146177075786514,
4.57684766499685));
#38711=CARTESIAN_POINT('Ctrl Pts',(8.54890970465722,-0.337137537856201,
4.52845700030318));
#38712=CARTESIAN_POINT('Ctrl Pts',(8.56481498334483,-0.501682220880061,
4.37582372178193));
#38713=CARTESIAN_POINT('Ctrl Pts',(8.58072026203244,-0.564259167724997,
4.18903057354857));
#38714=CARTESIAN_POINT('Ctrl Pts',(8.59662554072005,-0.626836114569933,
4.00223742531521));
#38715=CARTESIAN_POINT('Ctrl Pts',(8.61253081940767,-0.587445325235947,
3.78128440736974));
#38716=CARTESIAN_POINT('Ctrl Pts',(8.62843609809528,-0.464173383698336,
3.62762379780141));
#38717=CARTESIAN_POINT('Ctrl Pts',(8.6443413767829,-0.340901442160722,3.47396318823307));
#38718=CARTESIAN_POINT('Ctrl Pts',(8.66024665547051,-0.133748348419481,
3.38759498704188));
#38719=CARTESIAN_POINT('Ctrl Pts',(8.67615193415812,0.0621699608040676,
3.40817581827756));
#38720=CARTESIAN_POINT('Ctrl Pts',(8.69205721284573,0.25808827002761,3.42875664951325));
#38721=CARTESIAN_POINT('Ctrl Pts',(8.70796249153334,0.44277179473346,3.55628651317581));
#38722=CARTESIAN_POINT('Ctrl Pts',(8.72386777022095,0.531421673692279,3.73220909121499));
#38723=CARTESIAN_POINT('Ctrl Pts',(8.73977304890857,0.620071552651101,3.90813166925417));
#38724=CARTESIAN_POINT('Ctrl Pts',(8.75567832759618,0.612687785862888,4.13244696166997));
#38725=CARTESIAN_POINT('Ctrl Pts',(8.7715836062838,0.512660686655375,4.30215887618246));
#38726=CARTESIAN_POINT('Ctrl Pts',(8.78748888497141,0.412633587447865,4.47187079069495));
#38727=CARTESIAN_POINT('Ctrl Pts',(8.80339416365902,0.21996315582106,4.58697932730413));
#38728=CARTESIAN_POINT('Ctrl Pts',(8.81929944234663,0.0231155027642346,
4.59463151583965));
#38729=CARTESIAN_POINT('Ctrl Pts',(8.81991782447859,0.0154622529370322,
4.59492902566351));
#38730=CARTESIAN_POINT('Ctrl Pts',(8.82053620661054,0.00780268890311657,
4.59506410656044));
#38731=CARTESIAN_POINT('Ctrl Pts',(8.82115458874249,0.000142235148737217,
4.59503945166131));
#38732=CARTESIAN_POINT('Origin',(4.,0.,4.));
#38733=CARTESIAN_POINT('',(9.22884541125756,-0.000264402795292107,4.59322887297718));
#38734=CARTESIAN_POINT('',(9.12115458874249,0.000475196148639644,4.59357609051269));
#38735=CARTESIAN_POINT('',(4.,-7.27562663373442E-17,4.5941));
#38736=CARTESIAN_POINT('Ctrl Pts',(9.22884541125756,-0.000264402795292107,
4.59322887297718));
#38737=CARTESIAN_POINT('Ctrl Pts',(9.21955918153543,0.115675446261185,4.59276508993807));
#38738=CARTESIAN_POINT('Ctrl Pts',(9.21027295181329,0.231857423975292,4.55999255403315));
#38739=CARTESIAN_POINT('Ctrl Pts',(9.20098672209116,0.327844211240712,4.49662776730038));
#38740=CARTESIAN_POINT('Ctrl Pts',(9.18508144340355,0.492248565587605,4.38809775866155));
#38741=CARTESIAN_POINT('Ctrl Pts',(9.16917616471593,0.597407924103304,4.18982173958679));
#38742=CARTESIAN_POINT('Ctrl Pts',(9.15327088602831,0.595037558282966,3.99283966966863));
#38743=CARTESIAN_POINT('Ctrl Pts',(9.1373656073407,0.592667192462628,3.79585759975047));
#38744=CARTESIAN_POINT('Ctrl Pts',(9.12146032865309,0.482767102306254,3.60016947898891));
#38745=CARTESIAN_POINT('Ctrl Pts',(9.10555504996548,0.315798759724268,3.49562701355602));
#38746=CARTESIAN_POINT('Ctrl Pts',(9.08964977127787,0.148830417142278,3.39108454812312));
#38747=CARTESIAN_POINT('Ctrl Pts',(9.07374449259025,-0.0752061778653251,
3.37768773801888));
#38748=CARTESIAN_POINT('Ctrl Pts',(9.05783921390264,-0.253442899077741,
3.46158783167087));
#38749=CARTESIAN_POINT('Ctrl Pts',(9.04193393521502,-0.431679620290152,
3.54548792532286));
#38750=CARTESIAN_POINT('Ctrl Pts',(9.02602865652741,-0.56411646770738,3.72668492273107));
#38751=CARTESIAN_POINT('Ctrl Pts',(9.0101233778398,-0.589944043936388,3.92198082849844));
#38752=CARTESIAN_POINT('Ctrl Pts',(8.99421809915219,-0.615771620165397,
4.11727673426582));
#38753=CARTESIAN_POINT('Ctrl Pts',(8.97831282046457,-0.534989925206181,
4.32667154839236));
#38754=CARTESIAN_POINT('Ctrl Pts',(8.96240754177696,-0.384690495792338,
4.45402003099517));
#38755=CARTESIAN_POINT('Ctrl Pts',(8.95122016493716,-0.278973620993485,
4.54359378149875));
#38756=CARTESIAN_POINT('Ctrl Pts',(8.94003278809737,-0.138863784294423,
4.59257621560968));
#38757=CARTESIAN_POINT('Ctrl Pts',(8.92884541125757,0.000516595407308196,
4.59372894893997));
#38758=CARTESIAN_POINT('Ctrl Pts',(8.82115458874249,0.000142235148737217,
4.59503945166131));
#38759=CARTESIAN_POINT('Ctrl Pts',(8.83644148529816,-0.189230254871984,
4.59442996300828));
#38760=CARTESIAN_POINT('Ctrl Pts',(8.85172838185382,-0.379146468724227,
4.49620311855542));
#38761=CARTESIAN_POINT('Ctrl Pts',(8.86701527840948,-0.487657002993039,
4.34104488491935));
#38762=CARTESIAN_POINT('Ctrl Pts',(8.88292055709709,-0.600556981206626,
4.17961022500168));
#38763=CARTESIAN_POINT('Ctrl Pts',(8.89882583578469,-0.62533206314696,3.95654506470448));
#38764=CARTESIAN_POINT('Ctrl Pts',(8.91473111447231,-0.550606579334316,
3.77427148852754));
#38765=CARTESIAN_POINT('Ctrl Pts',(8.93063639315992,-0.47588109552167,3.5919979123506));
#38766=CARTESIAN_POINT('Ctrl Pts',(8.94654167184753,-0.301655045956043,
3.45051592029392));
#38767=CARTESIAN_POINT('Ctrl Pts',(8.96244695053515,-0.107925661701669,
3.41478805750048));
#38768=CARTESIAN_POINT('Ctrl Pts',(8.97835222922276,0.0858037225526985,
3.37906019470703));
#38769=CARTESIAN_POINT('Ctrl Pts',(8.99425750791037,0.299036441495806,3.4490864611768));
#38770=CARTESIAN_POINT('Ctrl Pts',(9.01016278659798,0.433865051721373,3.5927137579139));
#38771=CARTESIAN_POINT('Ctrl Pts',(9.0260680652856,0.568693661946943,3.736341054651));
#38772=CARTESIAN_POINT('Ctrl Pts',(9.04197334397321,0.625118163454969,3.95356938165542));
#38773=CARTESIAN_POINT('Ctrl Pts',(9.05787862266082,0.577230812276762,4.14465668133936));
#38774=CARTESIAN_POINT('Ctrl Pts',(9.07378390134844,0.529343461098555,4.3357439810233));
#38775=CARTESIAN_POINT('Ctrl Pts',(9.08968918003605,0.377144257234124,4.50069025338676));
#38776=CARTESIAN_POINT('Ctrl Pts',(9.10559445872366,0.190516636080703,4.56375914846174));
#38777=CARTESIAN_POINT('Ctrl Pts',(9.11078116872994,0.129657384941762,4.58432590969837));
#38778=CARTESIAN_POINT('Ctrl Pts',(9.11596787873622,0.0651369761893139,
4.59405891310139));
#38779=CARTESIAN_POINT('Ctrl Pts',(9.12115458874249,0.000475196148639644,
4.59357609051269));
#38780=CARTESIAN_POINT('Origin',(4.,0.,4.));
#38781=CARTESIAN_POINT('',(9.52884541125756,-0.000414715089906426,4.59470005288553));
#38782=CARTESIAN_POINT('',(9.4211545887425,-0.000345133784900094,4.59331940772745));
#38783=CARTESIAN_POINT('',(4.,-7.27562663373442E-17,4.5941));
#38784=CARTESIAN_POINT('Ctrl Pts',(9.52884541125756,-0.000414715089906426,
4.59470005288553));
#38785=CARTESIAN_POINT('Ctrl Pts',(9.5149908536611,0.17147269131647,4.59333531965569));
#38786=CARTESIAN_POINT('Ctrl Pts',(9.50113629606464,0.344448366351018,4.51470554290992));
#38787=CARTESIAN_POINT('Ctrl Pts',(9.48728173846818,0.455032043431697,4.38349290156166));
#38788=CARTESIAN_POINT('Ctrl Pts',(9.47137645978057,0.581984072756561,4.23285845412795));
#38789=CARTESIAN_POINT('Ctrl Pts',(9.45547118109296,0.626706888961734,4.01292269047354));
#38790=CARTESIAN_POINT('Ctrl Pts',(9.43956590240535,0.56866566691212,3.82467080855373));
#38791=CARTESIAN_POINT('Ctrl Pts',(9.42366062371773,0.510624444862503,3.63641892663391));
#38792=CARTESIAN_POINT('Ctrl Pts',(9.40775534503012,0.349819184558098,3.47985092644869));
#38793=CARTESIAN_POINT('Ctrl Pts',(9.39185006634251,0.160084858421151,3.42685620983728));
#38794=CARTESIAN_POINT('Ctrl Pts',(9.37594478765489,-0.0296494677157886,
3.37386149322587));
#38795=CARTESIAN_POINT('Ctrl Pts',(9.36003950896728,-0.248312859685263,
3.42444006018826));
#38796=CARTESIAN_POINT('Ctrl Pts',(9.34413423027966,-0.395504338780113,
3.55536837257802));
#38797=CARTESIAN_POINT('Ctrl Pts',(9.32822895159205,-0.542695817874971,
3.6862966849678));
#38798=CARTESIAN_POINT('Ctrl Pts',(9.31232367290444,-0.618415384095196,
3.89757474278496));
#38799=CARTESIAN_POINT('Ctrl Pts',(9.29641839421683,-0.587895816063128,
4.09219260031737));
#38800=CARTESIAN_POINT('Ctrl Pts',(9.28051311552922,-0.55737624803106,4.28681045784976));
#38801=CARTESIAN_POINT('Ctrl Pts',(9.26460783684159,-0.42061754574671,4.4647681150974));
#38802=CARTESIAN_POINT('Ctrl Pts',(9.24870255815398,-0.240413519515492,
4.54435494461976));
#38803=CARTESIAN_POINT('Ctrl Pts',(9.24208350918851,-0.165420852186184,
4.57747534017911));
#38804=CARTESIAN_POINT('Ctrl Pts',(9.23546446022304,-0.0829041350566004,
4.59355944875842));
#38805=CARTESIAN_POINT('Ctrl Pts',(9.22884541125756,-0.000264402795292107,
4.59322887297718));
#38806=CARTESIAN_POINT('Ctrl Pts',(9.12115458874249,0.000475196148639644,
4.59357609051269));
#38807=CARTESIAN_POINT('Ctrl Pts',(9.13187315742383,-0.133151270259641,
4.59257831599443));
#38808=CARTESIAN_POINT('Ctrl Pts',(9.14259172610516,-0.267381477949042,
4.54795275857003));
#38809=CARTESIAN_POINT('Ctrl Pts',(9.1533102947865,-0.371151898503526,4.46515291500219));
#38810=CARTESIAN_POINT('Ctrl Pts',(9.16921557347411,-0.525136773491911,
4.34228626868117));
#38811=CARTESIAN_POINT('Ctrl Pts',(9.18512085216173,-0.612050485026272,
4.13536145825263));
#38812=CARTESIAN_POINT('Ctrl Pts',(9.20102613084934,-0.591985933785934,
3.93938960239856));
#38813=CARTESIAN_POINT('Ctrl Pts',(9.21693140953695,-0.571921382545595,
3.74341774654449));
#38814=CARTESIAN_POINT('Ctrl Pts',(9.23283668822456,-0.444878568530549,
3.55839884526489));
#38815=CARTESIAN_POINT('Ctrl Pts',(9.24874196691217,-0.269190177198291,
3.46928575052316));
#38816=CARTESIAN_POINT('Ctrl Pts',(9.26464724559978,-0.0935017858660342,
3.38017265578144));
#38817=CARTESIAN_POINT('Ctrl Pts',(9.28055252428739,0.130832182783434,3.38696536757758));
#38818=CARTESIAN_POINT('Ctrl Pts',(9.29645780297501,0.300807061133818,3.48654496003073));
#38819=CARTESIAN_POINT('Ctrl Pts',(9.31236308166262,0.470781939484206,3.58612455248389));
#38820=CARTESIAN_POINT('Ctrl Pts',(9.32826836035024,0.586397727535503,3.77849102559406));
#38821=CARTESIAN_POINT('Ctrl Pts',(9.34417363903785,0.594568546715174,3.97531783326339));
#38822=CARTESIAN_POINT('Ctrl Pts',(9.36007891772546,0.602739365894845,4.17214464093271));
#38823=CARTESIAN_POINT('Ctrl Pts',(9.37598419641307,0.503465216202894,4.37343178316119));
#38824=CARTESIAN_POINT('Ctrl Pts',(9.39188947510069,0.342328587234952,4.48675671999422));
#38825=CARTESIAN_POINT('Ctrl Pts',(9.40164451298129,0.243500144778355,4.55626125828842));
#38826=CARTESIAN_POINT('Ctrl Pts',(9.41139955086189,0.121401365174849,4.59267772446372));
#38827=CARTESIAN_POINT('Ctrl Pts',(9.4211545887425,-0.000345133784900094,
4.59331940772745));
#38828=CARTESIAN_POINT('Origin',(4.,0.,4.));
#38829=CARTESIAN_POINT('',(9.82884541125756,0.000474857175501747,4.59454166667424));
#38830=CARTESIAN_POINT('',(9.7211545887425,-0.000338423355870402,4.59484023865297));
#38831=CARTESIAN_POINT('',(4.,-7.27562663373442E-17,4.5941));
#38832=CARTESIAN_POINT('Ctrl Pts',(9.82884541125756,0.000474857175501747,
4.59454166667424));
#38833=CARTESIAN_POINT('Ctrl Pts',(9.82632780447438,0.0317313679687054,
4.59481419231428));
#38834=CARTESIAN_POINT('Ctrl Pts',(9.82381019769121,0.0629485386443197,
4.59256288124703));
#38835=CARTESIAN_POINT('Ctrl Pts',(9.82129259090804,0.093741277189286,4.58765086492638));
#38836=CARTESIAN_POINT('Ctrl Pts',(9.80538731222043,0.288278045752977,4.55661862072519));
#38837=CARTESIAN_POINT('Ctrl Pts',(9.78948203353282,0.465874751366426,4.41939150759219));
#38838=CARTESIAN_POINT('Ctrl Pts',(9.77357675484521,0.54498650030893,4.23897841027765));
#38839=CARTESIAN_POINT('Ctrl Pts',(9.7576714761576,0.624098249251433,4.05856531296313));
#38840=CARTESIAN_POINT('Ctrl Pts',(9.74176619746998,0.604725041522997,3.83496623146707));
#38841=CARTESIAN_POINT('Ctrl Pts',(9.72586091878237,0.495762234499694,3.67084840431546));
#38842=CARTESIAN_POINT('Ctrl Pts',(9.70995564009475,0.386799427476386,3.50673057716384));
#38843=CARTESIAN_POINT('Ctrl Pts',(9.69405036140714,0.188247021158209,3.40209400435668));
#38844=CARTESIAN_POINT('Ctrl Pts',(9.67814508271953,-0.00872811953311764,
3.40498337331868));
#38845=CARTESIAN_POINT('Ctrl Pts',(9.66223980403192,-0.205703260224436,
3.40787274228067));
#38846=CARTESIAN_POINT('Ctrl Pts',(9.6463345253443,-0.4011011352889,3.51828805301183));
#38847=CARTESIAN_POINT('Ctrl Pts',(9.63042924665669,-0.505203307099277,
3.68553126611098));
#38848=CARTESIAN_POINT('Ctrl Pts',(9.61452396796908,-0.609305478909656,
3.85277447921013));
#38849=CARTESIAN_POINT('Ctrl Pts',(9.59861868928147,-0.622111947465945,
4.07684559467727));
#38850=CARTESIAN_POINT('Ctrl Pts',(9.58271341059386,-0.537742524204099,
4.25486063595701));
#38851=CARTESIAN_POINT('Ctrl Pts',(9.56680813190624,-0.453373100942255,
4.43287567723675));
#38852=CARTESIAN_POINT('Ctrl Pts',(9.55090285321863,-0.271827785862281,
4.5648346443291));
#38853=CARTESIAN_POINT('Ctrl Pts',(9.53499757453102,-0.0764645071000137,
4.59014756226876));
#38854=CARTESIAN_POINT('Ctrl Pts',(9.53294685343987,-0.0512756623106346,
4.5934112419387));
#38855=CARTESIAN_POINT('Ctrl Pts',(9.53089613234871,-0.025857110284879,
4.59490205769144));
#38856=CARTESIAN_POINT('Ctrl Pts',(9.52884541125756,-0.000414715089906426,
4.59470005288553));
#38857=CARTESIAN_POINT('Ctrl Pts',(9.4211545887425,-0.000345133784900094,
4.59331940772745));
#38858=CARTESIAN_POINT('Ctrl Pts',(9.42730482954951,-0.0771024252662454,
4.59372396859559));
#38859=CARTESIAN_POINT('Ctrl Pts',(9.43345507035652,-0.153719688677923,
4.57990840728947));
#38860=CARTESIAN_POINT('Ctrl Pts',(9.43960531116353,-0.224276981305518,
4.55119942103951));
#38861=CARTESIAN_POINT('Ctrl Pts',(9.45551058985114,-0.406746812634079,
4.47695445381419));
#38862=CARTESIAN_POINT('Ctrl Pts',(9.47141586853875,-0.548687367047265,
4.30310178792596));
#38863=CARTESIAN_POINT('Ctrl Pts',(9.48732114722636,-0.58492554696818,4.10946721245096));
#38864=CARTESIAN_POINT('Ctrl Pts',(9.50322642591398,-0.621163726889096,
3.91583263697596));
#38865=CARTESIAN_POINT('Ctrl Pts',(9.5191317046016,-0.55169953231774,3.70241615191419));
#38866=CARTESIAN_POINT('Ctrl Pts',(9.53503698328921,-0.408427982613559,
3.56720957829912));
#38867=CARTESIAN_POINT('Ctrl Pts',(9.55094226197682,-0.265156432909381,
3.43200300468405));
#38868=CARTESIAN_POINT('Ctrl Pts',(9.56684754066442,-0.0480775280723801,
3.37500634251568));
#38869=CARTESIAN_POINT('Ctrl Pts',(9.58275281935204,0.14313528264739,3.42239004773181));
#38870=CARTESIAN_POINT('Ctrl Pts',(9.59865809803965,0.334348093367161,3.46977375294793));
#38871=CARTESIAN_POINT('Ctrl Pts',(9.61456337672728,0.499694809969701,3.62153782554855));
#38872=CARTESIAN_POINT('Ctrl Pts',(9.63046865541489,0.563255215433827,3.80799862400389));
#38873=CARTESIAN_POINT('Ctrl Pts',(9.6463739341025,0.626815620897955,3.99445942245922));
#38874=CARTESIAN_POINT('Ctrl Pts',(9.6622792127901,0.588589715223662,4.21561694676927));
#38875=CARTESIAN_POINT('Ctrl Pts',(9.67818449147771,0.466129217091882,4.36992501817411));
#38876=CARTESIAN_POINT('Ctrl Pts',(9.69250785723264,0.355848439261942,4.50888586187125));
#38877=CARTESIAN_POINT('Ctrl Pts',(9.70683122298757,0.177255492135987,4.59363345408847));
#38878=CARTESIAN_POINT('Ctrl Pts',(9.7211545887425,-0.000338423355870402,
4.59484023865297));
#38879=CARTESIAN_POINT('Origin',(4.,0.,4.));
#38880=CARTESIAN_POINT('',(10.1288454112576,0.000175993811045716,4.59316417414361));
#38881=CARTESIAN_POINT('',(10.0211545887425,0.000517772199431355,4.59437035498519));
#38882=CARTESIAN_POINT('',(4.,-7.27562663373442E-17,4.5941));
#38883=CARTESIAN_POINT('Ctrl Pts',(10.1288454112576,0.000175993811045716,
4.59316417414361));
#38884=CARTESIAN_POINT('Ctrl Pts',(10.1217594766001,0.0886689559287146,
4.59339827721605));
#38885=CARTESIAN_POINT('Ctrl Pts',(10.1146735419426,0.177068724884878,4.57486525982572));
#38886=CARTESIAN_POINT('Ctrl Pts',(10.1075876072851,0.256276603526552,4.53706914692868));
#38887=CARTESIAN_POINT('Ctrl Pts',(10.0916823285975,0.434068729046268,4.45223097977176));
#38888=CARTESIAN_POINT('Ctrl Pts',(10.0757770499098,0.565548899719798,4.27033860735548));
#38889=CARTESIAN_POINT('Ctrl Pts',(10.0598717712222,0.590346983641159,4.0749093118617));
#38890=CARTESIAN_POINT('Ctrl Pts',(10.0439664925346,0.61514506756252,3.87948001636793));
#38891=CARTESIAN_POINT('Ctrl Pts',(10.028061213847,0.533261064731712,3.67051379779667));
#38892=CARTESIAN_POINT('Ctrl Pts',(10.0121559351594,0.382292645022166,3.5439591030842));
#38893=CARTESIAN_POINT('Ctrl Pts',(9.99625065647179,0.231324225312614,3.41740440837173));
#38894=CARTESIAN_POINT('Ctrl Pts',(9.98034537778417,0.011271388724311,3.37326123751805));
#38895=CARTESIAN_POINT('Ctrl Pts',(9.96444009909655,-0.17682691184915,3.43179826703564));
#38896=CARTESIAN_POINT('Ctrl Pts',(9.94853482040894,-0.364925212422603,
3.49033529655323));
#38897=CARTESIAN_POINT('Ctrl Pts',(9.93262954172133,-0.521068976981223,
3.65155252644206));
#38898=CARTESIAN_POINT('Ctrl Pts',(9.91672426303372,-0.573563594737602,
3.84142582527571));
#38899=CARTESIAN_POINT('Ctrl Pts',(9.90081898434611,-0.626058212493981,
4.03129912410937));
#38900=CARTESIAN_POINT('Ctrl Pts',(9.8849137056585,-0.574903683448118,4.24982849188785));
#38901=CARTESIAN_POINT('Ctrl Pts',(9.86900842697089,-0.443588003168223,
4.39667448814241));
#38902=CARTESIAN_POINT('Ctrl Pts',(9.85562075506645,-0.333057953489513,
4.52027659892262));
#38903=CARTESIAN_POINT('Ctrl Pts',(9.842233083162,-0.165735336637852,4.59309247934331));
#38904=CARTESIAN_POINT('Ctrl Pts',(9.82884541125756,0.000474857175501747,
4.59454166667424));
#38905=CARTESIAN_POINT('Ctrl Pts',(9.7211545887425,-0.000338423355870402,
4.59484023865297));
#38906=CARTESIAN_POINT('Ctrl Pts',(9.72273650167518,-0.0199523965301825,
4.59497351934566));
#38907=CARTESIAN_POINT('Ctrl Pts',(9.72431841460787,-0.0395541838993478,
4.59408780127083));
#38908=CARTESIAN_POINT('Ctrl Pts',(9.72590032754056,-0.0590504136254521,
4.592143576127));
#38909=CARTESIAN_POINT('Ctrl Pts',(9.74180560622817,-0.255074455621757,
4.57259544417541));
#38910=CARTESIAN_POINT('Ctrl Pts',(9.75771088491579,-0.4404274490251,4.4460405617726));
#38911=CARTESIAN_POINT('Ctrl Pts',(9.7736161636034,-0.530003140903138,4.2705875768224));
#38912=CARTESIAN_POINT('Ctrl Pts',(9.78952144229101,-0.619578832781174,
4.0951345918722));
#38913=CARTESIAN_POINT('Ctrl Pts',(9.80542672097862,-0.61337722313391,3.87078350437461));
#38914=CARTESIAN_POINT('Ctrl Pts',(9.82133199966623,-0.514245828742901,
3.70054684219675));
#38915=CARTESIAN_POINT('Ctrl Pts',(9.83723727835384,-0.41511443435189,3.53031018001889));
#38916=CARTESIAN_POINT('Ctrl Pts',(9.85314255704146,-0.223053255217129,
3.41418794316076));
#38917=CARTESIAN_POINT('Ctrl Pts',(9.86904783572907,-0.0262486593588972,
3.40549855006092));
#38918=CARTESIAN_POINT('Ctrl Pts',(9.88495311441669,0.170555936499329,3.39680915696108));
#38919=CARTESIAN_POINT('Ctrl Pts',(9.9008583931043,0.372103949081026,3.49555260761951));
#38920=CARTESIAN_POINT('Ctrl Pts',(9.91676367179191,0.485853057801912,3.65639008698476));
#38921=CARTESIAN_POINT('Ctrl Pts',(9.93266895047952,0.5996021665228,3.81722756635002));
#38922=CARTESIAN_POINT('Ctrl Pts',(9.94857422916713,0.625552371382872,4.04015907442209));
#38923=CARTESIAN_POINT('Ctrl Pts',(9.96447950785475,0.551788436173011,4.22282389414861));
#38924=CARTESIAN_POINT('Ctrl Pts',(9.98038478654236,0.478024500963153,4.40548871387512));
#38925=CARTESIAN_POINT('Ctrl Pts',(9.99629006522997,0.304546425683368,4.54788684525607));
#38926=CARTESIAN_POINT('Ctrl Pts',(10.0121953439176,0.111008003250015,4.58463509072946));
#38927=CARTESIAN_POINT('Ctrl Pts',(10.0151817588592,0.0746687445744621,
4.59153503329043));
#38928=CARTESIAN_POINT('Ctrl Pts',(10.0181681738009,0.0376222632219309,
4.59471031472953));
#38929=CARTESIAN_POINT('Ctrl Pts',(10.0211545887425,0.000517772199431355,
4.59437035498519));
#38930=CARTESIAN_POINT('Origin',(4.,0.,4.));
#38931=CARTESIAN_POINT('',(10.4288454112576,-0.000541293539476018,4.59389423388278));
#38932=CARTESIAN_POINT('',(10.3211545887425,8.19078234495683E-5,4.59312629593825));
#38933=CARTESIAN_POINT('',(4.,-7.27562663373442E-17,4.5941));
#38934=CARTESIAN_POINT('Ctrl Pts',(10.4288454112576,-0.000541293539476018,
4.59389423388278));
#38935=CARTESIAN_POINT('Ctrl Pts',(10.4171911487257,0.144553461780974,4.59260897165526));
#38936=CARTESIAN_POINT('Ctrl Pts',(10.4055368861939,0.290497422953868,4.53904330389552));
#38937=CARTESIAN_POINT('Ctrl Pts',(10.3938826236621,0.397841883685798,4.4425412994096));
#38938=CARTESIAN_POINT('Ctrl Pts',(10.3779773449745,0.544341377656434,4.31083916286766));
#38939=CARTESIAN_POINT('Ctrl Pts',(10.3620720662869,0.618946539098701,4.09916502578488));
#38940=CARTESIAN_POINT('Ctrl Pts',(10.3461667875993,0.587401834162399,3.90471069671543));
#38941=CARTESIAN_POINT('Ctrl Pts',(10.3302615089117,0.555857129226098,3.710256367646));
#38942=CARTESIAN_POINT('Ctrl Pts',(10.314356230224,0.418162557911234,3.5330218465899));
#38943=CARTESIAN_POINT('Ctrl Pts',(10.2984509515364,0.237541641988682,3.45438572744188));
#38944=CARTESIAN_POINT('Ctrl Pts',(10.2825456728488,0.0569207260661262,
3.37574960829385));
#38945=CARTESIAN_POINT('Ctrl Pts',(10.2666403941612,-0.16662653446412,3.3957118910539));
#38946=CARTESIAN_POINT('Ctrl Pts',(10.2507351154736,-0.330456695071223,
3.50510674001315));
#38947=CARTESIAN_POINT('Ctrl Pts',(10.234829836786,-0.494286855678321,3.61450158897239));
#38948=CARTESIAN_POINT('Ctrl Pts',(10.2189245580984,-0.59839991636228,3.81332900413083));
#38949=CARTESIAN_POINT('Ctrl Pts',(10.2030192794108,-0.594991564317383,
4.01029584814195));
#38950=CARTESIAN_POINT('Ctrl Pts',(10.1871140007231,-0.591583212272486,
4.20726269215308));
#38951=CARTESIAN_POINT('Ctrl Pts',(10.1712087220355,-0.480653447498727,
4.40236896501689));
#38952=CARTESIAN_POINT('Ctrl Pts',(10.1553034433479,-0.313136524928893,
4.50603012050002));
#38953=CARTESIAN_POINT('Ctrl Pts',(10.1464840993178,-0.220249792163878,
4.56350936438632));
#38954=CARTESIAN_POINT('Ctrl Pts',(10.1376647552877,-0.109964716607974,
4.59287280319057));
#38955=CARTESIAN_POINT('Ctrl Pts',(10.1288454112576,0.000175993811045716,
4.59316417414361));
#38956=CARTESIAN_POINT('Ctrl Pts',(10.0211545887425,0.000517772199431355,
4.59437035498519));
#38957=CARTESIAN_POINT('Ctrl Pts',(10.0340734524885,-0.159991692577292,
4.59289973094197));
#38958=CARTESIAN_POINT('Ctrl Pts',(10.0469923162344,-0.321586704601994,
4.52564765365589));
#38959=CARTESIAN_POINT('Ctrl Pts',(10.0599111799804,-0.431712787135162,
4.40956688772629));
#38960=CARTESIAN_POINT('Ctrl Pts',(10.075816458668,-0.567296385500051,4.2666520796839));
#38961=CARTESIAN_POINT('Ctrl Pts',(10.0917217373556,-0.624864812642908,
4.04972410403331));
#38962=CARTESIAN_POINT('Ctrl Pts',(10.1076270160433,-0.577985082339038,
3.85838710972745));
#38963=CARTESIAN_POINT('Ctrl Pts',(10.1235322947309,-0.531105352035168,
3.6670501154216));
#38964=CARTESIAN_POINT('Ctrl Pts',(10.1394375734185,-0.379777464284567,
3.50130410246047));
#38965=CARTESIAN_POINT('Ctrl Pts',(10.1553428521061,-0.193484782987353,
3.43725262786029));
#38966=CARTESIAN_POINT('Ctrl Pts',(10.1712481307937,-0.00719210169012799,
3.37320115326011));
#38967=CARTESIAN_POINT('Ctrl Pts',(10.1871534094813,0.214065373153706,3.41084421702088));
#38968=CARTESIAN_POINT('Ctrl Pts',(10.2030586881689,0.368695569727689,3.53289771681035));
#38969=CARTESIAN_POINT('Ctrl Pts',(10.2189639668565,0.523325766301663,3.65495121659981));
#38970=CARTESIAN_POINT('Ctrl Pts',(10.2348692455442,0.611328684605784,3.86141515241798));
#38971=CARTESIAN_POINT('Ctrl Pts',(10.2507745242318,0.592297107651237,4.05749001970593));
#38972=CARTESIAN_POINT('Ctrl Pts',(10.2666798029194,0.573265530696689,4.25356488699388));
#38973=CARTESIAN_POINT('Ctrl Pts',(10.282585081607,0.447199458483466,4.43925068575162));
#38974=CARTESIAN_POINT('Ctrl Pts',(10.2984903602946,0.271983097956201,4.5292883529079));
#38975=CARTESIAN_POINT('Ctrl Pts',(10.3060451031106,0.188758241169316,4.57205474716445));
#38976=CARTESIAN_POINT('Ctrl Pts',(10.3135998459265,0.0944446272328244,
4.59324204311815));
#38977=CARTESIAN_POINT('Ctrl Pts',(10.3211545887425,8.19078234495684E-5,
4.59312629593825));
#38978=CARTESIAN_POINT('Origin',(4.,0.,4.));
#38979=CARTESIAN_POINT('',(10.7288454112576,7.37317986114466E-5,4.59506942345298));
#38980=CARTESIAN_POINT('',(10.6211545887425,-0.000548317120500629,4.59406879148573));
#38981=CARTESIAN_POINT('',(4.,-7.27562663373442E-17,4.5941));
#38982=CARTESIAN_POINT('Ctrl Pts',(10.7288454112576,7.37317986114466E-5,
4.59506942345298));
#38983=CARTESIAN_POINT('Ctrl Pts',(10.728528099539,0.00400402563557926,
4.59507627971693));
#38984=CARTESIAN_POINT('Ctrl Pts',(10.7282107878205,0.00793419209028873,
4.59504072157671));
#38985=CARTESIAN_POINT('Ctrl Pts',(10.727893476102,0.0118635052742893,4.59496237136513));
#38986=CARTESIAN_POINT('Ctrl Pts',(10.7119881974144,0.208820685209451,4.59103505989901));
#38987=CARTESIAN_POINT('Ctrl Pts',(10.6960829187267,0.403634001393415,4.47959161118634));
#38988=CARTESIAN_POINT('Ctrl Pts',(10.6801776400391,0.506853420906232,4.31180214209248));
#38989=CARTESIAN_POINT('Ctrl Pts',(10.6642723613515,0.610072840419052,4.14401267299861));
#38990=CARTESIAN_POINT('Ctrl Pts',(10.6483670826639,0.621698363260717,3.91987718352354));
#38991=CARTESIAN_POINT('Ctrl Pts',(10.6324618039763,0.536392041177647,3.74230920804366));
#38992=CARTESIAN_POINT('Ctrl Pts',(10.6165565252887,0.451085719094577,3.56474123256377));
#38993=CARTESIAN_POINT('Ctrl Pts',(10.6006512466011,0.26884755208677,3.43374077107907));
#38994=CARTESIAN_POINT('Ctrl Pts',(10.5847459679135,0.0733535965831807,
3.40945769333085));
#38995=CARTESIAN_POINT('Ctrl Pts',(10.5688406892258,-0.122140358920403,
3.38517461558263));
#38996=CARTESIAN_POINT('Ctrl Pts',(10.5529354105382,-0.33089010291977,3.46760892157089));
#38997=CARTESIAN_POINT('Ctrl Pts',(10.5370301318506,-0.457046584443773,
3.61891026549369));
#38998=CARTESIAN_POINT('Ctrl Pts',(10.521124853163,-0.583203065967777,3.7702116094165));
#38999=CARTESIAN_POINT('Ctrl Pts',(10.5052195744754,-0.626766285016417,
3.99037999127385));
#39000=CARTESIAN_POINT('Ctrl Pts',(10.4893142957878,-0.567733854410369,
4.17832340467295));
#39001=CARTESIAN_POINT('Ctrl Pts',(10.4734090171002,-0.508701423804317,
4.36626681807206));
#39002=CARTESIAN_POINT('Ctrl Pts',(10.4575037384126,-0.347073343543565,
4.52198526301292));
#39003=CARTESIAN_POINT('Ctrl Pts',(10.4415984597249,-0.157062390163684,
4.57397941748279));
#39004=CARTESIAN_POINT('Ctrl Pts',(10.4373474435692,-0.106278015462724,
4.58787593542499));
#39005=CARTESIAN_POINT('Ctrl Pts',(10.4330964274134,-0.0534661480554494,
4.59436304694399));
#39006=CARTESIAN_POINT('Ctrl Pts',(10.4288454112576,-0.000541293539476018,
4.59389423388278));
#39007=CARTESIAN_POINT('Ctrl Pts',(10.3211545887425,8.19078234495684E-5,
4.59312629593825));
#39008=CARTESIAN_POINT('Ctrl Pts',(10.3295051246142,-0.104220686264852,
4.59299835631127));
#39009=CARTESIAN_POINT('Ctrl Pts',(10.3378556604858,-0.208583275928277,
4.56684300569277));
#39010=CARTESIAN_POINT('Ctrl Pts',(10.3462061963575,-0.298097175589899,
4.5150330474864));
#39011=CARTESIAN_POINT('Ctrl Pts',(10.3621114750451,-0.468594439767441,
4.41635053935381));
#39012=CARTESIAN_POINT('Ctrl Pts',(10.3780167537327,-0.585222319281217,
4.22459598753381));
#39013=CARTESIAN_POINT('Ctrl Pts',(10.3939220324203,-0.594430225977177,
4.02781496975607));
#39014=CARTESIAN_POINT('Ctrl Pts',(10.4098273111079,-0.603638132673137,
3.83103395197833));
#39015=CARTESIAN_POINT('Ctrl Pts',(10.4257325897955,-0.505426066551287,
3.62922646824286));
#39016=CARTESIAN_POINT('Ctrl Pts',(10.4416378684831,-0.344888853364916,
3.51505397731042));
#39017=CARTESIAN_POINT('Ctrl Pts',(10.4575431471707,-0.184351640178541,
3.40088148637798));
#39018=CARTESIAN_POINT('Ctrl Pts',(10.4734484258584,0.0385107200723601,
3.37434398824859));
#39019=CARTESIAN_POINT('Ctrl Pts',(10.489353704546,0.221369260089487,3.4476263793543));
#39020=CARTESIAN_POINT('Ctrl Pts',(10.5052589832336,0.40422780010661,3.52090877046001));
#39021=CARTESIAN_POINT('Ctrl Pts',(10.5211642619212,0.54708251988996,3.69401105080081));
#39022=CARTESIAN_POINT('Ctrl Pts',(10.5370695406088,0.584340575799814,3.88745197659776));
#39023=CARTESIAN_POINT('Ctrl Pts',(10.5529748192964,0.621598631709669,4.08089290239472));
#39024=CARTESIAN_POINT('Ctrl Pts',(10.568880097984,0.55326002374602,4.29467247364782));
#39025=CARTESIAN_POINT('Ctrl Pts',(10.5847853766716,0.4107029495177,4.43063215550545));
#39026=CARTESIAN_POINT('Ctrl Pts',(10.5969084473619,0.302045344566967,4.53426120008624));
#39027=CARTESIAN_POINT('Ctrl Pts',(10.6090315180522,0.150270129189204,4.59268036842864));
#39028=CARTESIAN_POINT('Ctrl Pts',(10.6211545887425,-0.000548317120500629,
4.59406879148573));
#39029=CARTESIAN_POINT('Origin',(4.,0.,4.));
#39030=CARTESIAN_POINT('',(11.0288454112576,0.000503618959454472,4.59367252935801));
#39031=CARTESIAN_POINT('',(10.9211545887425,0.000179316795020235,4.59501533910171));
#39032=CARTESIAN_POINT('',(4.,-7.27562663373442E-17,4.5941));
#39033=CARTESIAN_POINT('Ctrl Pts',(11.0288454112576,0.000503618959454472,
4.59367252935801));
#39034=CARTESIAN_POINT('Ctrl Pts',(11.0239597716647,0.0613870506829751,
4.59415995979602));
#39035=CARTESIAN_POINT('Ctrl Pts',(11.0190741320719,0.122135879976345,4.58554712933309));
#39036=CARTESIAN_POINT('Ctrl Pts',(11.014188492479,0.179818659528701,4.56726203449827));
#39037=CARTESIAN_POINT('Ctrl Pts',(10.9982832137914,0.36760588100072,4.50773461262244));
#39038=CARTESIAN_POINT('Ctrl Pts',(10.9823779351038,0.52289792528528,4.34569680405454));
#39039=CARTESIAN_POINT('Ctrl Pts',(10.9664726564162,0.574391255511512,4.15554951523459));
#39040=CARTESIAN_POINT('Ctrl Pts',(10.9505673777285,0.625884585737745,3.96540222641464));
#39041=CARTESIAN_POINT('Ctrl Pts',(10.9346620990409,0.573579201905647,3.74714545734266));
#39042=CARTESIAN_POINT('Ctrl Pts',(10.9187568203533,0.441491523412615,3.60099348269406));
#39043=CARTESIAN_POINT('Ctrl Pts',(10.9028515416657,0.309403844919578,3.45484150804546));
#39044=CARTESIAN_POINT('Ctrl Pts',(10.8869462629781,0.0975338717655902,
3.38079432782024));
#39045=CARTESIAN_POINT('Ctrl Pts',(10.8710409842905,-0.0968366678563846,
3.41285127449999));
#39046=CARTESIAN_POINT('Ctrl Pts',(10.8551357056029,-0.291207207478354,
3.44490822117975));
#39047=CARTESIAN_POINT('Ctrl Pts',(10.8392304269153,-0.468078313568319,
3.58306929476445));
#39048=CARTESIAN_POINT('Ctrl Pts',(10.8233251482276,-0.546238257009186,
3.76389677537701));
#39049=CARTESIAN_POINT('Ctrl Pts',(10.80741986954,-0.624398200450053,3.94472425598957));
#39050=CARTESIAN_POINT('Ctrl Pts',(10.7915145908524,-0.603846981241821,
4.16821814362997));
#39051=CARTESIAN_POINT('Ctrl Pts',(10.7756093121648,-0.494020849794526,
4.33175950034039));
#39052=CARTESIAN_POINT('Ctrl Pts',(10.7600213451957,-0.386385759396791,
4.49203819249975));
#39053=CARTESIAN_POINT('Ctrl Pts',(10.7444333782267,-0.193002309618558,
4.59473260886404));
#39054=CARTESIAN_POINT('Ctrl Pts',(10.7288454112576,7.37317986114466E-5,
4.59506942345298));
#39055=CARTESIAN_POINT('Ctrl Pts',(10.6211545887425,-0.000548317120500629,
4.59406879148573));
#39056=CARTESIAN_POINT('Ctrl Pts',(10.6249367967398,-0.0476013079303647,
4.5945019577127));
#39057=CARTESIAN_POINT('Ctrl Pts',(10.6287190047372,-0.0945611723716044,
4.58938408097059));
#39058=CARTESIAN_POINT('Ctrl Pts',(10.6325012127345,-0.140089514783682,
4.57835619988505));
#39059=CARTESIAN_POINT('Ctrl Pts',(10.6484064914221,-0.331549364363767,
4.53198076994489));
#39060=CARTESIAN_POINT('Ctrl Pts',(10.6643117701097,-0.497693523030948,
4.38109011760241));
#39061=CARTESIAN_POINT('Ctrl Pts',(10.6802170487973,-0.562235622104956,
4.19496684675621));
#39062=CARTESIAN_POINT('Ctrl Pts',(10.6961223274849,-0.626777721178965,
4.00884357591002));
#39063=CARTESIAN_POINT('Ctrl Pts',(10.7120276061725,-0.589717760659791,
3.78748768656011));
#39064=CARTESIAN_POINT('Ctrl Pts',(10.7279328848602,-0.468072106540212,
3.63253643830059));
#39065=CARTESIAN_POINT('Ctrl Pts',(10.7438381635478,-0.346426452420629,
3.47758519004106));
#39066=CARTESIAN_POINT('Ctrl Pts',(10.7597434422354,-0.140195104700642,
3.38903858287192));
#39067=CARTESIAN_POINT('Ctrl Pts',(10.775648720923,0.0559292266755373,3.40755347270721));
#39068=CARTESIAN_POINT('Ctrl Pts',(10.7915539996106,0.252053558051711,3.4260683625425));
#39069=CARTESIAN_POINT('Ctrl Pts',(10.8074592782982,0.438070873084069,3.55164474938222));
#39070=CARTESIAN_POINT('Ctrl Pts',(10.8233645569858,0.528569890453362,3.72662326908837));
#39071=CARTESIAN_POINT('Ctrl Pts',(10.8392698356734,0.619068907822657,3.90160178879453));
#39072=CARTESIAN_POINT('Ctrl Pts',(10.8551751143611,0.614049627528876,4.12598244136713));
#39073=CARTESIAN_POINT('Ctrl Pts',(10.8710803930487,0.515816690734684,4.29673912390739));
#39074=CARTESIAN_POINT('Ctrl Pts',(10.8869856717363,0.417583753940498,4.46749580644764));
#39075=CARTESIAN_POINT('Ctrl Pts',(10.9028909504239,0.226137160645921,4.58462851895556));
#39076=CARTESIAN_POINT('Ctrl Pts',(10.9187962291115,0.0293810870543861,
4.59435487532392));
#39077=CARTESIAN_POINT('Ctrl Pts',(10.9195823489885,0.0196563998352688,
4.59483560139116));
#39078=CARTESIAN_POINT('Ctrl Pts',(10.9203684688655,0.00991874240631306,
4.5950539509358));
#39079=CARTESIAN_POINT('Ctrl Pts',(10.9211545887425,0.000179316795020235,
4.59501533910171));
#39080=CARTESIAN_POINT('Origin',(4.,0.,4.));
#39081=CARTESIAN_POINT('',(11.3288454112576,-0.000294350894641693,4.59325842069974));
#39082=CARTESIAN_POINT('',(11.2211545887425,0.000456638431143918,4.59352536526061));
#39083=CARTESIAN_POINT('',(4.,-7.27562663373442E-17,4.5941));
#39084=CARTESIAN_POINT('Ctrl Pts',(11.3288454112576,-0.000294350894641693,
4.59325842069974));
#39085=CARTESIAN_POINT('Ctrl Pts',(11.3193914437904,0.117725031793324,4.59273125875086));
#39086=CARTESIAN_POINT('Ctrl Pts',(11.3099374763232,0.236024696118704,4.55868066117597));
#39087=CARTESIAN_POINT('Ctrl Pts',(11.300483508856,0.333060002447629,4.49314500997921));
#39088=CARTESIAN_POINT('Ctrl Pts',(11.2845782301684,0.496311419914153,4.38288835848583));
#39089=CARTESIAN_POINT('Ctrl Pts',(11.2686729514808,0.599375291650127,4.18351506848348));
#39090=CARTESIAN_POINT('Ctrl Pts',(11.2527676727932,0.594929048027223,3.98656891995295));
#39091=CARTESIAN_POINT('Ctrl Pts',(11.2368623941056,0.59048280440432,3.78962277142242));
#39092=CARTESIAN_POINT('Ctrl Pts',(11.220957115418,0.478526445422532,3.5951037643637));
#39093=CARTESIAN_POINT('Ctrl Pts',(11.2050518367303,0.310465594643358,3.49232679739763));
#39094=CARTESIAN_POINT('Ctrl Pts',(11.1891465580427,0.142404743864184,3.38954983043155));
#39095=CARTESIAN_POINT('Ctrl Pts',(11.1732412793551,-0.0817605987123653,
3.37851490355812));
#39096=CARTESIAN_POINT('Ctrl Pts',(11.1573360006675,-0.259103191428711,
3.46428878834836));
#39097=CARTESIAN_POINT('Ctrl Pts',(11.1414307219799,-0.436445784145052,
3.5500626731386));
#39098=CARTESIAN_POINT('Ctrl Pts',(11.1255254432923,-0.566965627001181,
3.73264536959251));
#39099=CARTESIAN_POINT('Ctrl Pts',(11.1096201646047,-0.590733529996744,
3.92820262793532));
#39100=CARTESIAN_POINT('Ctrl Pts',(11.0937148859171,-0.614501432992307,
4.12375988627813));
#39101=CARTESIAN_POINT('Ctrl Pts',(11.0778096072294,-0.531517396127296,
4.33229170650985));
#39102=CARTESIAN_POINT('Ctrl Pts',(11.0619043285418,-0.379884178365051,
4.45804909903384));
#39103=CARTESIAN_POINT('Ctrl Pts',(11.0508846894471,-0.274828280424841,
4.54517747360242));
#39104=CARTESIAN_POINT('Ctrl Pts',(11.0398650503523,-0.136819945681758,
4.59257312212411));
#39105=CARTESIAN_POINT('Ctrl Pts',(11.0288454112576,0.000503618959454472,
4.59367252935801));
#39106=CARTESIAN_POINT('Ctrl Pts',(10.9211545887425,0.000179316795020235,
4.59501533910171));
#39107=CARTESIAN_POINT('Ctrl Pts',(10.9362737475531,-0.187135527734918,
4.59427273168419));
#39108=CARTESIAN_POINT('Ctrl Pts',(10.9513929063637,-0.375104412928531,
4.49848156101044));
#39109=CARTESIAN_POINT('Ctrl Pts',(10.9665120651743,-0.484035620954107,
4.34616539940523));
#39110=CARTESIAN_POINT('Ctrl Pts',(10.982417343862,-0.598630701482551,4.1859295668894));
#39111=CARTESIAN_POINT('Ctrl Pts',(10.9983226225496,-0.625755308650954,
3.96313790162893));
#39112=CARTESIAN_POINT('Ctrl Pts',(11.0142279012372,-0.55295497039508,3.7800869107734));
#39113=CARTESIAN_POINT('Ctrl Pts',(11.0301331799248,-0.480154632139201,
3.59703591991786));
#39114=CARTESIAN_POINT('Ctrl Pts',(11.0460384586124,-0.307429348459053,
3.45372560346725));
#39115=CARTESIAN_POINT('Ctrl Pts',(11.0619437373,-0.114087262216405,3.41595799577618));
#39116=CARTESIAN_POINT('Ctrl Pts',(11.0778490159876,0.0792548240262376,
3.37819038808511));
#39117=CARTESIAN_POINT('Ctrl Pts',(11.0937542946752,0.293213712831377,3.4459654891536));
#39118=CARTESIAN_POINT('Ctrl Pts',(11.1096595733629,0.429548534313776,3.58816383989905));
#39119=CARTESIAN_POINT('Ctrl Pts',(11.1255648520505,0.565883355796175,3.7303621906445));
#39120=CARTESIAN_POINT('Ctrl Pts',(11.1414701307381,0.624594109955846,3.94698379106692));
#39121=CARTESIAN_POINT('Ctrl Pts',(11.1573754094257,0.578723302329844,4.13856516675647));
#39122=CARTESIAN_POINT('Ctrl Pts',(11.1732806881133,0.53285249470384,4.33014654244603));
#39123=CARTESIAN_POINT('Ctrl Pts',(11.1891859668009,0.382400125292158,4.49668769340272));
#39124=CARTESIAN_POINT('Ctrl Pts',(11.2050912454885,0.196447557013804,4.56171996888228));
#39125=CARTESIAN_POINT('Ctrl Pts',(11.2104456932399,0.133847376870746,4.58361282144047));
#39126=CARTESIAN_POINT('Ctrl Pts',(11.2158001409912,0.0672239414478651,
4.5940016224088));
#39127=CARTESIAN_POINT('Ctrl Pts',(11.2211545887425,0.000456638431143918,
4.59352536526061));
#39128=CARTESIAN_POINT('Origin',(4.,0.,4.));
#39129=CARTESIAN_POINT('',(11.6288454112576,-0.000389145320547679,4.59475273347735));
#39130=CARTESIAN_POINT('',(11.5211545887425,-0.0003715675665865,4.59335763259963));
#39131=CARTESIAN_POINT('',(4.,-7.27562663373442E-17,4.5941));
#39132=CARTESIAN_POINT('Ctrl Pts',(11.6288454112576,-0.000389145320547679,
4.59475273347735));
#39133=CARTESIAN_POINT('Ctrl Pts',(11.6148231159161,0.173538999407471,4.59343557735163));
#39134=CARTESIAN_POINT('Ctrl Pts',(11.6008008205746,0.348531733704351,4.51264940831536));
#39135=CARTESIAN_POINT('Ctrl Pts',(11.586778525233,0.459048433726307,4.37867598496766));
#39136=CARTESIAN_POINT('Ctrl Pts',(11.5708732465454,0.584405864209301,4.22671194604376));
#39137=CARTESIAN_POINT('Ctrl Pts',(11.5549679678578,0.626808276394098,4.00631705984067));
#39138=CARTESIAN_POINT('Ctrl Pts',(11.5390626891702,0.566786276503563,3.81868733396413));
#39139=CARTESIAN_POINT('Ctrl Pts',(11.5231574104826,0.506764276613028,3.6310576080876));
#39140=CARTESIAN_POINT('Ctrl Pts',(11.507252131795,0.344317864647159,3.47619304253762));
#39141=CARTESIAN_POINT('Ctrl Pts',(11.4913468531074,0.154035560439752,3.4252008940353));
#39142=CARTESIAN_POINT('Ctrl Pts',(11.4754415744198,-0.0362467437676612,
3.37420874553297));
#39143=CARTESIAN_POINT('Ctrl Pts',(11.4595362957322,-0.254364940216614,
3.4270890140783));
#39144=CARTESIAN_POINT('Ctrl Pts',(11.4436310170445,-0.400168380917644,
3.55956131753494));
#39145=CARTESIAN_POINT('Ctrl Pts',(11.4277257383569,-0.545971821618673,
3.69203362099157));
#39146=CARTESIAN_POINT('Ctrl Pts',(11.4118204596693,-0.619460506571779,
3.90409795935952));
#39147=CARTESIAN_POINT('Ctrl Pts',(11.3959151809817,-0.586891540696359,
4.09838336016249));
#39148=CARTESIAN_POINT('Ctrl Pts',(11.3800099022941,-0.554322574820941,
4.29266876096545));
#39149=CARTESIAN_POINT('Ctrl Pts',(11.3641046236065,-0.415695958117004,
4.46917522420345));
#39150=CARTESIAN_POINT('Ctrl Pts',(11.3481993449189,-0.234663168166497,
4.54685844933023));
#39151=CARTESIAN_POINT('Ctrl Pts',(11.3417480336984,-0.161234786808821,
4.57836740127901));
#39152=CARTESIAN_POINT('Ctrl Pts',(11.335296722478,-0.080829826651965,4.59361815176584));
#39153=CARTESIAN_POINT('Ctrl Pts',(11.3288454112576,-0.000294350894641693,
4.59325842069974));
#39154=CARTESIAN_POINT('Ctrl Pts',(11.2211545887425,0.000456638431143918,
4.59352536526061));
#39155=CARTESIAN_POINT('Ctrl Pts',(11.2317054196788,-0.131106980996848,
4.59258691018808));
#39156=CARTESIAN_POINT('Ctrl Pts',(11.2422562506151,-0.263229208150973,
4.54946171071576));
#39157=CARTESIAN_POINT('Ctrl Pts',(11.2528070815514,-0.366229002642205,
4.4690386804108));
#39158=CARTESIAN_POINT('Ctrl Pts',(11.268712360239,-0.521500226874852,4.34780171645731));
#39159=CARTESIAN_POINT('Ctrl Pts',(11.2846176389266,-0.610589908195122,
4.1418043885479));
#39160=CARTESIAN_POINT('Ctrl Pts',(11.3005229176142,-0.592591834014348,
3.94563195463032));
#39161=CARTESIAN_POINT('Ctrl Pts',(11.3164281963018,-0.574593759833574,
3.74945952071274));
#39162=CARTESIAN_POINT('Ctrl Pts',(11.3323334749894,-0.449507930151742,
3.56311198078699));
#39163=CARTESIAN_POINT('Ctrl Pts',(11.3482387536771,-0.274768466013715,
3.47215224147272));
#39164=CARTESIAN_POINT('Ctrl Pts',(11.3641440323647,-0.100029001875688,
3.38119250215845));
#39165=CARTESIAN_POINT('Ctrl Pts',(11.3800493110523,0.12436409671854,3.38562056345565));
#39166=CARTESIAN_POINT('Ctrl Pts',(11.3959545897399,0.295379012183608,3.48340324695247));
#39167=CARTESIAN_POINT('Ctrl Pts',(11.4118598684275,0.466393927648671,3.5811859304493));
#39168=CARTESIAN_POINT('Ctrl Pts',(11.4277651471151,0.584030659984583,3.77232323614575));
#39169=CARTESIAN_POINT('Ctrl Pts',(11.4436704258027,0.594275398502411,3.96905299961855));
#39170=CARTESIAN_POINT('Ctrl Pts',(11.4595757044903,0.60452013702024,4.16578276309136));
#39171=CARTESIAN_POINT('Ctrl Pts',(11.475480983178,0.507372881719984,4.36810498434052));
#39172=CARTESIAN_POINT('Ctrl Pts',(11.4913862618656,0.34743954227408,4.48312185891572));
#39173=CARTESIAN_POINT('Ctrl Pts',(11.5013090374912,0.247662438486696,4.55487707062799));
#39174=CARTESIAN_POINT('Ctrl Pts',(11.5112318131169,0.123448374926332,4.59265218509947));
#39175=CARTESIAN_POINT('Ctrl Pts',(11.5211545887425,-0.0003715675665865,
4.59335763259963));
#39176=CARTESIAN_POINT('Origin',(4.,0.,4.));
#39177=CARTESIAN_POINT('',(11.9288454112576,0.000492284285450728,4.5944814532616));
#39178=CARTESIAN_POINT('',(11.8211545887425,-0.000307672146732893,4.59488449882539));
#39179=CARTESIAN_POINT('',(4.,-7.27562663373442E-17,4.5941));
#39180=CARTESIAN_POINT('Ctrl Pts',(11.9288454112576,0.000492284285450728,
4.5944814532616));
#39181=CARTESIAN_POINT('Ctrl Pts',(11.9261600667293,0.0338400408399785,
4.59477876231094));
#39182=CARTESIAN_POINT('Ctrl Pts',(11.9234747222011,0.0671420792079604,
4.59221542322669));
#39183=CARTESIAN_POINT('Ctrl Pts',(11.9207893776729,0.0999293694653808,
4.5866302815369));
#39184=CARTESIAN_POINT('Ctrl Pts',(11.9048840989853,0.294128282668868,4.55354952256816));
#39185=CARTESIAN_POINT('Ctrl Pts',(11.8889788202977,0.470268877700486,4.41445832512751));
#39186=CARTESIAN_POINT('Ctrl Pts',(11.8730735416101,0.547474845215755,4.2332214826164));
#39187=CARTESIAN_POINT('Ctrl Pts',(11.8571682629225,0.624680812731027,4.05198464010529));
#39188=CARTESIAN_POINT('Ctrl Pts',(11.8412629842349,0.602952152729945,3.82860215252373));
#39189=CARTESIAN_POINT('Ctrl Pts',(11.8253577055472,0.492265746621211,3.66564180763548));
#39190=CARTESIAN_POINT('Ctrl Pts',(11.8094524268596,0.38157934051248,3.50268146274723));
#39191=CARTESIAN_POINT('Ctrl Pts',(11.793547148172,0.181935188296101,3.40014326055229));
#39192=CARTESIAN_POINT('Ctrl Pts',(11.7776418694844,-0.0149985615777061,
3.40510840546499));
#39193=CARTESIAN_POINT('Ctrl Pts',(11.7617365907968,-0.211932311451519,
3.41007355037768));
#39194=CARTESIAN_POINT('Ctrl Pts',(11.7458313121092,-0.406155658982761,
3.52254204239802));
#39195=CARTESIAN_POINT('Ctrl Pts',(11.7299260334216,-0.508489459897291,
3.69087310813977));
#39196=CARTESIAN_POINT('Ctrl Pts',(11.714020754734,-0.610823260811815,3.8592041738815));
#39197=CARTESIAN_POINT('Ctrl Pts',(11.6981154760463,-0.621267515109637,
4.08339781334463));
#39198=CARTESIAN_POINT('Ctrl Pts',(11.6822101973587,-0.53502666307716,4.26051379213839));
#39199=CARTESIAN_POINT('Ctrl Pts',(11.6663049186711,-0.448785811044678,
4.43762977093217));
#39200=CARTESIAN_POINT('Ctrl Pts',(11.6503996399835,-0.265859852681883,
4.56766808905658));
#39201=CARTESIAN_POINT('Ctrl Pts',(11.6344943612959,-0.070240649109886,
4.59092065229643));
#39202=CARTESIAN_POINT('Ctrl Pts',(11.6326113779498,-0.0470818155087989,
4.59367346098309));
#39203=CARTESIAN_POINT('Ctrl Pts',(11.6307283946037,-0.0237450789937817,
4.59492960773286));
#39204=CARTESIAN_POINT('Ctrl Pts',(11.6288454112576,-0.000389145320547679,
4.59475273347735));
#39205=CARTESIAN_POINT('Ctrl Pts',(11.5211545887425,-0.0003715675665865,
4.59335763259963));
#39206=CARTESIAN_POINT('Ctrl Pts',(11.5271370918045,-0.0750233800274846,
4.5937829512795));
#39207=CARTESIAN_POINT('Ctrl Pts',(11.5331195948664,-0.149531931096223,
4.58073359799715));
#39208=CARTESIAN_POINT('Ctrl Pts',(11.5391020979284,-0.218455391669058,
4.55353248138526));
#39209=CARTESIAN_POINT('Ctrl Pts',(11.555007376616,-0.40169756257477,4.48121470137836));
#39210=CARTESIAN_POINT('Ctrl Pts',(11.5709126553036,-0.545462480794654,
4.3088676134633));
#39211=CARTESIAN_POINT('Ctrl Pts',(11.5868179339912,-0.583739378074245,
4.1156257090067));
#39212=CARTESIAN_POINT('Ctrl Pts',(11.6027232126789,-0.622016275353834,
3.92238380455011));
#39213=CARTESIAN_POINT('Ctrl Pts',(11.6186284913665,-0.554805151693135,
3.70824708355197));
#39214=CARTESIAN_POINT('Ctrl Pts',(11.6345337700541,-0.412966511608993,
3.57153806891708));
#39215=CARTESIAN_POINT('Ctrl Pts',(11.6504390487417,-0.271127871524847,
3.43482905428217));
#39216=CARTESIAN_POINT('Ctrl Pts',(11.6663443274293,-0.0546617150172531,
3.37554774601052));
#39217=CARTESIAN_POINT('Ctrl Pts',(11.6822496061169,0.137039856773353,3.42091361287512));
#39218=CARTESIAN_POINT('Ctrl Pts',(11.6981548848045,0.328741428563947,3.46627947973972));
#39219=CARTESIAN_POINT('Ctrl Pts',(11.7140601634921,0.495678415637556,3.61629252174057));
#39220=CARTESIAN_POINT('Ctrl Pts',(11.7299654421798,0.56120041605148,3.80207309651931));
#39221=CARTESIAN_POINT('Ctrl Pts',(11.7458707208674,0.626722416465409,3.98785367129807));
#39222=CARTESIAN_POINT('Ctrl Pts',(11.761775999555,0.590829430219633,4.20940177885472));
#39223=CARTESIAN_POINT('Ctrl Pts',(11.7776812782426,0.470001998091193,4.36499190112672));
#39224=CARTESIAN_POINT('Ctrl Pts',(11.7921723817426,0.359917612963646,4.5067481450567));
#39225=CARTESIAN_POINT('Ctrl Pts',(11.8066634852425,0.179330777996457,4.59375393408315));
#39226=CARTESIAN_POINT('Ctrl Pts',(11.8211545887425,-0.000307672146732893,
4.59488449882539));
#39227=CARTESIAN_POINT('Origin',(4.,0.,4.));
#39228=CARTESIAN_POINT('',(12.2288454112576,0.000142795628640946,4.59314744373127));
#39229=CARTESIAN_POINT('',(12.1211545887425,0.00052868291625318,4.59430727435519));
#39230=CARTESIAN_POINT('',(4.,-7.27562663373442E-17,4.5941));
#39231=CARTESIAN_POINT('Ctrl Pts',(12.2288454112576,0.000142795628640946,
4.59314744373127));
#39232=CARTESIAN_POINT('Ctrl Pts',(12.221591738855,0.0907369315914116,4.59334157666405));
#39233=CARTESIAN_POINT('Ctrl Pts',(12.2143380664525,0.181251971066953,4.57388161006077));
#39234=CARTESIAN_POINT('Ctrl Pts',(12.2070843940499,0.261922584292681,4.53433840020651));
#39235=CARTESIAN_POINT('Ctrl Pts',(12.1911791153623,0.438810719578057,4.44763117963851));
#39236=CARTESIAN_POINT('Ctrl Pts',(12.1752738366747,0.56836661021043,4.26436322928705));
#39237=CARTESIAN_POINT('Ctrl Pts',(12.1593685579871,0.591103672269137,4.06868343852597));
#39238=CARTESIAN_POINT('Ctrl Pts',(12.1434632792995,0.613840734327844,3.87300364776488));
#39239=CARTESIAN_POINT('Ctrl Pts',(12.1275580006119,0.529758967812885,3.66491201659415));
#39240=CARTESIAN_POINT('Ctrl Pts',(12.1116527219243,0.377465162701742,3.53995541841648));
#39241=CARTESIAN_POINT('Ctrl Pts',(12.0957474432367,0.225171357590603,3.41499882023882));
#39242=CARTESIAN_POINT('Ctrl Pts',(12.0798421645491,0.00466551388328543,
3.37317725505421));
#39243=CARTESIAN_POINT('Ctrl Pts',(12.0639368858614,-0.182805413822737,
3.43369341627091));
#39244=CARTESIAN_POINT('Ctrl Pts',(12.0480316071738,-0.37027634152876,3.49420957748762));
#39245=CARTESIAN_POINT('Ctrl Pts',(12.0321263284862,-0.524712353233489,
3.65706346510565));
#39246=CARTESIAN_POINT('Ctrl Pts',(12.0162210497986,-0.575202966010955,
3.84747946371059));
#39247=CARTESIAN_POINT('Ctrl Pts',(12.000315771111,-0.625693578788423,4.03789546231555));
#39248=CARTESIAN_POINT('Ctrl Pts',(11.9844104924234,-0.572238792638624,
4.25587357190742));
#39249=CARTESIAN_POINT('Ctrl Pts',(11.9685052137358,-0.439382783876041,
4.40132746645495));
#39250=CARTESIAN_POINT('Ctrl Pts',(11.9552852795764,-0.328957325572706,
4.52222386487166));
#39251=CARTESIAN_POINT('Ctrl Pts',(11.942065345417,-0.163678510702966,4.59301780268865));
#39252=CARTESIAN_POINT('Ctrl Pts',(11.9288454112576,0.000492284285450728,
4.5944814532616));
#39253=CARTESIAN_POINT('Ctrl Pts',(11.8211545887425,-0.000307672146732893,
4.59488449882539));
#39254=CARTESIAN_POINT('Ctrl Pts',(11.8225687639301,-0.0178384446610953,
4.59499482973335));
#39255=CARTESIAN_POINT('Ctrl Pts',(11.8239829391178,-0.035360185088601,
4.59428731490513));
#39256=CARTESIAN_POINT('Ctrl Pts',(11.8253971143054,-0.0528064866265509,
4.59273302680715));
#39257=CARTESIAN_POINT('Ctrl Pts',(11.8413023929931,-0.249025661204777,
4.57525189322826));
#39258=CARTESIAN_POINT('Ctrl Pts',(11.8572076716807,-0.435702132350142,
4.45065748908313));
#39259=CARTESIAN_POINT('Ctrl Pts',(11.8731129503683,-0.527121962142897,
4.27615829360067));
#39260=CARTESIAN_POINT('Ctrl Pts',(11.8890182290559,-0.618541791935657,
4.10165909811819));
#39261=CARTESIAN_POINT('Ctrl Pts',(11.9049235077435,-0.614704980375792,
3.87725511129838));
#39262=CARTESIAN_POINT('Ctrl Pts',(11.9208287864311,-0.517373229009482,
3.70598315013913));
#39263=CARTESIAN_POINT('Ctrl Pts',(11.9367340651187,-0.420041477643178,
3.53471118897989));
#39264=CARTESIAN_POINT('Ctrl Pts',(11.9526393438063,-0.229214786470442,
3.41657125348121));
#39265=CARTESIAN_POINT('Ctrl Pts',(11.9685446224939,-0.0325126988662629,
3.4058082039356));
#39266=CARTESIAN_POINT('Ctrl Pts',(11.9844499011816,0.164189388737916,3.39504515438998));
#39267=CARTESIAN_POINT('Ctrl Pts',(12.0003551798692,0.366766872773537,3.49165899079743));
#39268=CARTESIAN_POINT('Ctrl Pts',(12.0162604585568,0.482204742918021,3.65128872687397));
#39269=CARTESIAN_POINT('Ctrl Pts',(12.0321657372444,0.597642613062508,3.81091846295053));
#39270=CARTESIAN_POINT('Ctrl Pts',(12.048071015932,0.625940869315854,4.03356409869619));
#39271=CARTESIAN_POINT('Ctrl Pts',(12.0639762946196,0.554106149607013,4.21699617753661));
#39272=CARTESIAN_POINT('Ctrl Pts',(12.0798815733072,0.482271429898174,4.40042825637702));
#39273=CARTESIAN_POINT('Ctrl Pts',(12.0957868519948,0.310303734227154,4.5446467783122));
#39274=CARTESIAN_POINT('Ctrl Pts',(12.1116921306825,0.117163353092859,4.583432699452));
#39275=CARTESIAN_POINT('Ctrl Pts',(12.1148462833691,0.0788619649798074,
4.59112427906975));
#39276=CARTESIAN_POINT('Ctrl Pts',(12.1180004360558,0.0397279339241207,
4.59466958677844));
#39277=CARTESIAN_POINT('Ctrl Pts',(12.1211545887425,0.00052868291625318,
4.59430727435519));
#39278=CARTESIAN_POINT('Origin',(4.,0.,4.));
#39279=CARTESIAN_POINT('',(12.5288454112576,-0.000545899910317726,4.59395595168017));
#39280=CARTESIAN_POINT('',(12.4211545887425,4.74932194801069E-5,4.59311952367199));
#39281=CARTESIAN_POINT('',(4.,-7.27562663373442E-17,4.5941));
#39282=CARTESIAN_POINT('Ctrl Pts',(12.5288454112576,-0.000545899910317726,
4.59395595168017));
#39283=CARTESIAN_POINT('Ctrl Pts',(12.5170234109807,0.14659828900878,4.5926299020853));
#39284=CARTESIAN_POINT('Ctrl Pts',(12.5052014107038,0.29463204299547,4.53735693360054));
#39285=CARTESIAN_POINT('Ctrl Pts',(12.493379410427,0.402483765871145,4.43832383497591));
#39286=CARTESIAN_POINT('Ctrl Pts',(12.4774741317394,0.547587104485886,4.30508504322883));
#39287=CARTESIAN_POINT('Ctrl Pts',(12.4615688530518,0.619957272242066,4.09263639239171));
#39288=CARTESIAN_POINT('Ctrl Pts',(12.4456635743641,0.586364949835353,3.89852531496775));
#39289=CARTESIAN_POINT('Ctrl Pts',(12.4297582956765,0.55277262742864,3.7044142375438));
#39290=CARTESIAN_POINT('Ctrl Pts',(12.4138530169889,0.41321781485904,3.52864073353302));
#39291=CARTESIAN_POINT('Ctrl Pts',(12.3979477383013,0.231778177981285,3.45191255961345));
#39292=CARTESIAN_POINT('Ctrl Pts',(12.3820424596137,0.0503385411035255,
3.37518438569388));
#39293=CARTESIAN_POINT('Ctrl Pts',(12.3661371809261,-0.172985920082391,
3.39750154186552));
#39294=CARTESIAN_POINT('Ctrl Pts',(12.3502319022385,-0.335654061078685,
3.50861693417539));
#39295=CARTESIAN_POINT('Ctrl Pts',(12.3343266235509,-0.498322202074975,
3.61973232648525));
#39296=CARTESIAN_POINT('Ctrl Pts',(12.3184213448632,-0.600334022881645,
3.81964595493332));
#39297=CARTESIAN_POINT('Ctrl Pts',(12.3025160661756,-0.594850011148503,
4.0165659389844));
#39298=CARTESIAN_POINT('Ctrl Pts',(12.286610787488,-0.58936599941536,4.21348592303547));
#39299=CARTESIAN_POINT('Ctrl Pts',(12.2707055088004,-0.476386155142398,
4.40741226268955));
#39300=CARTESIAN_POINT('Ctrl Pts',(12.2548002301128,-0.307786043036728,
4.50930218712431));
#39301=CARTESIAN_POINT('Ctrl Pts',(12.2461486238277,-0.216076754679914,
4.564724762732));
#39302=CARTESIAN_POINT('Ctrl Pts',(12.2374970175426,-0.107910718865932,
4.59291589733543));
#39303=CARTESIAN_POINT('Ctrl Pts',(12.2288454112576,0.000142795628640946,
4.59314744373127));
#39304=CARTESIAN_POINT('Ctrl Pts',(12.1211545887425,0.00052868291625318,
4.59430727435519));
#39305=CARTESIAN_POINT('Ctrl Pts',(12.1339057147434,-0.157940052872902,
4.59284257311225));
#39306=CARTESIAN_POINT('Ctrl Pts',(12.1466568407444,-0.317474678016714,
4.52751565545538));
#39307=CARTESIAN_POINT('Ctrl Pts',(12.1594079667453,-0.427372353356377,
4.41409399619463));
#39308=CARTESIAN_POINT('Ctrl Pts',(12.1753132454329,-0.564454612073754,
4.27261605145303));
#39309=CARTESIAN_POINT('Ctrl Pts',(12.1912185241205,-0.62430606291093,4.0563068416254));
#39310=CARTESIAN_POINT('Ctrl Pts',(12.2071238028081,-0.579445451749542,
3.8644864045766));
#39311=CARTESIAN_POINT('Ctrl Pts',(12.2230290814957,-0.534584840588155,
3.6726659675278));
#39312=CARTESIAN_POINT('Ctrl Pts',(12.2389343601834,-0.38501216742821,3.50533430325784));
#39313=CARTESIAN_POINT('Ctrl Pts',(12.254839638871,-0.199404875886796,3.43932303278057));
#39314=CARTESIAN_POINT('Ctrl Pts',(12.2707449175586,-0.0137975843453769,
3.37331176230329));
#39315=CARTESIAN_POINT('Ctrl Pts',(12.2866501962462,0.207844325577514,3.40862088561871));
#39316=CARTESIAN_POINT('Ctrl Pts',(12.3025554749338,0.363752265741203,3.52903794710619));
#39317=CARTESIAN_POINT('Ctrl Pts',(12.3184607536214,0.519660205904889,3.64945500859368));
#39318=CARTESIAN_POINT('Ctrl Pts',(12.334366032309,0.609834176309377,3.85498000825323));
#39319=CARTESIAN_POINT('Ctrl Pts',(12.3502713109967,0.592870104691008,4.05124456128685));
#39320=CARTESIAN_POINT('Ctrl Pts',(12.3661765896843,0.575906033072638,4.24750911432049));
#39321=CARTESIAN_POINT('Ctrl Pts',(12.3820818683719,0.451803919431404,4.4345132207282));
#39322=CARTESIAN_POINT('Ctrl Pts',(12.3979871470595,0.277546204023914,4.52639250633888));
#39323=CARTESIAN_POINT('Ctrl Pts',(12.4057096276205,0.192938958450368,4.57100260157974));
#39324=CARTESIAN_POINT('Ctrl Pts',(12.4134321081815,0.0965080911524262,
4.59318808505049));
#39325=CARTESIAN_POINT('Ctrl Pts',(12.4211545887425,4.74932194801069E-5,
4.59311952367199));
#39326=CARTESIAN_POINT('Origin',(4.,0.,4.));
#39327=CARTESIAN_POINT('',(12.8288454112576,0.000112157221815526,4.59505491513413));
#39328=CARTESIAN_POINT('',(12.7211545887425,-0.000546355209092884,4.59413239245978));
#39329=CARTESIAN_POINT('',(4.,-7.27562663373442E-17,4.5941));
#39330=CARTESIAN_POINT('Ctrl Pts',(12.8288454112576,0.000112157221815526,
4.59505491513413));
#39331=CARTESIAN_POINT('Ctrl Pts',(12.828360361794,0.00612048155630211,
4.59507046002904));
#39332=CARTESIAN_POINT('Ctrl Pts',(12.8278753123304,0.0121283652366354,
4.59498736156652));
#39333=CARTESIAN_POINT('Ctrl Pts',(12.8273902628668,0.0181332013859869,
4.59480429815638));
#39334=CARTESIAN_POINT('Ctrl Pts',(12.8114849841792,0.215038052543873,4.58880145767424));
#39335=CARTESIAN_POINT('Ctrl Pts',(12.7955797054916,0.408666038032992,4.47531104548453));
#39336=CARTESIAN_POINT('Ctrl Pts',(12.779674426804,0.510111378641258,4.30644305748136));
#39337=CARTESIAN_POINT('Ctrl Pts',(12.7637691481164,0.611556719249521,4.1375750694782));
#39338=CARTESIAN_POINT('Ctrl Pts',(12.7478638694288,0.620819414976937,3.9133295056616));
#39339=CARTESIAN_POINT('Ctrl Pts',(12.7319585907412,0.533646427817818,3.7366704418887));
#39340=CARTESIAN_POINT('Ctrl Pts',(12.7160533120536,0.446473440658691,3.56001137811579));
#39341=CARTESIAN_POINT('Ctrl Pts',(12.700148033366,0.26286477061301,3.43093881438659));
#39342=CARTESIAN_POINT('Ctrl Pts',(12.6842427546783,0.0671257511235207,
3.4087174113557));
#39343=CARTESIAN_POINT('Ctrl Pts',(12.6683374759907,-0.128613268365957,
3.38649600832481));
#39344=CARTESIAN_POINT('Ctrl Pts',(12.6524321973031,-0.336482637299241,
3.47112576599221));
#39345=CARTESIAN_POINT('Ctrl Pts',(12.6365269186155,-0.461037535689932,
3.62374828002683));
#39346=CARTESIAN_POINT('Ctrl Pts',(12.6206216399279,-0.585592434080627,
3.77637079406146));
#39347=CARTESIAN_POINT('Ctrl Pts',(12.6047163612403,-0.626832861928724,
3.9969860644633));
#39348=CARTESIAN_POINT('Ctrl Pts',(12.5888110825527,-0.565822959504995,
4.18429689252621));
#39349=CARTESIAN_POINT('Ctrl Pts',(12.5729058038651,-0.504813057081268,
4.37160772058911));
#39350=CARTESIAN_POINT('Ctrl Pts',(12.5570005251774,-0.341552824385721,
4.52561410631309));
#39351=CARTESIAN_POINT('Ctrl Pts',(12.5410952464898,-0.151004453301302,
4.57560283284656));
#39352=CARTESIAN_POINT('Ctrl Pts',(12.5370119680791,-0.102085973774189,
4.58843617527608));
#39353=CARTESIAN_POINT('Ctrl Pts',(12.5329286896683,-0.0513689988622793,
4.59441396466913));
#39354=CARTESIAN_POINT('Ctrl Pts',(12.5288454112576,-0.000545899910317726,
4.59395595168017));
#39355=CARTESIAN_POINT('Ctrl Pts',(12.4211545887425,4.74932194801069E-5,
4.59311952367199));
#39356=CARTESIAN_POINT('Ctrl Pts',(12.4293373868691,-0.102162877376194,
4.59304687552285));
#39357=CARTESIAN_POINT('Ctrl Pts',(12.4375201849957,-0.204406628577491,
4.5679880979308));
#39358=CARTESIAN_POINT('Ctrl Pts',(12.4457029831223,-0.292652646395614,
4.51814611323009));
#39359=CARTESIAN_POINT('Ctrl Pts',(12.4616082618099,-0.46418046423393,4.42126596969699));
#39360=CARTESIAN_POINT('Ctrl Pts',(12.4775135404976,-0.582822782736806,
4.23075121781716));
#39361=CARTESIAN_POINT('Ctrl Pts',(12.4934188191852,-0.594104068590283,
4.03407817163935));
#39362=CARTESIAN_POINT('Ctrl Pts',(12.5093240978728,-0.605385354443759,
3.83740512546155));
#39363=CARTESIAN_POINT('Ctrl Pts',(12.5252293765604,-0.509305607647849,
3.63457378498577));
#39364=CARTESIAN_POINT('Ctrl Pts',(12.541134655248,-0.34998058313236,3.51871572067214));
#39365=CARTESIAN_POINT('Ctrl Pts',(12.5570399339356,-0.19065555861687,3.4028576563585));
#39366=CARTESIAN_POINT('Ctrl Pts',(12.5729452126232,0.031914743618199,3.37397286820701));
#39367=CARTESIAN_POINT('Ctrl Pts',(12.5888504913108,0.215535456959467,3.44532402892222));
#39368=CARTESIAN_POINT('Ctrl Pts',(12.6047557699985,0.399156170300736,3.51667518963742));
#39369=CARTESIAN_POINT('Ctrl Pts',(12.6206610486861,0.543827294748204,3.68826229921932));
#39370=CARTESIAN_POINT('Ctrl Pts',(12.6365663273737,0.583121970486127,3.88129981619987));
#39371=CARTESIAN_POINT('Ctrl Pts',(12.6524716060613,0.622416646224052,4.07433733318042));
#39372=CARTESIAN_POINT('Ctrl Pts',(12.6683768847489,0.556334873252426,4.28882525755962));
#39373=CARTESIAN_POINT('Ctrl Pts',(12.6842821634365,0.415218606030559,4.42627980869829));
#39374=CARTESIAN_POINT('Ctrl Pts',(12.6965729718718,0.306170972122536,4.53249785050629));
#39375=CARTESIAN_POINT('Ctrl Pts',(12.7088637803072,0.152317016475741,4.59271595401221));
#39376=CARTESIAN_POINT('Ctrl Pts',(12.7211545887425,-0.000546355209092884,
4.59413239245978));
#39377=CARTESIAN_POINT('Origin',(4.,0.,4.));
#39378=CARTESIAN_POINT('',(13.1288454112576,0.000488576923893258,4.59361798633976));
#39379=CARTESIAN_POINT('',(13.0211545887425,0.000215375668158819,4.59498635240753));
#39380=CARTESIAN_POINT('',(4.,-7.27562663373442E-17,4.5941));
#39381=CARTESIAN_POINT('Ctrl Pts',(13.1288454112576,0.000488576923893258,
4.59361798633976));
#39382=CARTESIAN_POINT('Ctrl Pts',(13.1237920339197,0.0634769139372694,
4.59410397103046));
#39383=CARTESIAN_POINT('Ctrl Pts',(13.1187386565818,0.126326538027094,4.58487602541266));
#39384=CARTESIAN_POINT('Ctrl Pts',(13.1136852792439,0.185787091792062,4.56533540718874));
#39385=CARTESIAN_POINT('Ctrl Pts',(13.0977800005563,0.372936519850693,4.50383218710482));
#39386=CARTESIAN_POINT('Ctrl Pts',(13.0818747218686,0.526512210440984,4.34016674272733));
#39387=CARTESIAN_POINT('Ctrl Pts',(13.065969443181,0.575998703695535,4.14948732200047));
#39388=CARTESIAN_POINT('Ctrl Pts',(13.0500641644934,0.625485196950086,3.9588079012736));
#39389=CARTESIAN_POINT('Ctrl Pts',(13.0341588858058,0.570882492868891,3.74111450419737));
#39390=CARTESIAN_POINT('Ctrl Pts',(13.0182536071182,0.437261843116128,3.59636272886105));
#39391=CARTESIAN_POINT('Ctrl Pts',(13.0023483284306,0.303641193363369,3.45161095352474));
#39392=CARTESIAN_POINT('Ctrl Pts',(12.986443049743,0.0910025979390456,3.37980079992835));
#39393=CARTESIAN_POINT('Ctrl Pts',(12.9705377710554,-0.10301929613509,3.41390445256627));
#39394=CARTESIAN_POINT('Ctrl Pts',(12.9546324923678,-0.297041190209231,
3.4480081052042));
#39395=CARTESIAN_POINT('Ctrl Pts',(12.9387272136801,-0.472446382933184,
3.58802556407645));
#39396=CARTESIAN_POINT('Ctrl Pts',(12.9228219349925,-0.54869623058984,3.76966673571907));
#39397=CARTESIAN_POINT('Ctrl Pts',(12.9069166563049,-0.624946078246494,
3.95130790736168));
#39398=CARTESIAN_POINT('Ctrl Pts',(12.8910113776173,-0.602040580835857,
4.17457279177466));
#39399=CARTESIAN_POINT('Ctrl Pts',(12.8751060989297,-0.490496973717212,
4.33694759959386));
#39400=CARTESIAN_POINT('Ctrl Pts',(12.8596858697056,-0.382355015061345,
4.49437060399126));
#39401=CARTESIAN_POINT('Ctrl Pts',(12.8442656404816,-0.190898750836606,
4.59456072668396));
#39402=CARTESIAN_POINT('Ctrl Pts',(12.8288454112576,0.000112157221815526,
4.59505491513413));
#39403=CARTESIAN_POINT('Ctrl Pts',(12.7211545887425,-0.000546355209092884,
4.59413239245978));
#39404=CARTESIAN_POINT('Ctrl Pts',(12.7247690589948,-0.0455002825709059,
4.59454893744622));
#39405=CARTESIAN_POINT('Ctrl Pts',(12.7283835292471,-0.0903685417208244,
4.58988016539195));
#39406=CARTESIAN_POINT('Ctrl Pts',(12.7319979994994,-0.13398639330236,4.5798004937111));
#39407=CARTESIAN_POINT('Ctrl Pts',(12.747903278187,-0.325924363941296,4.53544544968711));
#39408=CARTESIAN_POINT('Ctrl Pts',(12.7638085568746,-0.493649543747071,
4.38631418374101));
#39409=CARTESIAN_POINT('Ctrl Pts',(12.7797138355622,-0.560149626020051,
4.20088146397168));
#39410=CARTESIAN_POINT('Ctrl Pts',(12.7956191142498,-0.626649708293032,
4.01544874420235));
#39411=CARTESIAN_POINT('Ctrl Pts',(12.8115243929374,-0.591924693033219,
3.79371457060979));
#39412=CARTESIAN_POINT('Ctrl Pts',(12.827429671625,-0.471918838153678,3.63748989490844));
#39413=CARTESIAN_POINT('Ctrl Pts',(12.8433349503126,-0.351912983274129,
3.48126521920708));
#39414=CARTESIAN_POINT('Ctrl Pts',(12.8592402290002,-0.146626288774854,
3.39055004139693));
#39415=CARTESIAN_POINT('Ctrl Pts',(12.8751455076879,0.0496822801939141,
3.40699693328572));
#39416=CARTESIAN_POINT('Ctrl Pts',(12.8910507863755,0.245990849162665,3.42344382517451));
#39417=CARTESIAN_POINT('Ctrl Pts',(12.9069560650631,0.433321292600904,3.54705278676224));
#39418=CARTESIAN_POINT('Ctrl Pts',(12.9228613437507,0.525659396179275,3.72106781235173));
#39419=CARTESIAN_POINT('Ctrl Pts',(12.9387666224383,0.617997499757654,3.89508283794124));
#39420=CARTESIAN_POINT('Ctrl Pts',(12.9546719011259,0.615343263476151,4.11950392753251));
#39421=CARTESIAN_POINT('Ctrl Pts',(12.9705771798135,0.518915400343756,4.29128641125856));
#39422=CARTESIAN_POINT('Ctrl Pts',(12.9864824585012,0.422487537211366,4.46306889498459));
#39423=CARTESIAN_POINT('Ctrl Pts',(13.0023877371888,0.232286047228094,4.58221277284539));
#39424=CARTESIAN_POINT('Ctrl Pts',(13.0182930158764,0.0356434078328121,
4.59401221668908));
#39425=CARTESIAN_POINT('Ctrl Pts',(13.0192468734984,0.0238505254767134,
4.59471984273368));
#39426=CARTESIAN_POINT('Ctrl Pts',(13.0202007311205,0.0120344772878951,
4.59504140054066));
#39427=CARTESIAN_POINT('Ctrl Pts',(13.0211545887425,0.000215375668158819,
4.59498635240753));
#39428=CARTESIAN_POINT('Origin',(4.,0.,4.));
#39429=CARTESIAN_POINT('',(13.4288454112576,-0.000323145728561625,4.59329116515504));
#39430=CARTESIAN_POINT('',(13.3211545887425,0.000436239896754628,4.59347700091179));
#39431=CARTESIAN_POINT('',(4.,-7.27562663373442E-17,4.5941));
#39432=CARTESIAN_POINT('Ctrl Pts',(13.4288454112576,-0.000323145728561625,
4.59329116515504));
#39433=CARTESIAN_POINT('Ctrl Pts',(13.4192237060453,0.11977362227264,4.59270025156928));
#39434=CARTESIAN_POINT('Ctrl Pts',(13.4096020008331,0.240190260834984,4.55734300206483));
#39435=CARTESIAN_POINT('Ctrl Pts',(13.3999802956209,0.338238798929947,4.48960747645051));
#39436=CARTESIAN_POINT('Ctrl Pts',(13.3840750169333,0.500319146323361,4.37763642888821));
#39437=CARTESIAN_POINT('Ctrl Pts',(13.3681697382457,0.601276083433826,4.17718801339723));
#39438=CARTESIAN_POINT('Ctrl Pts',(13.3522644595581,0.594754455875995,3.9802996620979));
#39439=CARTESIAN_POINT('Ctrl Pts',(13.3363591808704,0.588232828318166,3.78341131079859));
#39440=CARTESIAN_POINT('Ctrl Pts',(13.3204539021828,0.474232636092054,3.59008302369095));
#39441=CARTESIAN_POINT('Ctrl Pts',(13.3045486234952,0.305097944517489,3.48908297116948));
#39442=CARTESIAN_POINT('Ctrl Pts',(13.2886433448076,0.135963252942929,3.388082918648));
#39443=CARTESIAN_POINT('Ctrl Pts',(13.27273806612,-0.0883059379800925,3.3794111007127));
#39444=CARTESIAN_POINT('Ctrl Pts',(13.2568327874324,-0.264734703826722,
3.46704924928509));
#39445=CARTESIAN_POINT('Ctrl Pts',(13.2409275087448,-0.441163469673367,
3.55468739785749));
#39446=CARTESIAN_POINT('Ctrl Pts',(13.2250222300572,-0.569751810443623,
3.7386355129376));
#39447=CARTESIAN_POINT('Ctrl Pts',(13.2091169513696,-0.591457400179852,
3.9344324022836));
#39448=CARTESIAN_POINT('Ctrl Pts',(13.1932116726819,-0.613162989916079,
4.1302292916296));
#39449=CARTESIAN_POINT('Ctrl Pts',(13.1773063939943,-0.527985828618295,
4.33787495524147));
#39450=CARTESIAN_POINT('Ctrl Pts',(13.1614011153067,-0.375035665205916,
4.46202728915223));
#39451=CARTESIAN_POINT('Ctrl Pts',(13.150549213957,-0.270680367988337,4.54673431669939));
#39452=CARTESIAN_POINT('Ctrl Pts',(13.1396973126073,-0.134776053786733,
4.59257435599745));
#39453=CARTESIAN_POINT('Ctrl Pts',(13.1288454112576,0.000488576923893258,
4.59361798633976));
#39454=CARTESIAN_POINT('Ctrl Pts',(13.0211545887425,0.000215375668158819,
4.59498635240753));
#39455=CARTESIAN_POINT('Ctrl Pts',(13.0361060098081,-0.185045360160338,
4.59412349007018));
#39456=CARTESIAN_POINT('Ctrl Pts',(13.0510574308736,-0.371056311319581,
4.5007301079696));
#39457=CARTESIAN_POINT('Ctrl Pts',(13.0660088519392,-0.480360474535337,
4.35124746348123));
#39458=CARTESIAN_POINT('Ctrl Pts',(13.0819141306268,-0.596637928700896,
4.19222825660313));
#39459=CARTESIAN_POINT('Ctrl Pts',(13.0978194093145,-0.626109048224722,
3.96973483302036));
#39460=CARTESIAN_POINT('Ctrl Pts',(13.1137246880021,-0.555241941841719,
3.78592675992164));
#39461=CARTESIAN_POINT('Ctrl Pts',(13.1296299666897,-0.484374835458714,
3.60211868682292));
#39462=CARTESIAN_POINT('Ctrl Pts',(13.1455352453773,-0.313169503168878,
3.45699596420825));
#39463=CARTESIAN_POINT('Ctrl Pts',(13.1614405240649,-0.120236190459409,
3.4171928066662));
#39464=CARTESIAN_POINT('Ctrl Pts',(13.1773458027525,0.0726971222500488,
3.37738964912416));
#39465=CARTESIAN_POINT('Ctrl Pts',(13.1932510814401,0.287358415379145,3.44290605665475));
#39466=CARTESIAN_POINT('Ctrl Pts',(13.2091563601277,0.425184304693362,3.58365966669054));
#39467=CARTESIAN_POINT('Ctrl Pts',(13.2250616388154,0.563010194007583,3.72441327672633));
#39468=CARTESIAN_POINT('Ctrl Pts',(13.240966917503,0.624000679506934,3.94040408926733));
#39469=CARTESIAN_POINT('Ctrl Pts',(13.2568721961906,0.580151510544767,4.13245826101242));
#39470=CARTESIAN_POINT('Ctrl Pts',(13.2727774748782,0.536302341582597,4.32451243275751));
#39471=CARTESIAN_POINT('Ctrl Pts',(13.2886827535658,0.387613518158899,4.49262996370669));
#39472=CARTESIAN_POINT('Ctrl Pts',(13.3045880322534,0.202356657484476,4.55961839611428));
#39473=CARTESIAN_POINT('Ctrl Pts',(13.3101102177498,0.13803695776657,4.58287624384712));
#39474=CARTESIAN_POINT('Ctrl Pts',(13.3156324032461,0.0693092633201986,
4.59394375907155));
#39475=CARTESIAN_POINT('Ctrl Pts',(13.3211545887425,0.000436239896754628,
4.59347700091179));
#39476=CARTESIAN_POINT('Origin',(4.,0.,4.));
#39477=CARTESIAN_POINT('',(13.7288454112576,-0.000361622974213827,4.59480268714608));
#39478=CARTESIAN_POINT('',(13.6211545887425,-0.000396530615921017,4.59339874939382));
#39479=CARTESIAN_POINT('',(4.,-7.27562663373442E-17,4.5941));
#39480=CARTESIAN_POINT('Ctrl Pts',(13.7288454112576,-0.000361622974213827,
4.59480268714608));
#39481=CARTESIAN_POINT('Ctrl Pts',(13.714655378171,0.175608319374377,4.59354294412002));
#39482=CARTESIAN_POINT('Ctrl Pts',(13.7004653450845,0.352610168065205,4.51056419690263));
#39483=CARTESIAN_POINT('Ctrl Pts',(13.6862753119979,0.463013835099274,4.37381700684221));
#39484=CARTESIAN_POINT('Ctrl Pts',(13.6703700333103,0.586762742631886,4.22054025587244));
#39485=CARTESIAN_POINT('Ctrl Pts',(13.6544647546227,0.626840040937572,3.99971072753873));
#39486=CARTESIAN_POINT('Ctrl Pts',(13.6385594759351,0.564843930165024,3.81272399872504));
#39487=CARTESIAN_POINT('Ctrl Pts',(13.6226541972475,0.502847819392478,3.62573726991136));
#39488=CARTESIAN_POINT('Ctrl Pts',(13.6067489185599,0.338778299541704,3.4725933406177));
#39489=CARTESIAN_POINT('Ctrl Pts',(13.5908436398723,0.147969152919217,3.42360942419035));
#39490=CARTESIAN_POINT('Ctrl Pts',(13.5749383611846,-0.0428399937032757,
3.37462550776301));
#39491=CARTESIAN_POINT('Ctrl Pts',(13.559033082497,-0.260388767097474,3.42980160420198));
#39492=CARTESIAN_POINT('Ctrl Pts',(13.5431278038094,-0.404787974250376,
3.56380318433064));
#39493=CARTESIAN_POINT('Ctrl Pts',(13.5272225251218,-0.549187181403275,
3.6978047644593));
#39494=CARTESIAN_POINT('Ctrl Pts',(13.5113172464342,-0.620436822314871,
3.91063182827765));
#39495=CARTESIAN_POINT('Ctrl Pts',(13.4954119677466,-0.585822076202281,
4.10456319205082));
#39496=CARTESIAN_POINT('Ctrl Pts',(13.479506689059,-0.551207330089691,4.298494555824));
#39497=CARTESIAN_POINT('Ctrl Pts',(13.4636014103714,-0.410728196952908,
4.47353021955202));
#39498=CARTESIAN_POINT('Ctrl Pts',(13.4476961316837,-0.228886751546343,
4.54930121159921));
#39499=CARTESIAN_POINT('Ctrl Pts',(13.4414125582084,-0.15704808052867,4.57923546205676));
#39500=CARTESIAN_POINT('Ctrl Pts',(13.435128984733,-0.0787538239969463,
4.5936770685736));
#39501=CARTESIAN_POINT('Ctrl Pts',(13.4288454112576,-0.000323145728561625,
4.59329116515504));
#39502=CARTESIAN_POINT('Ctrl Pts',(13.3211545887425,0.000436239896754628,
4.59347700091179));
#39503=CARTESIAN_POINT('Ctrl Pts',(13.3315376819337,-0.129062311182503,
4.59259937855127));
#39504=CARTESIAN_POINT('Ctrl Pts',(13.341920775125,-0.259074650003773,4.55094414667863));
#39505=CARTESIAN_POINT('Ctrl Pts',(13.3523038683163,-0.361265427801182,
4.47287234722855));
#39506=CARTESIAN_POINT('Ctrl Pts',(13.3682091470039,-0.517805754487323,
4.35327853206923));
#39507=CARTESIAN_POINT('Ctrl Pts',(13.3841144256915,-0.609061509934468,
4.14823156788458));
#39508=CARTESIAN_POINT('Ctrl Pts',(13.4000197043791,-0.593131911953917,
3.95188034580653));
#39509=CARTESIAN_POINT('Ctrl Pts',(13.4159249830667,-0.577202313973367,
3.75552912372848));
#39510=CARTESIAN_POINT('Ctrl Pts',(13.4318302617543,-0.454087362565127,
3.56787364375704));
#39511=CARTESIAN_POINT('Ctrl Pts',(13.4477355404419,-0.280316234851803,
3.47507736324643));
#39512=CARTESIAN_POINT('Ctrl Pts',(13.4636408191295,-0.106545107138479,
3.38228108273583));
#39513=CARTESIAN_POINT('Ctrl Pts',(13.4795460978172,0.117882196879929,3.38434400168606));
#39514=CARTESIAN_POINT('Ctrl Pts',(13.4954513765048,0.2899181539344,3.48031891499009));
#39515=CARTESIAN_POINT('Ctrl Pts',(13.5113566551924,0.461954110988876,3.57629382829412));
#39516=CARTESIAN_POINT('Ctrl Pts',(13.52726193388,0.581598721079409,3.76618073595195));
#39517=CARTESIAN_POINT('Ctrl Pts',(13.5431672125676,0.593916240998451,3.96279160341967));
#39518=CARTESIAN_POINT('Ctrl Pts',(13.5590724912552,0.606233760917493,4.15940247088739));
#39519=CARTESIAN_POINT('Ctrl Pts',(13.5749777699428,0.511224190665043,4.362737298165));
#39520=CARTESIAN_POINT('Ctrl Pts',(13.5908830486304,0.352511905377589,4.47943333495374));
#39521=CARTESIAN_POINT('Ctrl Pts',(13.6009735620011,0.251822790258117,4.55346680161908));
#39522=CARTESIAN_POINT('Ctrl Pts',(13.6110640753718,0.125494626822297,4.59262991567553));
#39523=CARTESIAN_POINT('Ctrl Pts',(13.6211545887425,-0.000396530615921017,
4.59339874939382));
#39524=CARTESIAN_POINT('Origin',(4.,0.,4.));
#39525=CARTESIAN_POINT('',(14.0288454112576,0.000507412974116619,4.59441995931617));
#39526=CARTESIAN_POINT('',(13.9211545887425,-0.000275297881949146,4.59492513410986));
#39527=CARTESIAN_POINT('',(4.,-7.27562663373442E-17,4.5941));
#39528=CARTESIAN_POINT('Ctrl Pts',(14.0288454112576,0.000507412974116619,
4.59441995931617));
#39529=CARTESIAN_POINT('Ctrl Pts',(14.0259923289843,0.0359476882196221,
4.59474138052009));
#39530=CARTESIAN_POINT('Ctrl Pts',(14.0231392467111,0.0713355155074759,
4.59184535342408));
#39531=CARTESIAN_POINT('Ctrl Pts',(14.0202861644378,0.106106362061302,4.58554453803953));
#39532=CARTESIAN_POINT('Ctrl Pts',(14.0043808857502,0.299945849210873,4.55041893875697));
#39533=CARTESIAN_POINT('Ctrl Pts',(13.9884756070626,0.474610768799237,4.40947910659883));
#39534=CARTESIAN_POINT('Ctrl Pts',(13.972570328375,0.549902379214768,4.22743864981956));
#39535=CARTESIAN_POINT('Ctrl Pts',(13.9566650496873,0.625193989630293,4.04539819304031));
#39536=CARTESIAN_POINT('Ctrl Pts',(13.9407597709997,0.601112290873006,3.82225711163994));
#39537=CARTESIAN_POINT('Ctrl Pts',(13.9248544923121,0.488714580199595,3.66047234987686));
#39538=CARTESIAN_POINT('Ctrl Pts',(13.9089492136245,0.376316869526181,3.49868758811377));
#39539=CARTESIAN_POINT('Ctrl Pts',(13.8930439349369,0.175603146936639,3.39825914598798));
#39540=CARTESIAN_POINT('Ctrl Pts',(13.8771386562493,-0.0212673376532481,
3.40529951534663));
#39541=CARTESIAN_POINT('Ctrl Pts',(13.8612333775617,-0.218137822243141,
3.41233988470529));
#39542=CARTESIAN_POINT('Ctrl Pts',(13.8453280988741,-0.411165068833379,
3.52684906554841));
#39543=CARTESIAN_POINT('Ctrl Pts',(13.8294228201864,-0.511719132099071,
3.69624928651676));
#39544=CARTESIAN_POINT('Ctrl Pts',(13.8135175414988,-0.612273195364761,
3.8656495074851));
#39545=CARTESIAN_POINT('Ctrl Pts',(13.7976122628112,-0.62035407530591,4.08994076857866));
#39546=CARTESIAN_POINT('Ctrl Pts',(13.7817069841236,-0.532251373727382,
4.26613801168402));
#39547=CARTESIAN_POINT('Ctrl Pts',(13.765801705436,-0.44414867214885,4.44233525478938));
#39548=CARTESIAN_POINT('Ctrl Pts',(13.7498964267484,-0.259862389050636,
4.57043847990653));
#39549=CARTESIAN_POINT('Ctrl Pts',(13.7339911480608,-0.0640089891217576,
4.59162810566218));
#39550=CARTESIAN_POINT('Ctrl Pts',(13.7322759024597,-0.0428879079209441,
4.59391322201126));
#39551=CARTESIAN_POINT('Ctrl Pts',(13.7305606568586,-0.0216323041412813,
4.594954960835));
#39552=CARTESIAN_POINT('Ctrl Pts',(13.7288454112576,-0.000361622974213827,
4.59480268714608));
#39553=CARTESIAN_POINT('Ctrl Pts',(13.6211545887425,-0.000396530615921017,
4.59339874939382));
#39554=CARTESIAN_POINT('Ctrl Pts',(13.6269693540594,-0.0729426448807452,
4.59384179797573));
#39555=CARTESIAN_POINT('Ctrl Pts',(13.6327841193764,-0.145343639818557,
4.58153501668255));
#39556=CARTESIAN_POINT('Ctrl Pts',(13.6385988846933,-0.212609537044371,
4.5558040579697));
#39557=CARTESIAN_POINT('Ctrl Pts',(13.6545041633809,-0.396603693856438,
4.48542149789704));
#39558=CARTESIAN_POINT('Ctrl Pts',(13.6704094420685,-0.542177007158105,
4.31459913145184));
#39559=CARTESIAN_POINT('Ctrl Pts',(13.6863147207561,-0.582488370180261,
4.12177136240739));
#39560=CARTESIAN_POINT('Ctrl Pts',(13.7022199994437,-0.622799733202417,
3.92894359336294));
#39561=CARTESIAN_POINT('Ctrl Pts',(13.7181252781313,-0.557849145945042,
3.71411042171923));
#39562=CARTESIAN_POINT('Ctrl Pts',(13.734030556819,-0.417459170243993,3.57591415105311));
#39563=CARTESIAN_POINT('Ctrl Pts',(13.7499358355066,-0.277069194542941,
3.43771788038699));
#39564=CARTESIAN_POINT('Ctrl Pts',(13.7658411141942,-0.0612398303982075,
3.37615851069845));
#39565=CARTESIAN_POINT('Ctrl Pts',(13.7817463928818,0.130929209162332,3.41950150018632));
#39566=CARTESIAN_POINT('Ctrl Pts',(13.7976516715694,0.323098248722867,3.46284448967418));
#39567=CARTESIAN_POINT('Ctrl Pts',(13.813556950257,0.491606963699209,3.61108983833845));
#39568=CARTESIAN_POINT('Ctrl Pts',(13.8294622289446,0.559083281190044,3.79616955381596));
#39569=CARTESIAN_POINT('Ctrl Pts',(13.8453675076322,0.62655959868088,3.98124926929349));
#39570=CARTESIAN_POINT('Ctrl Pts',(13.8612727863198,0.593003518686204,4.20316335158427));
#39571=CARTESIAN_POINT('Ctrl Pts',(13.8771780650075,0.4738225734989,4.36001824251097));
#39572=CARTESIAN_POINT('Ctrl Pts',(13.8918369062525,0.363981395029584,4.50458099992985));
#39573=CARTESIAN_POINT('Ctrl Pts',(13.9064957474975,0.181409709145346,4.59388191268165));
#39574=CARTESIAN_POINT('Ctrl Pts',(13.9211545887425,-0.000275297881949146,
4.59492513410986));
#39575=CARTESIAN_POINT('Origin',(4.,0.,4.));
#39576=CARTESIAN_POINT('',(14.3288454112576,0.000109044058801022,4.5931342436645));
#39577=CARTESIAN_POINT('',(14.2211545887425,0.000537210645871958,4.59424369460725));
#39578=CARTESIAN_POINT('',(4.,-7.27562663373442E-17,4.5941));
#39579=CARTESIAN_POINT('Ctrl Pts',(14.3288454112576,0.000109044058801022,
4.5931342436645));
#39580=CARTESIAN_POINT('Ctrl Pts',(14.32142400111,0.0928032711674493,4.59328573107644));
#39581=CARTESIAN_POINT('Ctrl Pts',(14.3140025909624,0.185434358886594,4.57287353691408));
#39582=CARTESIAN_POINT('Ctrl Pts',(14.3065811808148,0.267539471941071,4.53154830171049));
#39583=CARTESIAN_POINT('Ctrl Pts',(14.2906759021272,0.443503969097433,4.44298165875801));
#39584=CARTESIAN_POINT('Ctrl Pts',(14.2747706234396,0.571121189235106,4.25835848700565));
#39585=CARTESIAN_POINT('Ctrl Pts',(14.258865344752,0.591794703906212,4.06244993615984));
#39586=CARTESIAN_POINT('Ctrl Pts',(14.2429600660644,0.612468218577319,3.86654138531401));
#39587=CARTESIAN_POINT('Ctrl Pts',(14.2270547873768,0.526198027781844,3.65934745537473));
#39588=CARTESIAN_POINT('Ctrl Pts',(14.2111495086891,0.372595753342289,3.53600283331781));
#39589=CARTESIAN_POINT('Ctrl Pts',(14.1952442300015,0.218993478902743,3.4126582112609));
#39590=CARTESIAN_POINT('Ctrl Pts',(14.1793389513139,-0.00194087918087354,
3.37316289708635));
#39591=CARTESIAN_POINT('Ctrl Pts',(14.1634336726263,-0.18876361063844,3.43565146815417));
#39592=CARTESIAN_POINT('Ctrl Pts',(14.1475283939387,-0.375586342096006,
3.49814003922198));
#39593=CARTESIAN_POINT('Ctrl Pts',(14.1316231152511,-0.528297446927522,
3.66261249553216));
#39594=CARTESIAN_POINT('Ctrl Pts',(14.1157178365635,-0.576778446468407,
3.85355004340287));
#39595=CARTESIAN_POINT('Ctrl Pts',(14.0998125578759,-0.625259446009293,
4.04448759127359));
#39596=CARTESIAN_POINT('Ctrl Pts',(14.0839072791882,-0.569510340259543,
4.26189023070484));
#39597=CARTESIAN_POINT('Ctrl Pts',(14.0680020005006,-0.435128760029281,
4.40593586721696));
#39598=CARTESIAN_POINT('Ctrl Pts',(14.0549498040863,-0.324852491748397,
4.52414265738481));
#39599=CARTESIAN_POINT('Ctrl Pts',(14.0418976076719,-0.161623710204441,
4.5929495310973));
#39600=CARTESIAN_POINT('Ctrl Pts',(14.0288454112576,0.000507412974116619,
4.59441995931617));
#39601=CARTESIAN_POINT('Ctrl Pts',(13.9211545887425,-0.000275297881949146,
4.59492513410986));
#39602=CARTESIAN_POINT('Ctrl Pts',(13.9224010261851,-0.015723926578741,
4.59501383895544));
#39603=CARTESIAN_POINT('Ctrl Pts',(13.9236474636277,-0.0311661445373128,
4.59446443570748));
#39604=CARTESIAN_POINT('Ctrl Pts',(13.9248939010703,-0.0465566941337027,
4.59325663951544));
#39605=CARTESIAN_POINT('Ctrl Pts',(13.9407991797579,-0.242949206199084,
4.5778444460306));
#39606=CARTESIAN_POINT('Ctrl Pts',(13.9567044584455,-0.430928419949921,
4.4552243594983));
#39607=CARTESIAN_POINT('Ctrl Pts',(13.9726097371331,-0.524182233176515,
4.28169833602613));
#39608=CARTESIAN_POINT('Ctrl Pts',(13.9885150158207,-0.617436046403107,
4.10817231255396));
#39609=CARTESIAN_POINT('Ctrl Pts',(14.0044202945084,-0.615964459105464,
3.88374035214192));
#39610=CARTESIAN_POINT('Ctrl Pts',(14.020325573196,-0.52044316191294,3.71145211607799));
#39611=CARTESIAN_POINT('Ctrl Pts',(14.0362308518836,-0.424921864720413,
3.53916388001405));
#39612=CARTESIAN_POINT('Ctrl Pts',(14.0521361305712,-0.235350857633014,
3.41901936829824));
#39613=CARTESIAN_POINT('Ctrl Pts',(14.0680414092588,-0.0387731270173405,
3.40618385781531));
#39614=CARTESIAN_POINT('Ctrl Pts',(14.0839466879464,0.157804603598333,3.39334834733239));
#39615=CARTESIAN_POINT('Ctrl Pts',(14.0998519666341,0.361389057742269,3.48782183808236));
#39616=CARTESIAN_POINT('Ctrl Pts',(14.1157572453217,0.478502867019537,3.64622609995664));
#39617=CARTESIAN_POINT('Ctrl Pts',(14.1316625240093,0.595616676296804,3.80463036183091));
#39618=CARTESIAN_POINT('Ctrl Pts',(14.1475678026969,0.626259840707404,4.02696539482948));
#39619=CARTESIAN_POINT('Ctrl Pts',(14.1634730813845,0.556362315559365,4.21114435801894));
#39620=CARTESIAN_POINT('Ctrl Pts',(14.1793783600721,0.486464790411328,4.3953233212084));
#39621=CARTESIAN_POINT('Ctrl Pts',(14.1952836387597,0.316026575704654,4.54134621458875));
#39622=CARTESIAN_POINT('Ctrl Pts',(14.2111889174473,0.123305688986428,4.58216550323889));
#39623=CARTESIAN_POINT('Ctrl Pts',(14.2145108078791,0.0830550475387342,
4.59069079896363));
#39624=CARTESIAN_POINT('Ctrl Pts',(14.2178326983108,0.0418324306113591,
4.59462708830176));
#39625=CARTESIAN_POINT('Ctrl Pts',(14.2211545887425,0.000537210645871958,
4.59424369460725));
#39626=CARTESIAN_POINT('Origin',(4.,0.,4.));
#39627=CARTESIAN_POINT('',(14.6288454112575,-0.000548182068839831,4.59401855345973));
#39628=CARTESIAN_POINT('',(14.5211545887425,1.28950532977596E-5,4.59311636453746));
#39629=CARTESIAN_POINT('',(4.,-7.27562663373442E-17,4.5941));
#39630=CARTESIAN_POINT('Ctrl Pts',(14.6288454112575,-0.000548182068839831,
4.59401855345973));
#39631=CARTESIAN_POINT('Ctrl Pts',(14.6168556732357,0.148643716013534,4.59265593252186));
#39632=CARTESIAN_POINT('Ctrl Pts',(14.6048659352138,0.29876355451001,4.53564313143304));
#39633=CARTESIAN_POINT('Ctrl Pts',(14.5928761971919,0.407080942069735,4.43405768361063));
#39634=CARTESIAN_POINT('Ctrl Pts',(14.5769709185042,0.55077200793829,4.29929703619113));
#39635=CARTESIAN_POINT('Ctrl Pts',(14.5610656398166,0.620899143473568,4.08609746938767));
#39636=CARTESIAN_POINT('Ctrl Pts',(14.545160361129,0.585262934872208,3.89235120454656));
#39637=CARTESIAN_POINT('Ctrl Pts',(14.5292550824414,0.549626726270847,3.69860493970543));
#39638=CARTESIAN_POINT('Ctrl Pts',(14.5133498037538,0.408227173532835,3.52431197682665));
#39639=CARTESIAN_POINT('Ctrl Pts',(14.4974445250662,0.225988969153725,3.44950027073699));
#39640=CARTESIAN_POINT('Ctrl Pts',(14.4815392463786,0.04375076477463,3.37468856464734));
#39641=CARTESIAN_POINT('Ctrl Pts',(14.465633967691,-0.179326091245555,3.39935811534679));
#39642=CARTESIAN_POINT('Ctrl Pts',(14.4497286890033,-0.340814144225853,
3.51218170883678));
#39643=CARTESIAN_POINT('Ctrl Pts',(14.4338234103157,-0.50230219720616,3.62500530232677));
#39644=CARTESIAN_POINT('Ctrl Pts',(14.4179181316281,-0.602201447146573,
3.82598293860731));
#39645=CARTESIAN_POINT('Ctrl Pts',(14.4020128529405,-0.594642384863179,
4.02283418976097));
#39646=CARTESIAN_POINT('Ctrl Pts',(14.3861075742529,-0.587083322579785,
4.21968544091462));
#39647=CARTESIAN_POINT('Ctrl Pts',(14.3702022955653,-0.47206594807259,4.4124103069414));
#39648=CARTESIAN_POINT('Ctrl Pts',(14.3542970168777,-0.302401373731467,
4.51251768287848));
#39649=CARTESIAN_POINT('Ctrl Pts',(14.3458131483376,-0.211902365642262,
4.565914912441));
#39650=CARTESIAN_POINT('Ctrl Pts',(14.3373292797976,-0.10585540495725,4.59296106912451));
#39651=CARTESIAN_POINT('Ctrl Pts',(14.3288454112576,0.000109044058801022,
4.5931342436645));
#39652=CARTESIAN_POINT('Ctrl Pts',(14.2211545887425,0.000537210645871958,
4.59424369460725));
#39653=CARTESIAN_POINT('Ctrl Pts',(14.2337379769984,-0.155889919212927,
4.59279139152499));
#39654=CARTESIAN_POINT('Ctrl Pts',(14.2463213652543,-0.313358837143528,
4.52935553548989));
#39655=CARTESIAN_POINT('Ctrl Pts',(14.2589047535102,-0.422984449084643,
4.4185751090669));
#39656=CARTESIAN_POINT('Ctrl Pts',(14.2748100321978,-0.561550141707708,
4.27854974232482));
#39657=CARTESIAN_POINT('Ctrl Pts',(14.2907153108854,-0.623677968224056,
4.06288332492072));
#39658=CARTESIAN_POINT('Ctrl Pts',(14.306620589573,-0.580841459108965,3.87060075163287));
#39659=CARTESIAN_POINT('Ctrl Pts',(14.3225258682606,-0.538004949993874,
3.67831817834502));
#39660=CARTESIAN_POINT('Ctrl Pts',(14.3384311469482,-0.390204105247342,
3.50941944917344));
#39661=CARTESIAN_POINT('Ctrl Pts',(14.3543364256359,-0.205302819838896,
3.44145571503774));
#39662=CARTESIAN_POINT('Ctrl Pts',(14.3702417043235,-0.0204015344304391,
3.37349198090203));
#39663=CARTESIAN_POINT('Ctrl Pts',(14.3861469830111,0.201600191639931,3.40646324180223));
#39664=CARTESIAN_POINT('Ctrl Pts',(14.4020522616987,0.358768557879186,3.52523048963197));
#39665=CARTESIAN_POINT('Ctrl Pts',(14.4179575403863,0.515936924118427,3.6439977374617));
#39666=CARTESIAN_POINT('Ctrl Pts',(14.4338628190739,0.608271930526566,3.84856097222098));
#39667=CARTESIAN_POINT('Ctrl Pts',(14.4497680977615,0.59337724853295,4.04499341086509));
#39668=CARTESIAN_POINT('Ctrl Pts',(14.4656733764491,0.578482566539332,4.2414258495092));
#39669=CARTESIAN_POINT('Ctrl Pts',(14.4815786551367,0.456358196143958,4.42972749203816));
#39670=CARTESIAN_POINT('Ctrl Pts',(14.4974839338244,0.283078481576349,4.52343819058819));
#39671=CARTESIAN_POINT('Ctrl Pts',(14.5053741521304,0.197118668938093,4.56992576768087));
#39672=CARTESIAN_POINT('Ctrl Pts',(14.5132643704364,0.0985699939877532,
4.59313537862966));
#39673=CARTESIAN_POINT('Ctrl Pts',(14.5211545887425,1.28950532977596E-5,
4.59311636453746));
#39674=CARTESIAN_POINT('Origin',(4.,0.,4.));
#39675=CARTESIAN_POINT('',(14.9288454112575,0.000149915246051877,4.59503491979621));
#39676=CARTESIAN_POINT('',(14.8211545887425,-0.000542004001680995,4.59419620878869));
#39677=CARTESIAN_POINT('',(4.,-7.27562663373442E-17,4.5941));
#39678=CARTESIAN_POINT('Ctrl Pts',(14.9288454112575,0.000149915246051877,
4.59503491979621));
#39679=CARTESIAN_POINT('Ctrl Pts',(14.9281926240489,0.00823674021970066,
4.59506221957623));
#39680=CARTESIAN_POINT('Ctrl Pts',(14.9275398368403,0.0163225255999611,
4.59491168338633));
#39681=CARTESIAN_POINT('Ctrl Pts',(14.9268870496317,0.0244008833477238,
4.59458015690877));
#39682=CARTESIAN_POINT('Ctrl Pts',(14.9109817709441,0.221231534471853,4.58650245417764));
#39683=CARTESIAN_POINT('Ctrl Pts',(14.8950764922565,0.413652681988333,4.47097768448731));
#39684=CARTESIAN_POINT('Ctrl Pts',(14.8791712135689,0.513312675625014,4.30104993462962));
#39685=CARTESIAN_POINT('Ctrl Pts',(14.8632659348813,0.612972669261697,4.13112218477192));
#39686=CARTESIAN_POINT('Ctrl Pts',(14.8473606561937,0.619871509018575,3.90679145474687));
#39687=CARTESIAN_POINT('Ctrl Pts',(14.831455377506,0.530841539545133,3.73106092513143));
#39688=CARTESIAN_POINT('Ctrl Pts',(14.8155500988184,0.441811570071688,3.55533039551599));
#39689=CARTESIAN_POINT('Ctrl Pts',(14.7996448201308,0.256852791367914,3.42820006631018));
#39690=CARTESIAN_POINT('Ctrl Pts',(14.7837395414432,0.0608904496539635,
3.40804280624462));
#39691=CARTESIAN_POINT('Ctrl Pts',(14.7678342627556,-0.135071892059981,
3.38788554617906));
#39692=CARTESIAN_POINT('Ctrl Pts',(14.751928984068,-0.342037796784102,3.47470135525375));
#39693=CARTESIAN_POINT('Ctrl Pts',(14.7360237053804,-0.464977277074429,
3.62862808681558));
#39694=CARTESIAN_POINT('Ctrl Pts',(14.7201184266927,-0.587916757364756,
3.78255481837741));
#39695=CARTESIAN_POINT('Ctrl Pts',(14.7042131480052,-0.62682981322129,4.00359247242638));
#39696=CARTESIAN_POINT('Ctrl Pts',(14.6883078693175,-0.56384921567034,4.19024990955517));
#39697=CARTESIAN_POINT('Ctrl Pts',(14.6724025906299,-0.500868618119389,
4.37690734668397));
#39698=CARTESIAN_POINT('Ctrl Pts',(14.6564973119423,-0.335994367160947,
4.52918456689258));
#39699=CARTESIAN_POINT('Ctrl Pts',(14.6405920332547,-0.144929743580805,
4.57716231297912));
#39700=CARTESIAN_POINT('Ctrl Pts',(14.636676492589,-0.097893704910838,4.5889734116427));
#39701=CARTESIAN_POINT('Ctrl Pts',(14.6327609519233,-0.0492704262804658,
4.59446355048005));
#39702=CARTESIAN_POINT('Ctrl Pts',(14.6288454112575,-0.000548182068839831,
4.59401855345973));
#39703=CARTESIAN_POINT('Ctrl Pts',(14.5211545887425,1.28950532977596E-5,
4.59311636453746));
#39704=CARTESIAN_POINT('Ctrl Pts',(14.5291696491241,-0.100103612291989,
4.59309704959697));
#39705=CARTESIAN_POINT('Ctrl Pts',(14.5371847095056,-0.200228812305367,
4.56910822985942));
#39706=CARTESIAN_POINT('Ctrl Pts',(14.5451997698872,-0.287175610734119,
4.52120162576233));
#39707=CARTESIAN_POINT('Ctrl Pts',(14.5611050485748,-0.459714929737158,
4.42613460781534));
#39708=CARTESIAN_POINT('Ctrl Pts',(14.5770103272624,-0.580358509003398,
4.23688081735026));
#39709=CARTESIAN_POINT('Ctrl Pts',(14.59291560595,-0.593711920942704,4.04033758828107));
#39710=CARTESIAN_POINT('Ctrl Pts',(14.6088208846377,-0.607065332882009,
3.84379435921188));
#39711=CARTESIAN_POINT('Ctrl Pts',(14.6247261633253,-0.513128577494387,
3.63996169153858));
#39712=CARTESIAN_POINT('Ctrl Pts',(14.6406314420129,-0.35503343871745,3.52243092280774));
#39713=CARTESIAN_POINT('Ctrl Pts',(14.6565367207005,-0.196938299940509,
3.40490015407689));
#39714=CARTESIAN_POINT('Ctrl Pts',(14.6724419993881,0.025315222225754,3.37367128428849));
#39715=CARTESIAN_POINT('Ctrl Pts',(14.6883472780757,0.209677713173688,3.44308328926485));
#39716=CARTESIAN_POINT('Ctrl Pts',(14.7042525567633,0.394040204121622,3.51249529424121));
#39717=CARTESIAN_POINT('Ctrl Pts',(14.720157835451,0.540511663851219,3.68254817398232));
#39718=CARTESIAN_POINT('Ctrl Pts',(14.7360631141386,0.581838594751101,3.87516084045512));
#39719=CARTESIAN_POINT('Ctrl Pts',(14.7519683928262,0.623165525650983,4.06777350692792));
#39720=CARTESIAN_POINT('Ctrl Pts',(14.7678736715138,0.559347927721136,4.2829459601324));
#39721=CARTESIAN_POINT('Ctrl Pts',(14.7837789502014,0.419688142031033,4.42188011275284));
#39722=CARTESIAN_POINT('Ctrl Pts',(14.7962374963817,0.310293146587505,4.53070672248707));
#39723=CARTESIAN_POINT('Ctrl Pts',(14.8086960425621,0.154364940471616,4.59275708529138));
#39724=CARTESIAN_POINT('Ctrl Pts',(14.8211545887425,-0.000542004001680995,
4.59419620878869));
#39725=CARTESIAN_POINT('Origin',(4.,0.,4.));
#39726=CARTESIAN_POINT('',(15.2288454112576,0.000471544078774977,4.59356550157774));
#39727=CARTESIAN_POINT('',(15.1211545887425,0.000250233060073018,4.59495282954609));
#39728=CARTESIAN_POINT('',(4.,-7.27562663373442E-17,4.5941));
#39729=CARTESIAN_POINT('Ctrl Pts',(15.2288454112576,0.000471544078774977,
4.59356550157774));
#39730=CARTESIAN_POINT('Ctrl Pts',(15.2236242961746,0.0655651715058866,
4.59404721416646));
#39731=CARTESIAN_POINT('Ctrl Pts',(15.2184031810917,0.130516835945995,4.58418155789741));
#39732=CARTESIAN_POINT('Ctrl Pts',(15.2131820660088,0.191734887706884,4.56334598510492));
#39733=CARTESIAN_POINT('Ctrl Pts',(15.1972767873211,0.378225734681762,4.49987379829874));
#39734=CARTESIAN_POINT('Ctrl Pts',(15.1813715086335,0.530068013118856,4.33459889729257));
#39735=CARTESIAN_POINT('Ctrl Pts',(15.1654662299459,0.577542172676889,4.143408524424));
#39736=CARTESIAN_POINT('Ctrl Pts',(15.1495609512583,0.625016332234921,3.95221815155542));
#39737=CARTESIAN_POINT('Ctrl Pts',(15.1336556725707,0.568122372913892,3.73511230682445));
#39738=CARTESIAN_POINT('Ctrl Pts',(15.1177503938831,0.432983593849097,3.59177680914072));
#39739=CARTESIAN_POINT('Ctrl Pts',(15.1018451151955,0.297844814784303,3.44844131145699));
#39740=CARTESIAN_POINT('Ctrl Pts',(15.0859398365078,0.0844612159757424,
3.37887616082051));
#39741=CARTESIAN_POINT('Ctrl Pts',(15.0700345578202,-0.109190481519281,
3.41502273134472));
#39742=CARTESIAN_POINT('Ctrl Pts',(15.0541292791326,-0.302842179014298,
3.45116930186893));
#39743=CARTESIAN_POINT('Ctrl Pts',(15.038224000445,-0.47676197519578,3.59302759355383));
#39744=CARTESIAN_POINT('Ctrl Pts',(15.0223187217574,-0.551093257596978,
3.77546228038711));
#39745=CARTESIAN_POINT('Ctrl Pts',(15.0064134430698,-0.625424539998176,
3.95789696722038));
#39746=CARTESIAN_POINT('Ctrl Pts',(14.9905081643822,-0.600167308619091,
4.18090804920204));
#39747=CARTESIAN_POINT('Ctrl Pts',(14.9746028856946,-0.486918615563658,
4.34209827230691));
#39748=CARTESIAN_POINT('Ctrl Pts',(14.9593503942156,-0.378317895025423,
4.49667289829699));
#39749=CARTESIAN_POINT('Ctrl Pts',(14.9440979027365,-0.188800216398263,
4.59439705548643));
#39750=CARTESIAN_POINT('Ctrl Pts',(14.9288454112575,0.000149915246051877,
4.59503491979621));
#39751=CARTESIAN_POINT('Ctrl Pts',(14.8211545887425,-0.000542004001680995,
4.59419620878869));
#39752=CARTESIAN_POINT('Ctrl Pts',(14.8246013212497,-0.0433979515083632,
4.5945943510493));
#39753=CARTESIAN_POINT('Ctrl Pts',(14.828048053757,-0.0861757330942537,
4.59035339483295));
#39754=CARTESIAN_POINT('Ctrl Pts',(14.8314947862642,-0.127868389248254,
4.58118038604969));
#39755=CARTESIAN_POINT('Ctrl Pts',(14.8474000649518,-0.320263161387096,
4.5388506546897));
#39756=CARTESIAN_POINT('Ctrl Pts',(14.8633053436395,-0.489550732214419,
4.39149533993331));
#39757=CARTESIAN_POINT('Ctrl Pts',(14.8792106223271,-0.558001411172811,
4.20677376822741));
#39758=CARTESIAN_POINT('Ctrl Pts',(14.8951159010147,-0.6264520901312,4.0220521965215));
#39759=CARTESIAN_POINT('Ctrl Pts',(14.9110211797023,-0.594065877220663,
3.79996436786608));
#39760=CARTESIAN_POINT('Ctrl Pts',(14.9269264583899,-0.475713151262041,
3.64248361741852));
#39761=CARTESIAN_POINT('Ctrl Pts',(14.9428317370775,-0.357360425303418,
3.48500286697096));
#39762=CARTESIAN_POINT('Ctrl Pts',(14.9587370157651,-0.153041186296697,
3.39212919473125));
#39763=CARTESIAN_POINT('Ctrl Pts',(14.9746422944528,0.0434298152403689,
3.40650626183085));
#39764=CARTESIAN_POINT('Ctrl Pts',(14.9905475731404,0.239900816777435,3.42088332893044));
#39765=CARTESIAN_POINT('Ctrl Pts',(15.006452851828,0.428523580844854,3.54251113536931));
#39766=CARTESIAN_POINT('Ctrl Pts',(15.0223581305156,0.522690514153935,3.71554333807889));
#39767=CARTESIAN_POINT('Ctrl Pts',(15.0382634092032,0.616857447463019,3.88857554078846));
#39768=CARTESIAN_POINT('Ctrl Pts',(15.0541686878908,0.616568550013756,4.11301213976874));
#39769=CARTESIAN_POINT('Ctrl Pts',(15.0700739665784,0.521956471292605,4.28580134389743));
#39770=CARTESIAN_POINT('Ctrl Pts',(15.085979245266,0.427344392571456,4.45859054802613));
#39771=CARTESIAN_POINT('Ctrl Pts',(15.1018845239536,0.238409132578427,4.57973235730324));
#39772=CARTESIAN_POINT('Ctrl Pts',(15.1177898026413,0.0419017695106382,
4.59360357799603));
#39773=CARTESIAN_POINT('Ctrl Pts',(15.1189113980083,0.0280446248267054,
4.59458173733358));
#39774=CARTESIAN_POINT('Ctrl Pts',(15.1200329933754,0.0141498265549413,
4.59502647517791));
#39775=CARTESIAN_POINT('Ctrl Pts',(15.1211545887425,0.000250233060073018,
4.59495282954609));
#39776=CARTESIAN_POINT('Origin',(4.,0.,4.));
#39777=CARTESIAN_POINT('',(15.5288454112575,-0.000350670266729247,4.59332700645389));
#39778=CARTESIAN_POINT('',(15.4211545887425,0.000414092275955974,4.59343115273787));
#39779=CARTESIAN_POINT('',(4.,-7.27562663373442E-17,4.5941));
#39780=CARTESIAN_POINT('Ctrl Pts',(15.5288454112575,-0.000350670266729247,
4.59332700645389));
#39781=CARTESIAN_POINT('Ctrl Pts',(15.5190559683003,0.121821298278883,4.59267222728074));
#39782=CARTESIAN_POINT('Ctrl Pts',(15.509266525343,0.244354036528086,4.55597946496206));
#39783=CARTESIAN_POINT('Ctrl Pts',(15.4994770823858,0.343380025451582,4.48601555964668));
#39784=CARTESIAN_POINT('Ctrl Pts',(15.4835718036982,0.504271299656008,4.37234255322809));
#39785=CARTESIAN_POINT('Ctrl Pts',(15.4676665250105,0.603110088323456,4.17084127710728));
#39786=CARTESIAN_POINT('Ctrl Pts',(15.4517612463229,0.594513801222153,3.97403259246294));
#39787=CARTESIAN_POINT('Ctrl Pts',(15.4358559676353,0.58591751412085,3.7772239078186));
#39788=CARTESIAN_POINT('Ctrl Pts',(15.4199506889477,0.469886151250777,3.58510781465072));
#39789=CARTESIAN_POINT('Ctrl Pts',(15.4040454102601,0.299696405559752,3.48589589518039));
#39790=CARTESIAN_POINT('Ctrl Pts',(15.3881401315725,0.129506659868722,3.38668397571006));
#39791=CARTESIAN_POINT('Ctrl Pts',(15.3722348528849,-0.0948414686432761,
3.38037622993726));
#39792=CARTESIAN_POINT('Ctrl Pts',(15.3563295741973,-0.270336810750117,
3.46986890786216));
#39793=CARTESIAN_POINT('Ctrl Pts',(15.3404242955096,-0.445832152856957,
3.55936158578705));
#39794=CARTESIAN_POINT('Ctrl Pts',(15.324519016822,-0.572474708558633,3.74465468740961));
#39795=CARTESIAN_POINT('Ctrl Pts',(15.3086137381344,-0.592115574081638,
3.94066945956945));
#39796=CARTESIAN_POINT('Ctrl Pts',(15.2927084594468,-0.611756439604643,
4.13668423172929));
#39797=CARTESIAN_POINT('Ctrl Pts',(15.2768031807592,-0.524395614948954,
4.3434206744264));
#39798=CARTESIAN_POINT('Ctrl Pts',(15.2608979020716,-0.370145494864779,
4.46595415947185));
#39799=CARTESIAN_POINT('Ctrl Pts',(15.2502137384669,-0.266529987624151,
4.54826443060822));
#39800=CARTESIAN_POINT('Ctrl Pts',(15.2395295748622,-0.13273198696893,4.59257975504152));
#39801=CARTESIAN_POINT('Ctrl Pts',(15.2288454112576,0.000471544078774977,
4.59356550157774));
#39802=CARTESIAN_POINT('Ctrl Pts',(15.1211545887425,0.000250233060073018,
4.59495282954609));
#39803=CARTESIAN_POINT('Ctrl Pts',(15.135938272063,-0.18295950063263,4.59398211075496));
#39804=CARTESIAN_POINT('Ctrl Pts',(15.1507219553836,-0.367002343096231,
4.50294888365168));
#39805=CARTESIAN_POINT('Ctrl Pts',(15.1655056387041,-0.476631971954554,
4.35629051265579));
#39806=CARTESIAN_POINT('Ctrl Pts',(15.1814109173917,-0.594578884209397,
4.19850559451431));
#39807=CARTESIAN_POINT('Ctrl Pts',(15.1973161960793,-0.626393242576541,
3.97633512612291));
#39808=CARTESIAN_POINT('Ctrl Pts',(15.2132214747669,-0.557467239648298,
3.79179038730953));
#39809=CARTESIAN_POINT('Ctrl Pts',(15.2291267534545,-0.488541236720055,
3.60724564849615));
#39810=CARTESIAN_POINT('Ctrl Pts',(15.2450320321422,-0.318874872496425,
3.46032663926078));
#39811=CARTESIAN_POINT('Ctrl Pts',(15.2609373108298,-0.126371763436977,
3.41849235301362));
#39812=CARTESIAN_POINT('Ctrl Pts',(15.2768425895174,0.0661313456224706,
3.37665806676646));
#39813=CARTESIAN_POINT('Ctrl Pts',(15.292747868205,0.281471199517752,3.4399085035075));
#39814=CARTESIAN_POINT('Ctrl Pts',(15.3086531468926,0.420772847618048,3.57920173859056));
#39815=CARTESIAN_POINT('Ctrl Pts',(15.3245584255802,0.560074495718348,3.71849497367363));
#39816=CARTESIAN_POINT('Ctrl Pts',(15.3404637042678,0.623337938023671,3.9338310070987));
#39817=CARTESIAN_POINT('Ctrl Pts',(15.3563689829554,0.581515278282945,4.12633664243329));
#39818=CARTESIAN_POINT('Ctrl Pts',(15.3722742616431,0.53969261854222,4.31884227776789));
#39819=CARTESIAN_POINT('Ctrl Pts',(15.3881795403307,0.392783856755445,4.48851751501199));
#39820=CARTESIAN_POINT('Ctrl Pts',(15.4040848190183,0.208243281137944,4.55745466359042));
#39821=CARTESIAN_POINT('Ctrl Pts',(15.4097747422597,0.142226097106806,4.58211610408423));
#39822=CARTESIAN_POINT('Ctrl Pts',(15.4154646655011,0.0713929250243718,
4.593885435962));
#39823=CARTESIAN_POINT('Ctrl Pts',(15.4211545887425,0.000414092275955974,
4.59343115273787));
#39824=CARTESIAN_POINT('Origin',(4.,0.,4.));
#39825=CARTESIAN_POINT('',(15.8288454112575,-0.000332254705457391,4.59484959654372));
#39826=CARTESIAN_POINT('',(15.7211545887425,-0.000419917270904514,4.59344262983929));
#39827=CARTESIAN_POINT('',(4.,-7.27562663373442E-17,4.5941));
#39828=CARTESIAN_POINT('Ctrl Pts',(15.8288454112575,-0.000332254705457391,
4.59484959654372));
#39829=CARTESIAN_POINT('Ctrl Pts',(15.814487640426,0.177680873019276,4.5936575613883));
#39830=CARTESIAN_POINT('Ctrl Pts',(15.8001298695944,0.356683508224643,4.50844978272675));
#39831=CARTESIAN_POINT('Ctrl Pts',(15.7857720987628,0.466927807092597,4.36891650689757));
#39832=CARTESIAN_POINT('Ctrl Pts',(15.7698668200752,0.589054446233417,4.21434406913608));
#39833=CARTESIAN_POINT('Ctrl Pts',(15.7539615413876,0.626802179063893,3.99310442736787));
#39834=CARTESIAN_POINT('Ctrl Pts',(15.7380562627,0.562838843643149,3.80678146521555));
#39835=CARTESIAN_POINT('Ctrl Pts',(15.7221509840123,0.498875508222402,3.62045850306322));
#39836=CARTESIAN_POINT('Ctrl Pts',(15.7062457053247,0.333201104550436,3.46905222052678));
#39837=CARTESIAN_POINT('Ctrl Pts',(15.6903404266371,0.141886309687413,3.42208197707538));
#39838=CARTESIAN_POINT('Ctrl Pts',(15.6744351479495,-0.0494284851756215,
3.37511173362399));
#39839=CARTESIAN_POINT('Ctrl Pts',(15.6585298692619,-0.266383671229707,
3.43257752925765));
#39840=CARTESIAN_POINT('Ctrl Pts',(15.6426245905743,-0.409362605655794,
3.5680935017987));
#39841=CARTESIAN_POINT('Ctrl Pts',(15.6267193118867,-0.552341540081869,
3.70360947433975));
#39842=CARTESIAN_POINT('Ctrl Pts',(15.6108140331991,-0.621344222879956,
3.9171756237882));
#39843=CARTESIAN_POINT('Ctrl Pts',(15.5949087545115,-0.584687541371933,
4.11073140955597));
#39844=CARTESIAN_POINT('Ctrl Pts',(15.5790034758238,-0.548030859863907,
4.30428719532377));
#39845=CARTESIAN_POINT('Ctrl Pts',(15.5630981971362,-0.405714814049763,
4.47783261741089));
#39846=CARTESIAN_POINT('Ctrl Pts',(15.5471929184486,-0.223084911271984,
4.55168296009627));
#39847=CARTESIAN_POINT('Ctrl Pts',(15.5410770827183,-0.152860773312716,
4.58007960584922));
#39848=CARTESIAN_POINT('Ctrl Pts',(15.5349612469879,-0.0766761255292402,
4.5937360717991));
#39849=CARTESIAN_POINT('Ctrl Pts',(15.5288454112575,-0.000350670266729247,
4.59332700645389));
#39850=CARTESIAN_POINT('Ctrl Pts',(15.4211545887425,0.000414092275955974,
4.59343115273787));
#39851=CARTESIAN_POINT('Ctrl Pts',(15.4313699441887,-0.12701715326484,4.59261555920332));
#39852=CARTESIAN_POINT('Ctrl Pts',(15.4415852996349,-0.254917899718674,
4.55240018390688));
#39853=CARTESIAN_POINT('Ctrl Pts',(15.4518006550811,-0.356261725310785,
4.47665348962993));
#39854=CARTESIAN_POINT('Ctrl Pts',(15.4677059337687,-0.514053766693778,
4.35871610717824));
#39855=CARTESIAN_POINT('Ctrl Pts',(15.4836112124564,-0.607465460011524,
4.15464228236211));
#39856=CARTESIAN_POINT('Ctrl Pts',(15.499516491144,-0.593606107615349,3.95813408188558));
#39857=CARTESIAN_POINT('Ctrl Pts',(15.5154217698316,-0.579746755219174,
3.76162588140906));
#39858=CARTESIAN_POINT('Ctrl Pts',(15.5313270485192,-0.458616357109098,
3.57268330527213));
#39859=CARTESIAN_POINT('Ctrl Pts',(15.5472323272068,-0.285832867492734,
3.47806079093568));
#39860=CARTESIAN_POINT('Ctrl Pts',(15.5631376058944,-0.113049377876356,
3.38343827659922));
#39861=CARTESIAN_POINT('Ctrl Pts',(15.579042884582,0.111387203246309,3.38313582406324));
#39862=CARTESIAN_POINT('Ctrl Pts',(15.5949481632696,0.284425092952457,3.47729230673655));
#39863=CARTESIAN_POINT('Ctrl Pts',(15.6108534419572,0.457462982658595,3.57144878940986));
#39864=CARTESIAN_POINT('Ctrl Pts',(15.6267587206449,0.579102180948212,3.76006420729246));
#39865=CARTESIAN_POINT('Ctrl Pts',(15.6426639993325,0.593491114096805,3.95653434015292));
#39866=CARTESIAN_POINT('Ctrl Pts',(15.6585692780201,0.607880047245398,4.15300447301339));
#39867=CARTESIAN_POINT('Ctrl Pts',(15.6744745567077,0.515018715252963,4.35732932085173));
#39868=CARTESIAN_POINT('Ctrl Pts',(15.6903798353953,0.357545113131455,4.47569155781202));
#39869=CARTESIAN_POINT('Ctrl Pts',(15.700638086511,0.255981111243369,4.55203033647815));
#39870=CARTESIAN_POINT('Ctrl Pts',(15.7108963376268,0.127540214881222,4.59261107697802));
#39871=CARTESIAN_POINT('Ctrl Pts',(15.7211545887425,-0.000419917270904514,
4.59344262983929));
#39872=CARTESIAN_POINT('Origin',(4.,0.,4.));
#39873=CARTESIAN_POINT('',(16.1288454112575,0.000520203518568921,4.59435747030618));
#39874=CARTESIAN_POINT('',(16.0211545887425,-0.00024144267326323,4.59496181546483));
#39875=CARTESIAN_POINT('',(4.,-7.27562663373442E-17,4.5941));
#39876=CARTESIAN_POINT('Ctrl Pts',(16.1288454112575,0.000520203518568921,
4.59435747030618));
#39877=CARTESIAN_POINT('Ctrl Pts',(16.1258245912393,0.0380542554257849,
4.59470210862833));
#39878=CARTESIAN_POINT('Ctrl Pts',(16.122803771221,0.0755288363057283,4.59145263304759));
#39879=CARTESIAN_POINT('Ctrl Pts',(16.1197829512027,0.112271568866026,4.58439375503351));
#39880=CARTESIAN_POINT('Ctrl Pts',(16.1038776725151,0.305730099191281,4.54722721702202));
#39881=CARTESIAN_POINT('Ctrl Pts',(16.0879723938275,0.478899942385972,4.40445440507416));
#39882=CARTESIAN_POINT('Ctrl Pts',(16.0720671151398,0.55226883266698,4.22163055421683));
#39883=CARTESIAN_POINT('Ctrl Pts',(16.0561618364522,0.625637722947984,4.03880670335952));
#39884=CARTESIAN_POINT('Ctrl Pts',(16.0402565577646,0.599205660315318,3.81593181359275));
#39885=CARTESIAN_POINT('Ctrl Pts',(16.024351279077,0.485109129681553,3.65534060523843));
#39886=CARTESIAN_POINT('Ctrl Pts',(16.0084460003894,0.371012599047788,3.4947493968841));
#39887=CARTESIAN_POINT('Ctrl Pts',(15.9925407217018,0.169251600412921,3.39644186994223));
#39888=CARTESIAN_POINT('Ctrl Pts',(15.9766354430142,-0.0275337514538456,
3.40555668173602));
#39889=CARTESIAN_POINT('Ctrl Pts',(15.9607301643265,-0.224319103320618,
3.41467149352982));
#39890=CARTESIAN_POINT('Ctrl Pts',(15.9448248856389,-0.416128808419276,
3.53120864405929));
#39891=CARTESIAN_POINT('Ctrl Pts',(15.9289196069513,-0.514891964967956,
3.70165920408156));
#39892=CARTESIAN_POINT('Ctrl Pts',(15.9130143282637,-0.613655121516638,
3.87210976410384));
#39893=CARTESIAN_POINT('Ctrl Pts',(15.8971090495761,-0.619371729515322,
4.09647373361892));
#39894=CARTESIAN_POINT('Ctrl Pts',(15.8812037708885,-0.52941696442075,4.27173266988224));
#39895=CARTESIAN_POINT('Ctrl Pts',(15.8652984922009,-0.439462199326184,
4.44699160614554));
#39896=CARTESIAN_POINT('Ctrl Pts',(15.8493932135132,-0.25383606113837,4.57314550915708));
#39897=CARTESIAN_POINT('Ctrl Pts',(15.8334879348256,-0.0577702193188812,
4.59226984378546));
#39898=CARTESIAN_POINT('Ctrl Pts',(15.8319404269696,-0.0386939468137543,
4.59413055045147));
#39899=CARTESIAN_POINT('Ctrl Pts',(15.8303929191136,-0.0195188482833839,
4.59497807636063));
#39900=CARTESIAN_POINT('Ctrl Pts',(15.8288454112575,-0.000332254705457391,
4.59484959654372));
#39901=CARTESIAN_POINT('Ctrl Pts',(15.7211545887425,-0.000419917270904514,
4.59344262983929));
#39902=CARTESIAN_POINT('Ctrl Pts',(15.7268016163144,-0.0708602278282204,
4.59390038836772));
#39903=CARTESIAN_POINT('Ctrl Pts',(15.7324486438863,-0.141154849878182,
4.58231274148771));
#39904=CARTESIAN_POINT('Ctrl Pts',(15.7380956714582,-0.206740066761224,
4.55801389847688));
#39905=CARTESIAN_POINT('Ctrl Pts',(15.7540009501458,-0.391465772281827,
4.48957437609924));
#39906=CARTESIAN_POINT('Ctrl Pts',(15.7699062288334,-0.538831311072463,
4.32029570526172));
#39907=CARTESIAN_POINT('Ctrl Pts',(15.785811507521,-0.58117266224226,4.12790349002296));
#39908=CARTESIAN_POINT('Ctrl Pts',(15.8017167862086,-0.62351401341206,3.93551127478418));
#39909=CARTESIAN_POINT('Ctrl Pts',(15.8176220648962,-0.560831176961022,
3.72000551514415));
#39910=CARTESIAN_POINT('Ctrl Pts',(15.8335273435838,-0.421905459495345,
3.58033733863277));
#39911=CARTESIAN_POINT('Ctrl Pts',(15.8494326222715,-0.282979742029676,
3.44066916212139));
#39912=CARTESIAN_POINT('Ctrl Pts',(15.8653379009591,-0.0678111435493865,
3.37683856873865));
#39913=CARTESIAN_POINT('Ctrl Pts',(15.8812431796467,0.124804018556085,3.41815386651619));
#39914=CARTESIAN_POINT('Ctrl Pts',(15.8971484583343,0.317419180661557,3.45946916429373));
#39915=CARTESIAN_POINT('Ctrl Pts',(15.9130537370219,0.487480906392202,3.60593035323155));
#39916=CARTESIAN_POINT('Ctrl Pts',(15.9289590157095,0.556904046010802,3.79028865163133));
#39917=CARTESIAN_POINT('Ctrl Pts',(15.9448642943971,0.6263271856294,3.9746469500311));
#39918=CARTESIAN_POINT('Ctrl Pts',(15.9607695730847,0.595111739135951,4.19690235789283));
#39919=CARTESIAN_POINT('Ctrl Pts',(15.9766748517723,0.477590518943614,4.35500459477727));
#39920=CARTESIAN_POINT('Ctrl Pts',(15.9915014307624,0.368039615220995,4.50238430120742));
#39921=CARTESIAN_POINT('Ctrl Pts',(16.0063280097524,0.18349252241573,4.59401752470064));
#39922=CARTESIAN_POINT('Ctrl Pts',(16.0211545887425,-0.00024144267326323,
4.59496181546483));
#39923=CARTESIAN_POINT('Origin',(4.,0.,4.));
#39924=CARTESIAN_POINT('',(16.4288454112575,7.48704377684928E-5,4.59312461313858));
#39925=CARTESIAN_POINT('',(16.3211545887425,0.000543344619121817,4.59417988242975));
#39926=CARTESIAN_POINT('',(4.,-7.27562663373442E-17,4.5941));
#39927=CARTESIAN_POINT('Ctrl Pts',(16.4288454112575,7.48704377684928E-5,
4.59312461313858));
#39928=CARTESIAN_POINT('Ctrl Pts',(16.4212562633649,0.0948679978941589,
4.5932308806522));
#39929=CARTESIAN_POINT('Ctrl Pts',(16.4136671154723,0.189615837117123,4.57184094704105));
#39930=CARTESIAN_POINT('Ctrl Pts',(16.4060779675797,0.273126642574496,4.52869916135151));
#39931=CARTESIAN_POINT('Ctrl Pts',(16.3901726888921,0.448147956300534,4.43828293357696));
#39932=CARTESIAN_POINT('Ctrl Pts',(16.3742674102045,0.573812330828296,4.25232504748949));
#39933=CARTESIAN_POINT('Ctrl Pts',(16.3583621315169,0.592420001795879,4.05620949715111));
#39934=CARTESIAN_POINT('Ctrl Pts',(16.3424568528292,0.611027672763462,3.86009394681272));
#39935=CARTESIAN_POINT('Ctrl Pts',(16.3265515741416,0.522578640170867,3.6538207322234));
#39936=CARTESIAN_POINT('Ctrl Pts',(16.310646295454,0.367684957814641,3.53210178682255));
#39937=CARTESIAN_POINT('Ctrl Pts',(16.2947410167664,0.212791275458425,3.4103828414217));
#39938=CARTESIAN_POINT('Ctrl Pts',(16.2788357380788,-0.00854705666138705,
3.3732181652093));
#39939=CARTESIAN_POINT('Ctrl Pts',(16.2629304593912,-0.19470084048803,3.43767220519428));
#39940=CARTESIAN_POINT('Ctrl Pts',(16.2470251807036,-0.380854624314662,
3.50212624517926));
#39941=CARTESIAN_POINT('Ctrl Pts',(16.231119902016,-0.531823859848111,3.66819900136163));
#39942=CARTESIAN_POINT('Ctrl Pts',(16.2152146233283,-0.578289861113055,
3.85963689006134));
#39943=CARTESIAN_POINT('Ctrl Pts',(16.1993093446407,-0.624755862378002,
4.05107477876107));
#39944=CARTESIAN_POINT('Ctrl Pts',(16.1834040659531,-0.566718629374431,
4.26787779997815));
#39945=CARTESIAN_POINT('Ctrl Pts',(16.1674987872655,-0.430826404144746,
4.41049917854914));
#39946=CARTESIAN_POINT('Ctrl Pts',(16.1546143285962,-0.320743594918802,
4.52603310245269));
#39947=CARTESIAN_POINT('Ctrl Pts',(16.1417298699269,-0.159570744489656,
4.592887512417));
#39948=CARTESIAN_POINT('Ctrl Pts',(16.1288454112575,0.000520203518568921,
4.59435747030618));
#39949=CARTESIAN_POINT('Ctrl Pts',(16.0211545887425,-0.00024144267326323,
4.59496181546483));
#39950=CARTESIAN_POINT('Ctrl Pts',(16.0222332884401,-0.0136089074611732,
4.59503051682625));
#39951=CARTESIAN_POINT('Ctrl Pts',(16.0233119881376,-0.0269720681925484,
4.59461918253551));
#39952=CARTESIAN_POINT('Ctrl Pts',(16.0243906878352,-0.0403017303441999,
4.59371435609144));
#39953=CARTESIAN_POINT('Ctrl Pts',(16.0402959665228,-0.236845765548457,
4.58037281461397));
#39954=CARTESIAN_POINT('Ctrl Pts',(16.0562012452104,-0.426106842065734,
4.45974066575184));
#39955=CARTESIAN_POINT('Ctrl Pts',(16.072106523898,-0.521184280535122,4.2872070887372));
#39956=CARTESIAN_POINT('Ctrl Pts',(16.0880118025856,-0.616261719004504,
4.11467351172257));
#39957=CARTESIAN_POINT('Ctrl Pts',(16.1039170812732,-0.61715551942601,3.89023850655542));
#39958=CARTESIAN_POINT('Ctrl Pts',(16.1198223599609,-0.523455286459661,
3.71695313254649));
#39959=CARTESIAN_POINT('Ctrl Pts',(16.1357276386485,-0.429755053493313,
3.54366775853756));
#39960=CARTESIAN_POINT('Ctrl Pts',(16.1516329173361,-0.241460787139106,
3.42153201568684));
#39961=CARTESIAN_POINT('Ctrl Pts',(16.1675381960237,-0.045029248433429,
3.40662546997421));
#39962=CARTESIAN_POINT('Ctrl Pts',(16.1834434747113,0.151402290272254,3.39171892426158));
#39963=CARTESIAN_POINT('Ctrl Pts',(16.1993487533989,0.355971101329402,3.48404157568705));
#39964=CARTESIAN_POINT('Ctrl Pts',(16.2152540320865,0.474747841293266,3.64120276856532));
#39965=CARTESIAN_POINT('Ctrl Pts',(16.2311593107741,0.593524581257127,3.79836396144359));
#39966=CARTESIAN_POINT('Ctrl Pts',(16.2470645894618,0.626509250127697,4.02036369577466));
#39967=CARTESIAN_POINT('Ctrl Pts',(16.2629698681494,0.558556683425868,4.20526908558792));
#39968=CARTESIAN_POINT('Ctrl Pts',(16.278875146837,0.490604116724039,4.39017447540119));
#39969=CARTESIAN_POINT('Ctrl Pts',(16.2947804255246,0.32171431444981,4.53798552069667));
#39970=CARTESIAN_POINT('Ctrl Pts',(16.3106857042122,0.129434328669215,4.58083364284428));
#39971=CARTESIAN_POINT('Ctrl Pts',(16.314175332389,0.0872479785030607,4.5902345478711));
#39972=CARTESIAN_POINT('Ctrl Pts',(16.3176649605657,0.0439357035691123,
4.5945828907904));
#39973=CARTESIAN_POINT('Ctrl Pts',(16.3211545887425,0.000543344619121817,
4.59417988242975));
#39974=CARTESIAN_POINT('Origin',(4.,0.,4.));
#39975=CARTESIAN_POINT('',(16.7288454112575,-0.000548108868865471,4.59408180714414));
#39976=CARTESIAN_POINT('',(16.6211545887425,-2.1752937549985E-5,4.5931168278739));
#39977=CARTESIAN_POINT('',(4.,-7.27562663373442E-17,4.5941));
#39978=CARTESIAN_POINT('Ctrl Pts',(16.7288454112575,-0.000548108868865471,
4.59408180714414));
#39979=CARTESIAN_POINT('Ctrl Pts',(16.7166879354906,0.15068989439403,4.59268722311157));
#39980=CARTESIAN_POINT('Ctrl Pts',(16.7045304597237,0.302891836883802,4.53390177381835));
#39981=CARTESIAN_POINT('Ctrl Pts',(16.6923729839567,0.411632901649024,4.42974331917764));
#39982=CARTESIAN_POINT('Ctrl Pts',(16.6764677052691,0.553895734249677,4.29347578465895));
#39983=CARTESIAN_POINT('Ctrl Pts',(16.6605624265815,0.621772048174623,4.07954898308531));
#39984=CARTESIAN_POINT('Ctrl Pts',(16.6446571478939,0.58409591167956,3.88618905124272));
#39985=CARTESIAN_POINT('Ctrl Pts',(16.6287518692063,0.546419775184499,3.69282911940014));
#39986=CARTESIAN_POINT('Ctrl Pts',(16.6128465905187,0.403191188269443,3.52003605728863));
#39987=CARTESIAN_POINT('Ctrl Pts',(16.596941311831,0.220174658543969,3.44714912875817));
#39988=CARTESIAN_POINT('Ctrl Pts',(16.5810360331434,0.0371581288184754,
3.37426220022769));
#39989=CARTESIAN_POINT('Ctrl Pts',(16.5651307544558,-0.185646343717467,
3.40128140527831));
#39990=CARTESIAN_POINT('Ctrl Pts',(16.5492254757682,-0.34593637135519,3.51580066803907));
#39991=CARTESIAN_POINT('Ctrl Pts',(16.5333201970806,-0.506226398992903,
3.63031993079982));
#39992=CARTESIAN_POINT('Ctrl Pts',(16.517414918393,-0.604001981732426,3.83233925127069));
#39993=CARTESIAN_POINT('Ctrl Pts',(16.5015096397054,-0.594368708523554,
4.02909990422408));
#39994=CARTESIAN_POINT('Ctrl Pts',(16.4856043610178,-0.584735435314682,
4.22586055717748));
#39995=CARTESIAN_POINT('Ctrl Pts',(16.4696990823301,-0.467693306157413,
4.4173625426134));
#39996=CARTESIAN_POINT('Ctrl Pts',(16.4537938036425,-0.296983115116624,
4.51567625060054));
#39997=CARTESIAN_POINT('Ctrl Pts',(16.4454776728475,-0.20772669247752,4.56707991793767));
#39998=CARTESIAN_POINT('Ctrl Pts',(16.4371615420525,-0.103798720846626,
4.59300816600183));
#39999=CARTESIAN_POINT('Ctrl Pts',(16.4288454112575,7.48704377684928E-5,
4.59312461313858));
#40000=CARTESIAN_POINT('Ctrl Pts',(16.3211545887425,0.000543344619121817,
4.59417988242975));
#40001=CARTESIAN_POINT('Ctrl Pts',(16.3335702392533,-0.153841115924154,
4.59274603025257));
#40002=CARTESIAN_POINT('Ctrl Pts',(16.3459858897642,-0.309239316255332,
4.53116741914846));
#40003=CARTESIAN_POINT('Ctrl Pts',(16.3584015402751,-0.418549561707542,
4.42300972860235));
#40004=CARTESIAN_POINT('Ctrl Pts',(16.3743068189627,-0.558583297016706,
4.28445249321304));
#40005=CARTESIAN_POINT('Ctrl Pts',(16.3902120976503,-0.622980598348072,
4.06945282343469));
#40006=CARTESIAN_POINT('Ctrl Pts',(16.4061173763379,-0.582172949355422,
3.87672947174358));
#40007=CARTESIAN_POINT('Ctrl Pts',(16.4220226550255,-0.541365300362771,
3.68400612005246));
#40008=CARTESIAN_POINT('Ctrl Pts',(16.4379279337131,-0.395352701046104,
3.5135590864486));
#40009=CARTESIAN_POINT('Ctrl Pts',(16.4538332124007,-0.211177959727979,
3.44365043774355));
#40010=CARTESIAN_POINT('Ctrl Pts',(16.4697384910883,-0.0270032184098532,
3.37374178903851));
#40011=CARTESIAN_POINT('Ctrl Pts',(16.485643769776,0.195333664909731,3.40437152523229));
#40012=CARTESIAN_POINT('Ctrl Pts',(16.5015490484636,0.353744999708243,3.52147576730199));
#40013=CARTESIAN_POINT('Ctrl Pts',(16.5174543271512,0.512156334506764,3.63858000937169));
#40014=CARTESIAN_POINT('Ctrl Pts',(16.5333596058388,0.606642120784206,3.84215875731731));
#40015=CARTESIAN_POINT('Ctrl Pts',(16.5492648845264,0.59381848284593,4.03873726278877));
#40016=CARTESIAN_POINT('Ctrl Pts',(16.565170163214,0.580994844907655,4.23531576826023));
#40017=CARTESIAN_POINT('Ctrl Pts',(16.5810754419016,0.460861782753675,4.42489403125753));
#40018=CARTESIAN_POINT('Ctrl Pts',(16.5969807205892,0.288579316114369,4.52042573380721));
#40019=CARTESIAN_POINT('Ctrl Pts',(16.6050386766403,0.201297315476928,4.56882414767653));
#40020=CARTESIAN_POINT('Ctrl Pts',(16.6130966326914,0.100630370301649,4.59308406930439));
#40021=CARTESIAN_POINT('Ctrl Pts',(16.6211545887425,-2.1752937549985E-5,
4.5931168278739));
#40022=CARTESIAN_POINT('Origin',(4.,0.,4.));
#40023=CARTESIAN_POINT('',(17.0288454112575,0.000186802344652959,4.59500977980842));
#40024=CARTESIAN_POINT('',(16.9211545887425,-0.000535257393875686,4.59425998651214));
#40025=CARTESIAN_POINT('',(4.,-7.27562663373442E-17,4.5941));
#40026=CARTESIAN_POINT('Ctrl Pts',(17.0288454112575,0.000186802344652959,
4.59500977980842));
#40027=CARTESIAN_POINT('Ctrl Pts',(17.0280248863039,0.0103527338555297,
4.59505157132578));
#40028=CARTESIAN_POINT('Ctrl Pts',(17.0272043613502,0.0205166685362397,
4.5948136789481));
#40029=CARTESIAN_POINT('Ctrl Pts',(17.0263838363966,0.0306658549750798,
4.59428997251885));
#40030=CARTESIAN_POINT('Ctrl Pts',(17.010478557709,0.227400443050786,4.58413830477164));
#40031=CARTESIAN_POINT('Ctrl Pts',(16.9945732790214,0.418593379366704,4.46659200952389));
#40032=CARTESIAN_POINT('Ctrl Pts',(16.9786680003338,0.516456956272638,4.29562337257973));
#40033=CARTESIAN_POINT('Ctrl Pts',(16.9627627216462,0.614320533178566,4.12465473563558));
#40034=CARTESIAN_POINT('Ctrl Pts',(16.9468574429585,0.618854750674521,3.90026375699502));
#40035=CARTESIAN_POINT('Ctrl Pts',(16.9309521642709,0.527977687913284,3.72548128085037));
#40036=CARTESIAN_POINT('Ctrl Pts',(16.9150468855833,0.437100625152047,3.55069880470573));
#40037=CARTESIAN_POINT('Ctrl Pts',(16.8991416068957,0.25081228213362,3.42552483105699));
#40038=CARTESIAN_POINT('Ctrl Pts',(16.8832363282081,0.054648384762208,3.40743395292956));
#40039=CARTESIAN_POINT('Ctrl Pts',(16.8673310495205,-0.141515512609204,
3.38934307480212));
#40040=CARTESIAN_POINT('Ctrl Pts',(16.8514257708328,-0.347554964333599,
3.47833529219599));
#40041=CARTESIAN_POINT('Ctrl Pts',(16.8355204921452,-0.468865370989487,
3.63354914383413));
#40042=CARTESIAN_POINT('Ctrl Pts',(16.8196152134576,-0.590175777645383,
3.78876299547228));
#40043=CARTESIAN_POINT('Ctrl Pts',(16.80370993477,-0.62675713923276,4.01019848135471));
#40044=CARTESIAN_POINT('Ctrl Pts',(16.7878046560824,-0.561812842140477,
4.19618179452704));
#40045=CARTESIAN_POINT('Ctrl Pts',(16.7718993773948,-0.496868545048197,
4.38216510769936));
#40046=CARTESIAN_POINT('Ctrl Pts',(16.7559940987072,-0.330398589276266,
4.53269624816158));
#40047=CARTESIAN_POINT('Ctrl Pts',(16.7400888200196,-0.138838935752124,
4.57865768466082));
#40048=CARTESIAN_POINT('Ctrl Pts',(16.7363410170989,-0.0937012275068688,
4.58948769960953));
#40049=CARTESIAN_POINT('Ctrl Pts',(16.7325932141782,-0.0471704703862807,
4.59451171761327));
#40050=CARTESIAN_POINT('Ctrl Pts',(16.7288454112575,-0.000548108868865471,
4.59408180714414));
#40051=CARTESIAN_POINT('Ctrl Pts',(16.6211545887425,-2.1752937549985E-5,
4.5931168278739));
#40052=CARTESIAN_POINT('Ctrl Pts',(16.629001911379,-0.0980428491191961,
4.59314873014073));
#40053=CARTESIAN_POINT('Ctrl Pts',(16.6368492340155,-0.196049888122182,
4.57020350190738));
#40054=CARTESIAN_POINT('Ctrl Pts',(16.6446965566521,-0.281666676968544,
4.52419924569128));
#40055=CARTESIAN_POINT('Ctrl Pts',(16.6606018353397,-0.455198332287519,
4.43095591292362));
#40056=CARTESIAN_POINT('Ctrl Pts',(16.6765071140273,-0.577829771800838,
4.24298410528626));
#40057=CARTESIAN_POINT('Ctrl Pts',(16.6924123927149,-0.593253826592341,
4.0465925244149));
#40058=CARTESIAN_POINT('Ctrl Pts',(16.7083176714025,-0.608677881383846,
3.85020094354353));
#40059=CARTESIAN_POINT('Ctrl Pts',(16.7242229500901,-0.516894551453523,
3.64538958943816));
#40060=CARTESIAN_POINT('Ctrl Pts',(16.7401282287778,-0.360046858872914,
3.52619917105016));
#40061=CARTESIAN_POINT('Ctrl Pts',(16.7560335074654,-0.203199166292313,
3.40700875266216));
#40062=CARTESIAN_POINT('Ctrl Pts',(16.771938786153,0.0187128889385656,3.37343926999153));
#40063=CARTESIAN_POINT('Ctrl Pts',(16.7878440648406,0.203796679382533,3.44090440927292));
#40064=CARTESIAN_POINT('Ctrl Pts',(16.8037493435282,0.388880469826499,3.50836954855431));
#40065=CARTESIAN_POINT('Ctrl Pts',(16.8196546222158,0.537135995483554,3.67686930978772));
#40066=CARTESIAN_POINT('Ctrl Pts',(16.8355599009034,0.58049059114602,3.86903573125179));
#40067=CARTESIAN_POINT('Ctrl Pts',(16.851465179591,0.623845186808487,4.06120215271587));
#40068=CARTESIAN_POINT('Ctrl Pts',(16.8673704582787,0.562298852476364,4.2770352344106));
#40069=CARTESIAN_POINT('Ctrl Pts',(16.8832757369663,0.424111061064287,4.41743355636644));
#40070=CARTESIAN_POINT('Ctrl Pts',(16.8959020208917,0.314411738992559,4.5288876912157));
#40071=CARTESIAN_POINT('Ctrl Pts',(16.9085283048171,0.156414067554279,4.59280392009262));
#40072=CARTESIAN_POINT('Ctrl Pts',(16.9211545887425,-0.000535257393875686,
4.59425998651214));
#40073=CARTESIAN_POINT('Origin',(4.,0.,4.));
#40074=CARTESIAN_POINT('',(17.3288454112575,0.000452601584348983,4.59351524744837));
#40075=CARTESIAN_POINT('',(17.2211545887425,0.000283723793354941,4.5949151055343));
#40076=CARTESIAN_POINT('',(4.,-7.27562663373442E-17,4.5941));
#40077=CARTESIAN_POINT('Ctrl Pts',(17.3288454112575,0.000452601584348983,
4.59351524744837));
#40078=CARTESIAN_POINT('Ctrl Pts',(17.3234565584296,0.0676518012035294,
4.59398979695312));
#40079=CARTESIAN_POINT('Ctrl Pts',(17.3180677056016,0.134706745978521,4.58346365752876));
#40080=CARTESIAN_POINT('Ctrl Pts',(17.3126788527736,0.197661386620268,4.56129398922237));
#40081=CARTESIAN_POINT('Ctrl Pts',(17.296773574086,0.383472937993069,4.49585988588324));
#40082=CARTESIAN_POINT('Ctrl Pts',(17.2808682953984,0.533564938357213,4.32899388620009));
#40083=CARTESIAN_POINT('Ctrl Pts',(17.2649630167108,0.579021491014364,4.13731379770915));
#40084=CARTESIAN_POINT('Ctrl Pts',(17.2490577380232,0.624478043671518,3.94563370921821));
#40085=CARTESIAN_POINT('Ctrl Pts',(17.2331524593355,0.565299148621668,3.72913953191949));
#40086=CARTESIAN_POINT('Ctrl Pts',(17.2172471806479,0.428657250819126,3.58723623291525));
#40087=CARTESIAN_POINT('Ctrl Pts',(17.2013419019603,0.292015353016592,3.44533293391101));
#40088=CARTESIAN_POINT('Ctrl Pts',(17.1854366232727,0.0779104524613767,
3.37802051320125));
#40089=CARTESIAN_POINT('Ctrl Pts',(17.1695313445851,-0.115349538542919,
3.41620598662221));
#40090=CARTESIAN_POINT('Ctrl Pts',(17.1536260658975,-0.308609529547215,
3.45439146004317));
#40091=CARTESIAN_POINT('Ctrl Pts',(17.1377207872099,-0.48102461100059,3.59807482759486));
#40092=CARTESIAN_POINT('Ctrl Pts',(17.1218155085223,-0.553429071780215,
3.78128276563952));
#40093=CARTESIAN_POINT('Ctrl Pts',(17.1059102298347,-0.625833532559839,
3.96449070368418));
#40094=CARTESIAN_POINT('Ctrl Pts',(17.090004951147,-0.598227372665711,4.18722321222181));
#40095=CARTESIAN_POINT('Ctrl Pts',(17.0740996724594,-0.483286172800906,
4.34721094636728));
#40096=CARTESIAN_POINT('Ctrl Pts',(17.0590149187255,-0.374274584390508,
4.4989451987145));
#40097=CARTESIAN_POINT('Ctrl Pts',(17.0439301649915,-0.186706445247169,
4.59424147319602));
#40098=CARTESIAN_POINT('Ctrl Pts',(17.0288454112575,0.000186802344652959,
4.59500977980842));
#40099=CARTESIAN_POINT('Ctrl Pts',(16.9211545887425,-0.000535257393875686,
4.59425998651214));
#40100=CARTESIAN_POINT('Ctrl Pts',(16.9244335835047,-0.0412943609811605,
4.59463812105998));
#40101=CARTESIAN_POINT('Ctrl Pts',(16.9277125782669,-0.0819827620002526,
4.59080381827239));
#40102=CARTESIAN_POINT('Ctrl Pts',(16.9309915730291,-0.121736182180322,
4.58249572362891));
#40103=CARTESIAN_POINT('Ctrl Pts',(16.9468968517167,-0.31456638552074,4.54219600671859));
#40104=CARTESIAN_POINT('Ctrl Pts',(16.9628021304043,-0.485397543709551,
4.39663301068103));
#40105=CARTESIAN_POINT('Ctrl Pts',(16.978707409092,-0.555791216176751,4.21264310503418));
#40106=CARTESIAN_POINT('Ctrl Pts',(16.9946126877796,-0.626184888643955,
4.02865319938731));
#40107=CARTESIAN_POINT('Ctrl Pts',(17.0105179664672,-0.596141075389537,
3.80623638413113));
#40108=CARTESIAN_POINT('Ctrl Pts',(17.0264232451548,-0.479454624411006,
3.64751705115182));
#40109=CARTESIAN_POINT('Ctrl Pts',(17.0423285238424,-0.362768173432475,
3.48879771817251));
#40110=CARTESIAN_POINT('Ctrl Pts',(17.05823380253,-0.159439084729831,3.39377586747005));
#40111=CARTESIAN_POINT('Ctrl Pts',(17.0741390812176,0.0371725263090214,
3.40608151284405));
#40112=CARTESIAN_POINT('Ctrl Pts',(17.0900443599052,0.233784137347885,3.41838715821804));
#40113=CARTESIAN_POINT('Ctrl Pts',(17.1059496385929,0.423678270722955,3.5380202996685));
#40114=CARTESIAN_POINT('Ctrl Pts',(17.1218549172805,0.519663574146654,3.71005045990219));
#40115=CARTESIAN_POINT('Ctrl Pts',(17.1377601959681,0.615648877570348,3.88208062013586));
#40116=CARTESIAN_POINT('Ctrl Pts',(17.1536654746557,0.617725351042682,4.10650779915277));
#40117=CARTESIAN_POINT('Ctrl Pts',(17.1695707533433,0.524939565793509,4.28028453107927));
#40118=CARTESIAN_POINT('Ctrl Pts',(17.1854760320309,0.432153780544336,4.45406126300578));
#40119=CARTESIAN_POINT('Ctrl Pts',(17.2013813107185,0.244505736573655,4.5771875478419));
#40120=CARTESIAN_POINT('Ctrl Pts',(17.2172865894061,0.0481554769387473,
4.59312900463441));
#40121=CARTESIAN_POINT('Ctrl Pts',(17.2185759225182,0.0322386925622284,
4.59442127046022));
#40122=CARTESIAN_POINT('Ctrl Pts',(17.2198652556304,0.0162647237884017,
4.5950091984451));
#40123=CARTESIAN_POINT('Ctrl Pts',(17.2211545887425,0.000283723793354941,
4.5949151055343));
#40124=CARTESIAN_POINT('Origin',(4.,0.,4.));
#40125=CARTESIAN_POINT('',(17.6288454112575,-0.000376811216598938,4.5933658344624));
#40126=CARTESIAN_POINT('',(17.5211545887425,0.000390292690419375,4.59338796628294));
#40127=CARTESIAN_POINT('',(4.,-7.27562663373442E-17,4.5941));
#40128=CARTESIAN_POINT('Ctrl Pts',(17.6288454112575,-0.000376811216598938,
4.5933658344624));
#40129=CARTESIAN_POINT('Ctrl Pts',(17.6188882305552,0.123868145157646,4.5926473455414));
#40130=CARTESIAN_POINT('Ctrl Pts',(17.608931049853,0.248515939035854,4.55458993700248));
#40131=CARTESIAN_POINT('Ctrl Pts',(17.5989738691507,0.348483110949462,4.48236965854082));
#40132=CARTESIAN_POINT('Ctrl Pts',(17.5830685904631,0.508167440925656,4.36700731952407));
#40133=CARTESIAN_POINT('Ctrl Pts',(17.5671633117754,0.604877102606476,4.16447556457896));
#40134=CARTESIAN_POINT('Ctrl Pts',(17.5512580330878,0.594207110796467,3.96776840716434));
#40135=CARTESIAN_POINT('Ctrl Pts',(17.5353527544002,0.583537118986457,3.77106124974973));
#40136=CARTESIAN_POINT('Ctrl Pts',(17.5194474757126,0.465487473685617,3.58017868986561));
#40137=CARTESIAN_POINT('Ctrl Pts',(17.503542197025,0.294261577747463,3.48276592343564));
#40138=CARTESIAN_POINT('Ctrl Pts',(17.4876369183374,0.123035681809298,3.38535315700567));
#40139=CARTESIAN_POINT('Ctrl Pts',(17.4717316396498,-0.101366464766187,
3.38141018402985));
#40140=CARTESIAN_POINT('Ctrl Pts',(17.4558263609621,-0.275908889943427,
3.47274745088526));
#40141=CARTESIAN_POINT('Ctrl Pts',(17.4399210822745,-0.450451315120656,
3.56408471774066));
#40142=CARTESIAN_POINT('Ctrl Pts',(17.4240158035869,-0.575134018899647,
3.75070222442727));
#40143=CARTESIAN_POINT('Ctrl Pts',(17.4081105248993,-0.592707978595278,
3.94691310701022));
#40144=CARTESIAN_POINT('Ctrl Pts',(17.3922052462117,-0.610281938290908,
4.14312398959316));
#40145=CARTESIAN_POINT('Ctrl Pts',(17.3762999675241,-0.520747153903178,
4.34892824807245));
#40146=CARTESIAN_POINT('Ctrl Pts',(17.3603946888365,-0.365214210518585,
4.46982927381454));
#40147=CARTESIAN_POINT('Ctrl Pts',(17.3498782629768,-0.262377240481122,
4.54976793433994));
#40148=CARTESIAN_POINT('Ctrl Pts',(17.3393618371172,-0.130687628661636,
4.59258915708319));
#40149=CARTESIAN_POINT('Ctrl Pts',(17.3288454112575,0.000452601584348983,
4.59351524744837));
#40150=CARTESIAN_POINT('Ctrl Pts',(17.2211545887425,0.000283723793354941,
4.5949151055343));
#40151=CARTESIAN_POINT('Ctrl Pts',(17.235770534318,-0.18087770297476,4.59384846352355));
#40152=CARTESIAN_POINT('Ctrl Pts',(17.2503864798935,-0.362942684182573,
4.50513801271133));
#40153=CARTESIAN_POINT('Ctrl Pts',(17.265002425469,-0.47285052735612,4.36129398677095));
#40154=CARTESIAN_POINT('Ctrl Pts',(17.2809077041566,-0.592453796716944,
4.20476088336606));
#40155=CARTESIAN_POINT('Ctrl Pts',(17.2968129828442,-0.626607860139456,
3.98293804780737));
#40156=CARTESIAN_POINT('Ctrl Pts',(17.3127182615318,-0.559630616639302,
3.79767714163318));
#40157=CARTESIAN_POINT('Ctrl Pts',(17.3286235402194,-0.492653373139145,
3.61241623545897));
#40158=CARTESIAN_POINT('Ctrl Pts',(17.3445288189071,-0.324544822716309,
3.46371725866926));
#40159=CARTESIAN_POINT('Ctrl Pts',(17.3604340975947,-0.132493299638714,
3.41985649047097));
#40160=CARTESIAN_POINT('Ctrl Pts',(17.3763393762823,0.0595582234388708,
3.37599572227269));
#40161=CARTESIAN_POINT('Ctrl Pts',(17.3922446549699,0.275552719171213,3.43697316266583));
#40162=CARTESIAN_POINT('Ctrl Pts',(17.4081499336575,0.416314653091553,3.5747905507646));
#40163=CARTESIAN_POINT('Ctrl Pts',(17.4240552123451,0.557076587011893,3.71260793886338));
#40164=CARTESIAN_POINT('Ctrl Pts',(17.4399604910327,0.622605959120231,3.92726527466781));
#40165=CARTESIAN_POINT('Ctrl Pts',(17.4558657697203,0.582814454063527,4.12020099097945));
#40166=CARTESIAN_POINT('Ctrl Pts',(17.4717710484079,0.543022949006823,4.31313670729109));
#40167=CARTESIAN_POINT('Ctrl Pts',(17.4876763270955,0.397910566785078,4.48435080410994));
#40168=CARTESIAN_POINT('Ctrl Pts',(17.5035816057832,0.214106774115907,4.55522901164789));
#40169=CARTESIAN_POINT('Ctrl Pts',(17.5094392667696,0.146414762764002,4.58133232736073));
#40170=CARTESIAN_POINT('Ctrl Pts',(17.515296927756,0.073474912906076,4.59382676872096));
#40171=CARTESIAN_POINT('Ctrl Pts',(17.5211545887425,0.000390292690419375,
4.59338796628294));
#40172=CARTESIAN_POINT('Origin',(4.,0.,4.));
#40173=CARTESIAN_POINT('',(17.9288454112575,-0.000301159635511528,4.59489313984584));
#40174=CARTESIAN_POINT('',(17.8211545887425,-0.000441626631060947,4.59348913571676));
#40175=CARTESIAN_POINT('',(4.,-7.27562663373442E-17,4.5941));
#40176=CARTESIAN_POINT('Ctrl Pts',(17.9288454112575,-0.000301159635511528,
4.59489313984584));
#40177=CARTESIAN_POINT('Ctrl Pts',(17.9143199026809,0.179756887528332,4.59377956832623));
#40178=CARTESIAN_POINT('Ctrl Pts',(17.8997943941043,0.360751589755073,4.50630604003092));
#40179=CARTESIAN_POINT('Ctrl Pts',(17.8852688855277,0.470789914960854,4.36397502945801));
#40180=CARTESIAN_POINT('Ctrl Pts',(17.8693636068401,0.591280720462369,4.20812407407766));
#40181=CARTESIAN_POINT('Ctrl Pts',(17.8534583281524,0.626694694978596,3.98649889312445));
#40182=CARTESIAN_POINT('Ctrl Pts',(17.8375530494648,0.560771239653389,3.80086039350393));
#40183=CARTESIAN_POINT('Ctrl Pts',(17.8216477707772,0.494847784328189,3.61522189388343));
#40184=CARTESIAN_POINT('Ctrl Pts',(17.8057424920896,0.327586899161578,3.46557007559562));
#40185=CARTESIAN_POINT('Ctrl Pts',(17.789837213402,0.135787706397568,3.42061872235194));
#40186=CARTESIAN_POINT('Ctrl Pts',(17.7739319347144,-0.0560114863664412,
3.37566736910827));
#40187=CARTESIAN_POINT('Ctrl Pts',(17.7580266560268,-0.272348986727849,
3.43541648090873));
#40188=CARTESIAN_POINT('Ctrl Pts',(17.7421213773392,-0.41389176700556,3.57243179339102));
#40189=CARTESIAN_POINT('Ctrl Pts',(17.7262160986515,-0.555434547283271,
3.7094471058733));
#40190=CARTESIAN_POINT('Ctrl Pts',(17.710310819964,-0.622182607477285,3.92372861903742));
#40191=CARTESIAN_POINT('Ctrl Pts',(17.6944055412763,-0.583488062224059,
4.11688732754162));
#40192=CARTESIAN_POINT('Ctrl Pts',(17.6785002625887,-0.544793516970831,
4.31004603604583));
#40193=CARTESIAN_POINT('Ctrl Pts',(17.6625949839011,-0.400656366270352,
4.48208193989012));
#40194=CARTESIAN_POINT('Ctrl Pts',(17.6466897052135,-0.217258291784321,
4.55400343026805));
#40195=CARTESIAN_POINT('Ctrl Pts',(17.6407416072282,-0.148672903323923,
4.58089991415997));
#40196=CARTESIAN_POINT('Ctrl Pts',(17.6347935092429,-0.0745967331795002,
4.59379503652584));
#40197=CARTESIAN_POINT('Ctrl Pts',(17.6288454112575,-0.000376811216598938,
4.5933658344624));
#40198=CARTESIAN_POINT('Ctrl Pts',(17.5211545887425,0.000390292690419375,
4.59338796628294));
#40199=CARTESIAN_POINT('Ctrl Pts',(17.5312022064437,-0.12497140465997,4.59263529057266));
#40200=CARTESIAN_POINT('Ctrl Pts',(17.5412498241448,-0.250759050797478,
4.55382993891589));
#40201=CARTESIAN_POINT('Ctrl Pts',(17.551297441846,-0.351218450958555,4.48038168762358));
#40202=CARTESIAN_POINT('Ctrl Pts',(17.5672027205336,-0.510244680247213,
4.36411383780432));
#40203=CARTESIAN_POINT('Ctrl Pts',(17.5831079992212,-0.605801935707933,
4.16103581990878));
#40204=CARTESIAN_POINT('Ctrl Pts',(17.5990132779088,-0.594014368327242,
3.96439246823218));
#40205=CARTESIAN_POINT('Ctrl Pts',(17.6149185565964,-0.58222680094655,3.76774911655557));
#40206=CARTESIAN_POINT('Ctrl Pts',(17.6308238352841,-0.463094410724447,
3.5775404310979));
#40207=CARTESIAN_POINT('Ctrl Pts',(17.6467291139717,-0.291317751175132,
3.48110219315546));
#40208=CARTESIAN_POINT('Ctrl Pts',(17.6626343926593,-0.119541091625818,
3.38466395521302));
#40209=CARTESIAN_POINT('Ctrl Pts',(17.6785396713469,0.104879837250709,3.38199616478582));
#40210=CARTESIAN_POINT('Ctrl Pts',(17.6944449500345,0.278900439380867,3.47432375837312));
#40211=CARTESIAN_POINT('Ctrl Pts',(17.7103502287221,0.452921041511034,3.56665135196042));
#40212=CARTESIAN_POINT('Ctrl Pts',(17.7262555074097,0.576541316894826,3.75397432956222));
#40213=CARTESIAN_POINT('Ctrl Pts',(17.7421607860974,0.593000065018554,3.95028190484542));
#40214=CARTESIAN_POINT('Ctrl Pts',(17.758066064785,0.60945881314228,4.1465894801286));
#40215=CARTESIAN_POINT('Ctrl Pts',(17.7739713434726,0.518756034005955,4.35188165309317));
#40216=CARTESIAN_POINT('Ctrl Pts',(17.7898766221602,0.362538606470845,4.47189694310939));
#40217=CARTESIAN_POINT('Ctrl Pts',(17.8003026110209,0.260137309937395,4.55056755941266));
#40218=CARTESIAN_POINT('Ctrl Pts',(17.8107285998817,0.129585238016204,4.59259583028147));
#40219=CARTESIAN_POINT('Ctrl Pts',(17.8211545887425,-0.000441626631060947,
4.59348913571676));
#40220=CARTESIAN_POINT('Origin',(4.,0.,4.));
#40221=CARTESIAN_POINT('',(18.2288454112575,0.000530626821107938,4.59429426521737));
#40222=CARTESIAN_POINT('',(18.1211545887425,-0.000206261771334874,4.59499421029555));
#40223=CARTESIAN_POINT('',(4.,-7.27562663373442E-17,4.5941));
#40224=CARTESIAN_POINT('Ctrl Pts',(18.2288454112575,0.000530626821107938,
4.59429426521737));
#40225=CARTESIAN_POINT('Ctrl Pts',(18.2256568534942,0.0401596894680921,
4.59466101186164));
#40226=CARTESIAN_POINT('Ctrl Pts',(18.2224682957309,0.0797220295111884,
4.5910372210354));
#40227=CARTESIAN_POINT('Ctrl Pts',(18.2192797379675,0.118424305077702,4.58317806034235));
#40228=CARTESIAN_POINT('Ctrl Pts',(18.2033744592799,0.311480390123117,4.54397471188459));
#40229=CARTESIAN_POINT('Ctrl Pts',(18.1874691805923,0.483135922039688,4.39938477867344));
#40230=CARTESIAN_POINT('Ctrl Pts',(18.1715639019047,0.554573942717995,4.21579784094385));
#40231=CARTESIAN_POINT('Ctrl Pts',(18.1556586232171,0.626011963396302,4.03221090321426));
#40232=CARTESIAN_POINT('Ctrl Pts',(18.1397533445295,0.597232472836345,3.80962696096622));
#40233=CARTESIAN_POINT('Ctrl Pts',(18.1238480658419,0.481449795543417,3.65024714373002));
#40234=CARTESIAN_POINT('Ctrl Pts',(18.1079427871543,0.365667118250483,3.49086732649381));
#40235=CARTESIAN_POINT('Ctrl Pts',(18.0920375084667,0.16288125422457,3.39469163426944));
#40236=CARTESIAN_POINT('Ctrl Pts',(18.076132229779,-0.0337971069360236,
3.40587987606835));
#40237=CARTESIAN_POINT('Ctrl Pts',(18.0602269510914,-0.230475468096606,
3.41706811786726));
#40238=CARTESIAN_POINT('Ctrl Pts',(18.0443216724038,-0.421046326391869,
3.53562029368944));
#40239=CARTESIAN_POINT('Ctrl Pts',(18.0284163937162,-0.518007606080761,
3.70710225992629));
#40240=CARTESIAN_POINT('Ctrl Pts',(18.0125111150286,-0.614968885769652,
3.87858422616314));
#40241=CARTESIAN_POINT('Ctrl Pts',(17.996605836341,-0.618320586852172,4.10299598281466));
#40242=CARTESIAN_POINT('Ctrl Pts',(17.9807005576534,-0.526523749990007,
4.27729714530494));
#40243=CARTESIAN_POINT('Ctrl Pts',(17.9647952789658,-0.434726913127837,
4.45159830779523));
#40244=CARTESIAN_POINT('Ctrl Pts',(17.9488900002781,-0.247781538320971,
4.57578887612429));
#40245=CARTESIAN_POINT('Ctrl Pts',(17.9329847215905,-0.0515250326741526,
4.59284579538505));
#40246=CARTESIAN_POINT('Ctrl Pts',(17.9316049514795,-0.0344999389365885,
4.59432546938787));
#40247=CARTESIAN_POINT('Ctrl Pts',(17.9302251813685,-0.0174047750035579,
4.59499891739512));
#40248=CARTESIAN_POINT('Ctrl Pts',(17.9288454112575,-0.000301159635511528,
4.59489313984584));
#40249=CARTESIAN_POINT('Ctrl Pts',(17.8211545887425,-0.000441626631060947,
4.59348913571676));
#40250=CARTESIAN_POINT('Ctrl Pts',(17.8266338785693,-0.0687761401428734,
4.59395860479535));
#40251=CARTESIAN_POINT('Ctrl Pts',(17.8321131683962,-0.136965594625977,
4.58306684864343));
#40252=CARTESIAN_POINT('Ctrl Pts',(17.837592458223,-0.200847632772524,4.56016175744822));
#40253=CARTESIAN_POINT('Ctrl Pts',(17.8534977369106,-0.386284368546891,
4.49367287470298));
#40254=CARTESIAN_POINT('Ctrl Pts',(17.8694030155983,-0.535425764161732,
4.32595670214462));
#40255=CARTESIAN_POINT('Ctrl Pts',(17.8853082942859,-0.579792400402821,
4.13402141072584));
#40256=CARTESIAN_POINT('Ctrl Pts',(17.9012135729735,-0.624159036643913,
3.94208611930704));
#40257=CARTESIAN_POINT('Ctrl Pts',(17.9171188516611,-0.563750913511241,
3.72593170902781));
#40258=CARTESIAN_POINT('Ctrl Pts',(17.9330241303487,-0.426304885490399,
3.58480714034942));
#40259=CARTESIAN_POINT('Ctrl Pts',(17.9489294090363,-0.288858857469565,
3.44368257167104));
#40260=CARTESIAN_POINT('Ctrl Pts',(17.9648346877239,-0.0743749245605683,
3.37758784459349));
#40261=CARTESIAN_POINT('Ctrl Pts',(17.9807399664116,0.118664965311668,3.41687086155347));
#40262=CARTESIAN_POINT('Ctrl Pts',(17.9966452450992,0.311704855183904,3.45615387851346));
#40263=CARTESIAN_POINT('Ctrl Pts',(18.0125505237868,0.483300702019379,3.60081463951098));
#40264=CARTESIAN_POINT('Ctrl Pts',(18.0284558024744,0.554662952572844,3.78443104318807));
#40265=CARTESIAN_POINT('Ctrl Pts',(18.044361081162,0.62602520312631,3.96804744686516));
#40266=CARTESIAN_POINT('Ctrl Pts',(18.0602663598496,0.597153857397765,4.19061949322182));
#40267=CARTESIAN_POINT('Ctrl Pts',(18.0761716385372,0.481305415899848,4.34995151481781));
#40268=CARTESIAN_POINT('Ctrl Pts',(18.0911659552723,0.372092100044007,4.50015792394613));
#40269=CARTESIAN_POINT('Ctrl Pts',(18.1061602720074,0.185579460002099,4.59416090236354));
#40270=CARTESIAN_POINT('Ctrl Pts',(18.1211545887425,-0.000206261771334874,
4.59499421029555));
#40271=CARTESIAN_POINT('Origin',(4.,0.,4.));
#40272=CARTESIAN_POINT('',(18.5288454112575,4.04073003155148E-5,4.59311858068669));
#40273=CARTESIAN_POINT('',(18.4211545887425,0.000547083855738422,4.59411609730493));
#40274=CARTESIAN_POINT('',(4.,-7.27562663373442E-17,4.5941));
#40275=CARTESIAN_POINT('Ctrl Pts',(18.5288454112575,4.04073003155148E-5,
4.59311858068669));
#40276=CARTESIAN_POINT('Ctrl Pts',(18.5210885256199,0.0969311390001333,
4.59317716754242));
#40277=CARTESIAN_POINT('Ctrl Pts',(18.5133316399822,0.193796352446061,4.57078374547556));
#40278=CARTESIAN_POINT('Ctrl Pts',(18.5055747543446,0.27868347559656,4.52579129559858));
#40279=CARTESIAN_POINT('Ctrl Pts',(18.489669475657,0.452742165355285,4.43353552600749));
#40280=CARTESIAN_POINT('Ctrl Pts',(18.4737641969693,0.576439736070726,4.24626358090446));
#40281=CARTESIAN_POINT('Ctrl Pts',(18.4578589182817,0.592979496483005,4.04996281465819));
#40282=CARTESIAN_POINT('Ctrl Pts',(18.4419536395941,0.609519256895283,3.85366204841193));
#40283=CARTESIAN_POINT('Ctrl Pts',(18.4260483609065,0.518901207004412,3.64833246102244));
#40284=CARTESIAN_POINT('Ctrl Pts',(18.4101430822189,0.362733321586741,3.52825271224048));
#40285=CARTESIAN_POINT('Ctrl Pts',(18.3942378035313,0.206565436169079,3.40817296345854));
#40286=CARTESIAN_POINT('Ctrl Pts',(18.3783325248437,-0.015152284775374,
3.37334305328413));
#40287=CARTESIAN_POINT('Ctrl Pts',(18.3624272461561,-0.200616443892158,
3.43975540293737));
#40288=CARTESIAN_POINT('Ctrl Pts',(18.3465219674685,-0.386080603008964,
3.50616775259061));
#40289=CARTESIAN_POINT('Ctrl Pts',(18.3306166887808,-0.535291200298091,
3.67382236207151));
#40290=CARTESIAN_POINT('Ctrl Pts',(18.3147114100932,-0.579737042064157,
3.86573932758804));
#40291=CARTESIAN_POINT('Ctrl Pts',(18.2988061314056,-0.624182883830224,
4.05765629310458));
#40292=CARTESIAN_POINT('Ctrl Pts',(18.282900852718,-0.563863970073232,4.27383561465674));
#40293=CARTESIAN_POINT('Ctrl Pts',(18.2669955740304,-0.426476194107598,
4.41501689358062));
#40294=CARTESIAN_POINT('Ctrl Pts',(18.2542788531061,-0.316630774880643,
4.52789532589669));
#40295=CARTESIAN_POINT('Ctrl Pts',(18.2415621321818,-0.157519428275204,
4.5928315930404));
#40296=CARTESIAN_POINT('Ctrl Pts',(18.2288454112575,0.000530626821107938,
4.59429426521737));
#40297=CARTESIAN_POINT('Ctrl Pts',(18.1211545887425,-0.000206261771334874,
4.59499421029555));
#40298=CARTESIAN_POINT('Ctrl Pts',(18.122065550695,-0.0114934532352288,
4.59504483693191));
#40299=CARTESIAN_POINT('Ctrl Pts',(18.1229765126475,-0.0227779616248223,
4.59475157188293));
#40300=CARTESIAN_POINT('Ctrl Pts',(18.1238874746001,-0.0340422900297544,
4.59410612569417));
#40301=CARTESIAN_POINT('Ctrl Pts',(18.1397927532877,-0.230716017194119,
4.58283671813918));
#40302=CARTESIAN_POINT('Ctrl Pts',(18.1556980319753,-0.421237934255556,
4.46420590619388));
#40303=CARTESIAN_POINT('Ctrl Pts',(18.1716033106629,-0.518128437217054,
4.29268393984778));
#40304=CARTESIAN_POINT('Ctrl Pts',(18.1875085893505,-0.615018940178556,
4.12116197350168));
#40305=CARTESIAN_POINT('Ctrl Pts',(18.2034138680381,-0.618278029040109,
3.89674885275477));
#40306=CARTESIAN_POINT('Ctrl Pts',(18.2193191467258,-0.526409268077163,
3.72248558851787));
#40307=CARTESIAN_POINT('Ctrl Pts',(18.2352244254134,-0.434540507114227,
3.54822232428098));
#40308=CARTESIAN_POINT('Ctrl Pts',(18.251129704101,-0.24754389632682,3.42410891655409));
#40309=CARTESIAN_POINT('Ctrl Pts',(18.2670349827886,-0.0512803682143169,
3.40713299136011));
#40310=CARTESIAN_POINT('Ctrl Pts',(18.2829402614762,0.144983159898198,3.39015706616613));
#40311=CARTESIAN_POINT('Ctrl Pts',(18.2988455401638,0.35051360533581,3.48031862350507));
#40312=CARTESIAN_POINT('Ctrl Pts',(18.3147508188514,0.470940082829639,3.63621929066782));
#40313=CARTESIAN_POINT('Ctrl Pts',(18.330656097539,0.591366560323475,3.79211995783059));
#40314=CARTESIAN_POINT('Ctrl Pts',(18.3465613762266,0.62668906987352,4.01375973481717));
#40315=CARTESIAN_POINT('Ctrl Pts',(18.3624666549143,0.560689009466533,4.199371012841));
#40316=CARTESIAN_POINT('Ctrl Pts',(18.3783719336019,0.49468894905955,4.38498229086483));
#40317=CARTESIAN_POINT('Ctrl Pts',(18.3942772122895,0.327366318695548,4.53456506992591));
#40318=CARTESIAN_POINT('Ctrl Pts',(18.4101824909771,0.135548591400956,4.57943726620491));
#40319=CARTESIAN_POINT('Ctrl Pts',(18.4138398568989,0.0914407431336166,
4.58975547846199));
#40320=CARTESIAN_POINT('Ctrl Pts',(18.4174972228207,0.0460377050408626,
4.59453706917327));
#40321=CARTESIAN_POINT('Ctrl Pts',(18.4211545887425,0.000547083855738422,
4.59411609730493));
#40322=CARTESIAN_POINT('Origin',(4.,0.,4.));
#40323=CARTESIAN_POINT('',(18.8288454112575,-0.000545657836941327,4.59414547262434));
#40324=CARTESIAN_POINT('',(18.7211545887425,-5.63168744233308E-5,4.59312091231189));
#40325=CARTESIAN_POINT('',(4.,-7.27562663373442E-17,4.5941));
#40326=CARTESIAN_POINT('Ctrl Pts',(18.8288454112575,-0.000545657836941327,
4.59414547262434));
#40327=CARTESIAN_POINT('Ctrl Pts',(18.8165201977456,0.15273698101805,4.59272393327212));
#40328=CARTESIAN_POINT('Ctrl Pts',(18.8041949842336,0.307016766534516,4.53213273669464));
#40329=CARTESIAN_POINT('Ctrl Pts',(18.7918697707216,0.416139138999065,4.42538122089617));
#40330=CARTESIAN_POINT('Ctrl Pts',(18.775964492034,0.556957936451544,4.28762193522949));
#40331=CARTESIAN_POINT('Ctrl Pts',(18.7600592133464,0.622575889387102,4.0729916608594));
#40332=CARTESIAN_POINT('Ctrl Pts',(18.7441539346588,0.582864009884755,3.88003953951897));
#40333=CARTESIAN_POINT('Ctrl Pts',(18.7282486559712,0.543152130382401,3.6870874181785));
#40334=CARTESIAN_POINT('Ctrl Pts',(18.7123433772835,0.3981104184421,3.51581344986768));
#40335=CARTESIAN_POINT('Ctrl Pts',(18.6964380985959,0.214335891977863,3.44485939483061));
#40336=CARTESIAN_POINT('Ctrl Pts',(18.6805328199083,0.0305613655136472,
3.37390533979354));
#40337=CARTESIAN_POINT('Ctrl Pts',(18.6646275412207,-0.191945975474496,
3.40327119803019));
#40338=CARTESIAN_POINT('Ctrl Pts',(18.6487222625331,-0.351020173514001,
3.51947340980541));
#40339=CARTESIAN_POINT('Ctrl Pts',(18.6328169838455,-0.510094371553506,
3.63567562158063));
#40340=CARTESIAN_POINT('Ctrl Pts',(18.6169117051579,-0.605735426644373,
3.83871418689441));
#40341=CARTESIAN_POINT('Ctrl Pts',(18.6010064264702,-0.594029012528289,
4.03536238640794));
#40342=CARTESIAN_POINT('Ctrl Pts',(18.5851011477826,-0.582322598412206,
4.23201058592146));
#40343=CARTESIAN_POINT('Ctrl Pts',(18.569195869095,-0.463268715089173,4.42226841963472));
#40344=CARTESIAN_POINT('Ctrl Pts',(18.5532905904074,-0.29153186902666,4.51877753945177));
#40345=CARTESIAN_POINT('Ctrl Pts',(18.5451421973574,-0.203549800283198,
4.56821988225003));
#40346=CARTESIAN_POINT('Ctrl Pts',(18.5369938043075,-0.101740616897797,
4.59305703682098));
#40347=CARTESIAN_POINT('Ctrl Pts',(18.5288454112575,4.04073003155148E-5,
4.59311858068669));
#40348=CARTESIAN_POINT('Ctrl Pts',(18.4211545887425,0.000547083855738422,
4.59411609730493));
#40349=CARTESIAN_POINT('Ctrl Pts',(18.4334025015083,-0.151793472668411,
4.59270633223614));
#40350=CARTESIAN_POINT('Ctrl Pts',(18.4456504142741,-0.305116246576315,
4.53295143150856));
#40351=CARTESIAN_POINT('Ctrl Pts',(18.4578983270399,-0.414068183831284,
4.42739736222451));
#40352=CARTESIAN_POINT('Ctrl Pts',(18.4738036057275,-0.555554407543751,
4.29032364846819));
#40353=CARTESIAN_POINT('Ctrl Pts',(18.4897088844152,-0.622214030743504,
4.07601460745865));
#40354=CARTESIAN_POINT('Ctrl Pts',(18.5056141631028,-0.583439774593308,
3.88287188415962));
#40355=CARTESIAN_POINT('Ctrl Pts',(18.5215194417904,-0.54466551844311,3.68972916086059));
#40356=CARTESIAN_POINT('Ctrl Pts',(18.537424720478,-0.400457382942952,3.51775275527208));
#40357=CARTESIAN_POINT('Ctrl Pts',(18.5533299991656,-0.217029642971419,
3.44590695711865));
#40358=CARTESIAN_POINT('Ctrl Pts',(18.5692352778532,-0.0336019029998957,
3.37406115896522));
#40359=CARTESIAN_POINT('Ctrl Pts',(18.5851405565408,0.189045441442997,3.40234596824686));
#40360=CARTESIAN_POINT('Ctrl Pts',(18.6010458352284,0.348682149221421,3.51777419717301));
#40361=CARTESIAN_POINT('Ctrl Pts',(18.6169511139161,0.508318856999844,3.63320242609916));
#40362=CARTESIAN_POINT('Ctrl Pts',(18.6328563926037,0.604944928113798,3.83577407466982));
#40363=CARTESIAN_POINT('Ctrl Pts',(18.6487616712913,0.594193758619731,4.03247681196108));
#40364=CARTESIAN_POINT('Ctrl Pts',(18.6646669499789,0.583442589125664,4.22917954925235));
#40365=CARTESIAN_POINT('Ctrl Pts',(18.6805722286665,0.465314179023576,4.42001337526422));
#40366=CARTESIAN_POINT('Ctrl Pts',(18.6964775073541,0.294048096631404,4.51735547060535));
#40367=CARTESIAN_POINT('Ctrl Pts',(18.7047032011502,0.205474838715737,4.56769764225005));
#40368=CARTESIAN_POINT('Ctrl Pts',(18.7129288949463,0.102689258835563,4.59303430424318));
#40369=CARTESIAN_POINT('Ctrl Pts',(18.7211545887425,-5.63168744233308E-5,
4.59312091231189));
#40370=CARTESIAN_POINT('Origin',(4.,0.,4.));
#40371=CARTESIAN_POINT('',(19.1288454112575,0.000222628893785728,4.59497983522242));
#40372=CARTESIAN_POINT('',(19.0211545887425,-0.000526118841417405,4.59432346427954));
#40373=CARTESIAN_POINT('',(4.,-7.27562663373442E-17,4.5941));
#40374=CARTESIAN_POINT('Ctrl Pts',(19.1288454112575,0.000222628893785728,
4.59497983522242));
#40375=CARTESIAN_POINT('Ctrl Pts',(19.1278571485589,0.012468395078646,4.59503853204781));
#40376=CARTESIAN_POINT('Ctrl Pts',(19.1268688858602,0.0247107891953784,
4.59469333777414));
#40377=CARTESIAN_POINT('Ctrl Pts',(19.1258806231615,0.0369274203756033,
4.59393377720877));
#40378=CARTESIAN_POINT('Ctrl Pts',(19.1099753444739,0.233544093050454,4.58170927203582));
#40379=CARTESIAN_POINT('Ctrl Pts',(19.0940700657862,0.423487581379576,4.46215450773496));
#40380=CARTESIAN_POINT('Ctrl Pts',(19.0781647870986,0.519543871337238,4.29016397409385));
#40381=CARTESIAN_POINT('Ctrl Pts',(19.062259508411,0.615600161294901,4.11817344045274));
#40382=CARTESIAN_POINT('Ctrl Pts',(19.0463542297234,0.617769252881104,3.89374713747137));
#40383=CARTESIAN_POINT('Ctrl Pts',(19.0304489510358,0.525055191022736,3.71993212880311));
#40384=CARTESIAN_POINT('Ctrl Pts',(19.0145436723482,0.432341129164367,3.54611712013485));
#40385=CARTESIAN_POINT('Ctrl Pts',(18.9986383936606,0.244743913861428,3.42291340577968));
#40386=CARTESIAN_POINT('Ctrl Pts',(18.982733114973,0.0484002497885746,3.40689091904056));
#40387=CARTESIAN_POINT('Ctrl Pts',(18.9668278362853,-0.147943414284278,
3.39086843230144));
#40388=CARTESIAN_POINT('Ctrl Pts',(18.9509225575977,-0.353033527127044,
3.48202717317836));
#40389=CARTESIAN_POINT('Ctrl Pts',(18.9350172789101,-0.472701385564812,
3.63851090447403));
#40390=CARTESIAN_POINT('Ctrl Pts',(18.9191120002225,-0.592369244002587,
3.79499463576972));
#40391=CARTESIAN_POINT('Ctrl Pts',(18.9032067215349,-0.626614848035354,
4.01680335748416));
#40392=CARTESIAN_POINT('Ctrl Pts',(18.8873014428473,-0.559714065105754,
4.20209188855652));
#40393=CARTESIAN_POINT('Ctrl Pts',(18.8713961641597,-0.492813282176159,
4.38738041962887));
#40394=CARTESIAN_POINT('Ctrl Pts',(18.8554908854721,-0.324766112284209,
4.53614876005914));
#40395=CARTESIAN_POINT('Ctrl Pts',(18.8395856067844,-0.132732706353525,
4.58008878179264));
#40396=CARTESIAN_POINT('Ctrl Pts',(18.8360055416088,-0.0895085590353085,
4.5899790920924));
#40397=CARTESIAN_POINT('Ctrl Pts',(18.8324254764332,-0.0450691735440342,
4.59455838259347));
#40398=CARTESIAN_POINT('Ctrl Pts',(18.8288454112575,-0.000545657836941327,
4.59414547262434));
#40399=CARTESIAN_POINT('Ctrl Pts',(18.7211545887425,-5.63168744233308E-5,
4.59312091231189));
#40400=CARTESIAN_POINT('Ctrl Pts',(18.728834173634,-0.0959805501911411,
4.59320177041728));
#40401=CARTESIAN_POINT('Ctrl Pts',(18.7365137585255,-0.191869914813978,
4.57127401300463));
#40402=CARTESIAN_POINT('Ctrl Pts',(18.744193343417,-0.276126457005151,4.5271386400555));
#40403=CARTESIAN_POINT('Ctrl Pts',(18.7600986221046,-0.450631173567243,
4.43572934949413));
#40404=CARTESIAN_POINT('Ctrl Pts',(18.7760039007922,-0.575236852009173,
4.249060403701));
#40405=CARTESIAN_POINT('Ctrl Pts',(18.7919091794798,-0.592729836422094,
4.05284228527226));
#40406=CARTESIAN_POINT('Ctrl Pts',(18.8078144581674,-0.610222820835014,
3.85662416684351));
#40407=CARTESIAN_POINT('Ctrl Pts',(18.823719736855,-0.520603111218926,3.65085687577915));
#40408=CARTESIAN_POINT('Ctrl Pts',(18.8396250155426,-0.365020286731977,
3.53002004684018));
#40409=CARTESIAN_POINT('Ctrl Pts',(18.8555302942302,-0.209437462245028,
3.40918321790122));
#40410=CARTESIAN_POINT('Ctrl Pts',(18.8714355729179,0.0121084771127808,
3.37327685108765));
#40411=CARTESIAN_POINT('Ctrl Pts',(18.8873408516055,0.197893008823487,3.43878763096633));
#40412=CARTESIAN_POINT('Ctrl Pts',(18.9032461302931,0.383677540534204,3.50429841084501));
#40413=CARTESIAN_POINT('Ctrl Pts',(18.9191514089807,0.533700664597814,3.67122633741595));
#40414=CARTESIAN_POINT('Ctrl Pts',(18.9350566876683,0.579078109400399,3.86292516893752));
#40415=CARTESIAN_POINT('Ctrl Pts',(18.9509619663559,0.624455554202981,4.05462400045908));
#40416=CARTESIAN_POINT('Ctrl Pts',(18.9668672450435,0.56518731974455,4.27109373693126));
#40417=CARTESIAN_POINT('Ctrl Pts',(18.9827725237311,0.428486871854059,4.41294063344238));
#40418=CARTESIAN_POINT('Ctrl Pts',(18.9955665454016,0.318526617336051,4.52704063153052));
#40419=CARTESIAN_POINT('Ctrl Pts',(19.008360567072,0.158464569423419,4.5928566151945));
#40420=CARTESIAN_POINT('Ctrl Pts',(19.0211545887425,-0.000526118841417405,
4.59432346427954));
#40421=CARTESIAN_POINT('Origin',(4.,0.,4.));
#40422=CARTESIAN_POINT('',(19.4288454112575,0.000431836873498515,4.59346738712276));
#40423=CARTESIAN_POINT('',(19.3211545887425,0.000315695961457875,4.59487351203822));
#40424=CARTESIAN_POINT('',(4.,-7.27562663373442E-17,4.5941));
#40425=CARTESIAN_POINT('Ctrl Pts',(19.4288454112575,0.000431836873498515,
4.59346738712276));
#40426=CARTESIAN_POINT('Ctrl Pts',(19.4232888206845,0.0697367837969298,
4.59393182999066));
#40427=CARTESIAN_POINT('Ctrl Pts',(19.4177322301115,0.13889623855249,4.58272225272434));
#40428=CARTESIAN_POINT('Ctrl Pts',(19.4121756395385,0.203565929825556,4.55917964700716));
#40429=CARTESIAN_POINT('Ctrl Pts',(19.3962703608509,0.38867754617092,4.49179089484985));
#40430=CARTESIAN_POINT('Ctrl Pts',(19.3803650821633,0.537002597765565,4.32335233206236));
#40431=CARTESIAN_POINT('Ctrl Pts',(19.3644598034757,0.580436494614329,4.13120381907284));
#40432=CARTESIAN_POINT('Ctrl Pts',(19.3485545247881,0.623870391463095,3.93905530608331));
#40433=CARTESIAN_POINT('Ctrl Pts',(19.3326492461004,0.562413133565966,3.72319684289176));
#40434=CARTESIAN_POINT('Ctrl Pts',(19.3167439674128,0.424283294458304,3.58274150440131));
#40435=CARTESIAN_POINT('Ctrl Pts',(19.3008386887252,0.286153455350651,3.44228616591086));
#40436=CARTESIAN_POINT('Ctrl Pts',(19.2849334100376,0.071351035032473,3.37723395212151));
#40437=CARTESIAN_POINT('Ctrl Pts',(19.26902813135,-0.12149578302492,3.4174540870367));
#40438=CARTESIAN_POINT('Ctrl Pts',(19.2531228526624,-0.314342601082313,
3.45767422195189));
#40439=CARTESIAN_POINT('Ctrl Pts',(19.2372175739748,-0.485233816878921,
3.60316670557164));
#40440=CARTESIAN_POINT('Ctrl Pts',(19.2213122952871,-0.555703413721375,
3.78712754492824));
#40441=CARTESIAN_POINT('Ctrl Pts',(19.2054070165995,-0.626173010563829,
3.97108838428485));
#40442=CARTESIAN_POINT('Ctrl Pts',(19.1895017379119,-0.59622098845213,4.19351757937831));
#40443=CARTESIAN_POINT('Ctrl Pts',(19.1735964592243,-0.479600048885993,
4.35228505390253));
#40444=CARTESIAN_POINT('Ctrl Pts',(19.1586794432354,-0.370225264934164,
4.50118762911129));
#40445=CARTESIAN_POINT('Ctrl Pts',(19.1437624272465,-0.184617181632464,
4.59409385471947));
#40446=CARTESIAN_POINT('Ctrl Pts',(19.1288454112575,0.000222628893785728,
4.59497983522242));
#40447=CARTESIAN_POINT('Ctrl Pts',(19.0211545887425,-0.000526118841417405,
4.59432346427954));
#40448=CARTESIAN_POINT('Ctrl Pts',(19.0242658457596,-0.0391895592568775,
4.59468017342281));
#40449=CARTESIAN_POINT('Ctrl Pts',(19.0273771027768,-0.0777896429211806,
4.59123148246997));
#40450=CARTESIAN_POINT('Ctrl Pts',(19.030488359794,-0.115590453236054,4.58374636034569));
#40451=CARTESIAN_POINT('Ctrl Pts',(19.0463936384816,-0.308834669113126,
4.5454811341878));
#40452=CARTESIAN_POINT('Ctrl Pts',(19.0622989171692,-0.481190439544719,
4.40172662532195));
#40453=CARTESIAN_POINT('Ctrl Pts',(19.0782041958568,-0.553519286527586,
4.21848882245705));
#40454=CARTESIAN_POINT('Ctrl Pts',(19.0941094745444,-0.625848133510457,
4.03525101959215));
#40455=CARTESIAN_POINT('Ctrl Pts',(19.1100147532321,-0.598150057044591,
3.81252992272818));
#40456=CARTESIAN_POINT('Ctrl Pts',(19.1259200319197,-0.483142842019737,
3.65258963701249));
#40457=CARTESIAN_POINT('Ctrl Pts',(19.1418253106073,-0.36813562699489,3.49264935129682));
#40458=CARTESIAN_POINT('Ctrl Pts',(19.1577305892949,-0.165819273411065,
3.39548987672941));
#40459=CARTESIAN_POINT('Ctrl Pts',(19.1736358679825,0.0309111084379188,
3.40572273351557));
#40460=CARTESIAN_POINT('Ctrl Pts',(19.1895411466701,0.227641490286902,3.41595559030173));
#40461=CARTESIAN_POINT('Ctrl Pts',(19.2054464253577,0.418785900401045,3.53358077844144));
#40462=CARTESIAN_POINT('Ctrl Pts',(19.2213517040453,0.516578912360374,3.70458978792342));
#40463=CARTESIAN_POINT('Ctrl Pts',(19.237256982733,0.614371924319703,3.87559879740541));
#40464=CARTESIAN_POINT('Ctrl Pts',(19.2531622614206,0.618813538124218,4.09999162822965));
#40465=CARTESIAN_POINT('Ctrl Pts',(19.2690675401082,0.527864352527146,4.27473658562515));
#40466=CARTESIAN_POINT('Ctrl Pts',(19.2849728187958,0.436915166930073,4.44948154302064));
#40467=CARTESIAN_POINT('Ctrl Pts',(19.3008780974834,0.250575181931413,4.5745786269874));
#40468=CARTESIAN_POINT('Ctrl Pts',(19.316783376171,0.0544038354309166,4.59258854924263));
#40469=CARTESIAN_POINT('Ctrl Pts',(19.3182404470282,0.0364327229714708,
4.59423842494573));
#40470=CARTESIAN_POINT('Ctrl Pts',(19.3196975178853,0.0183791031991185,
4.59498959766064));
#40471=CARTESIAN_POINT('Ctrl Pts',(19.3211545887425,0.000315695961457875,
4.59487351203822));
#40472=CARTESIAN_POINT('Origin',(4.,0.,4.));
#40473=CARTESIAN_POINT('',(19.7288454112575,-0.000401422265437046,4.59340756962635));
#40474=CARTESIAN_POINT('',(19.6211545887425,0.000364945106097663,4.59334757974602));
#40475=CARTESIAN_POINT('',(4.,-7.27562663373442E-17,4.5941));
#40476=CARTESIAN_POINT('Ctrl Pts',(19.7288454112575,-0.000401422265437046,
4.59340756962635));
#40477=CARTESIAN_POINT('Ctrl Pts',(19.7187204928102,0.125914276337785,4.59262579220321));
#40478=CARTESIAN_POINT('Ctrl Pts',(19.7085955743629,0.252675872983383,4.55317429478549));
#40479=CARTESIAN_POINT('Ctrl Pts',(19.6984706559155,0.353547469597214,4.47867015725961));
#40480=CARTESIAN_POINT('Ctrl Pts',(19.6825653772279,0.512007102052776,4.36163128164859));
#40481=CARTESIAN_POINT('Ctrl Pts',(19.6666600985403,0.606576931433326,4.15809158444534));
#40482=CARTESIAN_POINT('Ctrl Pts',(19.6507548198527,0.593834428727047,3.9615078130365));
#40483=CARTESIAN_POINT('Ctrl Pts',(19.6348495411651,0.581091926020768,3.76492404162769));
#40484=CARTESIAN_POINT('Ctrl Pts',(19.6189442624775,0.46103709122769,3.57529619601327));
#40485=CARTESIAN_POINT('Ctrl Pts',(19.6030389837899,0.288794059426421,3.47969339775167));
#40486=CARTESIAN_POINT('Ctrl Pts',(19.5871337051022,0.116551027625133,3.38409059949006));
#40487=CARTESIAN_POINT('Ctrl Pts',(19.5712284264146,-0.107880201184358,
3.38251284858128));
#40488=CARTESIAN_POINT('Ctrl Pts',(19.555323147727,-0.281450319664219,3.47568456171554));
#40489=CARTESIAN_POINT('Ctrl Pts',(19.5394178690394,-0.45502043814407,3.5688562748498));
#40490=CARTESIAN_POINT('Ctrl Pts',(19.5235125903518,-0.577729446294298,
3.75677745202708));
#40491=CARTESIAN_POINT('Ctrl Pts',(19.5076073116642,-0.593234549413986,
3.95316264945144));
#40492=CARTESIAN_POINT('Ctrl Pts',(19.4917020329766,-0.608739652533674,
4.1495478468758));
#40493=CARTESIAN_POINT('Ctrl Pts',(19.475796754289,-0.517040850622822,4.35439706454724));
#40494=CARTESIAN_POINT('Ctrl Pts',(19.4598914756013,-0.360242359119356,
4.47365220261941));
#40495=CARTESIAN_POINT('Ctrl Pts',(19.4495427874867,-0.258222223711561,
4.55124494740629));
#40496=CARTESIAN_POINT('Ctrl Pts',(19.4391940993721,-0.128642866595325,
4.59260240088276));
#40497=CARTESIAN_POINT('Ctrl Pts',(19.4288454112575,0.000431836873498515,
4.59346738712276));
#40498=CARTESIAN_POINT('Ctrl Pts',(19.3211545887425,0.000315695961457875,
4.59487351203822));
#40499=CARTESIAN_POINT('Ctrl Pts',(19.3356027965729,-0.178799726336078,
4.59372241551416));
#40500=CARTESIAN_POINT('Ctrl Pts',(19.3500510044034,-0.35887750705714,4.50729762043595));
#40501=CARTESIAN_POINT('Ctrl Pts',(19.3644992122339,-0.469016560662847,
4.36625733020606));
#40502=CARTESIAN_POINT('Ctrl Pts',(19.3804044909215,-0.590262902253753,
4.21099342837053));
#40503=CARTESIAN_POINT('Ctrl Pts',(19.3963097696091,-0.626752877433238,
3.98954286415574));
#40504=CARTESIAN_POINT('Ctrl Pts',(19.4122150482967,-0.561731832709929,
3.80358636875254));
#40505=CARTESIAN_POINT('Ctrl Pts',(19.4281203269843,-0.49671078798662,3.61762987334934));
#40506=CARTESIAN_POINT('Ctrl Pts',(19.4440256056719,-0.330178723360516,
3.46716744675772));
#40507=CARTESIAN_POINT('Ctrl Pts',(19.4599308843595,-0.138600118749324,
3.42128506802099));
#40508=CARTESIAN_POINT('Ctrl Pts',(19.4758361630471,0.0529784858618673,
3.37540268928427));
#40509=CARTESIAN_POINT('Ctrl Pts',(19.4917414417347,0.269603630458146,3.43410035840244));
#40510=CARTESIAN_POINT('Ctrl Pts',(19.5076467204224,0.411810215621333,3.57042659223364));
#40511=CARTESIAN_POINT('Ctrl Pts',(19.52355199911,0.554016800784528,3.70675282606484));
#40512=CARTESIAN_POINT('Ctrl Pts',(19.5394572777976,0.621804826514621,3.92070762460909));
#40513=CARTESIAN_POINT('Ctrl Pts',(19.5553625564852,0.584048894878601,4.11405198996909));
#40514=CARTESIAN_POINT('Ctrl Pts',(19.5712678351728,0.546292963242583,4.30739635532907));
#40515=CARTESIAN_POINT('Ctrl Pts',(19.5871731138604,0.402993074240464,4.4801302875048));
#40516=CARTESIAN_POINT('Ctrl Pts',(19.6030783925481,0.219946482677819,4.55294168410437));
#40517=CARTESIAN_POINT('Ctrl Pts',(19.6091037912795,0.150602919307179,4.5805248346624));
#40518=CARTESIAN_POINT('Ctrl Pts',(19.615129190011,0.0755552166468998,4.59376787586841));
#40519=CARTESIAN_POINT('Ctrl Pts',(19.6211545887425,0.000364945106097663,
4.59334757974602));
#40520=CARTESIAN_POINT('Origin',(4.,0.,4.));
#40521=CARTESIAN_POINT('',(20.0288454112575,-0.000266600559035268,4.5949350414008));
#40522=CARTESIAN_POINT('',(19.9211545887425,-0.000461335262921832,4.59353843444423));
#40523=CARTESIAN_POINT('',(4.,-7.27562663373442E-17,4.5941));
#40524=CARTESIAN_POINT('Ctrl Pts',(20.0288454112575,-0.000266600559035268,
4.5949350414008));
#40525=CARTESIAN_POINT('Ctrl Pts',(20.0141521649359,0.181839152323842,4.59391190659116));
#40526=CARTESIAN_POINT('Ctrl Pts',(19.9994589186142,0.364814066967773,4.50413264800542));
#40527=CARTESIAN_POINT('Ctrl Pts',(19.9847656722925,0.474598868642052,4.35899217880197));
#40528=CARTESIAN_POINT('Ctrl Pts',(19.9688603936049,0.593439717564554,4.20187920587587));
#40529=CARTESIAN_POINT('Ctrl Pts',(19.9529551149173,0.626517665065843,3.97989492921597));
#40530=CARTESIAN_POINT('Ctrl Pts',(19.9370498362297,0.558641803885684,3.79496194153783));
#40531=CARTESIAN_POINT('Ctrl Pts',(19.9211445575421,0.490765942705524,3.61002895385969));
#40532=CARTESIAN_POINT('Ctrl Pts',(19.9052392788545,0.321936272843916,3.46214725516331));
#40533=CARTESIAN_POINT('Ctrl Pts',(19.8893340001669,0.129673778938228,3.41921955761011));
#40534=CARTESIAN_POINT('Ctrl Pts',(19.8734287214793,-0.0625887149674591,
3.37629186005692));
#40535=CARTESIAN_POINT('Ctrl Pts',(19.8575234427916,-0.278284032917226,
3.43831816364691));
#40536=CARTESIAN_POINT('Ctrl Pts',(19.841618164104,-0.418374827314372,3.57681771754473));
#40537=CARTESIAN_POINT('Ctrl Pts',(19.8257128854164,-0.558465621711518,
3.71531727144255));
#40538=CARTESIAN_POINT('Ctrl Pts',(19.8098076067288,-0.622951892556044,
3.9302900756482));
#40539=CARTESIAN_POINT('Ctrl Pts',(19.7939023280412,-0.58222383973146,4.12303018792675));
#40540=CARTESIAN_POINT('Ctrl Pts',(19.7779970493536,-0.541495786906873,
4.3157703002053));
#40541=CARTESIAN_POINT('Ctrl Pts',(19.762091770666,-0.395553410413165,4.48627772055676));
#40542=CARTESIAN_POINT('Ctrl Pts',(19.7461864919784,-0.211407504401025,
4.55626240372308));
#40543=CARTESIAN_POINT('Ctrl Pts',(19.7404061317381,-0.144484459893097,
4.58169651826758));
#40544=CARTESIAN_POINT('Ctrl Pts',(19.7346257714978,-0.0725156072563085,
4.59385388977766));
#40545=CARTESIAN_POINT('Ctrl Pts',(19.7288454112575,-0.000401422265437046,
4.59340756962635));
#40546=CARTESIAN_POINT('Ctrl Pts',(19.6211545887425,0.000364945106097663,
4.59334757974602));
#40547=CARTESIAN_POINT('Ctrl Pts',(19.6310344686986,-0.122924963130536,
4.59265841784648));
#40548=CARTESIAN_POINT('Ctrl Pts',(19.6409143486547,-0.246598186964828,
4.55523353708024));
#40549=CARTESIAN_POINT('Ctrl Pts',(19.6507942286109,-0.346136160298313,
4.48405653351353));
#40550=CARTESIAN_POINT('Ctrl Pts',(19.6666995072985,-0.506378917588675,
4.36947112529969));
#40551=CARTESIAN_POINT('Ctrl Pts',(19.6826047859861,-0.60407113804621,4.16741144784858));
#40552=CARTESIAN_POINT('Ctrl Pts',(19.6985100646737,-0.5943566574826,3.97065479758251));
#40553=CARTESIAN_POINT('Ctrl Pts',(19.7144153433613,-0.584642176918989,
3.77389814731645));
#40554=CARTESIAN_POINT('Ctrl Pts',(19.7303206220489,-0.467520995334232,
3.58244452423543));
#40555=CARTESIAN_POINT('Ctrl Pts',(19.7462259007365,-0.296770260159971,
3.48420125495101));
#40556=CARTESIAN_POINT('Ctrl Pts',(19.7621311794242,-0.12601952498572,3.38595798566659));
#40557=CARTESIAN_POINT('Ctrl Pts',(19.7780364581118,0.098360763778029,3.38092507017875));
#40558=CARTESIAN_POINT('Ctrl Pts',(19.7939417367994,0.27334477570878,3.47141355644931));
#40559=CARTESIAN_POINT('Ctrl Pts',(19.809847015487,0.448328787639532,3.56190204271987));
#40560=CARTESIAN_POINT('Ctrl Pts',(19.8257522941746,0.573916522737285,3.74791193074883));
#40561=CARTESIAN_POINT('Ctrl Pts',(19.8416575728622,0.592443207149574,3.9440350735258));
#40562=CARTESIAN_POINT('Ctrl Pts',(19.8575628515498,0.610969891561863,4.14015821630277));
#40563=CARTESIAN_POINT('Ctrl Pts',(19.8734681302375,0.522435525288687,4.34639461382776));
#40564=CARTESIAN_POINT('Ctrl Pts',(19.8893734089251,0.367491719635661,4.46804975837363));
#40565=CARTESIAN_POINT('Ctrl Pts',(19.8999671355309,0.264291244586565,4.54907828775811));
#40566=CARTESIAN_POINT('Ctrl Pts',(19.9105608621367,0.131629953687138,4.59258455010229));
#40567=CARTESIAN_POINT('Ctrl Pts',(19.9211545887425,-0.000461335262921832,
4.59353843444423));
#40568=CARTESIAN_POINT('Origin',(4.,0.,4.));
#40569=CARTESIAN_POINT('',(20.3288454112575,0.000547175593784699,4.59423670486774));
#40570=CARTESIAN_POINT('',(20.2211545887425,-0.000159442692484791,4.59503650419094));
#40571=CARTESIAN_POINT('',(4.,-7.27562663373442E-17,4.5941));
#40572=CARTESIAN_POINT('Ctrl Pts',(20.3288454112575,0.000547175593784699,
4.59423670486774));
#40573=CARTESIAN_POINT('Ctrl Pts',(20.3254891157492,0.0422991098545892,
4.59465405164581));
#40574=CARTESIAN_POINT('Ctrl Pts',(20.3221328202408,0.0839734681026259,
4.59066114403672));
#40575=CARTESIAN_POINT('Ctrl Pts',(20.3187765247324,0.124636177719752,4.58197547152207));
#40576=CARTESIAN_POINT('Ctrl Pts',(20.3028712460448,0.317334266145104,4.54081460186972));
#40577=CARTESIAN_POINT('Ctrl Pts',(20.2869659673572,0.48731321493246,4.39426577643889));
#40578=CARTESIAN_POINT('Ctrl Pts',(20.2710606886696,0.556778600406793,4.20989870881916));
#40579=CARTESIAN_POINT('Ctrl Pts',(20.255155409982,0.626243985881127,4.02553164119943));
#40580=CARTESIAN_POINT('Ctrl Pts',(20.2392501312944,0.595195808042437,3.80334633139079));
#40581=CARTESIAN_POINT('Ctrl Pts',(20.2233448526068,0.477757630702126,3.64521515909767));
#40582=CARTESIAN_POINT('Ctrl Pts',(20.2074395739191,0.360319453361808,3.48708398680455));
#40583=CARTESIAN_POINT('Ctrl Pts',(20.1915342952315,0.156491276519859,3.39300695202695));
#40584=CARTESIAN_POINT('Ctrl Pts',(20.1756290165439,-0.04006765138094,3.40625706061923));
#40585=CARTESIAN_POINT('Ctrl Pts',(20.1597237378563,-0.236626579281727,
3.4195071692115));
#40586=CARTESIAN_POINT('Ctrl Pts',(20.1438184591687,-0.425916258241364,
3.54008442117362));
#40587=CARTESIAN_POINT('Ctrl Pts',(20.1279131804811,-0.521059912873915,
3.71258420787224));
#40588=CARTESIAN_POINT('Ctrl Pts',(20.1120079017935,-0.616203567506467,
3.88508399457085));
#40589=CARTESIAN_POINT('Ctrl Pts',(20.0961026231058,-0.617201197811932,
4.10950631600596));
#40590=CARTESIAN_POINT('Ctrl Pts',(20.0801973444182,-0.523575121773085,
4.28282745216878));
#40591=CARTESIAN_POINT('Ctrl Pts',(20.0642920657306,-0.429949045734243,
4.45614858833159));
#40592=CARTESIAN_POINT('Ctrl Pts',(20.048386787043,-0.241699263351099,4.57836853922213));
#40593=CARTESIAN_POINT('Ctrl Pts',(20.0324815083554,-0.0452724969876719,
4.59335768007126));
#40594=CARTESIAN_POINT('Ctrl Pts',(20.0312694759895,-0.030304158296608,
4.59449989984645));
#40595=CARTESIAN_POINT('Ctrl Pts',(20.0300574436235,-0.0152883365109376,
4.5950194388496));
#40596=CARTESIAN_POINT('Ctrl Pts',(20.0288454112575,-0.000266600559035268,
4.5949350414008));
#40597=CARTESIAN_POINT('Ctrl Pts',(19.9211545887425,-0.000461335262921832,
4.59353843444423));
#40598=CARTESIAN_POINT('Ctrl Pts',(19.9264661408243,-0.0666901315043342,
4.5940166992278));
#40599=CARTESIAN_POINT('Ctrl Pts',(19.9317776929061,-0.132775635823809,
4.58379778651276));
#40600=CARTESIAN_POINT('Ctrl Pts',(19.9370892449879,-0.194932679790098,
4.56224768701753));
#40601=CARTESIAN_POINT('Ctrl Pts',(19.9529945236755,-0.381060028529917,
4.49771657954882));
#40602=CARTESIAN_POINT('Ctrl Pts',(19.9688998023631,-0.531961480976676,
4.33158047304464));
#40603=CARTESIAN_POINT('Ctrl Pts',(19.9848050810507,-0.578348134104426,
4.14012389605102));
#40604=CARTESIAN_POINT('Ctrl Pts',(20.0007103597384,-0.624734787232175,
3.94866731905739));
#40605=CARTESIAN_POINT('Ctrl Pts',(20.016615638426,-0.566606641040915,3.73189027157431));
#40606=CARTESIAN_POINT('Ctrl Pts',(20.0325209171136,-0.430656211588969,
3.58932409618151));
#40607=CARTESIAN_POINT('Ctrl Pts',(20.0484261958012,-0.294705782137024,
3.44675792078871));
#40608=CARTESIAN_POINT('Ctrl Pts',(20.0643314744888,-0.080933069424392,
3.37840261748619));
#40609=CARTESIAN_POINT('Ctrl Pts',(20.0802367531764,0.112511319004002,3.41565067076361));
#40610=CARTESIAN_POINT('Ctrl Pts',(20.096142031864,0.305955707432406,3.45289872404102));
#40611=CARTESIAN_POINT('Ctrl Pts',(20.1120473105516,0.479071771576571,3.59575013389837));
#40612=CARTESIAN_POINT('Ctrl Pts',(20.1279525892393,0.552362916535151,3.77860107435498));
#40613=CARTESIAN_POINT('Ctrl Pts',(20.1438578679269,0.625654061493722,3.96145201481158));
#40614=CARTESIAN_POINT('Ctrl Pts',(20.1597631466145,0.599120287266732,4.18430248586742));
#40615=CARTESIAN_POINT('Ctrl Pts',(20.1756684253021,0.484961816589866,4.3448525870839));
#40616=CARTESIAN_POINT('Ctrl Pts',(20.1908304797822,0.376137759761604,4.49790047950022));
#40617=CARTESIAN_POINT('Ctrl Pts',(20.2059925342623,0.187686755696174,4.59433432972249));
#40618=CARTESIAN_POINT('Ctrl Pts',(20.2211545887425,-0.000159442692484791,
4.59503650419094));
#40619=CARTESIAN_POINT('Origin',(4.,0.,4.));
#40620=CARTESIAN_POINT('',(20.6288454112575,1.84392275237588E-6,4.59415158619139));
#40621=CARTESIAN_POINT('',(20.5211545887425,0.00014515264107467,4.59408556636595));
#40622=CARTESIAN_POINT('',(4.,-7.27562663373442E-17,4.5941));
#40623=CARTESIAN_POINT('Ctrl Pts',(20.6288454112575,1.84392275237588E-6,
4.59415158619139));
#40624=CARTESIAN_POINT('Ctrl Pts',(20.6209207878748,0.0985777406598016,
4.59414764832452));
#40625=CARTESIAN_POINT('Ctrl Pts',(20.6129961644921,0.197149291092008,4.56908802213256));
#40626=CARTESIAN_POINT('Ctrl Pts',(20.6050715411094,0.283761277174982,4.52200793915563));
#40627=CARTESIAN_POINT('Ctrl Pts',(20.5971189017656,0.370679463050262,4.47476141372331));
#40628=CARTESIAN_POINT('Ctrl Pts',(20.5891662624218,0.445553373684486,4.40533845822152));
#40629=CARTESIAN_POINT('Ctrl Pts',(20.581213623078,0.499196468040806,4.3222224876916));
#40630=CARTESIAN_POINT('Ctrl Pts',(20.5732609837342,0.552839562397126,4.23910651716169));
#40631=CARTESIAN_POINT('Ctrl Pts',(20.5653083443904,0.585251840475543,4.14229753160364));
#40632=CARTESIAN_POINT('Ctrl Pts',(20.5573557050466,0.592531230276538,4.04364021904617));
#40633=CARTESIAN_POINT('Ctrl Pts',(20.5494030657028,0.599810620077534,3.9449829064887));
#40634=CARTESIAN_POINT('Ctrl Pts',(20.541450426359,0.581957121601108,3.84447726693182));
#40635=CARTESIAN_POINT('Ctrl Pts',(20.5334977870152,0.541038843355354,3.75439549632807));
#40636=CARTESIAN_POINT('Ctrl Pts',(20.5255451476714,0.5001205651096,3.66431372572433));
#40637=CARTESIAN_POINT('Ctrl Pts',(20.5175925083276,0.436137507094518,3.58465582407373));
#40638=CARTESIAN_POINT('Ctrl Pts',(20.5096398689838,0.357128912623608,3.5251911792601));
#40639=CARTESIAN_POINT('Ctrl Pts',(20.50168722964,0.278120318152698,3.46572653444646));
#40640=CARTESIAN_POINT('Ctrl Pts',(20.4937345902962,0.184086187225959,3.42645514646979));
#40641=CARTESIAN_POINT('Ctrl Pts',(20.4857819509524,0.0861162623359374,
3.4121221101222));
#40642=CARTESIAN_POINT('Ctrl Pts',(20.4778293116085,-0.0118536625540841,
3.39778907377461));
#40643=CARTESIAN_POINT('Ctrl Pts',(20.4698766722647,-0.113759381407388,
3.4083943890561));
#40644=CARTESIAN_POINT('Ctrl Pts',(20.4619240329209,-0.206384677702653,
3.44274365129583));
#40645=CARTESIAN_POINT('Ctrl Pts',(20.4539713935771,-0.299009973997917,
3.47709291353557));
#40646=CARTESIAN_POINT('Ctrl Pts',(20.4460187542333,-0.382354847735142,
3.53518612273354));
#40647=CARTESIAN_POINT('Ctrl Pts',(20.4380661148895,-0.447563842371028,
3.60976099223211));
#40648=CARTESIAN_POINT('Ctrl Pts',(20.4301134755457,-0.512772837006921,
3.68433586173069));
#40649=CARTESIAN_POINT('Ctrl Pts',(20.4221608362019,-0.559845952541473,
3.77539239152987));
#40650=CARTESIAN_POINT('Ctrl Pts',(20.4142081968581,-0.580888308445953,
3.87190852591559));
#40651=CARTESIAN_POINT('Ctrl Pts',(20.3983029181705,-0.622973020254908,
4.06494079468701));
#40652=CARTESIAN_POINT('Ctrl Pts',(20.3823976394829,-0.5609346935436,4.27981148180459));
#40653=CARTESIAN_POINT('Ctrl Pts',(20.3664923607953,-0.422206916156273,
4.41936036842645));
#40654=CARTESIAN_POINT('Ctrl Pts',(20.353943377616,-0.312753156865475,4.52946196836027));
#40655=CARTESIAN_POINT('Ctrl Pts',(20.3413943944368,-0.155560747392339,
4.59267627084609));
#40656=CARTESIAN_POINT('Ctrl Pts',(20.3288454112575,0.000547175593784699,
4.59423670486774));
#40657=CARTESIAN_POINT('Ctrl Pts',(20.2211545887425,-0.000159442692484791,
4.59503650419094));
#40658=CARTESIAN_POINT('Ctrl Pts',(20.22189781295,-0.00936741923094289,
4.59507092387091));
#40659=CARTESIAN_POINT('Ctrl Pts',(20.2226410371574,-0.0185739425223631,
4.59487531632137));
#40660=CARTESIAN_POINT('Ctrl Pts',(20.2233842613649,-0.0277695625699301,
4.59444507412072));
#40661=CARTESIAN_POINT('Ctrl Pts',(20.2392895400526,-0.224559303926058,
4.58523772856393));
#40662=CARTESIAN_POINT('Ctrl Pts',(20.2551948187402,-0.416355619511548,
4.46857330607325));
#40663=CARTESIAN_POINT('Ctrl Pts',(20.2711000974278,-0.51503297954037,4.29810345018796));
#40664=CARTESIAN_POINT('Ctrl Pts',(20.2870053761154,-0.613710339569191,
4.12763359430267));
#40665=CARTESIAN_POINT('Ctrl Pts',(20.302910654803,-0.619268744041345,3.90335830502277));
#40666=CARTESIAN_POINT('Ctrl Pts',(20.3188159334906,-0.529271009537506,
3.72809546473432));
#40667=CARTESIAN_POINT('Ctrl Pts',(20.3347212121782,-0.439273275033663,
3.55283262444587));
#40668=CARTESIAN_POINT('Ctrl Pts',(20.3506264908658,-0.253719401553817,
3.42658223314887));
#40669=CARTESIAN_POINT('Ctrl Pts',(20.3665317695535,-0.0575887485100287,
3.40762076142476));
#40670=CARTESIAN_POINT('Ctrl Pts',(20.3824370482411,0.138541904533748,3.38865928970065));
#40671=CARTESIAN_POINT('Ctrl Pts',(20.3983423269287,0.345249337141466,3.47698673754941));
#40672=CARTESIAN_POINT('Ctrl Pts',(20.4142476056163,0.467192899405167,3.63141813202173));
#40673=CARTESIAN_POINT('Ctrl Pts',(20.4301528843039,0.589136461668875,3.78584952649406));
#40674=CARTESIAN_POINT('Ctrl Pts',(20.4460581629915,0.626316153588557,4.00638486758996));
#40675=CARTESIAN_POINT('Ctrl Pts',(20.4619634416791,0.562534942182983,4.19337293359078));
#40676=CARTESIAN_POINT('Ctrl Pts',(20.4699160810229,0.530644336480201,4.28686696659118));
#40677=CARTESIAN_POINT('Ctrl Pts',(20.4778687203667,0.473513504946115,4.3719741808178));
#40678=CARTESIAN_POINT('Ctrl Pts',(20.4858213597105,0.400240502138227,4.43864269813793));
#40679=CARTESIAN_POINT('Ctrl Pts',(20.4937739990544,0.326967499330329,4.50531121545807));
#40680=CARTESIAN_POINT('Ctrl Pts',(20.5017266383982,0.237552325248626,4.55354103587171));
#40681=CARTESIAN_POINT('Ctrl Pts',(20.509679277742,0.141619450488441,4.57712494713439));
#40682=CARTESIAN_POINT('Ctrl Pts',(20.5135043814088,0.0954771353210092,
4.58846846487098));
#40683=CARTESIAN_POINT('Ctrl Pts',(20.5173294850756,0.0478269697500401,
4.59411022582368));
#40684=CARTESIAN_POINT('Ctrl Pts',(20.5211545887425,0.00014515264107467,
4.59408556636595));
#40685=CARTESIAN_POINT('Origin',(4.,0.,4.));
#40686=CARTESIAN_POINT('',(20.9288454112575,-6.4040329070536E-6,4.59405282094147));
#40687=CARTESIAN_POINT('',(20.8211545887425,5.65245430726296E-6,4.59414685459231));
#40688=CARTESIAN_POINT('',(4.,-7.27562663373442E-17,4.5941));
#40689=CARTESIAN_POINT('Ctrl Pts',(20.9288454112575,-6.4040329070536E-6,
4.59405282094147));
#40690=CARTESIAN_POINT('Ctrl Pts',(20.9243050993443,0.0564994875152707,
4.59403151438501));
#40691=CARTESIAN_POINT('Ctrl Pts',(20.9197647874311,0.113011285737041,4.58603249222448));
#40692=CARTESIAN_POINT('Ctrl Pts',(20.9152244755179,0.167207550221224,4.57013805289591));
#40693=CARTESIAN_POINT('Ctrl Pts',(20.9072718361741,0.262135685878584,4.5422979516059));
#40694=CARTESIAN_POINT('Ctrl Pts',(20.8993191968303,0.349959832061366,4.49023494241839));
#40695=CARTESIAN_POINT('Ctrl Pts',(20.8913665574865,0.419942299057043,4.42031443844746));
#40696=CARTESIAN_POINT('Ctrl Pts',(20.8834139181427,0.489924766052721,4.35039393447653));
#40697=CARTESIAN_POINT('Ctrl Pts',(20.8754612787989,0.542065553861293,4.26261593572219));
#40698=CARTESIAN_POINT('Ctrl Pts',(20.8675086394551,0.569989725359365,4.16771249585991));
#40699=CARTESIAN_POINT('Ctrl Pts',(20.8595560001113,0.597913896857441,4.07280905599763));
#40700=CARTESIAN_POINT('Ctrl Pts',(20.8516033607674,0.601621452045013,3.97078017502742));
#40701=CARTESIAN_POINT('Ctrl Pts',(20.8436507214236,0.580659121393648,3.87410027737825));
#40702=CARTESIAN_POINT('Ctrl Pts',(20.8356980820798,0.559696790742287,3.77742037972911));
#40703=CARTESIAN_POINT('Ctrl Pts',(20.827745442736,0.514064574252002,3.686089465401));
#40704=CARTESIAN_POINT('Ctrl Pts',(20.8197928033922,0.44934157601673,3.61127397478397));
#40705=CARTESIAN_POINT('Ctrl Pts',(20.8118401640484,0.384618577781443,3.53645848416692));
#40706=CARTESIAN_POINT('Ctrl Pts',(20.8038875247046,0.300804797801161,3.47815841726095));
#40707=CARTESIAN_POINT('Ctrl Pts',(20.7959348853608,0.208147717693743,3.44350176598286));
#40708=CARTESIAN_POINT('Ctrl Pts',(20.787982246017,0.115490637586335,3.40884511470477));
#40709=CARTESIAN_POINT('Ctrl Pts',(20.7800296066732,0.0139902573517945,
3.39783187905454));
#40710=CARTESIAN_POINT('Ctrl Pts',(20.7720769673294,-0.0839438183138644,
3.41180854931868));
#40711=CARTESIAN_POINT('Ctrl Pts',(20.7641243279856,-0.181877893979523,
3.42578521958283));
#40712=CARTESIAN_POINT('Ctrl Pts',(20.7561716886418,-0.2762456650763,3.46475179576135));
#40713=CARTESIAN_POINT('Ctrl Pts',(20.748219049298,-0.355509010203556,3.52394413563581));
#40714=CARTESIAN_POINT('Ctrl Pts',(20.7402664099542,-0.434772355330821,
3.58313647551028));
#40715=CARTESIAN_POINT('Ctrl Pts',(20.7323137706103,-0.498931274488562,
3.66255457908069));
#40716=CARTESIAN_POINT('Ctrl Pts',(20.7243611312665,-0.54014217617541,3.75248840252759));
#40717=CARTESIAN_POINT('Ctrl Pts',(20.7164084919227,-0.581353077862249,
3.84242222597448));
#40718=CARTESIAN_POINT('Ctrl Pts',(20.7084558525789,-0.599615962078206,
3.94287176929784));
#40719=CARTESIAN_POINT('Ctrl Pts',(20.7005032132351,-0.592696601504336,
4.0415558946729));
#40720=CARTESIAN_POINT('Ctrl Pts',(20.6925505738913,-0.585777240930466,
4.14024002004797));
#40721=CARTESIAN_POINT('Ctrl Pts',(20.6845979345475,-0.553675635566762,
4.23715872747472));
#40722=CARTESIAN_POINT('Ctrl Pts',(20.6766452952037,-0.50031917594212,4.32046203197985));
#40723=CARTESIAN_POINT('Ctrl Pts',(20.6686926558599,-0.446962716317479,
4.40376533648498));
#40724=CARTESIAN_POINT('Ctrl Pts',(20.6607400165161,-0.3723514024319,4.47345323806848));
#40725=CARTESIAN_POINT('Ctrl Pts',(20.6527873771723,-0.285602702553558,
4.52100610813718));
#40726=CARTESIAN_POINT('Ctrl Pts',(20.6448347378285,-0.198854002675205,
4.56855897820588));
#40727=CARTESIAN_POINT('Ctrl Pts',(20.6368820984847,-0.099967916804087,
4.59397681675976));
#40728=CARTESIAN_POINT('Ctrl Pts',(20.6289294591409,-0.00104364331035449,
4.59415068835528));
#40729=CARTESIAN_POINT('Ctrl Pts',(20.6289014431798,-0.000695147863829354,
4.59415130087895));
#40730=CARTESIAN_POINT('Ctrl Pts',(20.6288734272186,-0.000346651943377611,
4.59415160011295));
#40731=CARTESIAN_POINT('Ctrl Pts',(20.6288454112575,1.84392275237588E-6,
4.59415158619139));
#40732=CARTESIAN_POINT('Ctrl Pts',(20.5211545887425,0.00014515264107467,
4.59408556636595));
#40733=CARTESIAN_POINT('Ctrl Pts',(20.5252821244194,-0.0513066296901884,
4.59405895720698));
#40734=CARTESIAN_POINT('Ctrl Pts',(20.5294096600964,-0.102795266482965,
4.58743447362686));
#40735=CARTESIAN_POINT('Ctrl Pts',(20.5335371957734,-0.152465997634008,
4.57425651377355));
#40736=CARTESIAN_POINT('Ctrl Pts',(20.5414898351172,-0.248167995557571,
4.5488661670383));
#40737=CARTESIAN_POINT('Ctrl Pts',(20.549442474461,-0.33712141596603,4.49914747145609));
#40738=CARTESIAN_POINT('Ctrl Pts',(20.5573951138048,-0.408848640915227,
4.43107686705031));
#40739=CARTESIAN_POINT('Ctrl Pts',(20.5653477531486,-0.480575865864423,
4.36300626264453));
#40740=CARTESIAN_POINT('Ctrl Pts',(20.5733003924924,-0.535076895354358,
4.27658374941519));
#40741=CARTESIAN_POINT('Ctrl Pts',(20.5812530318362,-0.565476628275392,
4.18243021985824));
#40742=CARTESIAN_POINT('Ctrl Pts',(20.58920567118,-0.595876361196427,4.08827669030129));
#40743=CARTESIAN_POINT('Ctrl Pts',(20.5971583105238,-0.602174797548561,
3.98639214441672));
#40744=CARTESIAN_POINT('Ctrl Pts',(20.6051109498677,-0.58371402745925,3.88920441471463));
#40745=CARTESIAN_POINT('Ctrl Pts',(20.6130635892115,-0.565253257369939,
3.79201668501254));
#40746=CARTESIAN_POINT('Ctrl Pts',(20.6210162285553,-0.522033280839182,
3.69952577149293));
#40747=CARTESIAN_POINT('Ctrl Pts',(20.6289688678991,-0.459278917219465,
3.62305528060961));
#40748=CARTESIAN_POINT('Ctrl Pts',(20.6369215072429,-0.396524553599749,
3.54658478972629));
#40749=CARTESIAN_POINT('Ctrl Pts',(20.6448741465867,-0.314235802891072,
3.48613472147926));
#40750=CARTESIAN_POINT('Ctrl Pts',(20.6528267859305,-0.222505051509483,
3.44908779917463));
#40751=CARTESIAN_POINT('Ctrl Pts',(20.6607794252743,-0.130774300127894,
3.41204087687));
#40752=CARTESIAN_POINT('Ctrl Pts',(20.6687320646181,-0.029601548073392,
3.39839710050778));
#40753=CARTESIAN_POINT('Ctrl Pts',(20.6766847039619,0.0686601223983595,
3.40982890848785));
#40754=CARTESIAN_POINT('Ctrl Pts',(20.6846373433057,0.1669217928701,3.42126071646792));
#40755=CARTESIAN_POINT('Ctrl Pts',(20.6925899826495,0.262272381759091,3.45776810879028));
#40756=CARTESIAN_POINT('Ctrl Pts',(20.7005426219933,0.343045155251024,3.51488528173127));
#40757=CARTESIAN_POINT('Ctrl Pts',(20.7084952613371,0.423817928742975,3.57200245467228));
#40758=CARTESIAN_POINT('Ctrl Pts',(20.7164479006809,0.490012886837861,3.64972940823193));
#40759=CARTESIAN_POINT('Ctrl Pts',(20.7244005400247,0.533541468465666,3.73856417004634));
#40760=CARTESIAN_POINT('Ctrl Pts',(20.7323531793686,0.577070050093471,3.82739893186076));
#40761=CARTESIAN_POINT('Ctrl Pts',(20.7403058187123,0.597932255254196,3.92734150192994));
#40762=CARTESIAN_POINT('Ctrl Pts',(20.7482584580562,0.593574919799613,4.02617190099588));
#40763=CARTESIAN_POINT('Ctrl Pts',(20.7562110974,0.589217584345031,4.1250023000618));
#40764=CARTESIAN_POINT('Ctrl Pts',(20.7641637367438,0.559640708275147,4.22272052812447));
#40765=CARTESIAN_POINT('Ctrl Pts',(20.7721163760876,0.508461778515953,4.30737953925928));
#40766=CARTESIAN_POINT('Ctrl Pts',(20.7800690154314,0.457282848756759,4.39203855039408));
#40767=CARTESIAN_POINT('Ctrl Pts',(20.7880216547752,0.384501865308254,4.46363834460102));
#40768=CARTESIAN_POINT('Ctrl Pts',(20.795974294119,0.299016600344635,4.51342469267633));
#40769=CARTESIAN_POINT('Ctrl Pts',(20.8039269334628,0.213531335381016,4.56321104075164));
#40770=CARTESIAN_POINT('Ctrl Pts',(20.8118795728066,0.115341788902283,4.59118394269532));
#40771=CARTESIAN_POINT('Ctrl Pts',(20.8198322121504,0.0164533379892873,
4.59392342516246));
#40772=CARTESIAN_POINT('Ctrl Pts',(20.8202730043478,0.0109722321971217,
4.59407526688998));
#40773=CARTESIAN_POINT('Ctrl Pts',(20.8207137965451,0.00548897925183007,
4.59414958726715));
#40774=CARTESIAN_POINT('Ctrl Pts',(20.8211545887425,5.65245430726296E-6,
4.59414685459231));
#40775=CARTESIAN_POINT('Origin',(4.,0.,4.));
#40776=CARTESIAN_POINT('',(21.2288454112575,1.28243205298473E-5,4.59412621697841));
#40777=CARTESIAN_POINT('',(21.1211545887425,-1.09306879613159E-5,4.5940621922514));
#40778=CARTESIAN_POINT('',(4.,-7.27562663373442E-17,4.5941));
#40779=CARTESIAN_POINT('Ctrl Pts',(21.2288454112575,1.28243205298473E-5,
4.59412621697841));
#40780=CARTESIAN_POINT('Ctrl Pts',(21.2276894108138,0.0143945780386088,
4.59413985249388));
#40781=CARTESIAN_POINT('Ctrl Pts',(21.2265334103701,0.028775363636007,4.59362827285675));
#40782=CARTESIAN_POINT('Ctrl Pts',(21.2253774099263,0.043117441953227,4.59258471957415));
#40783=CARTESIAN_POINT('Ctrl Pts',(21.2174247705826,0.141782954511012,4.58540565408365));
#40784=CARTESIAN_POINT('Ctrl Pts',(21.2094721312387,0.238616577754522,4.55305001116024));
#40785=CARTESIAN_POINT('Ctrl Pts',(21.2015194918949,0.321779082392626,4.49947370882601));
#40786=CARTESIAN_POINT('Ctrl Pts',(21.1935668525511,0.404941587030731,4.44589740649178));
#40787=CARTESIAN_POINT('Ctrl Pts',(21.1856142132073,0.474432973063433,4.37110044474674));
#40788=CARTESIAN_POINT('Ctrl Pts',(21.1776615738635,0.521756972098598,4.28422777087894));
#40789=CARTESIAN_POINT('Ctrl Pts',(21.1697089345197,0.569080971133768,4.19735509701114));
#40790=CARTESIAN_POINT('Ctrl Pts',(21.1617562951759,0.594237583171398,4.09840671102057));
#40791=CARTESIAN_POINT('Ctrl Pts',(21.1538036558321,0.594151069756079,3.9994804007435));
#40792=CARTESIAN_POINT('Ctrl Pts',(21.1458510164883,0.59406455634076,3.90055409046644));
#40793=CARTESIAN_POINT('Ctrl Pts',(21.1378983771445,0.568734917472505,3.80164985590287));
#40794=CARTESIAN_POINT('Ctrl Pts',(21.1299457378007,0.521259046500119,3.71486008677882));
#40795=CARTESIAN_POINT('Ctrl Pts',(21.1219930984569,0.473783175527722,3.62807031765475));
#40796=CARTESIAN_POINT('Ctrl Pts',(21.114040459113,0.40416107245118,3.5533950139702));
#40797=CARTESIAN_POINT('Ctrl Pts',(21.1060878197692,0.320904987578411,3.49996424865404));
#40798=CARTESIAN_POINT('Ctrl Pts',(21.0981351804254,0.237648902705652,3.44653348333788));
#40799=CARTESIAN_POINT('Ctrl Pts',(21.0901825410817,0.140758836036697,3.41434725639011));
#40800=CARTESIAN_POINT('Ctrl Pts',(21.0822299017378,0.042080917889342,3.40734077242984));
#40801=CARTESIAN_POINT('Ctrl Pts',(21.074277262394,-0.056597000258024,3.40033428846957));
#40802=CARTESIAN_POINT('Ctrl Pts',(21.0663246230502,-0.157062769883762,
3.41850754749682));
#40803=CARTESIAN_POINT('Ctrl Pts',(21.0583719837064,-0.247033082431791,
3.45963862106718));
#40804=CARTESIAN_POINT('Ctrl Pts',(21.0504193443626,-0.337003394979799,
3.50076969463752));
#40805=CARTESIAN_POINT('Ctrl Pts',(21.0424667050188,-0.416478250450111,
3.56485858275095));
#40806=CARTESIAN_POINT('Ctrl Pts',(21.034514065675,-0.475740765152555,3.644069545988));
#40807=CARTESIAN_POINT('Ctrl Pts',(21.0265614263312,-0.535003279855012,
3.72328050922507));
#40808=CARTESIAN_POINT('Ctrl Pts',(21.0186087869874,-0.574053453789596,
3.81761354758578));
#40809=CARTESIAN_POINT('Ctrl Pts',(21.0106561476436,-0.588116871685884,
3.91553516229212));
#40810=CARTESIAN_POINT('Ctrl Pts',(21.0027035082998,-0.60218028958217,4.01345677699845));
#40811=CARTESIAN_POINT('Ctrl Pts',(20.994750868956,-0.591256951440166,4.11496696805043));
#40812=CARTESIAN_POINT('Ctrl Pts',(20.9867982296121,-0.556682383467722,
4.20765473214191));
#40813=CARTESIAN_POINT('Ctrl Pts',(20.9788455902683,-0.522107815495282,
4.30034249623339));
#40814=CARTESIAN_POINT('Ctrl Pts',(20.9708929509246,-0.463882017692404,
4.38420783336438));
#40815=CARTESIAN_POINT('Ctrl Pts',(20.9629403115808,-0.389123888092725,
4.4489970636758));
#40816=CARTESIAN_POINT('Ctrl Pts',(20.9549876722369,-0.314365758493028,
4.51378629398723));
#40817=CARTESIAN_POINT('Ctrl Pts',(20.9470350328931,-0.223075297096518,
4.5594994174791));
#40818=CARTESIAN_POINT('Ctrl Pts',(20.9390823935493,-0.12641400383229,4.58054738252877));
#40819=CARTESIAN_POINT('Ctrl Pts',(20.9356700661187,-0.0849384674446181,
4.58957866703598));
#40820=CARTESIAN_POINT('Ctrl Pts',(20.9322577386881,-0.0424741039190781,
4.59406883414683));
#40821=CARTESIAN_POINT('Ctrl Pts',(20.9288454112575,-6.4040329070536E-6,
4.59405282094147));
#40822=CARTESIAN_POINT('Ctrl Pts',(20.8211545887425,5.65245430726296E-6,
4.59414685459231));
#40823=CARTESIAN_POINT('Ctrl Pts',(20.8286664358889,-0.0934395423672534,
4.59410028517524));
#40824=CARTESIAN_POINT('Ctrl Pts',(20.8361782830354,-0.18690618531264,4.57167601133058));
#40825=CARTESIAN_POINT('Ctrl Pts',(20.8436901301818,-0.270133012248912,
4.529191754035));
#40826=CARTESIAN_POINT('Ctrl Pts',(20.8516427695256,-0.358243556226857,
4.4842145374498));
#40827=CARTESIAN_POINT('Ctrl Pts',(20.8595954088694,-0.434877288835492,
4.41675404128879));
#40828=CARTESIAN_POINT('Ctrl Pts',(20.8675480482133,-0.490664589397756,
4.33505825661903));
#40829=CARTESIAN_POINT('Ctrl Pts',(20.8755006875571,-0.546451889960021,
4.25336247194927));
#40830=CARTESIAN_POINT('Ctrl Pts',(20.8834533269009,-0.581392758475918,
4.15743139877076));
#40831=CARTESIAN_POINT('Ctrl Pts',(20.8914059662447,-0.591215252505097,
4.05899390323763));
#40832=CARTESIAN_POINT('Ctrl Pts',(20.8993586055885,-0.601037746534278,
3.96055640770449));
#40833=CARTESIAN_POINT('Ctrl Pts',(20.9073112449323,-0.585741866076735,
3.85961248981672));
#40834=CARTESIAN_POINT('Ctrl Pts',(20.9152638842761,-0.547197711916726,
3.76850392583047));
#40835=CARTESIAN_POINT('Ctrl Pts',(20.9232165236199,-0.508653557756717,
3.67739536184422));
#40836=CARTESIAN_POINT('Ctrl Pts',(20.9311691629637,-0.446861129894262,
3.59612215175949));
#40837=CARTESIAN_POINT('Ctrl Pts',(20.9391218023075,-0.369375409551539,
3.53462104847409));
#40838=CARTESIAN_POINT('Ctrl Pts',(20.9470744416513,-0.291889689208826,
3.4731199451887));
#40839=CARTESIAN_POINT('Ctrl Pts',(20.9550270809951,-0.198710676385865,
3.43139094870266));
#40840=CARTESIAN_POINT('Ctrl Pts',(20.9629797203389,-0.101230766359376,
3.41453599926792));
#40841=CARTESIAN_POINT('Ctrl Pts',(20.9709323596827,-0.00375085633288601,
3.39768104983318));
#40842=CARTESIAN_POINT('Ctrl Pts',(20.9788849990265,0.0980299508971346,
3.40570014744973));
#40843=CARTESIAN_POINT('Ctrl Pts',(20.9868376383704,0.191667561123074,3.43761284710704));
#40844=CARTESIAN_POINT('Ctrl Pts',(20.9947902777142,0.285305171349014,3.46952554676435));
#40845=CARTESIAN_POINT('Ctrl Pts',(21.002742917058,0.37079958457088,3.52533184846243));
#40846=CARTESIAN_POINT('Ctrl Pts',(21.0106955564018,0.437697946637459,3.59820867233944));
#40847=CARTESIAN_POINT('Ctrl Pts',(21.0186481957456,0.504596308704037,3.67108549621644));
#40848=CARTESIAN_POINT('Ctrl Pts',(21.0266008350894,0.552898619615334,3.76103284227238));
#40849=CARTESIAN_POINT('Ctrl Pts',(21.0345534744332,0.576699262792956,3.8570534220826));
#40850=CARTESIAN_POINT('Ctrl Pts',(21.042506113777,0.600499905970578,3.95307400189282));
#40851=CARTESIAN_POINT('Ctrl Pts',(21.0504587531208,0.599798881414527,4.05516781545734));
#40852=CARTESIAN_POINT('Ctrl Pts',(21.0584113924646,0.574681899562831,4.15085250374278));
#40853=CARTESIAN_POINT('Ctrl Pts',(21.0663640318084,0.549564917711138,4.24653719202821));
#40854=CARTESIAN_POINT('Ctrl Pts',(21.0743166711522,0.500031978563804,4.33581275503458));
#40855=CARTESIAN_POINT('Ctrl Pts',(21.082269310496,0.432139158218639,4.40776403918836));
#40856=CARTESIAN_POINT('Ctrl Pts',(21.0902219498398,0.364246337873458,4.47971532334216));
#40857=CARTESIAN_POINT('Ctrl Pts',(21.0981745891836,0.277993636330433,4.53434232864337));
#40858=CARTESIAN_POINT('Ctrl Pts',(21.1061272285274,0.183926621270441,4.56496615973523));
#40859=CARTESIAN_POINT('Ctrl Pts',(21.1111363485991,0.124676735433976,4.5842551580617));
#40860=CARTESIAN_POINT('Ctrl Pts',(21.1161454686708,0.0623266393968894,
4.59402126159141));
#40861=CARTESIAN_POINT('Ctrl Pts',(21.1211545887425,-1.09306879613159E-5,
4.5940621922514));
#40862=CARTESIAN_POINT('Origin',(4.,0.,4.));
#40863=CARTESIAN_POINT('',(21.5288454112575,-1.51073027558624E-5,4.59408477831653));
#40864=CARTESIAN_POINT('',(21.4211545887425,1.51733402061755E-5,4.59410821609125));
#40865=CARTESIAN_POINT('',(4.,-7.27562663373442E-17,4.5941));
#40866=CARTESIAN_POINT('Ctrl Pts',(21.5288454112575,-1.51073027558624E-5,
4.59408477831653));
#40867=CARTESIAN_POINT('Ctrl Pts',(21.5231210829395,0.0712153309254728,
4.59401644885886));
#40868=CARTESIAN_POINT('Ctrl Pts',(21.5173967546214,0.142469702059594,4.58119587380047));
#40869=CARTESIAN_POINT('Ctrl Pts',(21.5116724263034,0.209120766622247,4.55613331912479));
#40870=CARTESIAN_POINT('Ctrl Pts',(21.5037197869596,0.301717111362981,4.52131465616629));
#40871=CARTESIAN_POINT('Ctrl Pts',(21.4957671476158,0.385428743083265,4.46286809139133));
#40872=CARTESIAN_POINT('Ctrl Pts',(21.4878145082719,0.450020774675764,4.38793951336988));
#40873=CARTESIAN_POINT('Ctrl Pts',(21.4798618689281,0.514612806268249,4.31301093534845));
#40874=CARTESIAN_POINT('Ctrl Pts',(21.4719092295843,0.560085237732952,4.22160034408054));
#40875=CARTESIAN_POINT('Ctrl Pts',(21.4639565902405,0.58087844500124,4.1248839293359));
#40876=CARTESIAN_POINT('Ctrl Pts',(21.4560039508967,0.601671652269532,4.02816751459124));
#40877=CARTESIAN_POINT('Ctrl Pts',(21.4480513115529,0.597785635341394,3.92614527636987));
#40878=CARTESIAN_POINT('Ctrl Pts',(21.4400986722091,0.569695512712777,3.83129082280931));
#40879=CARTESIAN_POINT('Ctrl Pts',(21.4321460328653,0.541605390084162,3.73643636924876));
#40880=CARTESIAN_POINT('Ctrl Pts',(21.4241933935215,0.489311161755075,3.64874970034904));
#40881=CARTESIAN_POINT('Ctrl Pts',(21.4162407541777,0.419206509371839,3.57895170565158));
#40882=CARTESIAN_POINT('Ctrl Pts',(21.4082881148339,0.349101856988603,3.50915371095413));
#40883=CARTESIAN_POINT('Ctrl Pts',(21.4003354754901,0.261186780551223,3.45724439045894));
#40884=CARTESIAN_POINT('Ctrl Pts',(21.3923828361463,0.16621009553345,3.42957036558731));
#40885=CARTESIAN_POINT('Ctrl Pts',(21.3844301968025,0.0712334105156764,
3.40189634071567));
#40886=CARTESIAN_POINT('Ctrl Pts',(21.3764775574587,-0.0308048830825163,
3.3984576114676));
#40887=CARTESIAN_POINT('Ctrl Pts',(21.3685249181149,-0.127429214135013,
3.41967460932821));
#40888=CARTESIAN_POINT('Ctrl Pts',(21.360572278771,-0.22405354518751,3.44089160718882));
#40889=CARTESIAN_POINT('Ctrl Pts',(21.3526196394272,-0.315263913694308,
3.4867643321581));
#40890=CARTESIAN_POINT('Ctrl Pts',(21.3446670000834,-0.389908609845283,
3.5516842188346));
#40891=CARTESIAN_POINT('Ctrl Pts',(21.3367143607396,-0.464553305996249,
3.6166041055111));
#40892=CARTESIAN_POINT('Ctrl Pts',(21.3287617213958,-0.522632329791381,
3.70057115389483));
#40893=CARTESIAN_POINT('Ctrl Pts',(21.320809082052,-0.557044729551177,3.79331924871262));
#40894=CARTESIAN_POINT('Ctrl Pts',(21.3128564427082,-0.591457129310977,
3.88606734353042));
#40895=CARTESIAN_POINT('Ctrl Pts',(21.3049038033644,-0.602202905035458,
3.9875964847823));
#40896=CARTESIAN_POINT('Ctrl Pts',(21.2969511640206,-0.587968239287942,
4.08549335215105));
#40897=CARTESIAN_POINT('Ctrl Pts',(21.2889985246768,-0.573733573540424,
4.18339021951981));
#40898=CARTESIAN_POINT('Ctrl Pts',(21.281045885333,-0.534518466320906,4.27765481300544));
#40899=CARTESIAN_POINT('Ctrl Pts',(21.2730932459892,-0.47511749858569,4.35676200219639));
#40900=CARTESIAN_POINT('Ctrl Pts',(21.2651406066454,-0.415716530850488,
4.43586919138732));
#40901=CARTESIAN_POINT('Ctrl Pts',(21.2571879673016,-0.336129702599601,
4.49981897628356));
#40902=CARTESIAN_POINT('Ctrl Pts',(21.2492353279577,-0.246087587538132,
4.54079262470289));
#40903=CARTESIAN_POINT('Ctrl Pts',(21.2424386890577,-0.169134048541188,
4.57581031891556));
#40904=CARTESIAN_POINT('Ctrl Pts',(21.2356420501576,-0.0845438791841879,
4.59404604774026));
#40905=CARTESIAN_POINT('Ctrl Pts',(21.2288454112575,1.28243205298473E-5,
4.59412621697841));
#40906=CARTESIAN_POINT('Ctrl Pts',(21.1211545887425,-1.09306879613159E-5,
4.5940621922514));
#40907=CARTESIAN_POINT('Ctrl Pts',(21.1240981080146,-0.0366424819978743,
4.5940862444172));
#40908=CARTESIAN_POINT('Ctrl Pts',(21.1270416272867,-0.0732697079540161,
4.59075208378119));
#40909=CARTESIAN_POINT('Ctrl Pts',(21.1299851465589,-0.109260984540888,
4.58401866488291));
#40910=CARTESIAN_POINT('Ctrl Pts',(21.1379377859027,-0.20650024671525,4.56582668205621));
#40911=CARTESIAN_POINT('Ctrl Pts',(21.1458904252465,-0.299097442487026,
4.52282205952027));
#40912=CARTESIAN_POINT('Ctrl Pts',(21.1538430645903,-0.375731303474415,
4.46026269810429));
#40913=CARTESIAN_POINT('Ctrl Pts',(21.1617957039341,-0.452365164461805,
4.3977033366883));
#40914=CARTESIAN_POINT('Ctrl Pts',(21.1697483432779,-0.513035690664809,
4.31558923639226));
#40915=CARTESIAN_POINT('Ctrl Pts',(21.1777009826217,-0.550325083965727,
4.22395996434209));
#40916=CARTESIAN_POINT('Ctrl Pts',(21.1856536219655,-0.587614477266646,
4.13233069229192));
#40917=CARTESIAN_POINT('Ctrl Pts',(21.1936062613093,-0.601522737665479,
4.03118624848761));
#40918=CARTESIAN_POINT('Ctrl Pts',(21.2015589006531,-0.590349390887683,
3.93289291874755));
#40919=CARTESIAN_POINT('Ctrl Pts',(21.2095115399969,-0.579176044109886,
3.83459958900749));
#40920=CARTESIAN_POINT('Ctrl Pts',(21.2174641793407,-0.542921090155459,
3.73915737333167));
#40921=CARTESIAN_POINT('Ctrl Pts',(21.2254168186845,-0.486017190935348,
3.65823538248142));
#40922=CARTESIAN_POINT('Ctrl Pts',(21.2333694580283,-0.429113291715238,
3.57731339163117));
#40923=CARTESIAN_POINT('Ctrl Pts',(21.2413220973721,-0.351560447229444,
3.51091162560648));
#40924=CARTESIAN_POINT('Ctrl Pts',(21.249274736716,-0.262840548960938,3.46714860467879));
#40925=CARTESIAN_POINT('Ctrl Pts',(21.2572273760598,-0.174120650692433,
3.4233855837511));
#40926=CARTESIAN_POINT('Ctrl Pts',(21.2651800154036,-0.0742336986412151,
3.40226130792041));
#40927=CARTESIAN_POINT('Ctrl Pts',(21.2731326547474,0.0246077668693877,
3.40635850761334));
#40928=CARTESIAN_POINT('Ctrl Pts',(21.2810852940912,0.123449232380002,3.41045570730627));
#40929=CARTESIAN_POINT('Ctrl Pts',(21.289037933435,0.221245211350001,3.43977438252282));
#40930=CARTESIAN_POINT('Ctrl Pts',(21.2969905727788,0.306038813396919,3.49072992590572));
#40931=CARTESIAN_POINT('Ctrl Pts',(21.3049432121226,0.390832415443818,3.54168546928862));
#40932=CARTESIAN_POINT('Ctrl Pts',(21.3128958514664,0.462623640567642,3.61427788083785));
#40933=CARTESIAN_POINT('Ctrl Pts',(21.3208484908102,0.512635033719562,3.69963174955258));
#40934=CARTESIAN_POINT('Ctrl Pts',(21.328801130154,0.562646426871494,3.78498561826733));
#40935=CARTESIAN_POINT('Ctrl Pts',(21.3367537694978,0.590877988051513,3.88310094414759));
#40936=CARTESIAN_POINT('Ctrl Pts',(21.3447064088416,0.59387802439953,3.98198179230066));
#40937=CARTESIAN_POINT('Ctrl Pts',(21.3526590481854,0.596878060747546,4.08086264045372));
#40938=CARTESIAN_POINT('Ctrl Pts',(21.3606116875293,0.574646572263566,4.1805090108796));
#40939=CARTESIAN_POINT('Ctrl Pts',(21.3685643268731,0.529901661201384,4.26873777763737));
#40940=CARTESIAN_POINT('Ctrl Pts',(21.3765169662169,0.485156750139203,4.35696654439514));
#40941=CARTESIAN_POINT('Ctrl Pts',(21.3844696055607,0.417898416498819,4.4337777074848));
#40942=CARTESIAN_POINT('Ctrl Pts',(21.3924222449045,0.336349907607971,4.48978005607163));
#40943=CARTESIAN_POINT('Ctrl Pts',(21.4003748842483,0.254801398717122,4.54578240465847));
#40944=CARTESIAN_POINT('Ctrl Pts',(21.4083275235921,0.158962714575808,4.58097593874246));
#40945=CARTESIAN_POINT('Ctrl Pts',(21.4162801629359,0.0605514396169286,
4.59105776945554));
#40946=CARTESIAN_POINT('Ctrl Pts',(21.4179049715381,0.0404449719157324,
4.59311759444699));
#40947=CARTESIAN_POINT('Ctrl Pts',(21.4195297801403,0.0202311170044278,
4.59412918598148));
#40948=CARTESIAN_POINT('Ctrl Pts',(21.4211545887425,1.51733402061755E-5,
4.59410821609125));
#40949=CARTESIAN_POINT('Origin',(4.,0.,4.));
#40950=CARTESIAN_POINT('',(21.8288454112575,1.47252919898561E-5,4.59408074293421));
#40951=CARTESIAN_POINT('',(21.7211545887425,-1.54601956517634E-5,4.59410286710644));
#40952=CARTESIAN_POINT('',(4.,-7.27562663373442E-17,4.5941));
#40953=CARTESIAN_POINT('Ctrl Pts',(21.8288454112575,1.47252919898561E-5,
4.59408074293421));
#40954=CARTESIAN_POINT('Ctrl Pts',(21.826505394409,0.0291331941223908,4.59410767674242));
#40955=CARTESIAN_POINT('Ctrl Pts',(21.8241653775604,0.0582478076928112,
4.59200528777341));
#40956=CARTESIAN_POINT('Ctrl Pts',(21.8218253607118,0.0870422430987805,
4.58774093918134));
#40957=CARTESIAN_POINT('Ctrl Pts',(21.813872721368,0.184901264939656,4.57324838268129));
#40958=CARTESIAN_POINT('Ctrl Pts',(21.8059200820242,0.279062206656402,4.53378504179028));
#40959=CARTESIAN_POINT('Ctrl Pts',(21.7979674426804,0.358012610677869,4.47417584741217));
#40960=CARTESIAN_POINT('Ctrl Pts',(21.7900148033366,0.436963014699336,4.41456665303406));
#40961=CARTESIAN_POINT('Ctrl Pts',(21.7820621639928,0.500702881025523,4.33481160516884));
#40962=CARTESIAN_POINT('Ctrl Pts',(21.774109524649,0.541439142878506,4.24466184465998));
#40963=CARTESIAN_POINT('Ctrl Pts',(21.7661568853052,0.58217540473149,4.15451208415111));
#40964=CARTESIAN_POINT('Ctrl Pts',(21.7582042459614,0.599908062111268,4.0539676109986));
#40965=CARTESIAN_POINT('Ctrl Pts',(21.7502516066176,0.59246905613922,3.95532135643358));
#40966=CARTESIAN_POINT('Ctrl Pts',(21.7422989672738,0.585030050167171,3.85667510186855));
#40967=CARTESIAN_POINT('Ctrl Pts',(21.73434632793,0.552419380843296,3.759927065891));
#40968=CARTESIAN_POINT('Ctrl Pts',(21.7263936885861,0.498624146640836,3.67690601358098));
#40969=CARTESIAN_POINT('Ctrl Pts',(21.7184410492423,0.444828912438376,3.59388496127097));
#40970=CARTESIAN_POINT('Ctrl Pts',(21.7104884098985,0.369849113357332,3.52459089262848));
#40971=CARTESIAN_POINT('Ctrl Pts',(21.7025357705547,0.28285205103972,3.47749595131133));
#40972=CARTESIAN_POINT('Ctrl Pts',(21.6945831312109,0.195854988722108,3.43040100999418));
#40973=CARTESIAN_POINT('Ctrl Pts',(21.6866304918671,0.0968406631679286,
3.40550519600236));
#40974=CARTESIAN_POINT('Ctrl Pts',(21.6786778525233,-0.00208507577578169,
3.40585236167057));
#40975=CARTESIAN_POINT('Ctrl Pts',(21.6707252131795,-0.101010814719503,
3.40619952733877));
#40976=CARTESIAN_POINT('Ctrl Pts',(21.6627725738357,-0.199847967052756,
3.431789672667));
#40977=CARTESIAN_POINT('Ctrl Pts',(21.6548199344919,-0.28651234476781,3.47949405385809));
#40978=CARTESIAN_POINT('Ctrl Pts',(21.6468672951481,-0.373176722482865,
3.52719843504918));
#40979=CARTESIAN_POINT('Ctrl Pts',(21.6389146558043,-0.44766832557972,3.59701705210314));
#40980=CARTESIAN_POINT('Ctrl Pts',(21.6309620164605,-0.500879541024521,
3.68041362817464));
#40981=CARTESIAN_POINT('Ctrl Pts',(21.6230093771167,-0.55409075646931,3.76381020424612));
#40982=CARTESIAN_POINT('Ctrl Pts',(21.6150567377728,-0.586021584262053,
3.86078473933514));
#40983=CARTESIAN_POINT('Ctrl Pts',(21.607104098429,-0.592768045815946,3.95948077576042));
#40984=CARTESIAN_POINT('Ctrl Pts',(21.5991514590852,-0.599514507369841,
4.05817681218572));
#40985=CARTESIAN_POINT('Ctrl Pts',(21.5911988197414,-0.581076602684875,
4.15859434994728));
#40986=CARTESIAN_POINT('Ctrl Pts',(21.5832461803976,-0.539708616728004,
4.24845597739434));
#40987=CARTESIAN_POINT('Ctrl Pts',(21.5752935410538,-0.498340630771147,
4.33831760484137));
#40988=CARTESIAN_POINT('Ctrl Pts',(21.56734090171,-0.434042563542403,4.41762332197391));
#40989=CARTESIAN_POINT('Ctrl Pts',(21.5593882623662,-0.354675729482573,
4.47667692475034));
#40990=CARTESIAN_POINT('Ctrl Pts',(21.5514356230224,-0.275308895422716,
4.53573052752678));
#40991=CARTESIAN_POINT('Ctrl Pts',(21.5434829836786,-0.180873294531764,
4.57453201594709));
#40992=CARTESIAN_POINT('Ctrl Pts',(21.5355303443348,-0.0829149652056982,
4.58833737958621));
#40993=CARTESIAN_POINT('Ctrl Pts',(21.533302033309,-0.055467269432644,4.59220561033096));
#40994=CARTESIAN_POINT('Ctrl Pts',(21.5310737222833,-0.0277430016607059,
4.5941113769453));
#40995=CARTESIAN_POINT('Ctrl Pts',(21.5288454112575,-1.51073027558624E-5,
4.59408477831653));
#40996=CARTESIAN_POINT('Ctrl Pts',(21.4211545887425,1.51733402061755E-5,
4.59410821609125));
#40997=CARTESIAN_POINT('Ctrl Pts',(21.4274824194841,-0.0787159889745399,
4.59402654867773));
#40998=CARTESIAN_POINT('Ctrl Pts',(21.4338102502257,-0.15747883181342,4.57828382012605));
#40999=CARTESIAN_POINT('Ctrl Pts',(21.4401380809673,-0.230053504748576,
4.54780575811717));
#41000=CARTESIAN_POINT('Ctrl Pts',(21.4480907203111,-0.321263308378747,
4.50950178872359));
#41001=CARTESIAN_POINT('Ctrl Pts',(21.4560433596549,-0.402699049862651,
4.44792372259427));
#41002=CARTESIAN_POINT('Ctrl Pts',(21.4639959989987,-0.464404100671371,
4.37060031698995));
#41003=CARTESIAN_POINT('Ctrl Pts',(21.4719486383425,-0.526109151480106,
4.2932769113856));
#41004=CARTESIAN_POINT('Ctrl Pts',(21.4799012776864,-0.568083511613643,
4.20020816630624));
#41005=CARTESIAN_POINT('Ctrl Pts',(21.4878539170302,-0.585195243866348,
4.10277300340868));
#41006=CARTESIAN_POINT('Ctrl Pts',(21.495806556374,-0.602306976119048,4.00533784051114));
#41007=CARTESIAN_POINT('Ctrl Pts',(21.5037591957178,-0.594556080490919,
3.90353625979537));
#41008=CARTESIAN_POINT('Ctrl Pts',(21.5117118350616,-0.562890209537588,
3.80981489101362));
#41009=CARTESIAN_POINT('Ctrl Pts',(21.5196644744054,-0.53122433858425,3.71609352223184));
#41010=CARTESIAN_POINT('Ctrl Pts',(21.5276171137492,-0.47564349230572,3.63045236538409));
#41011=CARTESIAN_POINT('Ctrl Pts',(21.535569753093,-0.402943186155437,3.56336221830407));
#41012=CARTESIAN_POINT('Ctrl Pts',(21.5435223924368,-0.330242880005154,
3.49627207122406));
#41013=CARTESIAN_POINT('Ctrl Pts',(21.5514750317806,-0.24042311398314,3.44773293391182));
#41014=CARTESIAN_POINT('Ctrl Pts',(21.5594276711244,-0.144465577806233,
3.42367937699355));
#41015=CARTESIAN_POINT('Ctrl Pts',(21.5673803104682,-0.0485080416293372,
3.39962582007528));
#41016=CARTESIAN_POINT('Ctrl Pts',(21.575332949812,0.0535872647024426,3.40005784355098));
#41017=CARTESIAN_POINT('Ctrl Pts',(21.5832855891558,0.149337799479898,3.42492262666669));
#41018=CARTESIAN_POINT('Ctrl Pts',(21.5912382284996,0.245088334257342,3.44978740978241));
#41019=CARTESIAN_POINT('Ctrl Pts',(21.5991908678434,0.33449409748049,3.49908495253815));
#41020=CARTESIAN_POINT('Ctrl Pts',(21.6071435071872,0.406624016913212,3.56678795891296));
#41021=CARTESIAN_POINT('Ctrl Pts',(21.6150961465311,0.478753936345942,3.63449096528778));
#41022=CARTESIAN_POINT('Ctrl Pts',(21.6230487858749,0.533608011988269,3.72059943528167));
#41023=CARTESIAN_POINT('Ctrl Pts',(21.6310014252187,0.564479585995414,3.81458543566408));
#41024=CARTESIAN_POINT('Ctrl Pts',(21.6389540645625,0.595351160002559,3.90857143604649));
#41025=CARTESIAN_POINT('Ctrl Pts',(21.6469067039063,0.602240232374519,4.0104349668174));
#41026=CARTESIAN_POINT('Ctrl Pts',(21.6548593432501,0.584304520186539,4.10772182398666));
#41027=CARTESIAN_POINT('Ctrl Pts',(21.6628119825939,0.566368807998562,4.2050086811559));
#41028=CARTESIAN_POINT('Ctrl Pts',(21.6707646219377,0.523608311250652,4.29771886472347));
#41029=CARTESIAN_POINT('Ctrl Pts',(21.6787172612815,0.461251083056512,4.37451729206089));
#41030=CARTESIAN_POINT('Ctrl Pts',(21.6866699006253,0.398893854862358,4.45131571939834));
#41031=CARTESIAN_POINT('Ctrl Pts',(21.6946225399691,0.316939895221968,4.51220239050563));
#41032=CARTESIAN_POINT('Ctrl Pts',(21.7025751793129,0.225409191891896,4.54973308058009));
#41033=CARTESIAN_POINT('Ctrl Pts',(21.7087683157894,0.15412944274098,4.5789601931952));
#41034=CARTESIAN_POINT('Ctrl Pts',(21.7149614522659,0.0770418275534371,
4.59402294959611));
#41035=CARTESIAN_POINT('Ctrl Pts',(21.7211545887425,-1.54601956517634E-5,
4.59410286710644));
#41036=CARTESIAN_POINT('Origin',(4.,0.,4.));
#41037=CARTESIAN_POINT('',(22.1288454112575,-1.19684274697274E-5,4.59413016891312));
#41038=CARTESIAN_POINT('',(22.0211545887425,1.20066176157995E-5,4.59406577061205));
#41039=CARTESIAN_POINT('',(4.,-7.27562663373442E-17,4.5941));
#41040=CARTESIAN_POINT('Ctrl Pts',(22.1288454112575,-1.19684274697274E-5,
4.59413016891312));
#41041=CARTESIAN_POINT('Ctrl Pts',(22.1219370665346,0.0859328098890183,
4.59405244111828));
#41042=CARTESIAN_POINT('Ctrl Pts',(22.1150287218117,0.171910584533005,4.57519344187135));
#41043=CARTESIAN_POINT('Ctrl Pts',(22.1081203770888,0.24987714748571,4.53905210772026));
#41044=CARTESIAN_POINT('Ctrl Pts',(22.100167737745,0.339629466009183,4.49744749656716));
#41045=CARTESIAN_POINT('Ctrl Pts',(22.0922150984012,0.418765494330909,4.4329406966096));
#41046=CARTESIAN_POINT('Ctrl Pts',(22.0842624590574,0.477609775176754,4.35341854270704));
#41047=CARTESIAN_POINT('Ctrl Pts',(22.0763098197136,0.536454056022584,4.2738963888045));
#41048=CARTESIAN_POINT('Ctrl Pts',(22.0683571803698,0.575006589392542,4.17935888095698));
#41049=CARTESIAN_POINT('Ctrl Pts',(22.060404541026,0.588553803007579,4.081364517074));
#41050=CARTESIAN_POINT('Ctrl Pts',(22.0524519016822,0.60210101662262,3.983370153191));
#41051=CARTESIAN_POINT('Ctrl Pts',(22.0444992623384,0.590642910482727,3.88191893327255));
#41052=CARTESIAN_POINT('Ctrl Pts',(22.0365466229946,0.55558039411957,3.78941465069146));
#41053=CARTESIAN_POINT('Ctrl Pts',(22.0285939836508,0.520517877756421,3.69691036811039));
#41054=CARTESIAN_POINT('Ctrl Pts',(22.020641344307,0.461850951170019,3.61335302286667));
#41055=CARTESIAN_POINT('Ctrl Pts',(22.0126887049632,0.386752445163155,3.5489586384446));
#41056=CARTESIAN_POINT('Ctrl Pts',(22.0047360656194,0.311653939156274,3.48456425402251));
#41057=CARTESIAN_POINT('Ctrl Pts',(21.9967834262756,0.220123853728924,3.43933283042207));
#41058=CARTESIAN_POINT('Ctrl Pts',(21.9888307869318,0.123352988439278,3.41879452521803));
#41059=CARTESIAN_POINT('Ctrl Pts',(21.980878147588,0.0265821231496428,3.398256220014));
#41060=CARTESIAN_POINT('Ctrl Pts',(21.9729255082441,-0.075429522002288,
3.40241103320635));
#41061=CARTESIAN_POINT('Ctrl Pts',(21.9649728689003,-0.170209634025949,
3.43075098229493));
#41062=CARTESIAN_POINT('Ctrl Pts',(21.9570202295565,-0.26498974604961,3.4590909313835));
#41063=CARTESIAN_POINT('Ctrl Pts',(21.9490675902127,-0.352538324945002,
3.5116160163683));
#41064=CARTESIAN_POINT('Ctrl Pts',(21.9411149508689,-0.422151364554475,
3.58190433023263));
#41065=CARTESIAN_POINT('Ctrl Pts',(21.9331623115251,-0.491764404163956,
3.65219264409696));
#41066=CARTESIAN_POINT('Ctrl Pts',(21.9252096721813,-0.543441904487514,
3.74024418684083));
#41067=CARTESIAN_POINT('Ctrl Pts',(21.9172570328375,-0.570865587277161,
3.83529345812586));
#41068=CARTESIAN_POINT('Ctrl Pts',(21.9093043934937,-0.598289270066803,
3.93034272941087));
#41069=CARTESIAN_POINT('Ctrl Pts',(21.9013517541499,-0.601459135322544,
4.03238972923704));
#41070=CARTESIAN_POINT('Ctrl Pts',(21.8933991148061,-0.579987623844179,
4.12895782202339));
#41071=CARTESIAN_POINT('Ctrl Pts',(21.8854464754623,-0.558516112365809,
4.22552591480976));
#41072=CARTESIAN_POINT('Ctrl Pts',(21.8774938361185,-0.512403224153321,
4.31661510055631));
#41073=CARTESIAN_POINT('Ctrl Pts',(21.8695411967747,-0.447286887835617,
4.39108848569571));
#41074=CARTESIAN_POINT('Ctrl Pts',(21.8615885574308,-0.38217055151792,4.46556187083511));
#41075=CARTESIAN_POINT('Ctrl Pts',(21.853635918087,-0.298050767095013,4.52341945536736));
#41076=CARTESIAN_POINT('Ctrl Pts',(21.8456832787432,-0.205212323901057,
4.55758736157894));
#41077=CARTESIAN_POINT('Ctrl Pts',(21.840070656248,-0.139691040693493,4.58170156451555));
#41078=CARTESIAN_POINT('Ctrl Pts',(21.8344580337528,-0.0698270680627233,
4.59401614113532));
#41079=CARTESIAN_POINT('Ctrl Pts',(21.8288454112575,1.47252919898561E-5,
4.59408074293421));
#41080=CARTESIAN_POINT('Ctrl Pts',(21.7211545887425,-1.54601956517634E-5,
4.59410286710644));
#41081=CARTESIAN_POINT('Ctrl Pts',(21.7229140916097,-0.0219078436841643,
4.59412557209431));
#41082=CARTESIAN_POINT('Ctrl Pts',(21.724673594477,-0.0437977792686499,
4.59293892497318));
#41083=CARTESIAN_POINT('Ctrl Pts',(21.7264330973443,-0.0655513867134097,
4.59052415646896));
#41084=CARTESIAN_POINT('Ctrl Pts',(21.7343857366881,-0.163873814968881,
4.57960983324176));
#41085=CARTESIAN_POINT('Ctrl Pts',(21.742338376032,-0.259411224460086,4.54360647774573));
#41086=CARTESIAN_POINT('Ctrl Pts',(21.7502910153758,-0.340482865683332,
4.48691599054611));
#41087=CARTESIAN_POINT('Ctrl Pts',(21.7582436547196,-0.421554506906578,
4.4302255033465));
#41088=CARTESIAN_POINT('Ctrl Pts',(21.7661962940634,-0.488160379861865,
4.3528478844433));
#41089=CARTESIAN_POINT('Ctrl Pts',(21.7741489334072,-0.532157009426634,
4.26424360160945));
#41090=CARTESIAN_POINT('Ctrl Pts',(21.782101572751,-0.576153638991403,4.1756393187756));
#41091=CARTESIAN_POINT('Ctrl Pts',(21.7900542120948,-0.597541025165654,
4.0758083720111));
#41092=CARTESIAN_POINT('Ctrl Pts',(21.7980068514386,-0.593704268699233,
3.9769564542281));
#41093=CARTESIAN_POINT('Ctrl Pts',(21.8059594907824,-0.589867512232813,
3.87810453644509));
#41094=CARTESIAN_POINT('Ctrl Pts',(21.8139121301262,-0.560806613125721,
3.78023164764359));
#41095=CARTESIAN_POINT('Ctrl Pts',(21.82186476947,-0.510074662095298,3.69530408148155));
#41096=CARTESIAN_POINT('Ctrl Pts',(21.8298174088138,-0.459342711064876,
3.61037651531951));
#41097=CARTESIAN_POINT('Ctrl Pts',(21.8377700481576,-0.386939708111122,
3.53839427179695));
#41098=CARTESIAN_POINT('Ctrl Pts',(21.8457226875014,-0.301717906454235,
3.48815816056295));
#41099=CARTESIAN_POINT('Ctrl Pts',(21.8536753268452,-0.216496104797349,
3.43792204932895));
#41100=CARTESIAN_POINT('Ctrl Pts',(21.8616279661891,-0.118455504437329,
3.40943207038352));
#41101=CARTESIAN_POINT('Ctrl Pts',(21.8695806055329,-0.0195829040543552,
3.40617151167847));
#41102=CARTESIAN_POINT('Ctrl Pts',(21.8775332448767,0.0792896963286298,
3.40291095297342));
#41103=CARTESIAN_POINT('Ctrl Pts',(21.8854858842205,0.178994296734569,3.42487981450875));
#41104=CARTESIAN_POINT('Ctrl Pts',(21.8934385235643,0.267340651814441,3.46939210375187));
#41105=CARTESIAN_POINT('Ctrl Pts',(21.9013911629081,0.355687006894294,3.51390439299499));
#41106=CARTESIAN_POINT('Ctrl Pts',(21.9093438022519,0.432675116648084,3.58096010994589));
#41107=CARTESIAN_POINT('Ctrl Pts',(21.9172964415957,0.488892136101412,3.66236077992681));
#41108=CARTESIAN_POINT('Ctrl Pts',(21.9252490809395,0.545109155554752,3.74376144990775));
#41109=CARTESIAN_POINT('Ctrl Pts',(21.9332017202833,0.580555084707621,3.8395070729187));
#41110=CARTESIAN_POINT('Ctrl Pts',(21.9411543596271,0.590896175957217,3.93789144251738));
#41111=CARTESIAN_POINT('Ctrl Pts',(21.9491069989709,0.601237267206812,4.03627581211605));
#41112=CARTESIAN_POINT('Ctrl Pts',(21.9570596383147,0.58647352055314,4.13729892830245));
#41113=CARTESIAN_POINT('Ctrl Pts',(21.9650122776585,0.548410005102802,4.22860933921557));
#41114=CARTESIAN_POINT('Ctrl Pts',(21.9729649170023,0.510346489652465,4.31991975012869));
#41115=CARTESIAN_POINT('Ctrl Pts',(21.9809175563462,0.448983205405461,4.40151745576853));
#41116=CARTESIAN_POINT('Ctrl Pts',(21.98887019569,0.371822649612145,4.46342602528218));
#41117=CARTESIAN_POINT('Ctrl Pts',(21.9968228350338,0.29466209381883,4.52533459479583));
#41118=CARTESIAN_POINT('Ctrl Pts',(22.0047754743776,0.201704266479203,4.5675540281833));
#41119=CARTESIAN_POINT('Ctrl Pts',(22.0127281137214,0.104314528045707,4.58492242469582));
#41120=CARTESIAN_POINT('Ctrl Pts',(22.0155369387284,0.069917050565085,4.59105683924014));
#41121=CARTESIAN_POINT('Ctrl Pts',(22.0183457637354,0.0349667096964542,
4.59409118517947));
#41122=CARTESIAN_POINT('Ctrl Pts',(22.0211545887425,1.20066176157995E-5,
4.59406577061205));
#41123=CARTESIAN_POINT('Origin',(4.,0.,4.));
#41124=CARTESIAN_POINT('',(22.4288454112575,5.18920962550018E-6,4.59405135764298));
#41125=CARTESIAN_POINT('',(22.3211545887424,-7.30827440488969E-6,4.59414400810326));
#41126=CARTESIAN_POINT('',(4.,-7.27562663373442E-17,4.5941));
#41127=CARTESIAN_POINT('Ctrl Pts',(22.4288454112575,5.18920962550018E-6,
4.59405135764298));
#41128=CARTESIAN_POINT('Ctrl Pts',(22.4253213780041,0.0438634191921666,
4.5940647188338));
#41129=CARTESIAN_POINT('Ctrl Pts',(22.4217973447507,0.0877187745911938,
4.589273164082));
#41130=CARTESIAN_POINT('Ctrl Pts',(22.4182733114973,0.130485535360993,4.57964583089408));
#41131=CARTESIAN_POINT('Ctrl Pts',(22.4103206721535,0.226996720088313,4.55791995512033));
#41132=CARTESIAN_POINT('Ctrl Pts',(22.4023680328097,0.317964089339764,4.51156722320365));
#41133=CARTESIAN_POINT('Ctrl Pts',(22.3944153934659,0.392265646131591,4.44625488916104));
#41134=CARTESIAN_POINT('Ctrl Pts',(22.3864627541221,0.4665672029234,4.38094255511845));
#41135=CARTESIAN_POINT('Ctrl Pts',(22.3785101147783,0.524202947255594,4.29667061894994));
#41136=CARTESIAN_POINT('Ctrl Pts',(22.3705574754345,0.558126122886914,4.20374247196213));
#41137=CARTESIAN_POINT('Ctrl Pts',(22.3626048360906,0.592049298518242,4.11081432497429));
#41138=CARTESIAN_POINT('Ctrl Pts',(22.3546521967468,0.602259905448686,4.00922996716717));
#41139=CARTESIAN_POINT('Ctrl Pts',(22.346699557403,0.587509558716917,3.91140947017845));
#41140=CARTESIAN_POINT('Ctrl Pts',(22.3387469180592,0.572759211985149,3.81358897318973));
#41141=CARTESIAN_POINT('Ctrl Pts',(22.3307942787154,0.533047911591167,3.71953233701942));
#41142=CARTESIAN_POINT('Ctrl Pts',(22.3228416393716,0.473230904440663,3.6407392662825));
#41143=CARTESIAN_POINT('Ctrl Pts',(22.3148890000278,0.413413897290173,3.5619461955456));
#41144=CARTESIAN_POINT('Ctrl Pts',(22.306936360684,0.333491183383171,3.49841669024209));
#41145=CARTESIAN_POINT('Ctrl Pts',(22.2989837213402,0.243234403245124,3.45791809774646));
#41146=CARTESIAN_POINT('Ctrl Pts',(22.2910310819964,0.152977623107077,3.41741950525082));
#41147=CARTESIAN_POINT('Ctrl Pts',(22.2830784426526,0.0523867767379842,
3.39995182556307));
#41148=CARTESIAN_POINT('Ctrl Pts',(22.2751258033088,-0.0462395349927855,
3.40765072037886));
#41149=CARTESIAN_POINT('Ctrl Pts',(22.267173163965,-0.144865846723578,3.41534961519466));
#41150=CARTESIAN_POINT('Ctrl Pts',(22.2592205246212,-0.241527623816046,
3.448215084514));
#41151=CARTESIAN_POINT('Ctrl Pts',(22.2512678852774,-0.324406647450603,
3.50222887712101));
#41152=CARTESIAN_POINT('Ctrl Pts',(22.2433152459336,-0.40728567108515,3.55624266972802));
#41153=CARTESIAN_POINT('Ctrl Pts',(22.2353626065897,-0.476381941261788,
3.63140478562268));
#41154=CARTESIAN_POINT('Ctrl Pts',(22.2274099672459,-0.523247497912515,
3.71852563243507));
#41155=CARTESIAN_POINT('Ctrl Pts',(22.2194573279021,-0.570113054563243,
3.80564647924745));
#41156=CARTESIAN_POINT('Ctrl Pts',(22.2115046885583,-0.59474789768806,3.90472605697756));
#41157=CARTESIAN_POINT('Ctrl Pts',(22.2035520492145,-0.594140082177443,
4.00365053781872));
#41158=CARTESIAN_POINT('Ctrl Pts',(22.1955994098707,-0.593532266666827,
4.10257501865988));
#41159=CARTESIAN_POINT('Ctrl Pts',(22.1876467705269,-0.567681792520777,
4.2013444026121));
#41160=CARTESIAN_POINT('Ctrl Pts',(22.1796941311831,-0.519749232289404,
4.2878827872712));
#41161=CARTESIAN_POINT('Ctrl Pts',(22.1717414918393,-0.471816672058032,
4.37442117193029));
#41162=CARTESIAN_POINT('Ctrl Pts',(22.1637888524955,-0.401802025741336,
4.44872855729627));
#41163=CARTESIAN_POINT('Ctrl Pts',(22.1558362131517,-0.318265537426909,
4.50171985346399));
#41164=CARTESIAN_POINT('Ctrl Pts',(22.1478835738079,-0.234729049112483,
4.55471114963171));
#41165=CARTESIAN_POINT('Ctrl Pts',(22.1399309344641,-0.137670718800326,
4.58638635660118));
#41166=CARTESIAN_POINT('Ctrl Pts',(22.1319782951203,-0.0389572492816432,
4.5928727489116));
#41167=CARTESIAN_POINT('Ctrl Pts',(22.1309340004994,-0.0259947671705595,
4.5937245044491));
#41168=CARTESIAN_POINT('Ctrl Pts',(22.1298897058784,-0.0130037447923657,
4.5941419185755));
#41169=CARTESIAN_POINT('Ctrl Pts',(22.1288454112575,-1.19684274697274E-5,
4.59413016891312));
#41170=CARTESIAN_POINT('Ctrl Pts',(22.0211545887425,1.20066176157995E-5,
4.59406577061205));
#41171=CARTESIAN_POINT('Ctrl Pts',(22.0262984030792,-0.064000704172389,
4.59401922879619));
#41172=CARTESIAN_POINT('Ctrl Pts',(22.031442217416,-0.128028044405449,4.5837112392356));
#41173=CARTESIAN_POINT('Ctrl Pts',(22.0365860317528,-0.188701337098646,
4.56338935830438));
#41174=CARTESIAN_POINT('Ctrl Pts',(22.0445386710966,-0.282505814282095,
4.53197053576284));
#41175=CARTESIAN_POINT('Ctrl Pts',(22.0524913104404,-0.368293119121642,
4.4766155310422));
#41176=CARTESIAN_POINT('Ctrl Pts',(22.0604439497842,-0.435574585201076,
4.40409224738955));
#41177=CARTESIAN_POINT('Ctrl Pts',(22.068396589128,-0.502856051280518,4.33156896373689));
#41178=CARTESIAN_POINT('Ctrl Pts',(22.0763492284718,-0.551631678599843,
4.24187740115222));
#41179=CARTESIAN_POINT('Ctrl Pts',(22.0843018678156,-0.575937982408454,
4.14598357473613));
#41180=CARTESIAN_POINT('Ctrl Pts',(22.0922545071594,-0.600244286217068,
4.05008974832002));
#41181=CARTESIAN_POINT('Ctrl Pts',(22.1002071465032,-0.600081266514962,
3.94799365807249));
#41182=CARTESIAN_POINT('Ctrl Pts',(22.1081597858471,-0.575468854681199,
3.85217794154701));
#41183=CARTESIAN_POINT('Ctrl Pts',(22.1161124251909,-0.550856442847438,
3.75636222502155));
#41184=CARTESIAN_POINT('Ctrl Pts',(22.1240650645347,-0.501794638882025,
3.66682688221814));
#41185=CARTESIAN_POINT('Ctrl Pts',(22.1320177038785,-0.434281916527717,
3.5945188282416));
#41186=CARTESIAN_POINT('Ctrl Pts',(22.1399703432223,-0.366769194173409,
3.52221077426505));
#41187=CARTESIAN_POINT('Ctrl Pts',(22.1479229825661,-0.280805553430205,
3.46713000911538));
#41188=CARTESIAN_POINT('Ctrl Pts',(22.1558756219099,-0.186901220180937,
3.43601090651668));
#41189=CARTESIAN_POINT('Ctrl Pts',(22.1638282612537,-0.0929968869316588,
3.40489180391798));
#41190=CARTESIAN_POINT('Ctrl Pts',(22.1717809005975,0.00884813882368474,
3.39773436387026));
#41191=CARTESIAN_POINT('Ctrl Pts',(22.1797335399413,0.106181915586414,3.41541368090248));
#41192=CARTESIAN_POINT('Ctrl Pts',(22.1876861792851,0.203515692349121,3.4330929979347));
#41193=CARTESIAN_POINT('Ctrl Pts',(22.1956388186289,0.296338220119215,3.47560907204686));
#41194=CARTESIAN_POINT('Ctrl Pts',(22.2035914579727,0.373300680656879,3.53776373412001));
#41195=CARTESIAN_POINT('Ctrl Pts',(22.2115440973165,0.450263141194552,3.59991839619317));
#41196=CARTESIAN_POINT('Ctrl Pts',(22.2194967366603,0.511365534499791,3.68171164622733));
#41197=CARTESIAN_POINT('Ctrl Pts',(22.2274493760041,0.549137260797828,3.7731431454068));
#41198=CARTESIAN_POINT('Ctrl Pts',(22.2354020153479,0.586908987095865,3.86457464458628));
#41199=CARTESIAN_POINT('Ctrl Pts',(22.2433546546918,0.6013500463867,3.96564439291107));
#41200=CARTESIAN_POINT('Ctrl Pts',(22.2513072940356,0.590694822479903,4.06399523710107));
#41201=CARTESIAN_POINT('Ctrl Pts',(22.2592599333794,0.580039598573106,4.16234608129106));
#41202=CARTESIAN_POINT('Ctrl Pts',(22.2672125727232,0.544288091468676,4.25797802134625));
#41203=CARTESIAN_POINT('Ctrl Pts',(22.275165212067,0.487811409852587,4.33919875012361));
#41204=CARTESIAN_POINT('Ctrl Pts',(22.2831178514108,0.431334728236497,4.42041947890096));
#41205=CARTESIAN_POINT('Ctrl Pts',(22.2910704907546,0.354132872108749,4.48722899640046));
#41206=CARTESIAN_POINT('Ctrl Pts',(22.2990231300984,0.265644819817582,4.53145892916239));
#41207=CARTESIAN_POINT('Ctrl Pts',(22.3064002829798,0.183560135512932,4.57248819778762));
#41208=CARTESIAN_POINT('Ctrl Pts',(22.3137774358611,0.0917635873240076,
4.59408754951618));
#41209=CARTESIAN_POINT('Ctrl Pts',(22.3211545887424,-7.30827440488969E-6,
4.59414400810326));
#41210=CARTESIAN_POINT('Origin',(4.,0.,4.));
#41211=CARTESIAN_POINT('',(22.7288454112575,-7.11440487624268E-7,4.59414971000239));
#41212=CARTESIAN_POINT('',(22.6211545887425,-1.51245797256638E-7,4.59404869726453));
#41213=CARTESIAN_POINT('',(4.,-7.27562663373442E-17,4.5941));
#41214=CARTESIAN_POINT('Ctrl Pts',(22.7288454112575,-7.11440487624268E-7,
4.59414971000239));
#41215=CARTESIAN_POINT('Ctrl Pts',(22.7287056894736,0.0017373052546791,
4.59414999869406));
#41216=CARTESIAN_POINT('Ctrl Pts',(22.7285659676897,0.0034753215591825,
4.59414251282321));
#41217=CARTESIAN_POINT('Ctrl Pts',(22.7284262459057,0.00521327185949689,
4.59412723628209));
#41218=CARTESIAN_POINT('Ctrl Pts',(22.7204736065619,0.104133365400505,4.59325773105135));
#41219=CARTESIAN_POINT('Ctrl Pts',(22.7125209672181,0.202839630323109,4.56714939948764));
#41220=CARTESIAN_POINT('Ctrl Pts',(22.7045683278743,0.289252680684759,4.51898953373575));
#41221=CARTESIAN_POINT('Ctrl Pts',(22.6966156885305,0.375665731046408,4.47082966798385));
#41222=CARTESIAN_POINT('Ctrl Pts',(22.6886630491867,0.449785566847107,4.40061826804377));
#41223=CARTESIAN_POINT('Ctrl Pts',(22.6807104098429,0.502555912967013,4.31694216252228));
#41224=CARTESIAN_POINT('Ctrl Pts',(22.6727577704991,0.555326259086918,4.23326605700079));
#41225=CARTESIAN_POINT('Ctrl Pts',(22.6648051311553,0.586747115526033,4.13612524589788));
#41226=CARTESIAN_POINT('Ctrl Pts',(22.6568524918115,0.592973744123511,4.03739517928057));
#41227=CARTESIAN_POINT('Ctrl Pts',(22.6488998524677,0.59920037272099,3.93866511266326));
#41228=CARTESIAN_POINT('Ctrl Pts',(22.6409472131239,0.580232773476834,3.83834579053153));
#41229=CARTESIAN_POINT('Ctrl Pts',(22.6329945737801,0.538391640361539,3.74870332422701));
#41230=CARTESIAN_POINT('Ctrl Pts',(22.6250419344363,0.496550507246239,3.65906085792248));
#41231=CARTESIAN_POINT('Ctrl Pts',(22.6170892950925,0.431835840259791,3.58009524744515));
#41232=CARTESIAN_POINT('Ctrl Pts',(22.6091366557487,0.35215901686313,3.52146073929621));
#41233=CARTESIAN_POINT('Ctrl Pts',(22.6011840164048,0.272482193466486,3.46282623114728));
#41234=CARTESIAN_POINT('Ctrl Pts',(22.593231377061,0.17784321365963,3.42452282532672));
#41235=CARTESIAN_POINT('Ctrl Pts',(22.5852787377172,0.0798134434713266,
3.41123383340666));
#41236=CARTESIAN_POINT('Ctrl Pts',(22.5773260983734,-0.0182163267169884,
3.3979448414866));
#41237=CARTESIAN_POINT('Ctrl Pts',(22.5693734590296,-0.119636887286728,
3.40967026346704));
#41238=CARTESIAN_POINT('Ctrl Pts',(22.5614208196858,-0.212048437952692,
3.44497640167274));
#41239=CARTESIAN_POINT('Ctrl Pts',(22.553468180342,-0.304459988618666,3.48028253987845));
#41240=CARTESIAN_POINT('Ctrl Pts',(22.5455155409982,-0.387862529380837,
3.53916939430943));
#41241=CARTESIAN_POINT('Ctrl Pts',(22.5375629016544,-0.452058834188948,
3.61443730067171));
#41242=CARTESIAN_POINT('Ctrl Pts',(22.5296102623106,-0.516255138997059,
3.689705207034));
#41243=CARTESIAN_POINT('Ctrl Pts',(22.5216576229668,-0.561245207851117,
3.7813541653276));
#41244=CARTESIAN_POINT('Ctrl Pts',(22.513704983623,-0.581528460676763,3.87817881267738));
#41245=CARTESIAN_POINT('Ctrl Pts',(22.5057523442792,-0.601811713502406,
3.97500346002715));
#41246=CARTESIAN_POINT('Ctrl Pts',(22.4977997049354,-0.597388150299644,
4.07700379643311));
#41247=CARTESIAN_POINT('Ctrl Pts',(22.4898470655916,-0.568798575589296,
4.17170890717095));
#41248=CARTESIAN_POINT('Ctrl Pts',(22.4818944262477,-0.540209000878948,
4.26641401790879));
#41249=CARTESIAN_POINT('Ctrl Pts',(22.4739417869039,-0.487453414661012,
4.35382390297851));
#41250=CARTESIAN_POINT('Ctrl Pts',(22.4659891475601,-0.416981925106977,
4.42325150516024));
#41251=CARTESIAN_POINT('Ctrl Pts',(22.4580365082163,-0.346510435552941,
4.49267910734197));
#41252=CARTESIAN_POINT('Ctrl Pts',(22.4500838688725,-0.258323042662803,
4.54412442663572));
#41253=CARTESIAN_POINT('Ctrl Pts',(22.4421312295287,-0.163201846116148,
4.57129757646718));
#41254=CARTESIAN_POINT('Ctrl Pts',(22.4377026234383,-0.11023146834083,4.58642955613285));
#41255=CARTESIAN_POINT('Ctrl Pts',(22.4332740173479,-0.0551108697057404,
4.59403456681078));
#41256=CARTESIAN_POINT('Ctrl Pts',(22.4288454112575,5.18920962550018E-6,
4.59405135764298));
#41257=CARTESIAN_POINT('Ctrl Pts',(22.3211545887424,-7.30827440488969E-6,
4.59414400810326));
#41258=CARTESIAN_POINT('Ctrl Pts',(22.3217300752049,-0.00716629073194701,
4.59414841239758));
#41259=CARTESIAN_POINT('Ctrl Pts',(22.3223055616673,-0.0143251170819474,
4.59402171850555));
#41260=CARTESIAN_POINT('Ctrl Pts',(22.3228810481298,-0.0214791647150919,
4.59376292335171));
#41261=CARTESIAN_POINT('Ctrl Pts',(22.3308336874736,-0.120340848501978,
4.59018663675477));
#41262=CARTESIAN_POINT('Ctrl Pts',(22.3387863268174,-0.218289967621164,
4.56138371553656));
#41263=CARTESIAN_POINT('Ctrl Pts',(22.3467389661612,-0.303350908332583,
4.51087570903952));
#41264=CARTESIAN_POINT('Ctrl Pts',(22.3546916055051,-0.388411849044011,
4.46036770254246));
#41265=CARTESIAN_POINT('Ctrl Pts',(22.3626442448489,-0.460584611347669,
4.38815461076656));
#41266=CARTESIAN_POINT('Ctrl Pts',(22.3705968841927,-0.511045091866278,
4.3030654678256));
#41267=CARTESIAN_POINT('Ctrl Pts',(22.3785495235365,-0.561505572384874,
4.21797632488466));
#41268=CARTESIAN_POINT('Ctrl Pts',(22.3865021628803,-0.590253771118432,
4.12001113077866));
#41269=CARTESIAN_POINT('Ctrl Pts',(22.3944548022241,-0.593774829630164,
4.02114746451658));
#41270=CARTESIAN_POINT('Ctrl Pts',(22.4024074415679,-0.597295888141896,
3.92228379825449));
#41271=CARTESIAN_POINT('Ctrl Pts',(22.4103600809117,-0.575589806431797,
3.82252165983632));
#41272=CARTESIAN_POINT('Ctrl Pts',(22.4183127202555,-0.531310447862662,
3.73405832985033));
#41273=CARTESIAN_POINT('Ctrl Pts',(22.4262653595993,-0.487031089293526,
3.64559499986435));
#41274=CARTESIAN_POINT('Ctrl Pts',(22.4342179989431,-0.420178453865353,
3.56843047831055));
#41275=CARTESIAN_POINT('Ctrl Pts',(22.4421706382869,-0.338926188203527,
3.51199917808983));
#41276=CARTESIAN_POINT('Ctrl Pts',(22.4501232776307,-0.257673922541701,
3.45556787786912));
#41277=CARTESIAN_POINT('Ctrl Pts',(22.4580759169745,-0.162022026646223,
3.41986979898149));
#41278=CARTESIAN_POINT('Ctrl Pts',(22.4660285563183,-0.0636652448434586,
3.40926951931498));
#41279=CARTESIAN_POINT('Ctrl Pts',(22.4739811956621,0.0346915369593057,
3.39866923964846));
#41280=CARTESIAN_POINT('Ctrl Pts',(22.4819338350059,0.135753204669356,3.41316675920307));
#41281=CARTESIAN_POINT('Ctrl Pts',(22.4898864743497,0.227163587879617,3.45098955584192));
#41282=CARTESIAN_POINT('Ctrl Pts',(22.4978391136936,0.318573971089878,3.48881235248077));
#41283=CARTESIAN_POINT('Ctrl Pts',(22.5057917530374,0.40033306980035,3.54996042620388));
#41284=CARTESIAN_POINT('Ctrl Pts',(22.5137443923812,0.462444730281743,3.62695759769032));
#41285=CARTESIAN_POINT('Ctrl Pts',(22.521697031725,0.524556390763143,3.70395476917678));
#41286=CARTESIAN_POINT('Ctrl Pts',(22.5296496710688,0.567020613015458,3.79680103842659));
#41287=CARTESIAN_POINT('Ctrl Pts',(22.5376023104126,0.584645549343987,3.89414467407578));
#41288=CARTESIAN_POINT('Ctrl Pts',(22.5455549497564,0.602270485672515,3.99148830972497));
#41289=CARTESIAN_POINT('Ctrl Pts',(22.5535075891002,0.595056136077256,4.09332931177355));
#41290=CARTESIAN_POINT('Ctrl Pts',(22.561460228444,0.563884587368514,4.18721625032571));
#41291=CARTESIAN_POINT('Ctrl Pts',(22.5694128677878,0.532713038659782,4.28110318887784));
#41292=CARTESIAN_POINT('Ctrl Pts',(22.5773655071316,0.477584290837583,4.36703606393356));
#41293=CARTESIAN_POINT('Ctrl Pts',(22.5853181464754,0.405238519368296,4.43450837402952));
#41294=CARTESIAN_POINT('Ctrl Pts',(22.5932707858192,0.332892747898984,4.5019806841255));
#41295=CARTESIAN_POINT('Ctrl Pts',(22.601223425163,0.24332995278257,4.55099242926169));
#41296=CARTESIAN_POINT('Ctrl Pts',(22.6091760645068,0.14750052788588,4.57555132613148));
#41297=CARTESIAN_POINT('Ctrl Pts',(22.6131689059187,0.0993867282199646,
4.58788179608141));
#41298=CARTESIAN_POINT('Ctrl Pts',(22.6171617473306,0.0496932250345643,
4.5940481472271));
#41299=CARTESIAN_POINT('Ctrl Pts',(22.6211545887425,-1.51173456864708E-7,
4.59404872180247));
#41300=CARTESIAN_POINT('Origin',(3.42660065607856,0.,4.));
#41301=CARTESIAN_POINT('',(22.7766006560786,-4.98014040841517E-7,4.41590979742004));
#41302=CARTESIAN_POINT('',(22.8,4.87367679877478E-13,4.415875));
#41303=CARTESIAN_POINT('',(3.42660065607856,4.87367679877478E-13,4.415875));
#41304=CARTESIAN_POINT('',(22.8,-0.195748955928421,4.36692555359082));
#41305=CARTESIAN_POINT('Ctrl Pts',(22.7766006560786,-4.98014040834069E-7,
4.41590979742004));
#41306=CARTESIAN_POINT('Ctrl Pts',(22.7844004373857,-0.0679170312443507,
4.41589851620688));
#41307=CARTESIAN_POINT('Ctrl Pts',(22.7922002186928,-0.135834416676695,
4.39892762624317));
#41308=CARTESIAN_POINT('Ctrl Pts',(22.8,-0.195762566582618,4.36695865185838));
#41309=CARTESIAN_POINT('Origin',(22.8,0.,4.));
#41310=CARTESIAN_POINT('Origin',(3.42660065607856,0.,4.));
#41311=CARTESIAN_POINT('',(22.4766006560785,3.63249072247605E-6,4.41584094994071));
#41312=CARTESIAN_POINT('',(22.5733993439214,-1.05822049303872E-7,4.41583910483016));
#41313=CARTESIAN_POINT('',(3.42660065607856,4.87367679877478E-13,4.415875));
#41314=CARTESIAN_POINT('Ctrl Pts',(22.4766006560785,3.63249072248342E-6,
4.41584094994071));
#41315=CARTESIAN_POINT('Ctrl Pts',(22.4810292621689,-0.0385780726118879,
4.41582919621688));
#41316=CARTESIAN_POINT('Ctrl Pts',(22.4934105076031,-0.146451497349971,
4.40094585736882));
#41317=CARTESIAN_POINT('Ctrl Pts',(22.5137443923812,-0.304292138366774,
4.30886736509782));
#41318=CARTESIAN_POINT('Ctrl Pts',(22.5376023104126,-0.415080201412036,
4.12530439950267));
#41319=CARTESIAN_POINT('Ctrl Pts',(22.561460228444,-0.424369795825249,3.91110111771763));
#41320=CARTESIAN_POINT('Ctrl Pts',(22.5853181464754,-0.329889515310188,
3.71863599132299));
#41321=CARTESIAN_POINT('Ctrl Pts',(22.6091760645068,-0.154742073939436,
3.59497211022641));
#41322=CARTESIAN_POINT('Ctrl Pts',(22.6330339825383,0.0582436639512456,
3.57034842802071));
#41323=CARTESIAN_POINT('Ctrl Pts',(22.6568919005697,0.256987911016647,3.65078654733876));
#41324=CARTESIAN_POINT('Ctrl Pts',(22.6807498186011,0.39289034562191,3.81661632308649));
#41325=CARTESIAN_POINT('Ctrl Pts',(22.7046077366325,0.432722782933869,4.02728943245291));
#41326=CARTESIAN_POINT('Ctrl Pts',(22.7284656546639,0.366738191089385,4.2312875884069));
#41327=CARTESIAN_POINT('Ctrl Pts',(22.7523235726953,0.211084664509997,4.37873330099785));
#41328=CARTESIAN_POINT('Ctrl Pts',(22.7683685731669,0.0716802821347026,
4.41560650088387));
#41329=CARTESIAN_POINT('Ctrl Pts',(22.7764609342946,0.00121612829983627,
4.41590999950663));
#41330=CARTESIAN_POINT('Ctrl Pts',(22.7766006560786,-4.98014040834069E-7,
4.41590979742004));
#41331=CARTESIAN_POINT('',(22.8,0.415641328671541,4.01393920819689));
#41332=CARTESIAN_POINT('Origin',(22.8,0.,4.));
#41333=CARTESIAN_POINT('Ctrl Pts',(22.5733993439214,-1.0582204931428E-7,
4.41583910483016));
#41334=CARTESIAN_POINT('Ctrl Pts',(22.5773591418533,-0.034498011376554,
4.41583950370926));
#41335=CARTESIAN_POINT('Ctrl Pts',(22.5892715791291,-0.138279341065089,
4.40307041914735));
#41336=CARTESIAN_POINT('Ctrl Pts',(22.6091366557487,-0.295063722636797,
4.31769517074077));
#41337=CARTESIAN_POINT('Ctrl Pts',(22.6329945737801,-0.411209141905604,
4.13747522778479));
#41338=CARTESIAN_POINT('Ctrl Pts',(22.6568524918115,-0.426804986482714,
3.92363755172126));
#41339=CARTESIAN_POINT('Ctrl Pts',(22.6807104098429,-0.33803111495158,3.72847502015617));
#41340=CARTESIAN_POINT('Ctrl Pts',(22.7045683278743,-0.16660749730952,3.59970312177549));
#41341=CARTESIAN_POINT('Ctrl Pts',(22.7284262459057,0.0455714674079685,
3.56882345794434));
#41342=CARTESIAN_POINT('Ctrl Pts',(22.7522841639372,0.246577802732478,3.64336153500176));
#41343=CARTESIAN_POINT('Ctrl Pts',(22.7761420819686,0.387346815298129,3.80514019809748));
#41344=CARTESIAN_POINT('Ctrl Pts',(22.7920473606562,0.417963038852713,3.94471011778788));
#41345=CARTESIAN_POINT('Ctrl Pts',(22.8,0.415641328671541,4.01393920819689));
#41346=CARTESIAN_POINT('Origin',(3.42660065607856,0.,4.));
#41347=CARTESIAN_POINT('',(22.1766006560786,-8.37799962078257E-6,4.41589611849309));
#41348=CARTESIAN_POINT('',(22.2733993439214,-5.11585294796223E-6,4.41590580604266));
#41349=CARTESIAN_POINT('',(3.42660065607856,4.87367679877478E-13,4.415875));
#41350=CARTESIAN_POINT('Ctrl Pts',(22.1766006560786,-8.37799962077716E-6,
4.41589611849309));
#41351=CARTESIAN_POINT('Ctrl Pts',(22.1776449506995,-0.0091027307950905,
4.41590434335565));
#41352=CARTESIAN_POINT('Ctrl Pts',(22.1866418846642,-0.0874489573854402,
4.4133870032437));
#41353=CARTESIAN_POINT('Ctrl Pts',(22.2035914579727,-0.232253957950086,
4.36612956178204));
#41354=CARTESIAN_POINT('Ctrl Pts',(22.2274493760041,-0.379286482964224,
4.21008217638027));
#41355=CARTESIAN_POINT('Ctrl Pts',(22.2513072940356,-0.433573131350875,
4.00266397632408));
#41356=CARTESIAN_POINT('Ctrl Pts',(22.275165212067,-0.381839338801546,3.79459436150246));
#41357=CARTESIAN_POINT('Ctrl Pts',(22.2990231300984,-0.236735426869051,
3.63675202040985));
#41358=CARTESIAN_POINT('Ctrl Pts',(22.3228810481298,-0.0337432544318164,
3.56773370504276));
#41359=CARTESIAN_POINT('Ctrl Pts',(22.3467389661613,0.177500062688638,3.60441627341574));
#41360=CARTESIAN_POINT('Ctrl Pts',(22.3705968841926,0.345339779804043,3.73782983856348));
#41361=CARTESIAN_POINT('Ctrl Pts',(22.3944548022241,0.428734513273282,3.93535114928888));
#41362=CARTESIAN_POINT('Ctrl Pts',(22.4183127202555,0.407291980919218,4.1486808655136));
#41363=CARTESIAN_POINT('Ctrl Pts',(22.4421706382869,0.286255462618544,4.32565405918856));
#41364=CARTESIAN_POINT('Ctrl Pts',(22.4615999502279,0.130682174689606,4.40492695636159));
#41365=CARTESIAN_POINT('Ctrl Pts',(22.4730766228251,0.0307047625933256,
4.41585030288671));
#41366=CARTESIAN_POINT('Ctrl Pts',(22.4766006560785,3.63249072248342E-6,
4.41584094994071));
#41367=CARTESIAN_POINT('Ctrl Pts',(22.2733993439214,-5.11585294797612E-6,
4.41590580604266));
#41368=CARTESIAN_POINT('Ctrl Pts',(22.2739748303838,-0.0050164638240448,
4.41590888908576));
#41369=CARTESIAN_POINT('Ctrl Pts',(22.2825029561901,-0.0792779396689182,
4.41459464077989));
#41370=CARTESIAN_POINT('Ctrl Pts',(22.2989837213402,-0.221370022215225,
4.37281103827166));
#41371=CARTESIAN_POINT('Ctrl Pts',(22.3228416393716,-0.372934645290675,
4.22116172228637));
#41372=CARTESIAN_POINT('Ctrl Pts',(22.346699557403,-0.43330658847365,4.01543234121164));
#41373=CARTESIAN_POINT('Ctrl Pts',(22.3705574754345,-0.387723268841402,
3.80592933171158));
#41374=CARTESIAN_POINT('Ctrl Pts',(22.3944153934659,-0.247331046528593,
3.64388188817752));
#41375=CARTESIAN_POINT('Ctrl Pts',(22.4182733114973,-0.0464596501027702,
3.56891502119853));
#41376=CARTESIAN_POINT('Ctrl Pts',(22.4421312295287,0.165772403721094,3.59936017830047));
#41377=CARTESIAN_POINT('Ctrl Pts',(22.4659891475602,0.337468575289321,3.7277726770023));
#41378=CARTESIAN_POINT('Ctrl Pts',(22.4898470655915,0.426644514167594,3.92275218663495));
#41379=CARTESIAN_POINT('Ctrl Pts',(22.513704983623,0.411494197867752,4.13662086224655));
#41380=CARTESIAN_POINT('Ctrl Pts',(22.5375629016544,0.295722435535401,4.31708206952049));
#41381=CARTESIAN_POINT('Ctrl Pts',(22.5574610217539,0.138855410360913,4.40292493148274));
#41382=CARTESIAN_POINT('Ctrl Pts',(22.5694065025095,0.0347856757474044,
4.41583870262252));
#41383=CARTESIAN_POINT('Ctrl Pts',(22.5733993439214,-1.0582204931428E-7,
4.41583910483016));
#41384=CARTESIAN_POINT('Origin',(3.42660065607856,0.,4.));
#41385=CARTESIAN_POINT('',(21.8766006560786,1.03078286340212E-5,4.41586151989188));
#41386=CARTESIAN_POINT('',(21.9733993439214,8.40473402259622E-6,4.41585103914036));
#41387=CARTESIAN_POINT('',(3.42660065607856,4.87367679877478E-13,4.415875));
#41388=CARTESIAN_POINT('Ctrl Pts',(21.8766006560786,1.03078286340201E-5,
4.41586151989188));
#41389=CARTESIAN_POINT('Ctrl Pts',(21.8822132785738,-0.0488795353146484,
4.415816298089));
#41390=CARTESIAN_POINT('Ctrl Pts',(21.8957785404128,-0.167079919178725,
4.39498170153279));
#41391=CARTESIAN_POINT('Ctrl Pts',(21.9172964415957,-0.326407159500644,
4.28539643168872));
#41392=CARTESIAN_POINT('Ctrl Pts',(21.9411543596271,-0.423245389017799,
4.09410684177624));
#41393=CARTESIAN_POINT('Ctrl Pts',(21.9650122776585,-0.416588591947193,
3.87980556563057));
#41394=CARTESIAN_POINT('Ctrl Pts',(21.98887019569,-0.30806453650007,3.69489510271888));
#41395=CARTESIAN_POINT('Ctrl Pts',(22.0127281137213,-0.12421031036921,3.58459109808296));
#41396=CARTESIAN_POINT('Ctrl Pts',(22.0365860317528,0.0900167200678817,
3.57586588547707));
#41397=CARTESIAN_POINT('Ctrl Pts',(22.0604439497842,0.282232210442068,3.67085301705332));
#41398=CARTESIAN_POINT('Ctrl Pts',(22.0843018678157,0.405434237512275,3.8463255517439));
#41399=CARTESIAN_POINT('Ctrl Pts',(22.108159785847,0.429496549703537,4.05937567504088));
#41400=CARTESIAN_POINT('Ctrl Pts',(22.1320177038785,0.348535256241736,4.25790682842971));
#41401=CARTESIAN_POINT('Ctrl Pts',(22.1548313272889,0.18962186617866,4.38744320371645));
#41402=CARTESIAN_POINT('Ctrl Pts',(22.1696923113557,0.0601536901409818,
4.41584170838249));
#41403=CARTESIAN_POINT('Ctrl Pts',(22.1766006560786,-8.37799962077716E-6,
4.41589611849309));
#41404=CARTESIAN_POINT('Ctrl Pts',(21.9733993439214,8.40473402260317E-6,
4.41585103914036));
#41405=CARTESIAN_POINT('Ctrl Pts',(21.9785431582582,-0.044801031555974,
4.41581845947763));
#41406=CARTESIAN_POINT('Ctrl Pts',(21.9916396119388,-0.158914563981884,
4.39744691543598));
#41407=CARTESIAN_POINT('Ctrl Pts',(22.0126887049632,-0.317860118355158,
4.29488591379237));
#41408=CARTESIAN_POINT('Ctrl Pts',(22.0365466229946,-0.420290167226249,
4.10653136780738));
#41409=CARTESIAN_POINT('Ctrl Pts',(22.060404541026,-0.419947821735935,3.89212700053744));
#41410=CARTESIAN_POINT('Ctrl Pts',(22.0842624590574,-0.316916794682727,
3.70410052003731));
#41411=CARTESIAN_POINT('Ctrl Pts',(22.1081203770888,-0.136390978688423,
3.58842952252864));
#41412=CARTESIAN_POINT('Ctrl Pts',(22.1319782951203,0.0774861468089536,
3.57339871771534));
#41413=CARTESIAN_POINT('Ctrl Pts',(22.1558362131517,0.27241579873489,3.66268354680831));
#41414=CARTESIAN_POINT('Ctrl Pts',(22.1796941311831,0.400732367405962,3.83445143701846));
#41415=CARTESIAN_POINT('Ctrl Pts',(22.2035520492145,0.431058956528623,4.04670046033727));
#41416=CARTESIAN_POINT('Ctrl Pts',(22.227409967246,0.355979888945518,4.24752994899471));
#41417=CARTESIAN_POINT('Ctrl Pts',(22.2506923988149,0.197764744804664,4.38444734931837));
#41418=CARTESIAN_POINT('Ctrl Pts',(22.26602219104,0.064235283418036,4.41586628455644));
#41419=CARTESIAN_POINT('Ctrl Pts',(22.2733993439214,-5.11585294797612E-6,
4.41590580604266));
#41420=CARTESIAN_POINT('Origin',(3.42660065607856,0.,4.));
#41421=CARTESIAN_POINT('',(21.5766006560785,-1.05752387382048E-5,4.41586434469346));
#41422=CARTESIAN_POINT('',(21.6733993439214,-1.08222664516599E-5,4.41587700699864));
#41423=CARTESIAN_POINT('',(3.42660065607856,4.87367679877478E-13,4.415875));
#41424=CARTESIAN_POINT('Ctrl Pts',(21.5766006560785,-1.05752387381843E-5,
4.41586434469346));
#41425=CARTESIAN_POINT('Ctrl Pts',(21.5788289671043,-0.0194203346498642,
4.41588296395747));
#41426=CARTESIAN_POINT('Ctrl Pts',(21.5890099174739,-0.10809016089515,4.40978779866957));
#41427=CARTESIAN_POINT('Ctrl Pts',(21.6071435071872,-0.258824259222961,
4.34785450957493));
#41428=CARTESIAN_POINT('Ctrl Pts',(21.6310014252187,-0.39385182381868,4.18131050126406));
#41429=CARTESIAN_POINT('Ctrl Pts',(21.6548593432501,-0.432571889182456,
3.97043113659525));
#41430=CARTESIAN_POINT('Ctrl Pts',(21.6787172612815,-0.365516344619441,
3.76678216446856));
#41431=CARTESIAN_POINT('Ctrl Pts',(21.702575179313,-0.209082097331647,3.62016130585559));
#41432=CARTESIAN_POINT('Ctrl Pts',(21.7264330973443,-0.00152158196427748,
3.56642135455923));
#41433=CARTESIAN_POINT('Ctrl Pts',(21.7502910153758,0.206411001640417,3.61870319251831));
#41434=CARTESIAN_POINT('Ctrl Pts',(21.7741489334072,0.363870472821225,3.76422248622317));
#41435=CARTESIAN_POINT('Ctrl Pts',(21.7980068514386,0.432353701764573,3.96739580449697));
#41436=CARTESIAN_POINT('Ctrl Pts',(21.82186476947,0.395114673548107,4.17854173669174));
#41437=CARTESIAN_POINT('Ctrl Pts',(21.8457226875014,0.261259344941517,4.3460293508861));
#41438=CARTESIAN_POINT('Ctrl Pts',(21.8639679830376,0.110037800305057,4.4094070875278));
#41439=CARTESIAN_POINT('Ctrl Pts',(21.87426063923,0.0203934810735595,4.41588037378429));
#41440=CARTESIAN_POINT('Ctrl Pts',(21.8766006560786,1.03078286340201E-5,
4.41586151989188));
#41441=CARTESIAN_POINT('Ctrl Pts',(21.6733993439214,-1.0822266451653E-5,
4.41587700699864));
#41442=CARTESIAN_POINT('Ctrl Pts',(21.6751588467887,-0.0153356749568721,
4.41589290068126));
#41443=CARTESIAN_POINT('Ctrl Pts',(21.6848709889998,-0.0999166717736498,
4.41130778913604));
#41444=CARTESIAN_POINT('Ctrl Pts',(21.7025357705547,-0.248467031045983,
4.35532645760922));
#41445=CARTESIAN_POINT('Ctrl Pts',(21.7263936885861,-0.388341045935521,
4.1928315042612));
#41446=CARTESIAN_POINT('Ctrl Pts',(21.7502516066176,-0.433255096896122,
3.98318399549658));
#41447=CARTESIAN_POINT('Ctrl Pts',(21.774109524649,-0.372226475033738,3.77764845789182));
#41448=CARTESIAN_POINT('Ctrl Pts',(21.7979674426804,-0.220178340780001,
3.62648392906691));
#41449=CARTESIAN_POINT('Ctrl Pts',(21.8218253607118,-0.0142906046679706,
3.56665425395863));
#41450=CARTESIAN_POINT('Ctrl Pts',(21.8456832787432,0.195091573553633,3.61278941785858));
#41451=CARTESIAN_POINT('Ctrl Pts',(21.8695411967747,0.356768547853618,3.75360811649661));
#41452=CARTESIAN_POINT('Ctrl Pts',(21.8933991148061,0.431205894023261,3.95467634223136));
#41453=CARTESIAN_POINT('Ctrl Pts',(21.9172570328375,0.400201653291494,4.16682743688221));
#41454=CARTESIAN_POINT('Ctrl Pts',(21.941114950869,0.271337207055788,4.33818467892719));
#41455=CARTESIAN_POINT('Ctrl Pts',(21.9598290545635,0.118211900824938,4.40773087908456));
#41456=CARTESIAN_POINT('Ctrl Pts',(21.9705905189143,0.0244769910710258,
4.41586882955141));
#41457=CARTESIAN_POINT('Ctrl Pts',(21.9733993439214,8.40473402260317E-6,
4.41585103914036));
#41458=CARTESIAN_POINT('Origin',(3.42660065607856,0.,4.));
#41459=CARTESIAN_POINT('',(21.2766006560785,8.9771325895615E-6,4.41589335210553));
#41460=CARTESIAN_POINT('',(21.3733993439214,1.06214664634743E-5,4.41588075133303));
#41461=CARTESIAN_POINT('',(3.42660065607856,4.87367679877478E-13,4.415875));
#41462=CARTESIAN_POINT('Ctrl Pts',(21.2766006560785,8.97713258955941E-6,
4.41589335210553));
#41463=CARTESIAN_POINT('Ctrl Pts',(21.2833972949786,-0.0591814269577189,
4.41583723296416));
#41464=CARTESIAN_POINT('Ctrl Pts',(21.2981465732225,-0.187680420990878,
4.38813575385326));
#41465=CARTESIAN_POINT('Ctrl Pts',(21.3208484908102,-0.346716519889314,
4.26034671465164));
#41466=CARTESIAN_POINT('Ctrl Pts',(21.3447064088417,-0.429069235164158,
4.0623886883135));
#41467=CARTESIAN_POINT('Ctrl Pts',(21.368564326873,-0.406502834830527,3.8491749282489));
#41468=CARTESIAN_POINT('Ctrl Pts',(21.3924222449045,-0.284535418465691,
3.67284200661995));
#41469=CARTESIAN_POINT('Ctrl Pts',(21.4162801629359,-0.0929913416969399,
3.5765081259772));
#41470=CARTESIAN_POINT('Ctrl Pts',(21.4401380809674,0.121291651150069,3.58372954422009));
#41471=CARTESIAN_POINT('Ctrl Pts',(21.4639959989987,0.305915531372611,3.69274042788069));
#41472=CARTESIAN_POINT('Ctrl Pts',(21.4878539170302,0.415734731202803,3.87688464650718));
#41473=CARTESIAN_POINT('Ctrl Pts',(21.5117118350615,0.423895464867194,4.09113392265755));
#41474=CARTESIAN_POINT('Ctrl Pts',(21.535569753093,0.328402210690932,4.28309847227994));
#41475=CARTESIAN_POINT('Ctrl Pts',(21.5571993600986,0.169024930905334,4.39437398220882));
#41476=CARTESIAN_POINT('Ctrl Pts',(21.5708763277605,0.0498513310028489,
4.41581651349798));
#41477=CARTESIAN_POINT('Ctrl Pts',(21.5766006560785,-1.05752387381843E-5,
4.41586434469346));
#41478=CARTESIAN_POINT('Ctrl Pts',(21.3733993439214,1.06214664634605E-5,
4.41588075133303));
#41479=CARTESIAN_POINT('Ctrl Pts',(21.379727174663,-0.0551018547626871,
4.41582358345633));
#41480=CARTESIAN_POINT('Ctrl Pts',(21.3940076447484,-0.1795281855266,4.39095386216025));
#41481=CARTESIAN_POINT('Ctrl Pts',(21.4162407541777,-0.338898428465248,
4.27044521104599));
#41482=CARTESIAN_POINT('Ctrl Pts',(21.4400986722091,-0.427045644525908,
4.07499849655415));
#41483=CARTESIAN_POINT('Ctrl Pts',(21.4639565902406,-0.410768568010174,
3.86121260673678));
#41484=CARTESIAN_POINT('Ctrl Pts',(21.4878145082719,-0.294047387504818,
3.68136401506497));
#41485=CARTESIAN_POINT('Ctrl Pts',(21.5116724263034,-0.105423611064507,
3.57943060117972));
#41486=CARTESIAN_POINT('Ctrl Pts',(21.5355303443348,0.108979109962582,3.58033786138646));
#41487=CARTESIAN_POINT('Ctrl Pts',(21.5593882623662,0.296733470072461,3.68386394585134));
#41488=CARTESIAN_POINT('Ctrl Pts',(21.5832461803976,0.411928413892185,3.86469390692879));
#41489=CARTESIAN_POINT('Ctrl Pts',(21.6071040984291,0.426395639810567,4.07860989342611));
#41490=CARTESIAN_POINT('Ctrl Pts',(21.6309620164605,0.33659751701124,4.27330361969026));
#41491=CARTESIAN_POINT('Ctrl Pts',(21.6530604316246,0.177184770587036,4.39173732935402));
#41492=CARTESIAN_POINT('Ctrl Pts',(21.6672062074449,0.0539299276789421,
4.41582106406873));
#41493=CARTESIAN_POINT('Ctrl Pts',(21.6733993439214,-1.0822266451653E-5,
4.41587700699864));
#41494=CARTESIAN_POINT('Origin',(3.42660065607856,0.,4.));
#41495=CARTESIAN_POINT('',(20.9766006560786,-4.48287659654576E-6,4.41584197426197));
#41496=CARTESIAN_POINT('',(21.0733993439214,-7.65157297119567E-6,4.41584853425778));
#41497=CARTESIAN_POINT('',(3.42660065607856,4.87367679877478E-13,4.415875));
#41498=CARTESIAN_POINT('Ctrl Pts',(20.9766006560786,-4.48287659652116E-6,
4.41584197426197));
#41499=CARTESIAN_POINT('Ctrl Pts',(20.9800129835092,-0.0297322302090305,
4.41585318364051));
#41500=CARTESIAN_POINT('Ctrl Pts',(20.9913779502836,-0.128734546054536,
4.40538471300776));
#41501=CARTESIAN_POINT('Ctrl Pts',(21.0106955564018,-0.28396276796243,4.32765515869354));
#41502=CARTESIAN_POINT('Ctrl Pts',(21.0345534744332,-0.40623841344949,4.15153583326342));
#41503=CARTESIAN_POINT('Ctrl Pts',(21.0584113924646,-0.429177699343215,
3.93836186909709));
#41504=CARTESIAN_POINT('Ctrl Pts',(21.082269310496,-0.347171348131155,3.74026010679315));
#41505=CARTESIAN_POINT('Ctrl Pts',(21.1061272285274,-0.180272145040548,
3.605671823621));
#41506=CARTESIAN_POINT('Ctrl Pts',(21.1299851465589,0.0307085077608185,
3.56750752082027));
#41507=CARTESIAN_POINT('Ctrl Pts',(21.1538430645903,0.234180094072738,3.63509941005724));
#41508=CARTESIAN_POINT('Ctrl Pts',(21.1777009826217,0.380388268371489,3.79191943321731));
#41509=CARTESIAN_POINT('Ctrl Pts',(21.2015589006531,0.433581149524578,3.99962082296209));
#41510=CARTESIAN_POINT('Ctrl Pts',(21.2254168186846,0.380751629084578,4.2074149318183));
#41511=CARTESIAN_POINT('Ctrl Pts',(21.2492747367159,0.234817963878357,4.36449043997717));
#41512=CARTESIAN_POINT('Ctrl Pts',(21.2663360158473,0.0893960873046664,
4.41308118928586));
#41513=CARTESIAN_POINT('Ctrl Pts',(21.2754446556348,0.0100763257733538,
4.41590289708112));
#41514=CARTESIAN_POINT('Ctrl Pts',(21.2766006560785,8.97713258955941E-6,
4.41589335210553));
#41515=CARTESIAN_POINT('Ctrl Pts',(21.0733993439214,-7.65157297121996E-6,
4.41584853425778));
#41516=CARTESIAN_POINT('Ctrl Pts',(21.0763428631935,-0.0256500457845501,
4.41586537097631));
#41517=CARTESIAN_POINT('Ctrl Pts',(21.0872390218095,-0.120560449820324,
4.40722571769055));
#41518=CARTESIAN_POINT('Ctrl Pts',(21.1060878197692,-0.274189543318984,
4.33587624407661));
#41519=CARTESIAN_POINT('Ctrl Pts',(21.1299457378007,-0.401599180171465,
4.16343456021562));
#41520=CARTESIAN_POINT('Ctrl Pts',(21.1538036558321,-0.430806878168669,
3.95102867450389));
#41521=CARTESIAN_POINT('Ctrl Pts',(21.1776615738635,-0.354670559489406,
3.75059761183336));
#41522=CARTESIAN_POINT('Ctrl Pts',(21.2015194918949,-0.191807627993766,
3.61115222665144));
#41523=CARTESIAN_POINT('Ctrl Pts',(21.2253774099264,0.0179574932869785,
3.56679071405539));
#41524=CARTESIAN_POINT('Ctrl Pts',(21.2492353279577,0.223331518303719,3.62836067225603));
#41525=CARTESIAN_POINT('Ctrl Pts',(21.2730932459892,0.374094903668402,3.78080656934254));
#41526=CARTESIAN_POINT('Ctrl Pts',(21.2969511640206,0.433381894944723,3.98685123093373));
#41527=CARTESIAN_POINT('Ctrl Pts',(21.320809082052,0.386695207821707,4.19611112472705));
#41528=CARTESIAN_POINT('Ctrl Pts',(21.3446670000834,0.245451009020076,4.35741650656472));
#41529=CARTESIAN_POINT('Ctrl Pts',(21.3621970873732,0.0975684711839555,
4.41172139589413));
#41530=CARTESIAN_POINT('Ctrl Pts',(21.3717745353192,0.014161952170494,4.41589543043265));
#41531=CARTESIAN_POINT('Ctrl Pts',(21.3733993439214,1.06214664634605E-5,
4.41588075133303));
#41532=CARTESIAN_POINT('Origin',(3.42660065607856,0.,4.));
#41533=CARTESIAN_POINT('',(20.6766006560786,1.29204965968245E-6,4.41591114679826));
#41534=CARTESIAN_POINT('',(20.7733993439214,3.9567662055099E-6,4.41590779860895));
#41535=CARTESIAN_POINT('',(3.42660065607856,4.87367679877478E-13,4.415875));
#41536=CARTESIAN_POINT('Ctrl Pts',(20.6766006560786,1.29076178055295E-6,
4.41591111076812));
#41537=CARTESIAN_POINT('Ctrl Pts',(20.6766286720397,-0.000242659277546582,
4.41591112051333));
#41538=CARTESIAN_POINT('Ctrl Pts',(20.6846093273446,-0.0697345275278937,
4.41585145172406));
#41539=CARTESIAN_POINT('Ctrl Pts',(20.7005426219933,-0.208420567790133,
4.38020336888205));
#41540=CARTESIAN_POINT('Ctrl Pts',(20.7244005400248,-0.365106210756856,
4.23385701605743));
#41541=CARTESIAN_POINT('Ctrl Pts',(20.7482584580562,-0.432520392530856,
4.03032528343114));
#41542=CARTESIAN_POINT('Ctrl Pts',(20.7721163760876,-0.394167874571092,
3.81937870627435));
#41543=CARTESIAN_POINT('Ctrl Pts',(20.795974294119,-0.259432524437891,3.65259868360638));
#41544=CARTESIAN_POINT('Ctrl Pts',(20.8198322121504,-0.0612578225112809,
3.57076788979259));
#41545=CARTESIAN_POINT('Ctrl Pts',(20.8436901301819,0.151895538690754,3.5938959627232));
#41546=CARTESIAN_POINT('Ctrl Pts',(20.8675480482132,0.327906592802717,3.71632757520176));
#41547=CARTESIAN_POINT('Ctrl Pts',(20.8914059662447,0.423735399567132,3.90812480123879));
#41548=CARTESIAN_POINT('Ctrl Pts',(20.9152638842761,0.415949440063929,4.12238802732943));
#41549=CARTESIAN_POINT('Ctrl Pts',(20.9391218023075,0.30645246920106,4.30672404095661));
#41550=CARTESIAN_POINT('Ctrl Pts',(20.9595673929083,0.148398440326279,4.40042000858165));
#41551=CARTESIAN_POINT('Ctrl Pts',(20.9720603441653,0.0395501167658222,
4.4158270594931));
#41552=CARTESIAN_POINT('Ctrl Pts',(20.9766006560786,-4.48287659652116E-6,
4.41584197426197));
#41553=CARTESIAN_POINT('Ctrl Pts',(20.7733993439214,3.95676620551077E-6,
4.41590779860895));
#41554=CARTESIAN_POINT('Ctrl Pts',(20.7809111910678,-0.0654084660523611,
4.41587519962517));
#41555=CARTESIAN_POINT('Ctrl Pts',(20.7963756775582,-0.200102595337945,
4.3835597345012));
#41556=CARTESIAN_POINT('Ctrl Pts',(20.8197928033922,-0.358062019934396,
4.24450842127602));
#41557=CARTESIAN_POINT('Ctrl Pts',(20.8436507214237,-0.431438726014498,
4.04305074550709));
#41558=CARTESIAN_POINT('Ctrl Pts',(20.867508639455,-0.399316990859146,3.83106596928302));
#41559=CARTESIAN_POINT('Ctrl Pts',(20.8913665574865,-0.269551332195825,
3.66039017609669));
#41560=CARTESIAN_POINT('Ctrl Pts',(20.9152244755179,-0.0738730526583281,
3.57275822989076));
#41561=CARTESIAN_POINT('Ctrl Pts',(20.9390823935493,0.139869212314499,3.58959853735383));
#41562=CARTESIAN_POINT('Ctrl Pts',(20.9629403115807,0.319409638666883,3.70679317993256));
#41563=CARTESIAN_POINT('Ctrl Pts',(20.9867982296122,0.420845711130686,3.8956848776653));
#41564=CARTESIAN_POINT('Ctrl Pts',(21.0106561476436,0.419373541863394,4.11008446384341));
#41565=CARTESIAN_POINT('Ctrl Pts',(21.034514065675,0.315353119032788,4.29756540021079));
#41566=CARTESIAN_POINT('Ctrl Pts',(21.0554284644342,0.156567902793621,4.39812991232556));
#41567=CARTESIAN_POINT('Ctrl Pts',(21.0683902238497,0.0436291721249729,
4.41581988245125));
#41568=CARTESIAN_POINT('Ctrl Pts',(21.0733993439214,-7.65157297121996E-6,
4.41584853425778));
#41569=CARTESIAN_POINT('Origin',(3.42660065607856,0.,4.));
#41570=CARTESIAN_POINT('',(20.3766006560786,0.000383027521040961,4.41597069455794));
#41571=CARTESIAN_POINT('',(20.4733993439214,0.000101608071013781,4.41586489633469));
#41572=CARTESIAN_POINT('',(3.42660065607856,4.87367679877478E-13,4.415875));
#41573=CARTESIAN_POINT('Ctrl Pts',(20.3766006560786,0.000383027521040954,
4.41597069455794));
#41574=CARTESIAN_POINT('Ctrl Pts',(20.3891496392578,-0.108893832387875,
4.41487837761012));
#41575=CARTESIAN_POINT('Ctrl Pts',(20.4176039011246,-0.35839559572325,4.31454223548297));
#41576=CARTESIAN_POINT('Ctrl Pts',(20.4540108023354,-0.457800032585507,
3.97025345815189));
#41577=CARTESIAN_POINT('Ctrl Pts',(20.4858213597105,-0.325993724402262,
3.71529210935379));
#41578=CARTESIAN_POINT('Ctrl Pts',(20.509679277742,-0.15096738523986,3.59329490328468));
#41579=CARTESIAN_POINT('Ctrl Pts',(20.5335371957734,0.0630371972956549,
3.57102347342756));
#41580=CARTESIAN_POINT('Ctrl Pts',(20.5573951138048,0.260511246441404,3.65349437971329));
#41581=CARTESIAN_POINT('Ctrl Pts',(20.5812530318362,0.394877283734959,3.82077798440408));
#41582=CARTESIAN_POINT('Ctrl Pts',(20.6051109498677,0.432370081305563,4.03184236506754));
#41583=CARTESIAN_POINT('Ctrl Pts',(20.6289688678991,0.364303478986858,4.23514367899931));
#41584=CARTESIAN_POINT('Ctrl Pts',(20.6527987699694,0.207251017164088,4.38076243960928));
#41585=CARTESIAN_POINT('Ctrl Pts',(20.6686760326959,0.0690052481014253,
4.41590835422812));
#41586=CARTESIAN_POINT('Ctrl Pts',(20.6766006560786,1.29076178055295E-6,
4.41591111076812));
#41587=CARTESIAN_POINT('Ctrl Pts',(20.4733993439214,0.000101608071013788,
4.4158648963347));
#41588=CARTESIAN_POINT('Ctrl Pts',(20.4775268795984,-0.0359150725839473,
4.41584626969953));
#41589=CARTESIAN_POINT('Ctrl Pts',(20.4896070546192,-0.141401612166324,
4.40227446254147));
#41590=CARTESIAN_POINT('Ctrl Pts',(20.5096398689838,-0.298255971346869,
4.31460392554555));
#41591=CARTESIAN_POINT('Ctrl Pts',(20.5334977870152,-0.412709509332759,
4.13311446574462));
#41592=CARTESIAN_POINT('Ctrl Pts',(20.5573557050466,-0.425936384696969,
3.91915434697803));
#41593=CARTESIAN_POINT('Ctrl Pts',(20.581213623078,-0.335173342752607,3.72492109335083));
#41594=CARTESIAN_POINT('Ctrl Pts',(20.6050715411095,-0.162364888615448,
3.59797442377207));
#41595=CARTESIAN_POINT('Ctrl Pts',(20.6289294591408,0.0501004451364318,
3.56932214892951));
#41596=CARTESIAN_POINT('Ctrl Pts',(20.6527873771723,0.250339089241223,3.64598859455508));
#41597=CARTESIAN_POINT('Ctrl Pts',(20.6766452952037,0.389350172549011,3.80921715950176));
#41598=CARTESIAN_POINT('Ctrl Pts',(20.7005032132352,0.433161330121289,4.01909908002448));
#41599=CARTESIAN_POINT('Ctrl Pts',(20.7243611312665,0.371049143609512,4.22430982617278));
#41600=CARTESIAN_POINT('Ctrl Pts',(20.748219049298,0.218207240773441,4.37467120177868));
#41601=CARTESIAN_POINT('Ctrl Pts',(20.7645651201829,0.0769305199015265,
4.41491906931248));
#41602=CARTESIAN_POINT('Ctrl Pts',(20.772958551724,0.00384233167249433,
4.41590971150433));
#41603=CARTESIAN_POINT('Ctrl Pts',(20.7733993439214,3.95676620551077E-6,
4.41590779860895));
#41604=CARTESIAN_POINT('Origin',(3.42660065607856,0.,4.));
#41605=CARTESIAN_POINT('',(20.0766006560786,-0.000186622634748148,4.41645953600834));
#41606=CARTESIAN_POINT('',(20.1733993439214,-0.000111611226006447,4.41653056081536));
#41607=CARTESIAN_POINT('',(3.42660065607856,4.87367679877478E-13,4.415875));
#41608=CARTESIAN_POINT('Ctrl Pts',(20.0766006560786,-0.000186622634748109,
4.41645953600834));
#41609=CARTESIAN_POINT('Ctrl Pts',(20.0778126884445,-0.0107019642254321,
4.4165186149328));
#41610=CARTESIAN_POINT('Ctrl Pts',(20.0949299994981,-0.159149739060163,
4.41138240526969));
#41611=CARTESIAN_POINT('Ctrl Pts',(20.1279525892393,-0.432744382500041,
4.23375285658289));
#41612=CARTESIAN_POINT('Ctrl Pts',(20.1756684253021,-0.430649333670284,
3.76246031529274));
#41613=CARTESIAN_POINT('Ctrl Pts',(20.223384261365,-0.033136228617316,3.50924504180455));
#41614=CARTESIAN_POINT('Ctrl Pts',(20.2711000974278,0.394908089060633,3.70680919012016));
#41615=CARTESIAN_POINT('Ctrl Pts',(20.3188159334906,0.460110046434968,4.17340395051402));
#41616=CARTESIAN_POINT('Ctrl Pts',(20.3539827863742,0.197028357007358,4.40022211154544));
#41617=CARTESIAN_POINT('Ctrl Pts',(20.3732443605702,0.0296097328916507,
4.416262840815));
#41618=CARTESIAN_POINT('Ctrl Pts',(20.3766006560786,0.000383027521040954,
4.41597069455794));
#41619=CARTESIAN_POINT('Ctrl Pts',(20.1733993439214,-0.000111611226006447,
4.41653056081536));
#41620=CARTESIAN_POINT('Ctrl Pts',(20.1741425681289,-0.00655727229825777,
4.41655465488103));
#41621=CARTESIAN_POINT('Ctrl Pts',(20.190791071024,-0.150919726673813,4.41348743992374));
#41622=CARTESIAN_POINT('Ctrl Pts',(20.2233448526067,-0.425711472830213,
4.24633918020534));
#41623=CARTESIAN_POINT('Ctrl Pts',(20.2710606886696,-0.437384262562023,
3.77535541015343));
#41624=CARTESIAN_POINT('Ctrl Pts',(20.3187765247324,-0.0477164433392854,
3.51022640082505));
#41625=CARTESIAN_POINT('Ctrl Pts',(20.3664923607953,0.386374384143037,3.69571627142296));
#41626=CARTESIAN_POINT('Ctrl Pts',(20.4062555575143,0.45143962727185,4.08165775845481));
#41627=CARTESIAN_POINT('Ctrl Pts',(20.4380661148895,0.291471375703242,4.31996082336987));
#41628=CARTESIAN_POINT('Ctrl Pts',(20.4577964972439,0.136183087716603,4.40372206768731));
#41629=CARTESIAN_POINT('Ctrl Pts',(20.4695742402546,0.0334792813416625,
4.41588215816259));
#41630=CARTESIAN_POINT('Ctrl Pts',(20.4733993439214,0.000101608071013788,
4.4158648963347));
#41631=CARTESIAN_POINT('Origin',(3.42660065607856,0.,4.));
#41632=CARTESIAN_POINT('',(19.7766006560786,-0.000280998963924209,4.41539029291088));
#41633=CARTESIAN_POINT('',(19.8733993439214,-0.000322938566065189,4.41548189938477));
#41634=CARTESIAN_POINT('',(3.42660065607856,4.87367679877478E-13,4.415875));
#41635=CARTESIAN_POINT('Ctrl Pts',(19.7766006560786,-0.000280998963924181,
4.41539029291088));
#41636=CARTESIAN_POINT('Ctrl Pts',(19.7823810163188,-0.0507615353771658,
4.41570272077311));
#41637=CARTESIAN_POINT('Ctrl Pts',(19.8040666552467,-0.23976299482565,4.3837755623668));
#41638=CARTESIAN_POINT('Ctrl Pts',(19.8416575728622,-0.481212499922896,
4.10168523844358));
#41639=CARTESIAN_POINT('Ctrl Pts',(19.8893734089251,-0.345789702982467,
3.65023692191923));
#41640=CARTESIAN_POINT('Ctrl Pts',(19.9370892449879,0.107175910646637,3.51998011832295));
#41641=CARTESIAN_POINT('Ctrl Pts',(19.9848050810508,0.461722480014006,3.83053541934297));
#41642=CARTESIAN_POINT('Ctrl Pts',(20.0313088847476,0.394022427012164,4.28486673161383));
#41643=CARTESIAN_POINT('Ctrl Pts',(20.0619074097569,0.127288937001902,4.4157433330307));
#41644=CARTESIAN_POINT('Ctrl Pts',(20.0766006560786,-0.000186622634748109,
4.41645953600834));
#41645=CARTESIAN_POINT('Ctrl Pts',(19.8733993439214,-0.000322938566065196,
4.41548189938477));
#41646=CARTESIAN_POINT('Ctrl Pts',(19.8787108960032,-0.0466836533228258,
4.41581668875846));
#41647=CARTESIAN_POINT('Ctrl Pts',(19.8999277267727,-0.231469429366377,
4.38724295332581));
#41648=CARTESIAN_POINT('Ctrl Pts',(19.9370498362297,-0.47800980043334,4.11581244897344));
#41649=CARTESIAN_POINT('Ctrl Pts',(19.9847656722926,-0.355939225796451,
3.66057517601247));
#41650=CARTESIAN_POINT('Ctrl Pts',(20.0324815083554,0.0929888682922082,
3.51702731322357));
#41651=CARTESIAN_POINT('Ctrl Pts',(20.0801973444182,0.456536973876988,3.81701888067549));
#41652=CARTESIAN_POINT('Ctrl Pts',(20.1271699562736,0.401683300383188,4.27772103607547));
#41653=CARTESIAN_POINT('Ctrl Pts',(20.1582372894413,0.131382308576697,4.41603903277767));
#41654=CARTESIAN_POINT('Ctrl Pts',(20.1733993439214,-0.000111611226006447,
4.41653056081536));
#41655=CARTESIAN_POINT('Origin',(3.42660065607856,0.,4.));
#41656=CARTESIAN_POINT('',(19.4766006560786,0.000302289446139524,4.41543216566181));
#41657=CARTESIAN_POINT('',(19.5733993439214,0.000255464646300079,4.41534829948978));
#41658=CARTESIAN_POINT('',(3.42660065607856,4.87367679877478E-13,4.415875));
#41659=CARTESIAN_POINT('Ctrl Pts',(19.4766006560786,0.000302289446139546,
4.41543216566181));
#41660=CARTESIAN_POINT('Ctrl Pts',(19.4869493441932,-0.0900510892866153,
4.41482666801407));
#41661=CARTESIAN_POINT('Ctrl Pts',(19.5132033109954,-0.320168095705801,
4.3413809155508));
#41662=CARTESIAN_POINT('Ctrl Pts',(19.5553625564852,-0.490312813065352,
3.96128857502183));
#41663=CARTESIAN_POINT('Ctrl Pts',(19.603078392548,-0.232620797759261,3.56664935826393));
#41664=CARTESIAN_POINT('Ctrl Pts',(19.6507942286109,0.238690449241969,3.56996267500769));
#41665=CARTESIAN_POINT('Ctrl Pts',(19.6985100646737,0.490808633485035,3.96818593857384));
#41666=CARTESIAN_POINT('Ctrl Pts',(19.7404455404963,0.316268156276861,4.34384396940031));
#41667=CARTESIAN_POINT('Ctrl Pts',(19.7664757376312,0.0881410531427697,
4.41484304213512));
#41668=CARTESIAN_POINT('Ctrl Pts',(19.7766006560786,-0.000280998963924181,
4.41539029291088));
#41669=CARTESIAN_POINT('Ctrl Pts',(19.5733993439214,0.000255464646300094,
4.41534829948978));
#41670=CARTESIAN_POINT('Ctrl Pts',(19.5832792238775,-0.0860485087386658,
4.41486588036018));
#41671=CARTESIAN_POINT('Ctrl Pts',(19.6090643825213,-0.311990568344336,
4.34649332259355));
#41672=CARTESIAN_POINT('Ctrl Pts',(19.6507548198527,-0.491240257057309,
3.97574594767572));
#41673=CARTESIAN_POINT('Ctrl Pts',(19.6984706559155,-0.245282818621706,
3.57368850533185));
#41674=CARTESIAN_POINT('Ctrl Pts',(19.7461864919783,0.225921452997342,3.56311925573479));
#41675=CARTESIAN_POINT('Ctrl Pts',(19.7939023280412,0.489658867576397,3.95374471702426));
#41676=CARTESIAN_POINT('Ctrl Pts',(19.8363066120222,0.324430886710512,4.33863507066385));
#41677=CARTESIAN_POINT('Ctrl Pts',(19.8628056173156,0.0921420753912029,
4.4148141723173));
#41678=CARTESIAN_POINT('Ctrl Pts',(19.8733993439214,-0.000322938566065196,
4.41548189938477));
#41679=CARTESIAN_POINT('Origin',(3.42660065607856,0.,4.));
#41680=CARTESIAN_POINT('',(19.1766006560786,0.000155842099650094,4.41649089206047));
#41681=CARTESIAN_POINT('',(19.2733993439214,0.000220989830587742,4.4164164649367));
#41682=CARTESIAN_POINT('',(3.42660065607856,4.87367679877478E-13,4.415875));
#41683=CARTESIAN_POINT('Ctrl Pts',(19.1766006560786,0.000155842099650088,
4.41649089206047));
#41684=CARTESIAN_POINT('Ctrl Pts',(19.1915176720675,-0.129233580897558,
4.41587069825202));
#41685=CARTESIAN_POINT('Ctrl Pts',(19.2223399667441,-0.397695790553126,
4.28149179527637));
#41686=CARTESIAN_POINT('Ctrl Pts',(19.2690675401082,-0.459293044881286,
3.82405931712685));
#41687=CARTESIAN_POINT('Ctrl Pts',(19.316783376171,-0.100417177000157,3.51852142809106));
#41688=CARTESIAN_POINT('Ctrl Pts',(19.3644992122339,0.350673329058588,3.65513271950473));
#41689=CARTESIAN_POINT('Ctrl Pts',(19.4122150482967,0.479735122332443,4.10844094226069));
#41690=CARTESIAN_POINT('Ctrl Pts',(19.4495821962449,0.235804435834584,4.38544967282755));
#41691=CARTESIAN_POINT('Ctrl Pts',(19.4710440655056,0.0488163355692654,
4.4157572795781));
#41692=CARTESIAN_POINT('Ctrl Pts',(19.4766006560786,0.000302289446139546,
4.41543216566181));
#41693=CARTESIAN_POINT('Ctrl Pts',(19.2733993439214,0.000220989830587761,
4.4164164649367));
#41694=CARTESIAN_POINT('Ctrl Pts',(19.2878475517519,-0.125161313229646,
4.41561068768233));
#41695=CARTESIAN_POINT('Ctrl Pts',(19.31820103827,-0.389985711500173,4.28851341748863));
#41696=CARTESIAN_POINT('Ctrl Pts',(19.3644598034757,-0.464275578741542,
3.8376626582024));
#41697=CARTESIAN_POINT('Ctrl Pts',(19.4121756395385,-0.114554038379521,
3.52168776344319));
#41698=CARTESIAN_POINT('Ctrl Pts',(19.4598914756013,0.340364234683876,3.64495435060606));
#41699=CARTESIAN_POINT('Ctrl Pts',(19.5076073116642,0.482720800247919,4.09426482953845));
#41700=CARTESIAN_POINT('Ctrl Pts',(19.5454432677708,0.244097666198316,4.38190156491584));
#41701=CARTESIAN_POINT('Ctrl Pts',(19.5673739451899,0.0528892875329133,
4.41564251031262));
#41702=CARTESIAN_POINT('Ctrl Pts',(19.5733993439214,0.000255464646300094,
4.41534829948978));
#41703=CARTESIAN_POINT('Origin',(3.42660065607856,0.,4.));
#41704=CARTESIAN_POINT('',(18.8766006560785,-0.00038196507782994,4.41590683121974));
#41705=CARTESIAN_POINT('',(18.9733993439214,-0.000368287616214491,4.41603142687637));
#41706=CARTESIAN_POINT('',(3.42660065607856,4.87367679877478E-13,4.415875));
#41707=CARTESIAN_POINT('Ctrl Pts',(18.8766006560785,-0.000381965077829925,
4.41590683121974));
#41708=CARTESIAN_POINT('Ctrl Pts',(18.8801807212542,-0.0315488007868432,
4.41619587167324));
#41709=CARTESIAN_POINT('Ctrl Pts',(18.8996660651174,-0.200861076696893,
4.39874895857547));
#41710=CARTESIAN_POINT('Ctrl Pts',(18.9350566876684,-0.462607878309702,
4.16703046362027));
#41711=CARTESIAN_POINT('Ctrl Pts',(18.9827725237311,-0.39069124519864,3.70122654773242));
#41712=CARTESIAN_POINT('Ctrl Pts',(19.030488359794,0.0400031699426168,3.50979089028978));
#41713=CARTESIAN_POINT('Ctrl Pts',(19.0782041958568,0.433962058584907,3.76852180111673));
#41714=CARTESIAN_POINT('Ctrl Pts',(19.1259200319197,0.429406911488226,4.23982270375453));
#41715=CARTESIAN_POINT('Ctrl Pts',(19.1587188519936,0.155221332864305,4.41240136130926));
#41716=CARTESIAN_POINT('Ctrl Pts',(19.1756123933799,0.00872798149047904,
4.41653198033223));
#41717=CARTESIAN_POINT('Ctrl Pts',(19.1766006560786,0.000155842099650088,
4.41649089206047));
#41718=CARTESIAN_POINT('Ctrl Pts',(18.9733993439214,-0.000368287616214533,
4.41603142687637));
#41719=CARTESIAN_POINT('Ctrl Pts',(18.9765106009386,-0.0274330213022572,
4.4162811262788));
#41720=CARTESIAN_POINT('Ctrl Pts',(18.9955271366434,-0.192586232161443,
4.40152565608163));
#41721=CARTESIAN_POINT('Ctrl Pts',(19.0304489510358,-0.457487847288108,
4.18058265263639));
#41722=CARTESIAN_POINT('Ctrl Pts',(19.0781647870987,-0.399321187381313,
3.71286272589862));
#41723=CARTESIAN_POINT('Ctrl Pts',(19.1258806231614,0.0255482632835279,
3.50882537619781));
#41724=CARTESIAN_POINT('Ctrl Pts',(19.1735964592243,0.426956350589889,3.75584124112414));
#41725=CARTESIAN_POINT('Ctrl Pts',(19.2213122952871,0.436283851722622,4.22707185138688));
#41726=CARTESIAN_POINT('Ctrl Pts',(19.2545799235195,0.163455264474221,4.41023200720537));
#41727=CARTESIAN_POINT('Ctrl Pts',(19.2719422730642,0.0128655269200745,
4.41649772584937));
#41728=CARTESIAN_POINT('Ctrl Pts',(19.2733993439214,0.000220989830587761,
4.4164164649367));
#41729=CARTESIAN_POINT('Origin',(3.42660065607856,0.,4.));
#41730=CARTESIAN_POINT('',(18.5766006560786,2.82854505807383E-5,4.41518799822097));
#41731=CARTESIAN_POINT('',(18.6733993439214,-3.94222854199766E-5,4.41518963037823));
#41732=CARTESIAN_POINT('',(3.42660065607856,4.87367679877478E-13,4.415875));
#41733=CARTESIAN_POINT('Ctrl Pts',(18.5766006560786,2.82854505807215E-5,
4.41518799822097));
#41734=CARTESIAN_POINT('Ctrl Pts',(18.5847490491285,-0.0712192880865648,
4.41514491699706));
#41735=CARTESIAN_POINT('Ctrl Pts',(18.6088027208661,-0.281596950705947,
4.36382162423513));
#41736=CARTESIAN_POINT('Ctrl Pts',(18.6487616712913,-0.49096944006335,4.0292272779409));
#41737=CARTESIAN_POINT('Ctrl Pts',(18.6964775073541,-0.290120809601049,
3.60284116440841));
#41738=CARTESIAN_POINT('Ctrl Pts',(18.744193343417,0.177150224400508,3.54117212067402));
#41739=CARTESIAN_POINT('Ctrl Pts',(18.7919091794797,0.481741481528227,3.90085177849878));
#41740=CARTESIAN_POINT('Ctrl Pts',(18.836044950367,0.354281053487698,4.31776308733785));
#41741=CARTESIAN_POINT('Ctrl Pts',(18.8642754425666,0.106917172161326,4.4149117417093));
#41742=CARTESIAN_POINT('Ctrl Pts',(18.8766006560785,-0.000381965077829925,
4.41590683121974));
#41743=CARTESIAN_POINT('Ctrl Pts',(18.6733993439214,-3.94222854199489E-5,
4.41518963037823));
#41744=CARTESIAN_POINT('Ctrl Pts',(18.6810789288129,-0.0671871929144198,
4.41524623173262));
#41745=CARTESIAN_POINT('Ctrl Pts',(18.704663792392,-0.273330541024821,4.36810584919535));
#41746=CARTESIAN_POINT('Ctrl Pts',(18.7441539346588,-0.489895661254576,
4.0436745456279));
#41747=CARTESIAN_POINT('Ctrl Pts',(18.7918697707216,-0.301692008317894,
3.6115580391236));
#41748=CARTESIAN_POINT('Ctrl Pts',(18.8395856067845,0.163560057986223,3.53615376224111));
#41749=CARTESIAN_POINT('Ctrl Pts',(18.8873014428472,0.478612406344963,3.88670662268212));
#41750=CARTESIAN_POINT('Ctrl Pts',(18.9319060218929,0.362263203066427,4.31165738429376));
#41751=CARTESIAN_POINT('Ctrl Pts',(18.960605322251,0.110926532249199,4.41500462017153));
#41752=CARTESIAN_POINT('Ctrl Pts',(18.9733993439214,-0.000368287616214533,
4.41603142687637));
#41753=CARTESIAN_POINT('Origin',(3.42660065607856,0.,4.));
#41754=CARTESIAN_POINT('',(18.2766006560786,0.000371443240938316,4.41601098728712));
#41755=CARTESIAN_POINT('',(18.3733993439214,0.000382963303967143,4.41588626824893));
#41756=CARTESIAN_POINT('',(3.42660065607856,4.87367679877478E-13,4.415875));
#41757=CARTESIAN_POINT('Ctrl Pts',(18.2766006560785,0.000371443240938293,
4.41601098728712));
#41758=CARTESIAN_POINT('Ctrl Pts',(18.2893173770028,-0.110264925490287,
4.41498710445335));
#41759=CARTESIAN_POINT('Ctrl Pts',(18.3179393766147,-0.360950442388199,
4.31267773405576));
#41760=CARTESIAN_POINT('Ctrl Pts',(18.3624666549143,-0.479157019140895,
3.88903254594255));
#41761=CARTESIAN_POINT('Ctrl Pts',(18.4101824909771,-0.165810997523729,
3.5369536330429));
#41762=CARTESIAN_POINT('Ctrl Pts',(18.4578983270399,0.299801814449608,3.61009732380414));
#41763=CARTESIAN_POINT('Ctrl Pts',(18.5056141631028,0.49010200717001,4.04129464153984));
#41764=CARTESIAN_POINT('Ctrl Pts',(18.5451816061157,0.274694351318236,4.36741107590602));
#41765=CARTESIAN_POINT('Ctrl Pts',(18.5688437704409,0.0678526130816757,
4.41522900951301));
#41766=CARTESIAN_POINT('Ctrl Pts',(18.5766006560786,2.82854505807215E-5,
4.41518799822097));
#41767=CARTESIAN_POINT('Ctrl Pts',(18.3733993439214,0.000382963303967157,
4.41588626824893));
#41768=CARTESIAN_POINT('Ctrl Pts',(18.3856472566872,-0.106256708375174,
4.41489942083623));
#41769=CARTESIAN_POINT('Ctrl Pts',(18.4138004481407,-0.352960303644862,
4.31875095920395));
#41770=CARTESIAN_POINT('Ctrl Pts',(18.4578589182817,-0.482217355384067,
3.90319273261591));
#41771=CARTESIAN_POINT('Ctrl Pts',(18.5055747543446,-0.179376629827252,
3.54203793877243));
#41772=CARTESIAN_POINT('Ctrl Pts',(18.5532905904074,0.288188414964166,3.60143675240633));
#41773=CARTESIAN_POINT('Ctrl Pts',(18.6010064264702,0.491105603945206,4.02684232898929));
#41774=CARTESIAN_POINT('Ctrl Pts',(18.6410426776416,0.282958802096416,4.36309886994028));
#41775=CARTESIAN_POINT('Ctrl Pts',(18.6651736501253,0.0718833454275778,
4.41512900400112));
#41776=CARTESIAN_POINT('Ctrl Pts',(18.6733993439214,-3.94222854199489E-5,
4.41518963037823));
#41777=CARTESIAN_POINT('Origin',(3.42660065607856,0.,4.));
#41778=CARTESIAN_POINT('',(17.9766006560786,-0.000210814279110197,4.41643020456723));
#41779=CARTESIAN_POINT('',(18.0733993439214,-0.000144384975211464,4.41650095473263));
#41780=CARTESIAN_POINT('',(3.42660065607856,4.87367679877478E-13,4.415875));
#41781=CARTESIAN_POINT('Ctrl Pts',(17.9766006560786,-0.000210814279110157,
4.41643020456723));
#41782=CARTESIAN_POINT('Ctrl Pts',(17.9779804261896,-0.0121834889824064,
4.41650424974197));
#41783=CARTESIAN_POINT('Ctrl Pts',(17.9952654749882,-0.162096873242269,
4.41059855206721));
#41784=CARTESIAN_POINT('Ctrl Pts',(18.0284558024744,-0.435175833605105,
4.22918817311999));
#41785=CARTESIAN_POINT('Ctrl Pts',(18.0761716385373,-0.428137176707308,
3.75791781814212));
#41786=CARTESIAN_POINT('Ctrl Pts',(18.1238874746,-0.0279335627019553,3.5089552556775));
#41787=CARTESIAN_POINT('Ctrl Pts',(18.1716033106629,0.397921871745719,3.71092663761881));
#41788=CARTESIAN_POINT('Ctrl Pts',(18.2193191467257,0.458359528554279,4.17835853620019));
#41789=CARTESIAN_POINT('Ctrl Pts',(18.2543182618643,0.193950155243433,4.40107745006558));
#41790=CARTESIAN_POINT('Ctrl Pts',(18.2734120983152,0.0281121206155762,
4.41626771302466));
#41791=CARTESIAN_POINT('Ctrl Pts',(18.2766006560785,0.000371443240938293,
4.41601098728712));
#41792=CARTESIAN_POINT('Ctrl Pts',(18.0733993439214,-0.000144384975211439,
4.41650095473263));
#41793=CARTESIAN_POINT('Ctrl Pts',(18.0743103058739,-0.00804551399413891,
4.41653639380418));
#41794=CARTESIAN_POINT('Ctrl Pts',(18.0911265465141,-0.153864670001157,
4.41274680364665));
#41795=CARTESIAN_POINT('Ctrl Pts',(18.1238480658419,-0.428237044548737,
4.24190547436581));
#41796=CARTESIAN_POINT('Ctrl Pts',(18.1715639019047,-0.435081213444543,
3.7706322547532));
#41797=CARTESIAN_POINT('Ctrl Pts',(18.2192797379675,-0.0423836094492617,
3.50999096487715));
#41798=CARTESIAN_POINT('Ctrl Pts',(18.2669955740304,0.389235515258945,3.69933251171255));
#41799=CARTESIAN_POINT('Ctrl Pts',(18.3147114100932,0.463413677146622,4.16478163940629));
#41800=CARTESIAN_POINT('Ctrl Pts',(18.3501793333902,0.202226156869028,4.39827758107438));
#41801=CARTESIAN_POINT('Ctrl Pts',(18.3697419779996,0.0322267809866215,
4.41618095209965));
#41802=CARTESIAN_POINT('Ctrl Pts',(18.3733993439214,0.000382963303967157,
4.41588626824893));
#41803=CARTESIAN_POINT('Origin',(3.42660065607856,0.,4.));
#41804=CARTESIAN_POINT('',(17.6766006560786,-0.000263771022561219,4.41536107794487));
#41805=CARTESIAN_POINT('',(17.7733993439214,-0.000309142357869163,4.41544738986064));
#41806=CARTESIAN_POINT('',(3.42660065607856,4.87367679877478E-13,4.415875));
#41807=CARTESIAN_POINT('Ctrl Pts',(17.6766006560786,-0.000263771022561289,
4.41536107794487));
#41808=CARTESIAN_POINT('Ctrl Pts',(17.6825487540639,-0.0522183410383149,
4.41566152300153));
#41809=CARTESIAN_POINT('Ctrl Pts',(17.7044021307368,-0.24273028972288,4.38249735042552));
#41810=CARTESIAN_POINT('Ctrl Pts',(17.7421607860973,-0.48225726547346,4.09660825404716));
#41811=CARTESIAN_POINT('Ctrl Pts',(17.7898766221602,-0.342084653792828,
3.64661166616396));
#41812=CARTESIAN_POINT('Ctrl Pts',(17.837592458223,0.112229559114723,3.52113702282083));
#41813=CARTESIAN_POINT('Ctrl Pts',(17.8853082942859,0.463481641013499,3.83540961967535));
#41814=CARTESIAN_POINT('Ctrl Pts',(17.9316443602377,0.391261919872151,4.28736986940801));
#41815=CARTESIAN_POINT('Ctrl Pts',(17.962075147502,0.125831334120538,4.41565069513148));
#41816=CARTESIAN_POINT('Ctrl Pts',(17.9766006560786,-0.000210814279110157,
4.41643020456723));
#41817=CARTESIAN_POINT('Ctrl Pts',(17.7733993439214,-0.000309142357869142,
4.41544738986064));
#41818=CARTESIAN_POINT('Ctrl Pts',(17.7788786337482,-0.0481438769258273,
4.41577602216682));
#41819=CARTESIAN_POINT('Ctrl Pts',(17.8002632022627,-0.23443694547481,4.38601982759396));
#41820=CARTESIAN_POINT('Ctrl Pts',(17.8375530494648,-0.479202773223469,
4.11076970247734));
#41821=CARTESIAN_POINT('Ctrl Pts',(17.8852688855277,-0.352344189444135,
3.65683998336499));
#41822=CARTESIAN_POINT('Ctrl Pts',(17.9329847215905,0.0980774850139738,
3.51803938772416));
#41823=CARTESIAN_POINT('Ctrl Pts',(17.9807005576534,0.458433095867658,3.82183063825345));
#41824=CARTESIAN_POINT('Ctrl Pts',(18.0275054317636,0.3989600628602,4.28031410431705));
#41825=CARTESIAN_POINT('Ctrl Pts',(18.0584050271863,0.129907183855675,4.41591763216682));
#41826=CARTESIAN_POINT('Ctrl Pts',(18.0733993439214,-0.000144384975211439,
4.41650095473263));
#41827=CARTESIAN_POINT('Origin',(3.42660065607856,0.,4.));
#41828=CARTESIAN_POINT('',(17.3766006560786,0.000316824918469052,4.41546566829253));
#41829=CARTESIAN_POINT('',(17.4733993439214,0.000273208168652644,4.41537657040552));
#41830=CARTESIAN_POINT('',(3.42660065607856,4.87367679877478E-13,4.415875));
#41831=CARTESIAN_POINT('Ctrl Pts',(17.3766006560786,0.000316824918469058,
4.41546566829253));
#41832=CARTESIAN_POINT('Ctrl Pts',(17.3871170819382,-0.0914824399419538,
4.4148173972429));
#41833=CARTESIAN_POINT('Ctrl Pts',(17.4135387864855,-0.323087181591141,
4.33950699049548));
#41834=CARTESIAN_POINT('Ctrl Pts',(17.4558657697204,-0.489877595596684,
3.956123284257));
#41835=CARTESIAN_POINT('Ctrl Pts',(17.5035816057832,-0.228040769637767,
3.56422180844494));
#41836=CARTESIAN_POINT('Ctrl Pts',(17.551297441846,0.243209403937772,3.57250215124727));
#41837=CARTESIAN_POINT('Ctrl Pts',(17.5990132779089,0.491116639619549,3.97336034645914));
#41838=CARTESIAN_POINT('Ctrl Pts',(17.6407810159864,0.313340775136121,4.34566293955037));
#41839=CARTESIAN_POINT('Ctrl Pts',(17.6666434753763,0.0867087440962768,
4.41485812965324));
#41840=CARTESIAN_POINT('Ctrl Pts',(17.6766006560786,-0.000263771022561289,
4.41536107794487));
#41841=CARTESIAN_POINT('Ctrl Pts',(17.4733993439214,0.000273208168652693,
4.41537657040552));
#41842=CARTESIAN_POINT('Ctrl Pts',(17.4834469616226,-0.0874810350323011,
4.41484969107387));
#41843=CARTESIAN_POINT('Ctrl Pts',(17.5093998580114,-0.314919534962053,
4.34468516187688));
#41844=CARTESIAN_POINT('Ctrl Pts',(17.5512580330878,-0.490957336521241,
3.97057010757845));
#41845=CARTESIAN_POINT('Ctrl Pts',(17.5989738691507,-0.240776309167652,
3.57112706567612));
#41846=CARTESIAN_POINT('Ctrl Pts',(17.6466897052135,0.230513307714322,3.56552463842171));
#41847=CARTESIAN_POINT('Ctrl Pts',(17.6944055412763,0.490119007219086,3.95890762096741));
#41848=CARTESIAN_POINT('Ctrl Pts',(17.7366420875123,0.321513805022658,4.34052027563639));
#41849=CARTESIAN_POINT('Ctrl Pts',(17.7629733550606,0.090710757213051,4.41482206853766));
#41850=CARTESIAN_POINT('Ctrl Pts',(17.7733993439214,-0.000309142357869142,
4.41544738986064));
#41851=CARTESIAN_POINT('Origin',(3.42660065607856,0.,4.));
#41852=CARTESIAN_POINT('',(17.0766006560786,0.000130763213737631,4.41651185352269));
#41853=CARTESIAN_POINT('',(17.1733993439214,0.000198609043858391,4.41644558073401));
#41854=CARTESIAN_POINT('',(3.42660065607856,4.87367679877478E-13,4.415875));
#41855=CARTESIAN_POINT('Ctrl Pts',(17.0766006560786,0.000130763213737628,
4.41651185352269));
#41856=CARTESIAN_POINT('Ctrl Pts',(17.0916854098125,-0.130696083011285,
4.41597403242798));
#41857=CARTESIAN_POINT('Ctrl Pts',(17.1226754422341,-0.400436570105288,
4.2789290971087));
#41858=CARTESIAN_POINT('Ctrl Pts',(17.1695707533433,-0.457413284126125,
3.81922856321607));
#41859=CARTESIAN_POINT('Ctrl Pts',(17.2172865894061,-0.0953372598908034,
3.51748986360026));
#41860=CARTESIAN_POINT('Ctrl Pts',(17.265002425469,0.354288437054553,3.6588476466131));
#41861=CARTESIAN_POINT('Ctrl Pts',(17.3127182615318,0.478565610824392,4.11349088504481));
#41862=CARTESIAN_POINT('Ctrl Pts',(17.349917671735,0.232837083242772,4.38668157013213));
#41863=CARTESIAN_POINT('Ctrl Pts',(17.3712118032506,0.0473568302064652,
4.41579785693967));
#41864=CARTESIAN_POINT('Ctrl Pts',(17.3766006560786,0.000316824918469058,
4.41546566829253));
#41865=CARTESIAN_POINT('Ctrl Pts',(17.1733993439214,0.000198609043858397,
4.41644558073401));
#41866=CARTESIAN_POINT('Ctrl Pts',(17.1880152894969,-0.126615914365149,
4.41569892234974));
#41867=CARTESIAN_POINT('Ctrl Pts',(17.2185365137601,-0.392752582168809,
4.28602487069057));
#41868=CARTESIAN_POINT('Ctrl Pts',(17.2649630167107,-0.462538907526291,
3.83277863809798));
#41869=CARTESIAN_POINT('Ctrl Pts',(17.3126788527736,-0.109506707187599,
3.52050703244687));
#41870=CARTESIAN_POINT('Ctrl Pts',(17.3603946888365,0.344087187338735,3.64856119684745));
#41871=CARTESIAN_POINT('Ctrl Pts',(17.4081105248993,0.481700523269991,4.09934702176407));
#41872=CARTESIAN_POINT('Ctrl Pts',(17.4457787432609,0.241130489326423,4.3831889686244));
#41873=CARTESIAN_POINT('Ctrl Pts',(17.467541682935,0.0514330574063097,4.41568373580506));
#41874=CARTESIAN_POINT('Ctrl Pts',(17.4733993439214,0.000273208168652693,
4.41537657040552));
#41875=CARTESIAN_POINT('Origin',(3.42660065607856,0.,4.));
#41876=CARTESIAN_POINT('',(16.7766006560786,-0.000383680820852129,4.41586226484778));
#41877=CARTESIAN_POINT('',(16.8733993439214,-0.000374684679869397,4.41598699190495));
#41878=CARTESIAN_POINT('',(3.42660065607856,4.87367679877478E-13,4.415875));
#41879=CARTESIAN_POINT('Ctrl Pts',(16.7766006560786,-0.000383680820852189,
4.41586226484779));
#41880=CARTESIAN_POINT('Ctrl Pts',(16.7803484589992,-0.0330197262611539,
4.41616320579436));
#41881=CARTESIAN_POINT('Ctrl Pts',(16.8000015406075,-0.203823433586872,
4.39772119122577));
#41882=CARTESIAN_POINT('Ctrl Pts',(16.8355599009034,-0.464342533291602,
4.16214572651883));
#41883=CARTESIAN_POINT('Ctrl Pts',(16.8832757369663,-0.387520750342007,
3.69712561530174));
#41884=CARTESIAN_POINT('Ctrl Pts',(16.9309915730291,0.0451673004198413,
3.51023971187451));
#41885=CARTESIAN_POINT('Ctrl Pts',(16.978707409092,0.436377524217892,3.7731082169636));
#41886=CARTESIAN_POINT('Ctrl Pts',(17.0264232451548,0.426855552995382,4.24433493759383));
#41887=CARTESIAN_POINT('Ctrl Pts',(17.0590543274837,0.152277829190936,4.41314658311127));
#41888=CARTESIAN_POINT('Ctrl Pts',(17.0757801311249,0.00724700082869906,
4.41654110793655));
#41889=CARTESIAN_POINT('Ctrl Pts',(17.0766006560786,0.000130763213737628,
4.41651185352269));
#41890=CARTESIAN_POINT('Ctrl Pts',(16.8733993439214,-0.000374684679869387,
4.41598699190495));
#41891=CARTESIAN_POINT('Ctrl Pts',(16.8766783386836,-0.0289064002234668,
4.4162516892709));
#41892=CARTESIAN_POINT('Ctrl Pts',(16.8958626121335,-0.195546116663039,
4.40054826733105));
#41893=CARTESIAN_POINT('Ctrl Pts',(16.9309521642709,-0.459365614209645,
4.17575112327883));
#41894=CARTESIAN_POINT('Ctrl Pts',(16.9786680003337,-0.396272847821079,
3.70867019559999));
#41895=CARTESIAN_POINT('Ctrl Pts',(17.0263838363966,0.0307233721630972,
3.5091219099869));
#41896=CARTESIAN_POINT('Ctrl Pts',(17.0740996724594,0.429505846750062,3.76035452756312));
#41897=CARTESIAN_POINT('Ctrl Pts',(17.1218155085223,0.433866493469502,4.23165726989771));
#41898=CARTESIAN_POINT('Ctrl Pts',(17.1549153990096,0.160507997039396,4.41102293437065));
#41899=CARTESIAN_POINT('Ctrl Pts',(17.1721100108093,0.0113854435377776,
4.41651144656345));
#41900=CARTESIAN_POINT('Ctrl Pts',(17.1733993439214,0.000198609043858397,
4.41644558073401));
#41901=CARTESIAN_POINT('Origin',(3.42660065607856,0.,4.));
#41902=CARTESIAN_POINT('',(16.4766006560786,5.2409936866527E-5,4.41519222098806));
#41903=CARTESIAN_POINT('',(16.5733993439214,-1.52272386678698E-5,4.41518677123726));
#41904=CARTESIAN_POINT('',(3.42660065607856,4.87367679877478E-13,4.415875));
#41905=CARTESIAN_POINT('Ctrl Pts',(16.4766006560786,5.2409936866539E-5,
4.41519222098806));
#41906=CARTESIAN_POINT('Ctrl Pts',(16.4849167868736,-0.0726599781719204,
4.41511070701236));
#41907=CARTESIAN_POINT('Ctrl Pts',(16.5091381963562,-0.284551613766983,
4.36224737480062));
#41908=CARTESIAN_POINT('Ctrl Pts',(16.5492648845264,-0.4912502013546,4.02405128938415));
#41909=CARTESIAN_POINT('Ctrl Pts',(16.5969807205893,-0.285919008936969,
3.59980561575594));
#41910=CARTESIAN_POINT('Ctrl Pts',(16.6446965566521,0.181976008816936,3.54306460296116));
#41911=CARTESIAN_POINT('Ctrl Pts',(16.6924123927149,0.482759657613431,3.90593439612197));
#41912=CARTESIAN_POINT('Ctrl Pts',(16.7363804258571,0.351413532087107,4.31989995948535));
#41913=CARTESIAN_POINT('Ctrl Pts',(16.7644431803116,0.105484194296011,4.41488604428797));
#41914=CARTESIAN_POINT('Ctrl Pts',(16.7766006560786,-0.000383680820852189,
4.41586226484779));
#41915=CARTESIAN_POINT('Ctrl Pts',(16.5733993439214,-1.52272386678906E-5,
4.41518677123726));
#41916=CARTESIAN_POINT('Ctrl Pts',(16.5812466665579,-0.0686308195205231,
4.41520910309265));
#41917=CARTESIAN_POINT('Ctrl Pts',(16.6049992678821,-0.276289552895371,
4.36659242126669));
#41918=CARTESIAN_POINT('Ctrl Pts',(16.6446571478939,-0.490328743065594,
4.03850907134293));
#41919=CARTESIAN_POINT('Ctrl Pts',(16.6923729839567,-0.297581432841348,
3.60840005658827));
#41920=CARTESIAN_POINT('Ctrl Pts',(16.7400888200196,0.168439486040012,3.53790329540825));
#41921=CARTESIAN_POINT('Ctrl Pts',(16.7878046560824,0.479779833116189,3.89175704832657));
#41922=CARTESIAN_POINT('Ctrl Pts',(16.832241497383,0.359412856911567,4.31386464726761));
#41923=CARTESIAN_POINT('Ctrl Pts',(16.860773059996,0.109491163683573,4.41496773315674));
#41924=CARTESIAN_POINT('Ctrl Pts',(16.8733993439214,-0.000374684679869387,
4.41598699190495));
#41925=CARTESIAN_POINT('Origin',(3.42660065607856,0.,4.));
#41926=CARTESIAN_POINT('',(16.1766006560786,0.000364146841390381,4.41605523138122));
#41927=CARTESIAN_POINT('',(16.2733993439214,0.000380345806842055,4.41593091837313));
#41928=CARTESIAN_POINT('',(3.42660065607856,4.87367679877478E-13,4.415875));
#41929=CARTESIAN_POINT('Ctrl Pts',(16.1766006560786,0.000364146841390366,
4.41605523138122));
#41930=CARTESIAN_POINT('Ctrl Pts',(16.1894851147479,-0.111700864104492,
4.41502624848758));
#41931=CARTESIAN_POINT('Ctrl Pts',(16.2182748521048,-0.363797281821349,
4.31045679267864));
#41932=CARTESIAN_POINT('Ctrl Pts',(16.2629698681494,-0.477960913216358,
3.88398883549692));
#41933=CARTESIAN_POINT('Ctrl Pts',(16.3106857042122,-0.160921706883503,
3.53523185446324));
#41934=CARTESIAN_POINT('Ctrl Pts',(16.358401540275,0.303894378979202,3.6132786128531));
#41935=CARTESIAN_POINT('Ctrl Pts',(16.4061173763379,0.489639580609251,4.04645757153336));
#41936=CARTESIAN_POINT('Ctrl Pts',(16.4455170816057,0.271734615807756,4.36891289568356));
#41937=CARTESIAN_POINT('Ctrl Pts',(16.4690115081859,0.0664083969439258,
4.41526660914191));
#41938=CARTESIAN_POINT('Ctrl Pts',(16.4766006560786,5.2409936866539E-5,
4.41519222098806));
#41939=CARTESIAN_POINT('Ctrl Pts',(16.2733993439214,0.000380345806842052,
4.41593091837313));
#41940=CARTESIAN_POINT('Ctrl Pts',(16.2858149944323,-0.107690075887363,
4.41492720978183));
#41941=CARTESIAN_POINT('Ctrl Pts',(16.3141359236307,-0.35582464097624,4.31660057631701));
#41942=CARTESIAN_POINT('Ctrl Pts',(16.3583621315169,-0.481170314810987,
3.89811598262401));
#41943=CARTESIAN_POINT('Ctrl Pts',(16.4060779675797,-0.174540169679895,
3.54017290856226));
#41944=CARTESIAN_POINT('Ctrl Pts',(16.4537938036425,0.292372898913969,3.60449612791703));
#41945=CARTESIAN_POINT('Ctrl Pts',(16.5015096397054,0.490795435699827,4.0320166386149));
#41946=CARTESIAN_POINT('Ctrl Pts',(16.5413781531317,0.280003220364278,4.36466130212541));
#41947=CARTESIAN_POINT('Ctrl Pts',(16.5653413878703,0.0704421061260754,
4.4151638399628));
#41948=CARTESIAN_POINT('Ctrl Pts',(16.5733993439214,-1.52272386678906E-5,
4.41518677123726));
#41949=CARTESIAN_POINT('Origin',(3.42660065607856,0.,4.));
#41950=CARTESIAN_POINT('',(15.8766006560786,-0.00023258108979477,4.41639972388928));
#41951=CARTESIAN_POINT('',(15.9733993439214,-0.000169011902647176,4.4164782780785));
#41952=CARTESIAN_POINT('',(3.42660065607856,4.87367679877478E-13,4.415875));
#41953=CARTESIAN_POINT('Ctrl Pts',(15.8766006560786,-0.000232581089794846,
4.41639972388928));
#41954=CARTESIAN_POINT('Ctrl Pts',(15.8781481639346,-0.0136633580705269,
4.41648966084242));
#41955=CARTESIAN_POINT('Ctrl Pts',(15.8956009504782,-0.165044849757219,
4.40979870506104));
#41956=CARTESIAN_POINT('Ctrl Pts',(15.9289590157095,-0.437567097060412,
4.22458909239344));
#41957=CARTESIAN_POINT('Ctrl Pts',(15.9766748517724,-0.425562075928853,
3.75341909160864));
#41958=CARTESIAN_POINT('Ctrl Pts',(16.0243906878352,-0.0227568523576073,
3.50868813313462));
#41959=CARTESIAN_POINT('Ctrl Pts',(16.072106523898,0.400946338892803,3.71513642180785));
#41960=CARTESIAN_POINT('Ctrl Pts',(16.1198223599609,0.456454337785543,4.1831793175245));
#41961=CARTESIAN_POINT('Ctrl Pts',(16.1546537373544,0.190990792023167,4.40204523666471));
#41962=CARTESIAN_POINT('Ctrl Pts',(16.1735798360603,0.0266382990664043,
4.41629648110721));
#41963=CARTESIAN_POINT('Ctrl Pts',(16.1766006560786,0.000364146841390366,
4.41605523138122));
#41964=CARTESIAN_POINT('Ctrl Pts',(15.9733993439214,-0.000169011902647174,
4.4164782780785));
#41965=CARTESIAN_POINT('Ctrl Pts',(15.974478043619,-0.00952634975615679,
4.4165263696097));
#41966=CARTESIAN_POINT('Ctrl Pts',(15.9914620220042,-0.156808910032117,
4.4119928338179));
#41967=CARTESIAN_POINT('Ctrl Pts',(16.024351279077,-0.430762722000766,4.23737881579128));
#41968=CARTESIAN_POINT('Ctrl Pts',(16.0720671151398,-0.432639725453012,
3.76605963834362));
#41969=CARTESIAN_POINT('Ctrl Pts',(16.1197829512026,-0.0372170120039125,
3.50957149464017));
#41970=CARTESIAN_POINT('Ctrl Pts',(16.1674987872655,0.392382656225717,3.70345139362117));
#41971=CARTESIAN_POINT('Ctrl Pts',(16.2152146233283,0.461651293660056,4.16965644082667));
#41972=CARTESIAN_POINT('Ctrl Pts',(16.2505148088803,0.199264245432362,4.39929555075695));
#41973=CARTESIAN_POINT('Ctrl Pts',(16.2699097157447,0.0307553622657438,
4.41621302761729));
#41974=CARTESIAN_POINT('Ctrl Pts',(16.2733993439214,0.000380345806842052,
4.41593091837313));
#41975=CARTESIAN_POINT('Origin',(3.42660065607856,0.,4.));
#41976=CARTESIAN_POINT('',(15.5766006560786,-0.000245472137683418,4.41533389801214));
#41977=CARTESIAN_POINT('',(15.6733993439214,-0.00029394562308721,4.41541483535501));
#41978=CARTESIAN_POINT('',(3.42660065607856,4.87367679877478E-13,4.415875));
#41979=CARTESIAN_POINT('Ctrl Pts',(15.5766006560786,-0.000245472137683396,
4.41533389801214));
#41980=CARTESIAN_POINT('Ctrl Pts',(15.5827164918089,-0.0536739331835165,
4.41562024719655));
#41981=CARTESIAN_POINT('Ctrl Pts',(15.6047376062269,-0.245697356182912,
4.38119912149661));
#41982=CARTESIAN_POINT('Ctrl Pts',(15.6426639993325,-0.483248643997369,
4.09152034160055));
#41983=CARTESIAN_POINT('Ctrl Pts',(15.6903798353953,-0.338341267922855,
3.64302603558196));
#41984=CARTESIAN_POINT('Ctrl Pts',(15.7380956714582,0.117270100534806,3.52234641383892));
#41985=CARTESIAN_POINT('Ctrl Pts',(15.785811507521,0.465190531238913,3.84030342991275));
#41986=CARTESIAN_POINT('Ctrl Pts',(15.8319798357278,0.388490242362186,4.28984418805176));
#41987=CARTESIAN_POINT('Ctrl Pts',(15.862242885247,0.124378106492246,4.41556528924811));
#41988=CARTESIAN_POINT('Ctrl Pts',(15.8766006560786,-0.000232581089794846,
4.41639972388928));
#41989=CARTESIAN_POINT('Ctrl Pts',(15.6733993439214,-0.000293945623087231,
4.41541483535501));
#41990=CARTESIAN_POINT('Ctrl Pts',(15.6790463714933,-0.0496027558454661,
4.41573527017753));
#41991=CARTESIAN_POINT('Ctrl Pts',(15.7005986777528,-0.23740431922453,4.38477730872224));
#41992=CARTESIAN_POINT('Ctrl Pts',(15.7380562626999,-0.480343569999647,
4.1057131950703));
#41993=CARTESIAN_POINT('Ctrl Pts',(15.7857720987628,-0.348708030819167,
3.6531456586776));
#41994=CARTESIAN_POINT('Ctrl Pts',(15.8334879348256,0.103151458625294,3.5190998009613));
#41995=CARTESIAN_POINT('Ctrl Pts',(15.8812037708885,0.460285376424935,3.82667199562295));
#41996=CARTESIAN_POINT('Ctrl Pts',(15.9278409072537,0.396214095655672,4.28286244744368));
#41997=CARTESIAN_POINT('Ctrl Pts',(15.9585727649314,0.128446309981357,4.41581726659612));
#41998=CARTESIAN_POINT('Ctrl Pts',(15.9733993439214,-0.000169011902647174,
4.4164782780785));
#41999=CARTESIAN_POINT('Origin',(3.42660065607856,0.,4.));
#42000=CARTESIAN_POINT('',(15.2766006560786,0.000330084823988869,4.41550084660604));
#42001=CARTESIAN_POINT('',(15.3733993439214,0.000289868078815952,4.41540680128743));
#42002=CARTESIAN_POINT('',(3.42660065607856,4.87367679877478E-13,4.415875));
#42003=CARTESIAN_POINT('Ctrl Pts',(15.2766006560786,0.000330084823988861,
4.41550084660604));
#42004=CARTESIAN_POINT('Ctrl Pts',(15.2872848196833,-0.0929135079625664,
4.41481081573461));
#42005=CARTESIAN_POINT('Ctrl Pts',(15.3138742619755,-0.32600240339937,4.33760928826424));
#42006=CARTESIAN_POINT('Ctrl Pts',(15.3563689829555,-0.489387968817152,
3.95096286275689));
#42007=CARTESIAN_POINT('Ctrl Pts',(15.4040848190183,-0.223435404337718,
3.56184267101825));
#42008=CARTESIAN_POINT('Ctrl Pts',(15.4518006550811,0.24770132994065,3.57508909640066));
#42009=CARTESIAN_POINT('Ctrl Pts',(15.499516491144,0.491370121559653,3.97853774265298));
#42010=CARTESIAN_POINT('Ctrl Pts',(15.5411164914764,0.310410063586636,4.3474585185963));
#42011=CARTESIAN_POINT('Ctrl Pts',(15.5668112131213,0.0852759340546689,
4.41487554708019));
#42012=CARTESIAN_POINT('Ctrl Pts',(15.5766006560786,-0.000245472137683396,
4.41533389801214));
#42013=CARTESIAN_POINT('Ctrl Pts',(15.3733993439214,0.000289868078815973,
4.41540680128743));
#42014=CARTESIAN_POINT('Ctrl Pts',(15.3836146993676,-0.0889130762729256,
4.41483587894927));
#42015=CARTESIAN_POINT('Ctrl Pts',(15.4097353335015,-0.317845114095608,
4.34285359523591));
#42016=CARTESIAN_POINT('Ctrl Pts',(15.4517612463229,-0.490619905976795,
3.96539750426199));
#42017=CARTESIAN_POINT('Ctrl Pts',(15.4994770823858,-0.236243011612202,
3.56861332390027));
#42018=CARTESIAN_POINT('Ctrl Pts',(15.5471929184486,0.235079475381852,3.56797816593814));
#42019=CARTESIAN_POINT('Ctrl Pts',(15.5949087545115,0.490524862970081,3.9640753057054));
#42020=CARTESIAN_POINT('Ctrl Pts',(15.6369775630024,0.318592711010818,4.34238143198936));
#42021=CARTESIAN_POINT('Ctrl Pts',(15.6631410928057,0.0892792238074376,
4.41483274135358));
#42022=CARTESIAN_POINT('Ctrl Pts',(15.6733993439214,-0.000293945623087231,
4.41541483535501));
#42023=CARTESIAN_POINT('Origin',(3.42660065607856,0.,4.));
#42024=CARTESIAN_POINT('',(14.9766006560786,0.000104941934236194,4.41652945172571));
#42025=CARTESIAN_POINT('',(15.0733993439214,0.000175165248676303,4.41647198785975));
#42026=CARTESIAN_POINT('',(3.42660065607856,4.87367679877478E-13,4.415875));
#42027=CARTESIAN_POINT('Ctrl Pts',(14.9766006560786,0.000104941934236227,
4.41652945172572));
#42028=CARTESIAN_POINT('Ctrl Pts',(14.9918531475576,-0.132161740438444,
4.41608294134065));
#42029=CARTESIAN_POINT('Ctrl Pts',(15.0230109177242,-0.40316752945992,4.27633971254324));
#42030=CARTESIAN_POINT('Ctrl Pts',(15.0700739665785,-0.455482716161518,
3.8144178884426));
#42031=CARTESIAN_POINT('Ctrl Pts',(15.1177898026413,-0.0902467530057116,
3.51651189422706));
#42032=CARTESIAN_POINT('Ctrl Pts',(15.1655056387041,0.357864192060027,3.66260046696357));
#42033=CARTESIAN_POINT('Ctrl Pts',(15.2132214747669,0.47734294310866,4.11852822244656));
#42034=CARTESIAN_POINT('Ctrl Pts',(15.2502531472251,0.229869832763757,4.3878938710325));
#42035=CARTESIAN_POINT('Ctrl Pts',(15.2713795409956,0.0458961718568525,
4.41583804947224));
#42036=CARTESIAN_POINT('Ctrl Pts',(15.2766006560786,0.000330084823988861,
4.41550084660604));
#42037=CARTESIAN_POINT('Ctrl Pts',(15.0733993439214,0.000175165248676341,
4.41647198785975));
#42038=CARTESIAN_POINT('Ctrl Pts',(15.0881830272419,-0.128073190246274,
4.41579247653651));
#42039=CARTESIAN_POINT('Ctrl Pts',(15.1188719892501,-0.395510344386944,
4.28350986851547));
#42040=CARTESIAN_POINT('Ctrl Pts',(15.1654662299459,-0.46075086019608,3.82791319143947));
#42041=CARTESIAN_POINT('Ctrl Pts',(15.2131820660087,-0.104447211543591,
3.51937956259357));
#42042=CARTESIAN_POINT('Ctrl Pts',(15.2608979020716,0.347771918596306,3.652207076714));
#42043=CARTESIAN_POINT('Ctrl Pts',(15.3086137381344,0.480626744730421,4.10441818376995));
#42044=CARTESIAN_POINT('Ctrl Pts',(15.346114218751,0.238163166260598,4.38445638366753));
#42045=CARTESIAN_POINT('Ctrl Pts',(15.36770942068,0.0499756483669043,4.41572480336754));
#42046=CARTESIAN_POINT('Ctrl Pts',(15.3733993439214,0.000289868078815973,
4.41540680128743));
#42047=CARTESIAN_POINT('Origin',(3.42660065607856,0.,4.));
#42048=CARTESIAN_POINT('',(14.6766006560786,-0.000383732061438463,4.41581798673635));
#42049=CARTESIAN_POINT('',(14.7733993439214,-0.000379407362125217,4.41594234696178));
#42050=CARTESIAN_POINT('',(3.42660065607856,4.87367679877478E-13,4.415875));
#42051=CARTESIAN_POINT('Ctrl Pts',(14.6766006560786,-0.000383732061438387,
4.41581798673635));
#42052=CARTESIAN_POINT('Ctrl Pts',(14.6805161967443,-0.0344897130604965,
4.41612948839573));
#42053=CARTESIAN_POINT('Ctrl Pts',(14.7003370160976,-0.206786574235377,
4.39667515056147));
#42054=CARTESIAN_POINT('Ctrl Pts',(14.7360631141386,-0.466025611307368,
4.15724297904063));
#42055=CARTESIAN_POINT('Ctrl Pts',(14.7837789502014,-0.38430721152129,3.69305832471834));
#42056=CARTESIAN_POINT('Ctrl Pts',(14.8314947862642,0.0503264139313189,
3.51074293371195));
#42057=CARTESIAN_POINT('Ctrl Pts',(14.8792106223271,0.438744519099385,3.77771983486548));
#42058=CARTESIAN_POINT('Ctrl Pts',(14.9269264583899,0.42425678142631,4.24882003188202));
#42059=CARTESIAN_POINT('Ctrl Pts',(14.9593898029737,0.149335702075518,4.41387566524124));
#42060=CARTESIAN_POINT('Ctrl Pts',(14.97594786887,0.00576578747519492,4.41654856180149));
#42061=CARTESIAN_POINT('Ctrl Pts',(14.9766006560786,0.000104941934236227,
4.41652945172572));
#42062=CARTESIAN_POINT('Ctrl Pts',(14.7733993439214,-0.000379407362125234,
4.41594234696178));
#42063=CARTESIAN_POINT('Ctrl Pts',(14.7768460764287,-0.0303789312965351,
4.41622104989506));
#42064=CARTESIAN_POINT('Ctrl Pts',(14.7961980876235,-0.198506931257387,
4.39955296987463));
#42065=CARTESIAN_POINT('Ctrl Pts',(14.831455377506,-0.461192356972643,4.17090007232882));
#42066=CARTESIAN_POINT('Ctrl Pts',(14.8791712135689,-0.393180492164677,
3.7045100248179));
#42067=CARTESIAN_POINT('Ctrl Pts',(14.9268870496317,0.0358950684576197,
3.50947296821438));
#42068=CARTESIAN_POINT('Ctrl Pts',(14.9746028856945,0.432007635398663,3.76489443262817));
#42069=CARTESIAN_POINT('Ctrl Pts',(15.0223187217574,0.431400943461215,4.23621695712364));
#42070=CARTESIAN_POINT('Ctrl Pts',(15.0552508744997,0.157562060208247,4.41179740605063));
#42071=CARTESIAN_POINT('Ctrl Pts',(15.0722777485543,0.00990499767517082,
4.41652354042182));
#42072=CARTESIAN_POINT('Ctrl Pts',(15.0733993439214,0.000175165248676341,
4.41647198785975));
#42073=CARTESIAN_POINT('Origin',(3.42660065607856,0.,4.));
#42074=CARTESIAN_POINT('',(14.3766006560786,7.63317591858645E-5,4.41519896243726));
#42075=CARTESIAN_POINT('',(14.4733993439214,9.02664646690309E-6,4.41518644689786));
#42076=CARTESIAN_POINT('',(3.42660065607856,4.87367679877478E-13,4.415875));
#42077=CARTESIAN_POINT('Ctrl Pts',(14.3766006560786,7.63317591858798E-5,
4.41519896243726));
#42078=CARTESIAN_POINT('Ctrl Pts',(14.3850845246186,-0.0740996743586071,
4.41507773880187));
#42079=CARTESIAN_POINT('Ctrl Pts',(14.4094736718463,-0.287504468978829,
4.360651101065));
#42080=CARTESIAN_POINT('Ctrl Pts',(14.4497680977616,-0.491476396904638,
4.01887262932433));
#42081=CARTESIAN_POINT('Ctrl Pts',(14.4974839338244,-0.281685449746218,
3.59681451879656));
#42082=CARTESIAN_POINT('Ctrl Pts',(14.5451997698872,0.186781580201919,3.54500783946397));
#42083=CARTESIAN_POINT('Ctrl Pts',(14.59291560595,0.483724211046603,3.91102746210588));
#42084=CARTESIAN_POINT('Ctrl Pts',(14.6367159013472,0.348540265561382,4.32201186060262));
#42085=CARTESIAN_POINT('Ctrl Pts',(14.6646109180567,0.104051852208848,4.41486414061182));
#42086=CARTESIAN_POINT('Ctrl Pts',(14.6766006560786,-0.000383732061438387,
4.41581798673635));
#42087=CARTESIAN_POINT('Ctrl Pts',(14.4733993439214,9.0266464668684E-6,
4.41518644689786));
#42088=CARTESIAN_POINT('Ctrl Pts',(14.481414404303,-0.0700733710850898,
4.41517292627706));
#42089=CARTESIAN_POINT('Ctrl Pts',(14.5053347433722,-0.279247125311621,
4.3650573561381));
#42090=CARTESIAN_POINT('Ctrl Pts',(14.545160361129,-0.490707361486496,4.03333931965322));
#42091=CARTESIAN_POINT('Ctrl Pts',(14.5928761971918,-0.293437803431633,
3.60528557111603));
#42092=CARTESIAN_POINT('Ctrl Pts',(14.6405920332547,0.173300204635467,3.53970415608515));
#42093=CARTESIAN_POINT('Ctrl Pts',(14.6883078693175,0.480893968219416,3.89681949708321));
#42094=CARTESIAN_POINT('Ctrl Pts',(14.7325769728731,0.356556173733762,4.31604662460621));
#42095=CARTESIAN_POINT('Ctrl Pts',(14.760940797741,0.10805675748006,4.41493494840171));
#42096=CARTESIAN_POINT('Ctrl Pts',(14.7733993439214,-0.000379407362125234,
4.41594234696178));
#42097=CARTESIAN_POINT('Origin',(3.42660065607856,0.,4.));
#42098=CARTESIAN_POINT('',(14.0766006560786,0.000355193352615291,4.41609897421413));
#42099=CARTESIAN_POINT('',(14.1733993439214,0.000376051973931104,4.41597558743442));
#42100=CARTESIAN_POINT('',(3.42660065607856,4.87367679877478E-13,4.415875));
#42101=CARTESIAN_POINT('Ctrl Pts',(14.0766006560786,0.000355193352615277,
4.41609897421413));
#42102=CARTESIAN_POINT('Ctrl Pts',(14.0896528524929,-0.113137957382804,
4.41506966208575));
#42103=CARTESIAN_POINT('Ctrl Pts',(14.1186103275949,-0.366637448157006,
4.30821039815648));
#42104=CARTESIAN_POINT('Ctrl Pts',(14.1634730813845,-0.476711717661702,
3.87895801102093));
#42105=CARTESIAN_POINT('Ctrl Pts',(14.2111889174473,-0.156014541823709,
3.53356170012368));
#42106=CARTESIAN_POINT('Ctrl Pts',(14.2589047535102,0.307953188363286,3.61650285707861));
#42107=CARTESIAN_POINT('Ctrl Pts',(14.306620589573,0.4891227672074,4.05161534124029));
#42108=CARTESIAN_POINT('Ctrl Pts',(14.3458525570958,0.268773633406098,4.37039329245586));
#42109=CARTESIAN_POINT('Ctrl Pts',(14.369179245931,0.0649630708582953,4.4153050049005));
#42110=CARTESIAN_POINT('Ctrl Pts',(14.3766006560786,7.63317591858798E-5,
4.41519896243726));
#42111=CARTESIAN_POINT('Ctrl Pts',(14.1733993439214,0.000376051973931098,
4.41597558743442));
#42112=CARTESIAN_POINT('Ctrl Pts',(14.1859827321773,-0.109124255432428,
4.41495896305428));
#42113=CARTESIAN_POINT('Ctrl Pts',(14.2144713991208,-0.358682910161539,
4.31442504752535));
#42114=CARTESIAN_POINT('Ctrl Pts',(14.258865344752,-0.480069828122688,3.8930505494253));
#42115=CARTESIAN_POINT('Ctrl Pts',(14.3065811808148,-0.169684322438749,
3.53835895376334));
#42116=CARTESIAN_POINT('Ctrl Pts',(14.3542970168777,0.296524907469595,3.60759943412104));
#42117=CARTESIAN_POINT('Ctrl Pts',(14.4020128529405,0.49043075222644,4.0371873919842));
#42118=CARTESIAN_POINT('Ctrl Pts',(14.4417136286217,0.277046036654804,4.36620192284859));
#42119=CARTESIAN_POINT('Ctrl Pts',(14.4655091256154,0.0689998253659925,
4.41519975692232));
#42120=CARTESIAN_POINT('Ctrl Pts',(14.4733993439214,9.0266464668684E-6,
4.41518644689786));
#42121=CARTESIAN_POINT('Origin',(3.42660065607856,0.,4.));
#42122=CARTESIAN_POINT('',(13.7766006560786,-0.000253139125078747,4.41636688691614));
#42123=CARTESIAN_POINT('',(13.8733993439214,-0.000192710833643805,4.4164526008213));
#42124=CARTESIAN_POINT('',(3.42660065607856,4.87367679877478E-13,4.415875));
#42125=CARTESIAN_POINT('Ctrl Pts',(13.7766006560786,-0.000253139125078718,
4.41636688691614));
#42126=CARTESIAN_POINT('Ctrl Pts',(13.7783159016796,-0.0151427949580853,
4.41647347977994));
#42127=CARTESIAN_POINT('Ctrl Pts',(13.7959364259683,-0.167994124135391,
4.40898222403799));
#42128=CARTESIAN_POINT('Ctrl Pts',(13.8294622289446,-0.439909757638992,
4.21996506537626));
#42129=CARTESIAN_POINT('Ctrl Pts',(13.8771780650075,-0.422939705734467,
3.74894775411238));
#42130=CARTESIAN_POINT('Ctrl Pts',(13.9248939010703,-0.0175776142901187,
3.50847558318244));
#42131=CARTESIAN_POINT('Ctrl Pts',(13.9726097371332,0.403926270823208,3.71937784729135));
#42132=CARTESIAN_POINT('Ctrl Pts',(14.020325573196,0.454498446235019,4.18797975215946));
#42133=CARTESIAN_POINT('Ctrl Pts',(14.0549892128445,0.188032430710383,4.40299531219535));
#42134=CARTESIAN_POINT('Ctrl Pts',(14.0737475738053,0.0251636842930195,
4.41632397176197));
#42135=CARTESIAN_POINT('Ctrl Pts',(14.0766006560786,0.000355193352615277,
4.41609897421413));
#42136=CARTESIAN_POINT('Ctrl Pts',(13.8733993439214,-0.000192710833643682,
4.4164526008213));
#42137=CARTESIAN_POINT('Ctrl Pts',(13.874645781364,-0.0110068809386406,
4.41651469495978));
#42138=CARTESIAN_POINT('Ctrl Pts',(13.8917974974943,-0.15975450351916,4.41122255187585));
#42139=CARTESIAN_POINT('Ctrl Pts',(13.9248544923121,-0.433240552373761,
4.23282579030437));
#42140=CARTESIAN_POINT('Ctrl Pts',(13.9725703283749,-0.430150181893835,
3.76151300691929));
#42141=CARTESIAN_POINT('Ctrl Pts',(14.0202861644378,-0.032046280669499,
3.50920649887429));
#42142=CARTESIAN_POINT('Ctrl Pts',(14.0680020005006,0.39548621318905,3.70760321474174));
#42143=CARTESIAN_POINT('Ctrl Pts',(14.1157178365634,0.459837632138507,4.1745123976147));
#42144=CARTESIAN_POINT('Ctrl Pts',(14.1508502843704,0.196303200904851,4.40029544879449));
#42145=CARTESIAN_POINT('Ctrl Pts',(14.1700774534897,0.0292830534939708,
4.41624396624722));
#42146=CARTESIAN_POINT('Ctrl Pts',(14.1733993439214,0.000376051973931098,
4.41597558743442));
#42147=CARTESIAN_POINT('Origin',(3.42660065607856,0.,4.));
#42148=CARTESIAN_POINT('',(13.4766006560786,-0.000226204729293368,4.4153088088013));
#42149=CARTESIAN_POINT('',(13.5733993439214,-0.000277574767750837,4.41538411867388));
#42150=CARTESIAN_POINT('',(3.42660065607856,4.87367679877478E-13,4.415875));
#42151=CARTESIAN_POINT('Ctrl Pts',(13.4766006560786,-0.000226204729293314,
4.4153088088013));
#42152=CARTESIAN_POINT('Ctrl Pts',(13.482884229554,-0.0551283395969922,
4.41557894444213));
#42153=CARTESIAN_POINT('Ctrl Pts',(13.505073081717,-0.248664136397309,4.37988069596112));
#42154=CARTESIAN_POINT('Ctrl Pts',(13.5431672125676,-0.484186345555107,
4.08642226350871));
#42155=CARTESIAN_POINT('Ctrl Pts',(13.5908830486304,-0.334560300710407,
3.63948005597396));
#42156=CARTESIAN_POINT('Ctrl Pts',(13.6385988846933,0.122297616148583,3.52360886035071));
#42157=CARTESIAN_POINT('Ctrl Pts',(13.6863147207561,0.466847750307624,3.8452149784873));
#42158=CARTESIAN_POINT('Ctrl Pts',(13.7323153112179,0.38570983934117,4.29229218593957));
#42159=CARTESIAN_POINT('Ctrl Pts',(13.762410622992,0.122927301498021,4.41548505619568));
#42160=CARTESIAN_POINT('Ctrl Pts',(13.7766006560786,-0.000253139125078718,
4.41636688691614));
#42161=CARTESIAN_POINT('Ctrl Pts',(13.5733993439214,-0.000277574767750817,
4.41538411867388));
#42162=CARTESIAN_POINT('Ctrl Pts',(13.5792141092383,-0.0510604653080308,
4.41569425641003));
#42163=CARTESIAN_POINT('Ctrl Pts',(13.6009341532429,-0.240371663949131,
4.38351498152559));
#42164=CARTESIAN_POINT('Ctrl Pts',(13.6385594759351,-0.481431012491488,
4.10064494554323));
#42165=CARTESIAN_POINT('Ctrl Pts',(13.6862753119979,-0.345033139360895,
3.64948986092447));
#42166=CARTESIAN_POINT('Ctrl Pts',(13.7339911480608,0.108213974662067,3.52021363031051));
#42167=CARTESIAN_POINT('Ctrl Pts',(13.7817069841236,0.462086530666827,3.83153260544464));
#42168=CARTESIAN_POINT('Ctrl Pts',(13.8281763827438,0.393458703070077,4.28538422885222));
#42169=CARTESIAN_POINT('Ctrl Pts',(13.8587405026764,0.126988323162951,4.4157223370415));
#42170=CARTESIAN_POINT('Ctrl Pts',(13.8733993439214,-0.000192710833643682,
4.4164526008213));
#42171=CARTESIAN_POINT('Origin',(3.42660065607856,0.,4.));
#42172=CARTESIAN_POINT('',(13.1766006560786,0.000342007958933446,4.41553758638116));
#42173=CARTESIAN_POINT('',(13.2733993439214,0.000305371599794934,4.41543889539504));
#42174=CARTESIAN_POINT('',(3.42660065607856,4.87367679877478E-13,4.415875));
#42175=CARTESIAN_POINT('Ctrl Pts',(13.1766006560786,0.000342007958933428,
4.41553758638117));
#42176=CARTESIAN_POINT('Ctrl Pts',(13.1874525574283,-0.0943443719380771,
4.41480703635833));
#42177=CARTESIAN_POINT('Ctrl Pts',(13.2142097374657,-0.328913583769224,
4.33568767983454));
#42178=CARTESIAN_POINT('Ctrl Pts',(13.2568721961906,-0.488843983144383,
3.94580788806928));
#42179=CARTESIAN_POINT('Ctrl Pts',(13.3045880322534,-0.218805220893238,
3.55951220202843));
#42180=CARTESIAN_POINT('Ctrl Pts',(13.3523038683163,0.252165742455243,3.57772323864086));
#42181=CARTESIAN_POINT('Ctrl Pts',(13.4000197043791,0.491569024438394,3.98371752277252));
#42182=CARTESIAN_POINT('Ctrl Pts',(13.4414519669665,0.307476227900318,4.34923088347422));
#42183=CARTESIAN_POINT('Ctrl Pts',(13.4669789508664,0.0838425436168888,
4.41489516431802));
#42184=CARTESIAN_POINT('Ctrl Pts',(13.4766006560786,-0.000226204729293314,
4.4153088088013));
#42185=CARTESIAN_POINT('Ctrl Pts',(13.2733993439214,0.000305371599794949,
4.41543889539504));
#42186=CARTESIAN_POINT('Ctrl Pts',(13.2837824371127,-0.0903447040275099,
4.41482455235666));
#42187=CARTESIAN_POINT('Ctrl Pts',(13.3100708089916,-0.320767143545349,
4.3409984814332));
#42188=CARTESIAN_POINT('Ctrl Pts',(13.352264459558,-0.490227979701372,3.96022874442655));
#42189=CARTESIAN_POINT('Ctrl Pts',(13.3999802956209,-0.23168347330409,3.56614749850931));
#42190=CARTESIAN_POINT('Ctrl Pts',(13.4476961316837,0.239619531536799,3.57047968038978));
#42191=CARTESIAN_POINT('Ctrl Pts',(13.4954119677466,0.490876233547033,3.96924698078795));
#42192=CARTESIAN_POINT('Ctrl Pts',(13.5373130384925,0.315668023336251,4.34421900798688));
#42193=CARTESIAN_POINT('Ctrl Pts',(13.5633088305507,0.0878472949503496,
4.41484592860038));
#42194=CARTESIAN_POINT('Ctrl Pts',(13.5733993439214,-0.000277574767750817,
4.41538411867388));
#42195=CARTESIAN_POINT('Origin',(3.42660065607856,0.,4.));
#42196=CARTESIAN_POINT('',(12.8766006560786,7.85109994957766E-5,4.41654344863055));
#42197=CARTESIAN_POINT('',(12.9733993439214,0.000150764780949702,4.41649545414489));
#42198=CARTESIAN_POINT('',(3.42660065607856,4.87367679877478E-13,4.415875));
#42199=CARTESIAN_POINT('Ctrl Pts',(12.8766006560786,7.85109994958138E-5,
4.41654344863055));
#42200=CARTESIAN_POINT('Ctrl Pts',(12.8920208853026,-0.133630732206743,
4.41619751255639));
#42201=CARTESIAN_POINT('Ctrl Pts',(12.9233463932143,-0.405888408666218,
4.27372356364211));
#42202=CARTESIAN_POINT('Ctrl Pts',(12.9705771798136,-0.453501555338242,
3.80962782724943));
#42203=CARTESIAN_POINT('Ctrl Pts',(13.0182930158764,-0.0851462219395619,
3.51558762841831));
#42204=CARTESIAN_POINT('Ctrl Pts',(13.0660088519392,0.361400197209248,3.66639076405307));
#42205=CARTESIAN_POINT('Ctrl Pts',(13.1137246880021,0.476067254403989,4.1235523942958));
#42206=CARTESIAN_POINT('Ctrl Pts',(13.1505886227152,0.226902767145371,4.38908671404106));
#42207=CARTESIAN_POINT('Ctrl Pts',(13.1715472787407,0.0444343739838573,
4.41587777975472));
#42208=CARTESIAN_POINT('Ctrl Pts',(13.1766006560786,0.000342007958933428,
4.41553758638117));
#42209=CARTESIAN_POINT('Ctrl Pts',(12.9733993439214,0.000150764780949724,
4.4164954541449));
#42210=CARTESIAN_POINT('Ctrl Pts',(12.988350764987,-0.12953330947047,4.41589144324702));
#42211=CARTESIAN_POINT('Ctrl Pts',(13.0192074647402,-0.39825874617628,4.28096832590395));
#42212=CARTESIAN_POINT('Ctrl Pts',(13.065969443181,-0.458911634846768,3.82306685936703));
#42213=CARTESIAN_POINT('Ctrl Pts',(13.1136852792439,-0.0993761143989603,
3.51830547777773));
#42214=CARTESIAN_POINT('Ctrl Pts',(13.1614011153067,0.351418020999476,3.65589158776806));
#42215=CARTESIAN_POINT('Ctrl Pts',(13.2091169513695,0.479499580452807,4.10947774749948));
#42216=CARTESIAN_POINT('Ctrl Pts',(13.2464496942411,0.235195791588524,4.38570395495548));
#42217=CARTESIAN_POINT('Ctrl Pts',(13.2678771584251,0.0485170676377186,
4.41576563003508));
#42218=CARTESIAN_POINT('Ctrl Pts',(13.2733993439214,0.000305371599794949,
4.41543889539504));
#42219=CARTESIAN_POINT('Origin',(3.42660065607856,0.,4.));
#42220=CARTESIAN_POINT('',(12.5766006560786,-0.000382134531266273,4.41577416496379));
#42221=CARTESIAN_POINT('',(12.6733993439214,-0.000382453243898073,4.41589767499446));
#42222=CARTESIAN_POINT('',(3.42660065607856,4.87367679877478E-13,4.415875));
#42223=CARTESIAN_POINT('Ctrl Pts',(12.5766006560786,-0.000382134531266193,
4.41577416496379));
#42224=CARTESIAN_POINT('Ctrl Pts',(12.5806839344893,-0.0359587315295452,
4.41609477791077));
#42225=CARTESIAN_POINT('Ctrl Pts',(12.6006724915877,-0.209750441210566,
4.39561070447123));
#42226=CARTESIAN_POINT('Ctrl Pts',(12.6365663273737,-0.4676569254097,4.15232276575852));
#42227=CARTESIAN_POINT('Ctrl Pts',(12.6842821634365,-0.381050985679211,
3.68902512775968));
#42228=CARTESIAN_POINT('Ctrl Pts',(12.7319979994994,0.0554799374235607,
3.5113004999026));
#42229=CARTESIAN_POINT('Ctrl Pts',(12.7797138355622,0.441062780321708,3.78235614259331));
#42230=CARTESIAN_POINT('Ctrl Pts',(12.8274296716251,0.421610885427219,4.2532774884218));
#42231=CARTESIAN_POINT('Ctrl Pts',(12.8597252784638,0.146394963767536,4.4145887178469));
#42232=CARTESIAN_POINT('Ctrl Pts',(12.876115606615,0.00428438860018927,
4.4165543301878));
#42233=CARTESIAN_POINT('Ctrl Pts',(12.8766006560786,7.85109994958138E-5,
4.41654344863055));
#42234=CARTESIAN_POINT('Ctrl Pts',(12.6733993439214,-0.000382453243898042,
4.41589767499447));
#42235=CARTESIAN_POINT('Ctrl Pts',(12.6770138141737,-0.0318505807336982,
4.4161892599907));
#42236=CARTESIAN_POINT('Ctrl Pts',(12.6965335631136,-0.201468625965512,
4.39853963407534));
#42237=CARTESIAN_POINT('Ctrl Pts',(12.7319585907412,-0.462967872677167,
4.16603003860975));
#42238=CARTESIAN_POINT('Ctrl Pts',(12.779674426804,-0.390044463885,3.70038267566003));
#42239=CARTESIAN_POINT('Ctrl Pts',(12.8273902628668,0.0410627776982723,
3.50987851185683));
#42240=CARTESIAN_POINT('Ctrl Pts',(12.8751060989297,0.434461438689172,3.76946045210395));
#42241=CARTESIAN_POINT('Ctrl Pts',(12.9228219349925,0.42888747548329,4.24075040649094));
#42242=CARTESIAN_POINT('Ctrl Pts',(12.9555863499897,0.154617472482897,4.41255553662561));
#42243=CARTESIAN_POINT('Ctrl Pts',(12.9724454862994,0.00842423538524961,
4.41653398830136));
#42244=CARTESIAN_POINT('Ctrl Pts',(12.9733993439214,0.000150764780949724,
4.4164954541449));
#42245=CARTESIAN_POINT('Origin',(3.42660065607856,0.,4.));
#42246=CARTESIAN_POINT('',(12.2766006560786,9.99581421417901E-5,4.41520820259509));
#42247=CARTESIAN_POINT('',(12.3733993439214,3.32456539758885E-5,4.41518865831861));
#42248=CARTESIAN_POINT('',(3.42660065607856,4.87367679877478E-13,4.415875));
#42249=CARTESIAN_POINT('Ctrl Pts',(12.2766006560786,9.99581421418094E-5,
4.41520820259509));
#42250=CARTESIAN_POINT('Ctrl Pts',(12.2852522623637,-0.0755384113923865,
4.41504611816934));
#42251=CARTESIAN_POINT('Ctrl Pts',(12.3098091473364,-0.290455378639464,
4.35903266527152));
#42252=CARTESIAN_POINT('Ctrl Pts',(12.3502713109967,-0.49164800158875,4.0136918729824));
#42253=CARTESIAN_POINT('Ctrl Pts',(12.3979871470595,-0.277420602272412,
3.59386820576715));
#42254=CARTESIAN_POINT('Ctrl Pts',(12.4457029831224,0.191566404775332,3.54700161433684));
#42255=CARTESIAN_POINT('Ctrl Pts',(12.4934188191852,0.484635034689867,3.91613041073711));
#42256=CARTESIAN_POINT('Ctrl Pts',(12.5370513768373,0.345661459897227,4.32409890635003));
#42257=CARTESIAN_POINT('Ctrl Pts',(12.5647786558017,0.102620036091023,4.41484591908716));
#42258=CARTESIAN_POINT('Ctrl Pts',(12.5766006560786,-0.000382134531266193,
4.41577416496379));
#42259=CARTESIAN_POINT('Ctrl Pts',(12.3733993439214,3.32456539758746E-5,
4.41518865831861));
#42260=CARTESIAN_POINT('Ctrl Pts',(12.381582142048,-0.071514873974996,4.41513780400291));
#42261=CARTESIAN_POINT('Ctrl Pts',(12.4056702188623,-0.282203129244181,
4.36350051499509));
#42262=CARTESIAN_POINT('Ctrl Pts',(12.4456635743641,-0.491031474462283,
4.0281658647901));
#42263=CARTESIAN_POINT('Ctrl Pts',(12.493379410427,-0.289261580343189,3.60221492864948));
#42264=CARTESIAN_POINT('Ctrl Pts',(12.5410952464898,0.178141673866572,3.54155614424011));
#42265=CARTESIAN_POINT('Ctrl Pts',(12.5888110825527,0.481954687902679,3.90189340664049));
#42266=CARTESIAN_POINT('Ctrl Pts',(12.6329124483632,0.353693368040787,4.31820342736526));
#42267=CARTESIAN_POINT('Ctrl Pts',(12.6611085354861,0.106623193447456,4.41490615616012));
#42268=CARTESIAN_POINT('Ctrl Pts',(12.6733993439214,-0.000382453243898042,
4.41589767499447));
#42269=CARTESIAN_POINT('Origin',(3.42660065607856,0.,4.));
#42270=CARTESIAN_POINT('',(11.9766006560786,0.000344603143201134,4.41614202049347));
#42271=CARTESIAN_POINT('',(12.0733993439214,0.00037008249145147,4.41602009379307));
#42272=CARTESIAN_POINT('',(3.42660065607856,4.87367679877478E-13,4.415875));
#42273=CARTESIAN_POINT('Ctrl Pts',(11.9766006560786,0.000344603143201134,
4.41614202049347));
#42274=CARTESIAN_POINT('Ctrl Pts',(11.989820590238,-0.114576335025177,4.41511745277426));
#42275=CARTESIAN_POINT('Ctrl Pts',(12.018945803085,-0.369470719226983,4.30593844396252));
#42276=CARTESIAN_POINT('Ctrl Pts',(12.0639762946196,-0.475409571231627,
3.87394063131468));
#42277=CARTESIAN_POINT('Ctrl Pts',(12.1116921306825,-0.151090047408964,
3.53194335553704));
#42278=CARTESIAN_POINT('Ctrl Pts',(12.1594079667453,0.311977791768556,3.61976969834691));
#42279=CARTESIAN_POINT('Ctrl Pts',(12.2071238028081,0.488551624369653,4.05676737776005));
#42280=CARTESIAN_POINT('Ctrl Pts',(12.2461880325859,0.265811525316043,4.37185240566124));
#42281=CARTESIAN_POINT('Ctrl Pts',(12.269346983676,0.0635166157645696,4.41534409728183));
#42282=CARTESIAN_POINT('Ctrl Pts',(12.2766006560786,9.99581421418094E-5,
4.41520820259509));
#42283=CARTESIAN_POINT('Ctrl Pts',(12.0733993439214,0.000370082491451453,
4.41602009379308));
#42284=CARTESIAN_POINT('Ctrl Pts',(12.0861504699224,-0.110559366248508,
4.41499479059613));
#42285=CARTESIAN_POINT('Ctrl Pts',(12.1148068746109,-0.361534897467509,
4.3122242613332));
#42286=CARTESIAN_POINT('Ctrl Pts',(12.1593685579871,-0.478916017555994,
3.88799699566402));
#42287=CARTESIAN_POINT('Ctrl Pts',(12.2070843940499,-0.164809627468288,
3.53659627586117));
#42288=CARTESIAN_POINT('Ctrl Pts',(12.2548002301128,0.300643979445627,3.61074632631782));
#42289=CARTESIAN_POINT('Ctrl Pts',(12.3025160661756,0.490011594032383,4.04235401475446));
#42290=CARTESIAN_POINT('Ctrl Pts',(12.3420491041118,0.274087380788525,4.36772087084377));
#42291=CARTESIAN_POINT('Ctrl Pts',(12.3656768633604,0.0675564760281007,
4.41523665186048));
#42292=CARTESIAN_POINT('Ctrl Pts',(12.3733993439214,3.32456539758746E-5,
4.41518865831861));
#42293=CARTESIAN_POINT('Origin',(3.42660065607856,0.,4.));
#42294=CARTESIAN_POINT('',(11.6766006560786,-0.000272404999166542,4.41633191892761));
#42295=CARTESIAN_POINT('',(11.7733993439214,-0.000215373091504267,4.41642415578018));
#42296=CARTESIAN_POINT('',(3.42660065607856,4.87367679877478E-13,4.415875));
#42297=CARTESIAN_POINT('Ctrl Pts',(11.6766006560786,-0.000272404999166455,
4.41633191892761));
#42298=CARTESIAN_POINT('Ctrl Pts',(11.6784836394247,-0.0166217551361539,
4.41645573239506));
#42299=CARTESIAN_POINT('Ctrl Pts',(11.6962719014584,-0.170944672110958,
4.40814899119985));
#42300=CARTESIAN_POINT('Ctrl Pts',(11.7299654421798,-0.44220355512924,4.21531660568344));
#42301=CARTESIAN_POINT('Ctrl Pts',(11.7776812782426,-0.420270357404582,
3.74450430230823));
#42302=CARTESIAN_POINT('Ctrl Pts',(11.8253971143054,-0.0123964237846327,
3.50831762943));
#42303=CARTESIAN_POINT('Ctrl Pts',(11.8731129503683,0.406861336540243,3.72365044295193));
#42304=CARTESIAN_POINT('Ctrl Pts',(11.9208287864311,0.452492071153857,4.1927593068956));
#42305=CARTESIAN_POINT('Ctrl Pts',(11.9553246883346,0.185075114683736,4.40392780377));
#42306=CARTESIAN_POINT('Ctrl Pts',(11.9739153115504,0.0236883133891,4.41635013933017));
#42307=CARTESIAN_POINT('Ctrl Pts',(11.9766006560786,0.000344603143201134,
4.41614202049347));
#42308=CARTESIAN_POINT('Ctrl Pts',(11.7733993439214,-0.000215373091504231,
4.41642415578018));
#42309=CARTESIAN_POINT('Ctrl Pts',(11.7748135191091,-0.0124870613922979,
4.41650138834433));
#42310=CARTESIAN_POINT('Ctrl Pts',(11.7921329729843,-0.162701432614141,
4.41043584391465));
#42311=CARTESIAN_POINT('Ctrl Pts',(11.8253577055472,-0.435670260442099,
4.22824690363353));
#42312=CARTESIAN_POINT('Ctrl Pts',(11.8730735416101,-0.427612859293677,
3.75699286549843));
#42313=CARTESIAN_POINT('Ctrl Pts',(11.9207893776729,-0.0268719897862959,
3.50889601812151));
#42314=CARTESIAN_POINT('Ctrl Pts',(11.9685052137357,0.398545841420554,3.71178751390968));
#42315=CARTESIAN_POINT('Ctrl Pts',(12.0162210497986,0.457972894034889,4.17934897039372));
#42316=CARTESIAN_POINT('Ctrl Pts',(12.0511857598605,0.193343073938706,4.40127740506484));
#42317=CARTESIAN_POINT('Ctrl Pts',(12.0702451912347,0.0278098881012828,
4.41627371553856));
#42318=CARTESIAN_POINT('Ctrl Pts',(12.0733993439214,0.000370082491451453,
4.41602009379308));
#42319=CARTESIAN_POINT('Origin',(3.42660065607856,0.,4.));
#42320=CARTESIAN_POINT('',(11.3766006560786,-0.000206048103233091,4.41528588740701));
#42321=CARTESIAN_POINT('',(11.4733993439214,-0.000260100423148973,4.41535533657191));
#42322=CARTESIAN_POINT('',(3.42660065607856,4.87367679877478E-13,4.415875));
#42323=CARTESIAN_POINT('Ctrl Pts',(11.3766006560786,-0.000206048103232999,
4.41528588740701));
#42324=CARTESIAN_POINT('Ctrl Pts',(11.383051967299,-0.0565815589273492,
4.41553770218085));
#42325=CARTESIAN_POINT('Ctrl Pts',(11.4054085572071,-0.251630532720247,
4.37854193442951));
#42326=CARTESIAN_POINT('Ctrl Pts',(11.4436704258028,-0.485070265991237,
4.08131458604192));
#42327=CARTESIAN_POINT('Ctrl Pts',(11.4913862618656,-0.330742172127369,
3.63597412121053));
#42328=CARTESIAN_POINT('Ctrl Pts',(11.5391020979284,0.127311547523522,3.52492422212962));
#42329=CARTESIAN_POINT('Ctrl Pts',(11.5868179339912,0.468453114143607,3.85014371984754));
#42330=CARTESIAN_POINT('Ctrl Pts',(11.632650786708,0.382920955827079,4.29471395365306));
#42331=CARTESIAN_POINT('Ctrl Pts',(11.6625783607371,0.121478760105588,4.41540989855421));
#42332=CARTESIAN_POINT('Ctrl Pts',(11.6766006560786,-0.000272404999166455,
4.41633191892761));
#42333=CARTESIAN_POINT('Ctrl Pts',(11.4733993439214,-0.000260100423148869,
4.41535533657191));
#42334=CARTESIAN_POINT('Ctrl Pts',(11.4793818469834,-0.0525169974224216,
4.41565306322741));
#42335=CARTESIAN_POINT('Ctrl Pts',(11.501269628733,-0.243338890257842,4.3822327073369));
#42336=CARTESIAN_POINT('Ctrl Pts',(11.5390626891702,-0.482464979911041,
4.09556551685319));
#42337=CARTESIAN_POINT('Ctrl Pts',(11.586778525233,-0.341319923258817,3.64587299617429));
#42338=CARTESIAN_POINT('Ctrl Pts',(11.6344943612959,0.113264470804062,3.5213807520529));
#42339=CARTESIAN_POINT('Ctrl Pts',(11.6822101973587,0.463836358529674,3.83641192782507));
#42340=CARTESIAN_POINT('Ctrl Pts',(11.7285118582339,0.390694138047139,4.28787953265104));
#42341=CARTESIAN_POINT('Ctrl Pts',(11.7589082404215,0.125533053862222,4.41563275094549));
#42342=CARTESIAN_POINT('Ctrl Pts',(11.7733993439214,-0.000215373091504231,
4.41642415578018));
#42343=CARTESIAN_POINT('Origin',(3.42660065607856,0.,4.));
#42344=CARTESIAN_POINT('',(11.0766006560786,0.000352537510456688,4.41557576695298));
#42345=CARTESIAN_POINT('',(11.1733993439214,0.000319650745578964,4.41547275084625));
#42346=CARTESIAN_POINT('',(3.42660065607856,4.87367679877478E-13,4.415875));
#42347=CARTESIAN_POINT('Ctrl Pts',(11.0766006560786,0.000352537510456667,
4.41557576695298));
#42348=CARTESIAN_POINT('Ctrl Pts',(11.0876202951733,-0.0957751134661499,
4.41480617263661));
#42349=CARTESIAN_POINT('Ctrl Pts',(11.1145452129557,-0.331820540820521,
4.33374203885914));
#42350=CARTESIAN_POINT('Ctrl Pts',(11.1573754094257,-0.488245699001722,
3.94065893278431));
#42351=CARTESIAN_POINT('Ctrl Pts',(11.2050912454886,-0.214150733603143,
3.55723066033293));
#42352=CARTESIAN_POINT('Ctrl Pts',(11.2528070815514,0.256602145595791,3.58040428537983));
#42353=CARTESIAN_POINT('Ctrl Pts',(11.3005229176142,0.491713326162588,3.98889911147238));
#42354=CARTESIAN_POINT('Ctrl Pts',(11.3417874424566,0.304539430122629,4.35098016691413));
#42355=CARTESIAN_POINT('Ctrl Pts',(11.3671466886114,0.0824085130402235,
4.41491686960609));
#42356=CARTESIAN_POINT('Ctrl Pts',(11.3766006560786,-0.000206048103232999,
4.41528588740701));
#42357=CARTESIAN_POINT('Ctrl Pts',(11.1733993439214,0.000319650745578978,
4.41547275084625));
#42358=CARTESIAN_POINT('Ctrl Pts',(11.1839501748577,-0.0917759901056567,
4.4148158243975));
#42359=CARTESIAN_POINT('Ctrl Pts',(11.2104062844816,-0.32368545017211,4.33911969104981));
#42360=CARTESIAN_POINT('Ctrl Pts',(11.2527676727932,-0.489781601228288,
3.95506440219344));
#42361=CARTESIAN_POINT('Ctrl Pts',(11.300483508856,-0.227098200695192,3.56372986339542));
#42362=CARTESIAN_POINT('Ctrl Pts',(11.3481993449188,0.244132971891272,3.57302890392028));
#42363=CARTESIAN_POINT('Ctrl Pts',(11.3959151809817,0.491173079921361,3.97442207176994));
#42364=CARTESIAN_POINT('Ctrl Pts',(11.4376485139825,0.312739912806573,4.34603313379779));
#42365=CARTESIAN_POINT('Ctrl Pts',(11.4634765682958,0.0864149014017155,
4.41486151738456));
#42366=CARTESIAN_POINT('Ctrl Pts',(11.4733993439214,-0.000260100423148869,
4.41535533657191));
#42367=CARTESIAN_POINT('Origin',(3.42660065607856,0.,4.));
#42368=CARTESIAN_POINT('',(10.7766006560786,5.16128798610187E-5,4.41655360457584));
#42369=CARTESIAN_POINT('',(10.8733993439214,0.000125523266313186,4.41651574507477));
#42370=CARTESIAN_POINT('',(3.42660065607856,4.87367679877478E-13,4.415875));
#42371=CARTESIAN_POINT('Ctrl Pts',(10.7766006560786,5.16128798610299E-5,
4.41655360457584));
#42372=CARTESIAN_POINT('Ctrl Pts',(10.7921886230477,-0.135103241057852,
4.41631783152902));
#42373=CARTESIAN_POINT('Ctrl Pts',(10.8236818687044,-0.408598944994929,
4.27108057505162));
#42374=CARTESIAN_POINT('Ctrl Pts',(10.8710803930487,-0.451470021714238,
3.80485891169382));
#42375=CARTESIAN_POINT('Ctrl Pts',(10.9187962291115,-0.080036233235122,
3.51471716883706));
#42376=CARTESIAN_POINT('Ctrl Pts',(10.9665120651743,0.364896059739551,3.6702181168734));
#42377=CARTESIAN_POINT('Ctrl Pts',(11.0142279012372,0.47473868640782,4.1285628425314));
#42378=CARTESIAN_POINT('Ctrl Pts',(11.0509240982053,0.223935965514619,4.3902602363912));
#42379=CARTESIAN_POINT('Ctrl Pts',(11.0717150164857,0.0429714521173939,
4.4159169723618));
#42380=CARTESIAN_POINT('Ctrl Pts',(11.0766006560786,0.000352537510456667,
4.41557576695298));
#42381=CARTESIAN_POINT('Ctrl Pts',(10.8733993439214,0.000125523266313226,
4.41651574507477));
#42382=CARTESIAN_POINT('Ctrl Pts',(10.888518502732,-0.130996444363694,4.41599591363288));
#42383=CARTESIAN_POINT('Ctrl Pts',(10.9195429402303,-0.400997532511054,
4.27840016053723));
#42384=CARTESIAN_POINT('Ctrl Pts',(10.9664726564161,-0.45702143577077,3.81824018018824));
#42385=CARTESIAN_POINT('Ctrl Pts',(11.014188492479,-0.0942939790271268,
3.51728489730359));
#42386=CARTESIAN_POINT('Ctrl Pts',(11.0619043285418,0.355025089556487,3.65961432075161));
#42387=CARTESIAN_POINT('Ctrl Pts',(11.1096201646047,0.478319155637209,4.11452515096033));
#42388=CARTESIAN_POINT('Ctrl Pts',(11.1467851697312,0.23222845252417,4.38693182090163));
#42389=CARTESIAN_POINT('Ctrl Pts',(11.1680448961701,0.0470573247768451,
4.41580613485813));
#42390=CARTESIAN_POINT('Ctrl Pts',(11.1733993439214,0.000319650745578978,
4.41547275084625));
#42391=CARTESIAN_POINT('Origin',(3.42660065607856,0.,4.));
#42392=CARTESIAN_POINT('',(10.4766006560786,-0.000378910032885682,4.4157309619862));
#42393=CARTESIAN_POINT('',(10.5733993439214,-0.000383826598418624,4.41585315377736));
#42394=CARTESIAN_POINT('',(3.42660065607856,4.87367679877478E-13,4.415875));
#42395=CARTESIAN_POINT('Ctrl Pts',(10.4766006560786,-0.000378910032885704,
4.4157309619862));
#42396=CARTESIAN_POINT('Ctrl Pts',(10.4808516722344,-0.0374267536145521,
4.41605913507464));
#42397=CARTESIAN_POINT('Ctrl Pts',(10.5010079670778,-0.212714974368116,
4.3945277200383));
#42398=CARTESIAN_POINT('Ctrl Pts',(10.5370695406088,-0.469236294399976,
4.14738563318641));
#42399=CARTESIAN_POINT('Ctrl Pts',(10.5847853766716,-0.377752434501872,
3.68502647241413));
#42400=CARTESIAN_POINT('Ctrl Pts',(10.6325012127345,0.0606272984676223,
3.51191234851464));
#42401=CARTESIAN_POINT('Ctrl Pts',(10.6802170487973,0.443332050383407,3.78701662516801));
#42402=CARTESIAN_POINT('Ctrl Pts',(10.7279328848602,0.418918158891686,4.25770681210006));
#42403=CARTESIAN_POINT('Ctrl Pts',(10.7600607539539,0.143455624352724,4.41528584951654));
#42404=CARTESIAN_POINT('Ctrl Pts',(10.7762833443601,0.00280285164340033,
4.41655840401831));
#42405=CARTESIAN_POINT('Ctrl Pts',(10.7766006560786,5.16128798610299E-5,
4.41655360457584));
#42406=CARTESIAN_POINT('Ctrl Pts',(10.5733993439214,-0.000383826598418617,
4.41585315377736));
#42407=CARTESIAN_POINT('Ctrl Pts',(10.5771815519187,-0.0333213161677604,
4.41615637378185));
#42408=CARTESIAN_POINT('Ctrl Pts',(10.5968690386037,-0.20443114816448,4.39750812937281));
#42409=CARTESIAN_POINT('Ctrl Pts',(10.6324618039763,-0.464691964107356,
4.16114156306187));
#42410=CARTESIAN_POINT('Ctrl Pts',(10.6801776400391,-0.386865111317189,
3.69628860657276));
#42411=CARTESIAN_POINT('Ctrl Pts',(10.7278934761019,0.0462259258804368,
3.51033849586834));
#42412=CARTESIAN_POINT('Ctrl Pts',(10.7756093121648,0.436866984064762,3.77405207881873));
#42413=CARTESIAN_POINT('Ctrl Pts',(10.8233251482276,0.426326368719826,4.24525711444552));
#42414=CARTESIAN_POINT('Ctrl Pts',(10.8559218254798,0.151674250044741,4.4132974389186));
#42415=CARTESIAN_POINT('Ctrl Pts',(10.8726132240444,0.00694320316194716,
4.41654277368359));
#42416=CARTESIAN_POINT('Ctrl Pts',(10.8733993439214,0.000125523266313226,
4.41651574507477));
#42417=CARTESIAN_POINT('Origin',(3.42660065607856,0.,4.));
#42418=CARTESIAN_POINT('',(10.1766006560786,0.000123197149224082,4.41521991402453));
#42419=CARTESIAN_POINT('',(10.2733993439214,5.7336166378985E-5,4.41519339896199));
#42420=CARTESIAN_POINT('',(3.42660065607856,4.87367679877478E-13,4.415875));
#42421=CARTESIAN_POINT('Ctrl Pts',(10.1766006560786,0.000123197149224097,
4.41521991402453));
#42422=CARTESIAN_POINT('Ctrl Pts',(10.1854200001087,-0.0769762270984491,
4.41501595190525));
#42423=CARTESIAN_POINT('Ctrl Pts',(10.2101446228264,-0.293404201931947,
4.35739193013711));
#42424=CARTESIAN_POINT('Ctrl Pts',(10.2507745242318,-0.491764996345908,
4.00850959581219));
#42425=CARTESIAN_POINT('Ctrl Pts',(10.2984903602946,-0.273124940234581,
3.59096700393021));
#42426=CARTESIAN_POINT('Ctrl Pts',(10.3462061963575,0.196329951061554,3.54904570612073));
#42427=CARTESIAN_POINT('Ctrl Pts',(10.3939220324203,0.485492027373267,3.92124267520431));
#42428=CARTESIAN_POINT('Ctrl Pts',(10.4373868523273,0.34277731801193,4.32616121393696));
#42429=CARTESIAN_POINT('Ctrl Pts',(10.4649463935468,0.101188639822117,4.41483126760997));
#42430=CARTESIAN_POINT('Ctrl Pts',(10.4766006560786,-0.000378910032885704,
4.4157309619862));
#42431=CARTESIAN_POINT('Ctrl Pts',(10.2733993439214,5.73361663789851E-5,
4.41519339896199));
#42432=CARTESIAN_POINT('Ctrl Pts',(10.2817498797931,-0.0729553575157724,
4.41510384014646));
#42433=CARTESIAN_POINT('Ctrl Pts',(10.3060056943524,-0.285157432566911,
4.36192175935665));
#42434=CARTESIAN_POINT('Ctrl Pts',(10.3461667875993,-0.491301045992024,
4.02298928139638));
#42435=CARTESIAN_POINT('Ctrl Pts',(10.3938826236621,-0.285053227451061,
3.599188470261));
#42436=CARTESIAN_POINT('Ctrl Pts',(10.4415984597249,0.182963355965895,3.54345905416307));
#42437=CARTESIAN_POINT('Ctrl Pts',(10.4893142957878,0.482961874346273,3.9069782134126));
#42438=CARTESIAN_POINT('Ctrl Pts',(10.5332479238533,0.35082465130295,4.32033516829581));
#42439=CARTESIAN_POINT('Ctrl Pts',(10.5612762732311,0.105190355120073,4.41488124595214));
#42440=CARTESIAN_POINT('Ctrl Pts',(10.5733993439214,-0.000383826598418617,
4.41585315377736));
#42441=CARTESIAN_POINT('Origin',(3.42660065607856,0.,4.));
#42442=CARTESIAN_POINT('',(9.87660065607859,0.000332404019580576,4.41618417038907));
#42443=CARTESIAN_POINT('',(9.9733993439214,0.000362444897862246,4.41606425076498));
#42444=CARTESIAN_POINT('',(3.42660065607856,4.87367679877478E-13,4.415875));
#42445=CARTESIAN_POINT('Ctrl Pts',(9.87660065607859,0.000332404019580564,
4.41618417038907));
#42446=CARTESIAN_POINT('Ctrl Pts',(9.88998832798303,-0.116016130490024,
4.41516972706101));
#42447=CARTESIAN_POINT('Ctrl Pts',(9.91928127857509,-0.372296869871387,
4.30364082544554));
#42448=CARTESIAN_POINT('Ctrl Pts',(9.96447950785476,-0.474054618562381,
3.8689372536849));
#42449=CARTESIAN_POINT('Ctrl Pts',(10.0121953439176,-0.146148770628728,
3.53037700046135));
#42450=CARTESIAN_POINT('Ctrl Pts',(10.0599111799804,0.315967742161179,3.62307877379278));
#42451=CARTESIAN_POINT('Ctrl Pts',(10.1076270160433,0.487926215535836,4.06191310882887));
#42452=CARTESIAN_POINT('Ctrl Pts',(10.146523508076,0.262848409674369,4.37329037489646));
#42453=CARTESIAN_POINT('Ctrl Pts',(10.1695147214211,0.062069015396409,4.41538378814543));
#42454=CARTESIAN_POINT('Ctrl Pts',(10.1766006560786,0.000123197149224097,
4.41521991402453));
#42455=CARTESIAN_POINT('Ctrl Pts',(9.9733993439214,0.000362444897862267,
4.41606425076498));
#42456=CARTESIAN_POINT('Ctrl Pts',(9.9863182076674,-0.111995531308361,4.41503480155798));
#42457=CARTESIAN_POINT('Ctrl Pts',(10.015142350101,-0.364380386131072,4.30999810797653));
#42458=CARTESIAN_POINT('Ctrl Pts',(10.0598717712222,-0.477709011270712,
3.88295588266498));
#42459=CARTESIAN_POINT('Ctrl Pts',(10.1075876072851,-0.159916626226494,
3.53488507064564));
#42460=CARTESIAN_POINT('Ctrl Pts',(10.1553034433479,0.304729657315094,3.61393645496551));
#42461=CARTESIAN_POINT('Ctrl Pts',(10.2030192794107,0.489538007675758,4.04751593304174));
#42462=CARTESIAN_POINT('Ctrl Pts',(10.2423845796019,0.271127379494919,4.3692182851415));
#42463=CARTESIAN_POINT('Ctrl Pts',(10.2658446011055,0.0661120339180705,
4.41527442296197));
#42464=CARTESIAN_POINT('Ctrl Pts',(10.2733993439214,5.73361663789851E-5,
4.41519339896199));
#42465=CARTESIAN_POINT('Origin',(3.42660065607856,0.,4.));
#42466=CARTESIAN_POINT('',(9.57660065607859,-0.000290304052950346,4.41629504206998));
#42467=CARTESIAN_POINT('',(9.6733993439214,-0.000236899196693507,4.41639317328699));
#42468=CARTESIAN_POINT('',(3.42660065607856,4.87367679877478E-13,4.415875));
#42469=CARTESIAN_POINT('Ctrl Pts',(9.57660065607859,-0.000290304052950335,
4.41629504206998));
#42470=CARTESIAN_POINT('Ctrl Pts',(9.57865137716975,-0.0181001948149981,
4.41643644713422));
#42471=CARTESIAN_POINT('Ctrl Pts',(9.59660737694851,-0.173896467062472,
4.40729888742394));
#42472=CARTESIAN_POINT('Ctrl Pts',(9.63046865541489,-0.444448234747017,
4.21064422964382));
#42473=CARTESIAN_POINT('Ctrl Pts',(9.67818449147773,-0.41755432743774,3.74008922975375));
#42474=CARTESIAN_POINT('Ctrl Pts',(9.72590032754057,-0.00721385634321597,
3.50821428942208));
#42475=CARTESIAN_POINT('Ctrl Pts',(9.77361616360341,0.40975121003073,3.72795373420991));
#42476=CARTESIAN_POINT('Ctrl Pts',(9.82133199966624,0.450435435400681,4.19751745084266));
#42477=CARTESIAN_POINT('Ctrl Pts',(9.85566016382464,0.182118884769847,4.40484283743537));
#42478=CARTESIAN_POINT('Ctrl Pts',(9.87408304929542,0.0222122246324328,
4.41637494063069));
#42479=CARTESIAN_POINT('Ctrl Pts',(9.87660065607859,0.000332404019580564,
4.41618417038907));
#42480=CARTESIAN_POINT('Ctrl Pts',(9.6733993439214,-0.00023689919669354,
4.41639317328699));
#42481=CARTESIAN_POINT('Ctrl Pts',(9.67498125685411,-0.0139668454918635,
4.4164864708936));
#42482=CARTESIAN_POINT('Ctrl Pts',(9.69246844847443,-0.165649677201134,
4.40963259460397));
#42483=CARTESIAN_POINT('Ctrl Pts',(9.72586091878235,-0.438051576325333,
4.22364266437974));
#42484=CARTESIAN_POINT('Ctrl Pts',(9.77357675484519,-0.425028039486299,
3.75249971615691));
#42485=CARTESIAN_POINT('Ctrl Pts',(9.82129259090803,-0.0216947140899849,
3.50864008686857));
#42486=CARTESIAN_POINT('Ctrl Pts',(9.86900842697087,0.401561201071248,3.7160038263529));
#42487=CARTESIAN_POINT('Ctrl Pts',(9.91672426303371,0.456057286475463,4.18416562194019));
#42488=CARTESIAN_POINT('Ctrl Pts',(9.95152123535055,0.190383912560376,4.40224154849284));
#42489=CARTESIAN_POINT('Ctrl Pts',(9.97041292897978,0.0263359008882403,
4.4163022254471));
#42490=CARTESIAN_POINT('Ctrl Pts',(9.9733993439214,0.000362444897862267,
4.41606425076498));
#42491=CARTESIAN_POINT('Origin',(3.42660065607856,0.,4.));
#42492=CARTESIAN_POINT('',(9.27660065607858,-0.000185084181660103,4.41526520375254));
#42493=CARTESIAN_POINT('',(9.37339934392141,-0.000241596553487405,4.41532857883968));
#42494=CARTESIAN_POINT('',(3.42660065607856,4.87367679877478E-13,4.415875));
#42495=CARTESIAN_POINT('Ctrl Pts',(9.27660065607858,-0.000185084181660189,
4.41526520375254));
#42496=CARTESIAN_POINT('Ctrl Pts',(9.28321970504406,-0.0580335922681754,
4.4154966095816));
#42497=CARTESIAN_POINT('Ctrl Pts',(9.30574403269715,-0.254596444523232,
4.37718269734299));
#42498=CARTESIAN_POINT('Ctrl Pts',(9.34417363903789,-0.485900307124067,
4.07619787653679));
#42499=CARTESIAN_POINT('Ctrl Pts',(9.39188947510068,-0.326887306273347,
3.63250862071426));
#42500=CARTESIAN_POINT('Ctrl Pts',(9.43960531116356,0.13231133773591,3.52629235307153));
#42501=CARTESIAN_POINT('Ctrl Pts',(9.48732114722637,0.470006444430667,3.85508910653225));
#42502=CARTESIAN_POINT('Ctrl Pts',(9.53298626219807,0.380123833963086,4.29710958399465));
#42503=CARTESIAN_POINT('Ctrl Pts',(9.56274609848214,0.120032327051623,4.41533971732329));
#42504=CARTESIAN_POINT('Ctrl Pts',(9.57660065607859,-0.000290304052950335,
4.41629504206998));
#42505=CARTESIAN_POINT('Ctrl Pts',(9.3733993439214,-0.000241596553487357,
4.41532857883968));
#42506=CARTESIAN_POINT('Ctrl Pts',(9.37954958472843,-0.0539723465869793,
4.41561177485228));
#42507=CARTESIAN_POINT('Ctrl Pts',(9.40160510422307,-0.246305905820531,
4.3809303471886));
#42508=CARTESIAN_POINT('Ctrl Pts',(9.43956590240532,-0.483445357410111,
4.09047547319903));
#42509=CARTESIAN_POINT('Ctrl Pts',(9.48728173846818,-0.337568794959357,
3.64229546617122));
#42510=CARTESIAN_POINT('Ctrl Pts',(9.53499757453099,0.118302386066128,3.5226010365501));
#42511=CARTESIAN_POINT('Ctrl Pts',(9.58271341059386,0.465534665650901,3.84130942079228));
#42512=CARTESIAN_POINT('Ctrl Pts',(9.62884733372396,0.387920650713885,4.29034844530944));
#42513=CARTESIAN_POINT('Ctrl Pts',(9.65907597816649,0.124080336294106,4.41554841393524));
#42514=CARTESIAN_POINT('Ctrl Pts',(9.6733993439214,-0.00023689919669354,
4.41639317328699));
#42515=CARTESIAN_POINT('Origin',(3.42660065607856,0.,4.));
#42516=CARTESIAN_POINT('',(8.97660065607858,0.000361621133123973,4.41561526113518));
#42517=CARTESIAN_POINT('',(9.0733993439214,0.00033264130393823,4.41550825894961));
#42518=CARTESIAN_POINT('',(3.42660065607856,4.87367679877478E-13,4.415875));
#42519=CARTESIAN_POINT('Ctrl Pts',(8.97660065607858,0.000361621133123963,
4.41561526113518));
#42520=CARTESIAN_POINT('Ctrl Pts',(8.98778803291839,-0.097205817696177,
4.41480833810253));
#42521=CARTESIAN_POINT('Ctrl Pts',(9.01488068844582,-0.334723089553266,
4.33177224018802));
#42522=CARTESIAN_POINT('Ctrl Pts',(9.05787862266083,-0.487593182843731,
3.93551656882348));
#42523=CARTESIAN_POINT('Ctrl Pts',(9.10559445872368,-0.209472459465777,
3.55499829935456));
#42524=CARTESIAN_POINT('Ctrl Pts',(9.15331029478651,0.261010046587687,3.58313193881964));
#42525=CARTESIAN_POINT('Ctrl Pts',(9.20102613084934,0.491803010703882,3.99408193320625));
#42526=CARTESIAN_POINT('Ctrl Pts',(9.24212291794672,0.301599829163518,4.35270650246492));
#42527=CARTESIAN_POINT('Ctrl Pts',(9.26731442635645,0.0809737859182142,
4.41494055172187));
#42528=CARTESIAN_POINT('Ctrl Pts',(9.27660065607858,-0.000185084181660189,
4.41526520375254));
#42529=CARTESIAN_POINT('Ctrl Pts',(9.0733993439214,0.000332641303938268,
4.41550825894961));
#42530=CARTESIAN_POINT('Ctrl Pts',(9.08411791260276,-0.093207009794584,
4.4148098083896));
#42531=CARTESIAN_POINT('Ctrl Pts',(9.11074175997173,-0.326599857706223,
4.33721709571948));
#42532=CARTESIAN_POINT('Ctrl Pts',(9.1532708860283,-0.489280820139143,3.94990505119329));
#42533=CARTESIAN_POINT('Ctrl Pts',(9.20098672209113,-0.222487703095825,
3.56136068709803));
#42534=CARTESIAN_POINT('Ctrl Pts',(9.24870255815399,0.248619295113741,3.57562555337399));
#42535=CARTESIAN_POINT('Ctrl Pts',(9.29641839421681,0.49141536912078,3.97960000382683));
#42536=CARTESIAN_POINT('Ctrl Pts',(9.33798398947263,0.309808547095179,4.34782394055348));
#42537=CARTESIAN_POINT('Ctrl Pts',(9.36364430604082,0.0849819773478622,
4.41487939515448));
#42538=CARTESIAN_POINT('Ctrl Pts',(9.3733993439214,-0.000241596553487357,
4.41532857883968));
#42539=CARTESIAN_POINT('Origin',(3.42660065607856,0.,4.));
#42540=CARTESIAN_POINT('',(8.67660065607859,2.43999233753954E-5,4.41655967853978));
#42541=CARTESIAN_POINT('',(8.77339934392141,9.9565801791445E-5,4.41653262406943));
#42542=CARTESIAN_POINT('',(3.42660065607856,4.87367679877478E-13,4.415875));
#42543=CARTESIAN_POINT('Ctrl Pts',(8.67660065607859,2.43999233753836E-5,
4.41655967853978));
#42544=CARTESIAN_POINT('Ctrl Pts',(8.69235636079272,-0.136579453435425,
4.41644398151286));
#42545=CARTESIAN_POINT('Ctrl Pts',(8.72401734419445,-0.411298873006737,
4.26841067400337));
#42546=CARTESIAN_POINT('Ctrl Pts',(8.7715836062838,-0.449388340942622,3.80011167148426));
#42547=CARTESIAN_POINT('Ctrl Pts',(8.81929944234665,-0.0749173544856965,
3.51390061216986));
#42548=CARTESIAN_POINT('Ctrl Pts',(8.86701527840948,0.368351391347115,3.67408210030036));
#42549=CARTESIAN_POINT('Ctrl Pts',(8.91473111447233,0.473357386691186,4.13355901061654));
#42550=CARTESIAN_POINT('Ctrl Pts',(8.95125957369535,0.220969504140389,4.39141457480799));
#42551=CARTESIAN_POINT('Ctrl Pts',(8.97188275423077,0.0415074238114615,
4.41595555392421));
#42552=CARTESIAN_POINT('Ctrl Pts',(8.97660065607858,0.000361621133123963,
4.41561526113518));
#42553=CARTESIAN_POINT('Ctrl Pts',(8.77339934392141,9.95658017914599E-5,
4.41653262406943));
#42554=CARTESIAN_POINT('Ctrl Pts',(8.78868624047708,-0.132462770989084,
4.416105976883));
#42555=CARTESIAN_POINT('Ctrl Pts',(8.81987841572037,-0.403726445587972,
4.27580529254432));
#42556=CARTESIAN_POINT('Ctrl Pts',(8.86697586965126,-0.455080472922433,
3.81343369002772));
#42557=CARTESIAN_POINT('Ctrl Pts',(8.91469170571412,-0.0892013699275644,
3.51631793453238));
#42558=CARTESIAN_POINT('Ctrl Pts',(8.96240754177693,0.358592723611288,3.66337486216116));
#42559=CARTESIAN_POINT('Ctrl Pts',(9.0101233778398,0.477085601399612,4.11955983351088));
#42560=CARTESIAN_POINT('Ctrl Pts',(9.04712064522126,0.229261233371815,4.38814011953822));
#42561=CARTESIAN_POINT('Ctrl Pts',(9.06821263391514,0.0455964315317218,
4.41584623882512));
#42562=CARTESIAN_POINT('Ctrl Pts',(9.0733993439214,0.000332641303938268,
4.41550825894961));
#42563=CARTESIAN_POINT('Origin',(3.42660065607856,0.,4.));
#42564=CARTESIAN_POINT('',(8.37660065607859,-0.000374086211409503,4.41568853448753));
#42565=CARTESIAN_POINT('',(8.47339934392141,-0.000383538171196851,4.41580895574666));
#42566=CARTESIAN_POINT('',(3.42660065607856,4.87367679877478E-13,4.415875));
#42567=CARTESIAN_POINT('Ctrl Pts',(8.37660065607859,-0.000374086211409545,
4.41568853448753));
#42568=CARTESIAN_POINT('Ctrl Pts',(8.38101940997943,-0.0388937529272332,
4.41602262289185));
#42569=CARTESIAN_POINT('Ctrl Pts',(8.40134344256788,-0.215680110827853,
4.3934260635833));
#42570=CARTESIAN_POINT('Ctrl Pts',(8.43757275384394,-0.470763542849379,
4.14243212971755));
#42571=CARTESIAN_POINT('Ctrl Pts',(8.48528858990678,-0.37441192437669,3.68106280283335));
#42572=CARTESIAN_POINT('Ctrl Pts',(8.53300442596962,0.0657679253190804,
3.51257841158684));
#42573=CARTESIAN_POINT('Ctrl Pts',(8.58072026203246,0.445552077224736,3.79170076492532));
#42574=CARTESIAN_POINT('Ctrl Pts',(8.62843609809529,0.41617890091499,4.26210751092856));
#42575=CARTESIAN_POINT('Ctrl Pts',(8.66039622944401,0.140517691799823,4.41596716726027));
#42576=CARTESIAN_POINT('Ctrl Pts',(8.6764510821051,0.00132122424898086,
4.41656077688887));
#42577=CARTESIAN_POINT('Ctrl Pts',(8.67660065607859,2.43999233753836E-5,
4.41655967853978));
#42578=CARTESIAN_POINT('Ctrl Pts',(8.47339934392141,-0.000383538171196768,
4.41580895574666));
#42579=CARTESIAN_POINT('Ctrl Pts',(8.47734928966379,-0.0347911067166248,
4.41612244784963));
#42580=CARTESIAN_POINT('Ctrl Pts',(8.4972045140938,-0.207394442561863,4.39645832432586));
#42581=CARTESIAN_POINT('Ctrl Pts',(8.5329650172114,-0.466364439759318,4.15623518867385));
#42582=CARTESIAN_POINT('Ctrl Pts',(8.58068085327425,-0.383642787608637,
3.69222827230584));
#42583=CARTESIAN_POINT('Ctrl Pts',(8.62839668933707,0.0513839395061145,
3.51085286915611));
#42584=CARTESIAN_POINT('Ctrl Pts',(8.67611252539993,0.439224004328866,3.77866880275638));
#42585=CARTESIAN_POINT('Ctrl Pts',(8.72382836146275,0.42371790764641,4.24973658040369));
#42586=CARTESIAN_POINT('Ctrl Pts',(8.75625730096992,0.148732406864234,4.41402322426773));
#42587=CARTESIAN_POINT('Ctrl Pts',(8.77278096178947,0.00546194790078228,
4.41654988270631));
#42588=CARTESIAN_POINT('Ctrl Pts',(8.77339934392141,9.95658017914599E-5,
4.41653262406943));
#42589=CARTESIAN_POINT('Origin',(3.42660065607856,0.,4.));
#42590=CARTESIAN_POINT('',(8.07660065607859,0.000145957947245773,4.41523406184916));
#42591=CARTESIAN_POINT('',(8.1733993439214,8.12049300508987E-5,4.41520065480005));
#42592=CARTESIAN_POINT('',(3.42660065607856,4.87367679877478E-13,4.415875));
#42593=CARTESIAN_POINT('Ctrl Pts',(8.07660065607858,0.00014595794724577,
4.41523406184916));
#42594=CARTESIAN_POINT('Ctrl Pts',(8.08558773785375,-0.0784131624224431,
4.41498734772332));
#42595=CARTESIAN_POINT('Ctrl Pts',(8.11048009831652,-0.296350794919178,
4.35572875890285));
#42596=CARTESIAN_POINT('Ctrl Pts',(8.15127773746691,-0.491827368180951,
4.00332637343646));
#42597=CARTESIAN_POINT('Ctrl Pts',(8.19899357352975,-0.268798940774433,
3.58811123553743));
#42598=CARTESIAN_POINT('Ctrl Pts',(8.24670940959259,0.201071689948468,3.55113988776764));
#42599=CARTESIAN_POINT('Ctrl Pts',(8.29442524565542,0.486295093906121,3.92636368766143));
#42600=CARTESIAN_POINT('Ctrl Pts',(8.33772232781743,0.339888039743562,4.32819890206972));
#42601=CARTESIAN_POINT('Ctrl Pts',(8.36511413129181,0.0997575609540166,
4.41482007364463));
#42602=CARTESIAN_POINT('Ctrl Pts',(8.37660065607859,-0.000374086211409545,
4.41568853448753));
#42603=CARTESIAN_POINT('Ctrl Pts',(8.1733993439214,8.12049300509751E-5,
4.41520065480005));
#42604=CARTESIAN_POINT('Ctrl Pts',(8.18191761753811,-0.0743948540356096,
4.41507113968239));
#42605=CARTESIAN_POINT('Ctrl Pts',(8.20634116984244,-0.288109900049694,
4.36032095112539));
#42606=CARTESIAN_POINT('Ctrl Pts',(8.24667000083438,-0.491516046133,4.01781014446235));
#42607=CARTESIAN_POINT('Ctrl Pts',(8.29438583689722,-0.280813212199106,
3.59620653211525));
#42608=CARTESIAN_POINT('Ctrl Pts',(8.34210167296004,0.187764715363875,3.54541267448783));
#42609=CARTESIAN_POINT('Ctrl Pts',(8.38981750902289,0.483915415676709,3.91207335260334));
#42610=CARTESIAN_POINT('Ctrl Pts',(8.43358339934334,0.347950231939931,4.32244196179047));
#42611=CARTESIAN_POINT('Ctrl Pts',(8.46144401097618,0.1037581297464,4.41486010664565));
#42612=CARTESIAN_POINT('Ctrl Pts',(8.47339934392141,-0.000383538171196768,
4.41580895574666));
#42613=CARTESIAN_POINT('Origin',(3.42660065607856,0.,4.));
#42614=CARTESIAN_POINT('',(7.77660065607858,0.000318631424802313,4.41622521972442));
#42615=CARTESIAN_POINT('',(7.8733993439214,0.000353153796088606,4.4161078667978));
#42616=CARTESIAN_POINT('',(3.42660065607856,4.87367679877478E-13,4.415875));
#42617=CARTESIAN_POINT('Ctrl Pts',(7.77660065607859,0.000318631424802297,
4.41622521972442));
#42618=CARTESIAN_POINT('Ctrl Pts',(7.79015606572807,-0.117457481003694,
4.41522659035305));
#42619=CARTESIAN_POINT('Ctrl Pts',(7.81961675406517,-0.375115671948731,
4.30131743988157));
#42620=CARTESIAN_POINT('Ctrl Pts',(7.86498272108989,-0.472647010158531,
3.86394843388276));
#42621=CARTESIAN_POINT('Ctrl Pts',(7.91269855715272,-0.141191260335066,
3.52886280888004));
#42622=CARTESIAN_POINT('Ctrl Pts',(7.96041439321556,0.31992259635559,3.62642971585976));
#42623=CARTESIAN_POINT('Ctrl Pts',(8.0081302292784,0.48724661017382,4.0670519628834));
#42624=CARTESIAN_POINT('Ctrl Pts',(8.04685898356608,0.259884401562094,4.37470733986759));
#42625=CARTESIAN_POINT('Ctrl Pts',(8.06968245916614,0.0606202562326388,
4.41542398077349));
#42626=CARTESIAN_POINT('Ctrl Pts',(8.07660065607858,0.00014595794724577,
4.41523406184916));
#42627=CARTESIAN_POINT('Ctrl Pts',(7.8733993439214,0.000353153796088627,
4.4161078667978));
#42628=CARTESIAN_POINT('Ctrl Pts',(7.88648594541244,-0.113432877329791,
4.41507910421771));
#42629=CARTESIAN_POINT('Ctrl Pts',(7.9154778255911,-0.367219156371593,4.30774647947464));
#42630=CARTESIAN_POINT('Ctrl Pts',(7.96037498445733,-0.476448943335793,
3.87792777037096));
#42631=CARTESIAN_POINT('Ctrl Pts',(8.0080908205202,-0.1550058622045,3.53322552818936));
#42632=CARTESIAN_POINT('Ctrl Pts',(8.05580665658301,0.308781487260178,3.61716946571973));
#42633=CARTESIAN_POINT('Ctrl Pts',(8.10352249264587,0.489010045760349,4.0526725734847));
#42634=CARTESIAN_POINT('Ctrl Pts',(8.14272005509199,0.26816615642074,4.37069430501912));
#42635=CARTESIAN_POINT('Ctrl Pts',(8.1660123388505,0.064666477720629,4.4153129696744));
#42636=CARTESIAN_POINT('Ctrl Pts',(8.1733993439214,8.12049300509751E-5,
4.41520065480005));
#42637=CARTESIAN_POINT('Origin',(3.42660065607856,0.,4.));
#42638=CARTESIAN_POINT('',(7.47660065607859,-0.000306770237538029,4.41625647512786));
#42639=CARTESIAN_POINT('',(7.5733993439214,-0.000257198714157858,4.41635988094829));
#42640=CARTESIAN_POINT('',(3.42660065607856,4.87367679877478E-13,4.415875));
#42641=CARTESIAN_POINT('Ctrl Pts',(7.47660065607859,-0.00030677023753798,
4.41625647512786));
#42642=CARTESIAN_POINT('Ctrl Pts',(7.47881911491479,-0.0195780710793754,
4.41641565502598));
#42643=CARTESIAN_POINT('Ctrl Pts',(7.4969428524386,-0.176849480241104,4.4064317922735));
#42644=CARTESIAN_POINT('Ctrl Pts',(7.53097186865002,-0.44664354691983,4.20594845626764));
#42645=CARTESIAN_POINT('Ctrl Pts',(7.57868770471286,-0.414791917646955,
3.73570302684109));
#42646=CARTESIAN_POINT('Ctrl Pts',(7.62640354077569,-0.00203048755240202,
3.50816557464413));
#42647=CARTESIAN_POINT('Ctrl Pts',(7.67411937683853,0.412595570264971,3.73228724307244));
#42648=CARTESIAN_POINT('Ctrl Pts',(7.72183521290137,0.448328767436039,4.20225365549051));
#42649=CARTESIAN_POINT('Ctrl Pts',(7.75599563931472,0.179163779268806,4.40574053813273));
#42650=CARTESIAN_POINT('Ctrl Pts',(7.77425078704046,0.0207354574140521,
4.41639833498254));
#42651=CARTESIAN_POINT('Ctrl Pts',(7.77660065607859,0.000318631424802297,
4.41622521972442));
#42652=CARTESIAN_POINT('Ctrl Pts',(7.5733993439214,-0.000257198714157839,
4.41635988094829));
#42653=CARTESIAN_POINT('Ctrl Pts',(7.57514899459915,-0.0154461882200338,
4.41646996636401));
#42654=CARTESIAN_POINT('Ctrl Pts',(7.59280392396451,-0.168599214901356,
4.40881268721627));
#42655=CARTESIAN_POINT('Ctrl Pts',(7.62636413201748,-0.440384235482588,
4.21901358396786));
#42656=CARTESIAN_POINT('Ctrl Pts',(7.67407996808031,-0.422396009600076,
3.7480340579683));
#42657=CARTESIAN_POINT('Ctrl Pts',(7.72179580414317,-0.0165150286377962,
3.50843873354525));
#42658=CARTESIAN_POINT('Ctrl Pts',(7.76951164020598,0.404531957204003,3.72025168374225));
#42659=CARTESIAN_POINT('Ctrl Pts',(7.81722747626884,0.454091022239626,4.18896181724392));
#42660=CARTESIAN_POINT('Ctrl Pts',(7.85185671084063,0.187425762196077,4.40318800700955));
#42661=CARTESIAN_POINT('Ctrl Pts',(7.87058066672482,0.02486112795907,4.41632944836175));
#42662=CARTESIAN_POINT('Ctrl Pts',(7.8733993439214,0.000353153796088627,
4.4161078667978));
#42663=CARTESIAN_POINT('Origin',(3.42660065607856,0.,4.));
#42664=CARTESIAN_POINT('',(7.17660065607858,-0.000163391746992416,4.4152468210878));
#42665=CARTESIAN_POINT('',(7.2733993439214,-0.000222139526412562,4.4153039283715));
#42666=CARTESIAN_POINT('',(3.42660065607856,4.87367679877478E-13,4.415875));
#42667=CARTESIAN_POINT('Ctrl Pts',(7.17660065607859,-0.000163391746992363,
4.4152468210878));
#42668=CARTESIAN_POINT('Ctrl Pts',(7.18338744278911,-0.0594844418834033,
4.41545575762517));
#42669=CARTESIAN_POINT('Ctrl Pts',(7.20607950818724,-0.257561782965025,
4.37580284351512));
#42670=CARTESIAN_POINT('Ctrl Pts',(7.24467685227299,-0.486676365692783,
4.07107270446015));
#42671=CARTESIAN_POINT('Ctrl Pts',(7.29239268833582,-0.322996137187983,
3.62908393881966));
#42672=CARTESIAN_POINT('Ctrl Pts',(7.34010852439867,0.137296434535941,3.52771310152703));
#42673=CARTESIAN_POINT('Ctrl Pts',(7.3878243604615,0.471507566988788,3.86005058906394));
#42674=CARTESIAN_POINT('Ctrl Pts',(7.43332173768814,0.377318713751663,4.29947917201381));
#42675=CARTESIAN_POINT('Ctrl Pts',(7.46291383622717,0.118587850938607,4.41527441201542));
#42676=CARTESIAN_POINT('Ctrl Pts',(7.47660065607859,-0.00030677023753798,
4.41625647512786));
#42677=CARTESIAN_POINT('Ctrl Pts',(7.2733993439214,-0.000222139526412493,
4.4153039283715));
#42678=CARTESIAN_POINT('Ctrl Pts',(7.27971732247348,-0.0554265094472961,
4.41557047734173));
#42679=CARTESIAN_POINT('Ctrl Pts',(7.30194057971316,-0.249272617462211,
4.37960776139715));
#42680=CARTESIAN_POINT('Ctrl Pts',(7.34006911564044,-0.484372034479295,
4.08537538031203));
#42681=CARTESIAN_POINT('Ctrl Pts',(7.3877849517033,-0.333780171974684,3.63875766810317));
#42682=CARTESIAN_POINT('Ctrl Pts',(7.43550078776612,0.123327161313159,3.52387434835784));
#42683=CARTESIAN_POINT('Ctrl Pts',(7.48321662382897,0.467181263150904,3.84622454030349));
#42684=CARTESIAN_POINT('Ctrl Pts',(7.52918280921405,0.385138488472668,4.29279105563264));
#42685=CARTESIAN_POINT('Ctrl Pts',(7.55924371591154,0.122630008444172,4.41546922990911));
#42686=CARTESIAN_POINT('Ctrl Pts',(7.5733993439214,-0.000257198714157839,
4.41635988094829));
#42687=CARTESIAN_POINT('Origin',(3.42660065607856,0.,4.));
#42688=CARTESIAN_POINT('',(6.87660065607859,0.000369753976522709,4.4156559906262));
#42689=CARTESIAN_POINT('',(6.9733993439214,0.000344359613660638,4.41554532105972));
#42690=CARTESIAN_POINT('',(3.42660065607856,4.87367679877478E-13,4.415875));
#42691=CARTESIAN_POINT('Ctrl Pts',(6.87660065607859,0.000369753976522759,
4.4156559906262));
#42692=CARTESIAN_POINT('Ctrl Pts',(6.88795577066343,-0.0986361616094132,
4.41481368816743));
#42693=CARTESIAN_POINT('Ctrl Pts',(6.91521616393589,-0.337621850525623,
4.32977807754403));
#42694=CARTESIAN_POINT('Ctrl Pts',(6.95838183589596,-0.486886005735063,
3.93038141845316));
#42695=CARTESIAN_POINT('Ctrl Pts',(7.0060976719588,-0.204771183672361,3.55281534000283));
#42696=CARTESIAN_POINT('Ctrl Pts',(7.05381350802163,0.265389096458903,3.58590591031157));
#42697=CARTESIAN_POINT('Ctrl Pts',(7.10152934408448,0.491837993618785,3.99926540470374));
#42698=CARTESIAN_POINT('Ctrl Pts',(7.14245839343679,0.298657604039877,4.35441002681052));
#42699=CARTESIAN_POINT('Ctrl Pts',(7.16748216410149,0.0795383202432945,
4.41496610118));
#42700=CARTESIAN_POINT('Ctrl Pts',(7.17660065607859,-0.000163391746992363,
4.4152468210878));
#42701=CARTESIAN_POINT('Ctrl Pts',(6.9733993439214,0.00034435961366068,
4.41554532105972));
#42702=CARTESIAN_POINT('Ctrl Pts',(6.9842856503478,-0.0946377878655052,
4.41480662962373));
#42703=CARTESIAN_POINT('Ctrl Pts',(7.0110772354618,-0.329510302625179,4.33529054280597));
#42704=CARTESIAN_POINT('Ctrl Pts',(7.05377409926342,-0.488725618924084,
3.94475128051735));
#42705=CARTESIAN_POINT('Ctrl Pts',(7.10148993532626,-0.21785253135038,3.55904022429238));
#42706=CARTESIAN_POINT('Ctrl Pts',(7.14920577138909,0.253078023397415,3.57826934481931));
#42707=CARTESIAN_POINT('Ctrl Pts',(7.19692160745195,0.491603063369337,3.98478019943955));
#42708=CARTESIAN_POINT('Ctrl Pts',(7.2383194649627,0.306874094293292,4.34959156107453));
#42709=CARTESIAN_POINT('Ctrl Pts',(7.26381204378586,0.0835484619188193,
4.41489945011039));
#42710=CARTESIAN_POINT('Ctrl Pts',(7.2733993439214,-0.000222139526412493,
4.4153039283715));
#42711=CARTESIAN_POINT('Origin',(3.42660065607856,0.,4.));
#42712=CARTESIAN_POINT('',(6.57660065607858,1.8302248101926E-5,4.41656360501758));
#42713=CARTESIAN_POINT('',(6.6733993439214,7.63499956435865E-5,4.4165465803965));
#42714=CARTESIAN_POINT('',(3.42660065607856,4.87367679877478E-13,4.415875));
#42715=CARTESIAN_POINT('Ctrl Pts',(6.57660065607858,1.83022481018748E-5,
4.41656360501758));
#42716=CARTESIAN_POINT('Ctrl Pts',(6.57661881985014,-0.000139156870309867,
4.41656362372179));
#42717=CARTESIAN_POINT('Ctrl Pts',(6.59254226230931,-0.138177237712184,
4.41649399470799));
#42718=CARTESIAN_POINT('Ctrl Pts',(6.62437098345609,-0.41404349770976,4.26553045144514));
#42719=CARTESIAN_POINT('Ctrl Pts',(6.67208681951894,-0.447234019333667,
3.79538894860702));
#42720=CARTESIAN_POINT('Ctrl Pts',(6.71980265558177,-0.0698021891909718,
3.51313682319347));
#42721=CARTESIAN_POINT('Ctrl Pts',(6.76751849164461,0.371772181936036,3.67798293440124));
#42722=CARTESIAN_POINT('Ctrl Pts',(6.81523432770745,0.471920133146607,4.13853999974893));
#42723=CARTESIAN_POINT('Ctrl Pts',(6.85159504918544,0.21800401543618,4.39254992240466));
#42724=CARTESIAN_POINT('Ctrl Pts',(6.87205049197582,0.0400429038769189,
4.41599351380864));
#42725=CARTESIAN_POINT('Ctrl Pts',(6.87660065607859,0.000369753976522759,
4.4156559906262));
#42726=CARTESIAN_POINT('Ctrl Pts',(6.6733993439214,7.63499956435956E-5,
4.4165465803965));
#42727=CARTESIAN_POINT('Ctrl Pts',(6.68885397822212,-0.133927014866661,
4.41622291450327));
#42728=CARTESIAN_POINT('Ctrl Pts',(6.72021389121046,-0.406451392834186,
4.27318229388465));
#42729=CARTESIAN_POINT('Ctrl Pts',(6.76747908288639,-0.453085647428837,
3.80864864857145));
#42730=CARTESIAN_POINT('Ctrl Pts',(6.81519491894923,-0.0841006081168706,
3.51540431248109));
#42731=CARTESIAN_POINT('Ctrl Pts',(6.86291075501207,0.362121456530253,3.66717299786736));
#42732=CARTESIAN_POINT('Ctrl Pts',(6.91062659107491,0.475798562415156,4.124581128109));
#42733=CARTESIAN_POINT('Ctrl Pts',(6.94745612071136,0.226294304474162,4.38932900794447));
#42734=CARTESIAN_POINT('Ctrl Pts',(6.96838037166019,0.0441344886838037,
4.41588588393584));
#42735=CARTESIAN_POINT('Ctrl Pts',(6.9733993439214,0.00034435961366068,
4.41554532105972));
#42736=CARTESIAN_POINT('Origin',(3.42660065607856,0.,4.));
#42737=CARTESIAN_POINT('',(6.27660065607859,-8.94903747701068E-6,4.41582842213685));
#42738=CARTESIAN_POINT('',(6.3733993439214,-0.000441664590319634,4.4157663968931));
#42739=CARTESIAN_POINT('',(3.42660065607856,4.87367679877478E-13,4.415875));
#42740=CARTESIAN_POINT('Ctrl Pts',(6.27660065607859,-8.94903747701223E-6,
4.41582842213685));
#42741=CARTESIAN_POINT('Ctrl Pts',(6.28118714772447,-0.0399801639742102,
4.41579747358059));
#42742=CARTESIAN_POINT('Ctrl Pts',(6.29372627871415,-0.149263049162913,
4.40013952362907));
#42743=CARTESIAN_POINT('Ctrl Pts',(6.31421804904765,-0.307151379675736,
4.3060270879454));
#42744=CARTESIAN_POINT('Ctrl Pts',(6.33807596707907,-0.416657206472865,
4.12081787696614));
#42745=CARTESIAN_POINT('Ctrl Pts',(6.36193388511048,-0.422829889105799,
3.9075587958503));
#42746=CARTESIAN_POINT('Ctrl Pts',(6.39374444248571,-0.296437506874183,
3.64987069373525));
#42747=CARTESIAN_POINT('Ctrl Pts',(6.43350763920474,0.0703302468340302,
3.51324810367198));
#42748=CARTESIAN_POINT('Ctrl Pts',(6.48122347526758,0.448014600657906,3.7964368525222));
#42749=CARTESIAN_POINT('Ctrl Pts',(6.52892114755886,0.413253290380966,4.26628466471864));
#42750=CARTESIAN_POINT('Ctrl Pts',(6.56071354116253,0.137741412285014,4.41654724519979));
#42751=CARTESIAN_POINT('Ctrl Pts',(6.57660065607858,1.83022481018748E-5,
4.41656360501758));
#42752=CARTESIAN_POINT('Ctrl Pts',(6.3733993439214,-0.000441664590319611,
4.4157663968931));
#42753=CARTESIAN_POINT('Ctrl Pts',(6.37751702740883,-0.0362476131304844,
4.41610293027605));
#42754=CARTESIAN_POINT('Ctrl Pts',(6.39753998958387,-0.210006484715375,
4.39546152579387));
#42755=CARTESIAN_POINT('Ctrl Pts',(6.43346823044653,-0.468271923807345,
4.15124960425567));
#42756=CARTESIAN_POINT('Ctrl Pts',(6.48118406650937,-0.380227249479543,
3.6882349865083));
#42757=CARTESIAN_POINT('Ctrl Pts',(6.52889990257221,0.0564566449812287,
3.51140415777354));
#42758=CARTESIAN_POINT('Ctrl Pts',(6.57661573863504,0.441574375138847,3.78331933667001));
#42759=CARTESIAN_POINT('Ctrl Pts',(6.62433157469789,0.421040068198854,4.25418342072721));
#42760=CARTESIAN_POINT('Ctrl Pts',(6.65659277646,0.145792717270209,4.41473316952435));
#42761=CARTESIAN_POINT('Ctrl Pts',(6.6729486995345,0.00398377756883227,
4.41655601822694));
#42762=CARTESIAN_POINT('Ctrl Pts',(6.6733993439214,7.63499956435956E-5,
4.4165465803965));
#42763=CARTESIAN_POINT('Origin',(3.42660065607856,0.,4.));
#42764=CARTESIAN_POINT('',(5.97660065607859,-9.19412645702589E-6,4.41589218083175));
#42765=CARTESIAN_POINT('',(6.0733993439214,-6.65563173402051E-6,4.41590255337155));
#42766=CARTESIAN_POINT('',(3.42660065607856,4.87367679877478E-13,4.415875));
#42767=CARTESIAN_POINT('Ctrl Pts',(5.97660065607858,-9.19412645705893E-6,
4.41589218083175));
#42768=CARTESIAN_POINT('Ctrl Pts',(5.97780283625498,-0.0104787976275591,
4.4159022685469));
#42769=CARTESIAN_POINT('Ctrl Pts',(5.98695765577519,-0.0902010538040918,
4.41295272969856));
#42770=CARTESIAN_POINT('Ctrl Pts',(6.0040651146392,-0.23587461323539,4.36380751861078));
#42771=CARTESIAN_POINT('Ctrl Pts',(6.02792303267061,-0.381351759249696,
4.20630938167977));
#42772=CARTESIAN_POINT('Ctrl Pts',(6.05178095070204,-0.433578399193506,
3.9983625870902));
#42773=CARTESIAN_POINT('Ctrl Pts',(6.07563886873346,-0.379782579589031,
3.79081692866841));
#42774=CARTESIAN_POINT('Ctrl Pts',(6.09949678676487,-0.233120953551068,
3.63442082419035));
#42775=CARTESIAN_POINT('Ctrl Pts',(6.12335470479629,-0.0294522997972467,
3.5674214393556));
#42776=CARTESIAN_POINT('Ctrl Pts',(6.14721262282771,0.181413325723775,3.60619428643423));
#42777=CARTESIAN_POINT('Ctrl Pts',(6.17107054085913,0.347927737305898,3.74127281623538));
#42778=CARTESIAN_POINT('Ctrl Pts',(6.19492845889055,0.429346806292137,3.93959933010928));
#42779=CARTESIAN_POINT('Ctrl Pts',(6.21878637692197,0.405811992579865,4.15272917617017));
#42780=CARTESIAN_POINT('Ctrl Pts',(6.24264429495339,0.282982581651336,4.32844890303245));
#42781=CARTESIAN_POINT('Ctrl Pts',(6.26191572133893,0.127967070080381,4.40561019629887));
#42782=CARTESIAN_POINT('Ctrl Pts',(6.27323450838066,0.029326984292613,4.415851136102));
#42783=CARTESIAN_POINT('Ctrl Pts',(6.27660065607859,-8.94903747701223E-6,
4.41582842213685));
#42784=CARTESIAN_POINT('Ctrl Pts',(6.0733993439214,-6.65563173397714E-6,
4.41590255337156));
#42785=CARTESIAN_POINT('Ctrl Pts',(6.07413271593935,-0.00639299139291402,
4.41590724351385));
#42786=CARTESIAN_POINT('Ctrl Pts',(6.0828187273011,-0.0820297780542147,
4.41420140028919));
#42787=CARTESIAN_POINT('Ctrl Pts',(6.09945737800665,-0.2250554921608,4.3705991908187));
#42788=CARTESIAN_POINT('Ctrl Pts',(6.12331529603809,-0.375113923638194,
4.21744656883549));
#42789=CARTESIAN_POINT('Ctrl Pts',(6.1471732140695,-0.433431396087355,4.01114207710762));
#42790=CARTESIAN_POINT('Ctrl Pts',(6.17103113210093,-0.385792139046387,
3.80207577201042));
#42791=CARTESIAN_POINT('Ctrl Pts',(6.19488905013233,-0.243761337718234,
3.64147770828707));
#42792=CARTESIAN_POINT('Ctrl Pts',(6.21874696816376,-0.042227823444436,
3.56841523311022));
#42793=CARTESIAN_POINT('Ctrl Pts',(6.24260488619517,0.16982704650124,3.60113783246665));
#42794=CARTESIAN_POINT('Ctrl Pts',(6.2664628042266,0.339985970990829,3.73091992247201));
#42795=CARTESIAN_POINT('Ctrl Pts',(6.29032072225801,0.427700638223926,3.92738904240251));
#42796=CARTESIAN_POINT('Ctrl Pts',(6.31417864028943,0.409561128158778,4.13996490148311));
#42797=CARTESIAN_POINT('Ctrl Pts',(6.34187151417723,0.27471212230801,4.35031587281991));
#42798=CARTESIAN_POINT('Ctrl Pts',(6.36161174872122,0.102059178040878,4.41480301073152));
#42799=CARTESIAN_POINT('Ctrl Pts',(6.3733993439214,-0.000441664590319611,
4.4157663968931));
#42800=CARTESIAN_POINT('Origin',(3.42660065607856,0.,4.));
#42801=CARTESIAN_POINT('',(5.67660065607858,1.06631253201556E-5,4.41586554077139));
#42802=CARTESIAN_POINT('',(5.7733993439214,9.17748676071416E-6,4.4158542849441));
#42803=CARTESIAN_POINT('',(3.42660065607856,4.87367679877478E-13,4.415875));
#42804=CARTESIAN_POINT('Ctrl Pts',(5.67660065607858,1.06631253201268E-5,
4.41586554077139));
#42805=CARTESIAN_POINT('Ctrl Pts',(5.68237116412931,-0.050253077703417,
4.41581669384736));
#42806=CARTESIAN_POINT('Ctrl Pts',(5.69609431152383,-0.169828933264711,
4.3941204493343));
#42807=CARTESIAN_POINT('Ctrl Pts',(5.71777009826218,-0.329222253834466,
4.28214440376531));
#42808=CARTESIAN_POINT('Ctrl Pts',(5.74162801629359,-0.424158110434281,
4.08990358344764));
#42809=CARTESIAN_POINT('Ctrl Pts',(5.76548593432501,-0.415375755386326,
3.8756788878607));
#42810=CARTESIAN_POINT('Ctrl Pts',(5.78934385235642,-0.305022713182347,
3.69185409099321));
#42811=CARTESIAN_POINT('Ctrl Pts',(5.81320177038785,-0.120083309624962,
3.58337936191985));
#42812=CARTESIAN_POINT('Ctrl Pts',(5.83705968841926,0.0942197354074567,
3.57677972866706));
#42813=CARTESIAN_POINT('Ctrl Pts',(5.86091760645069,0.285483486244351,3.673668977605));
#42814=CARTESIAN_POINT('Ctrl Pts',(5.8847755244821,0.406938752801468,3.85035505520226));
#42815=CARTESIAN_POINT('Ctrl Pts',(5.90863344251353,0.428886400972996,4.06363338935351));
#42816=CARTESIAN_POINT('Ctrl Pts',(5.93249136054494,0.345959657594393,4.261351642888));
#42817=CARTESIAN_POINT('Ctrl Pts',(5.95514709839996,0.186877681905787,4.38841966610496));
#42818=CARTESIAN_POINT('Ctrl Pts',(5.96985019691118,0.0587795235055939,
4.41583553648629));
#42819=CARTESIAN_POINT('Ctrl Pts',(5.97660065607858,-9.19412645705893E-6,
4.41589218083175));
#42820=CARTESIAN_POINT('Ctrl Pts',(5.7733993439214,9.17748676073846E-6,
4.4158542849441));
#42821=CARTESIAN_POINT('Ctrl Pts',(5.77870104381367,-0.0461746181927863,
4.41581721944429));
#42822=CARTESIAN_POINT('Ctrl Pts',(5.79195538304975,-0.161664917198308,
4.3966319946429));
#42823=CARTESIAN_POINT('Ctrl Pts',(5.81316236162963,-0.320769768688322,
4.29171820750724));
#42824=CARTESIAN_POINT('Ctrl Pts',(5.83702027966105,-0.421326288178809,
4.10235681181338));
#42825=CARTESIAN_POINT('Ctrl Pts',(5.86087819769247,-0.418857046020503,
3.88796639709818));
#42826=CARTESIAN_POINT('Ctrl Pts',(5.88473611572389,-0.313965860818636,
3.70097123187977));
#42827=CARTESIAN_POINT('Ctrl Pts',(5.90859403375531,-0.132301443679057,
3.58709678011166));
#42828=CARTESIAN_POINT('Ctrl Pts',(5.93245195178673,0.0817142298265842,
3.57418834816524));
#42829=CARTESIAN_POINT('Ctrl Pts',(5.95630986981814,0.275748643515392,3.66540258613358));
#42830=CARTESIAN_POINT('Ctrl Pts',(5.98016778784957,0.402354822815078,3.83843477537114));
#42831=CARTESIAN_POINT('Ctrl Pts',(6.00402570588098,0.430574627524036,4.05097449853386));
#42832=CARTESIAN_POINT('Ctrl Pts',(6.02788362391241,0.353506566116634,4.25104874587108));
#42833=CARTESIAN_POINT('Ctrl Pts',(6.05100816992587,0.195023852357142,4.38547315270063));
#42834=CARTESIAN_POINT('Ctrl Pts',(6.06618007659554,0.06286002589468,4.4158563839102));
#42835=CARTESIAN_POINT('Ctrl Pts',(6.0733993439214,-6.65563173397714E-6,
4.41590255337156));
#42836=CARTESIAN_POINT('Origin',(3.42660065607856,0.,4.));
#42837=CARTESIAN_POINT('',(5.37660065607858,-1.01751121954902E-5,4.41586038335289));
#42838=CARTESIAN_POINT('',(5.4733993439214,-1.09014992595302E-5,4.41587264340464));
#42839=CARTESIAN_POINT('',(3.42660065607856,4.87367679877478E-13,4.415875));
#42840=CARTESIAN_POINT('Ctrl Pts',(5.37660065607859,-1.01751121954468E-5,
4.41586038335289));
#42841=CARTESIAN_POINT('Ctrl Pts',(5.37898685265982,-0.0207957689391596,
4.41587928195339));
#42842=CARTESIAN_POINT('Ctrl Pts',(5.38932568858487,-0.110842971866809,
4.40924760552439));
#42843=CARTESIAN_POINT('Ctrl Pts',(5.40761716385372,-0.26226226804932,4.34526983614494));
#42844=CARTESIAN_POINT('Ctrl Pts',(5.43147508188515,-0.395631058815178,
4.17739453851434));
#42845=CARTESIAN_POINT('Ctrl Pts',(5.45533299991656,-0.432257278927009,
3.96614144408682));
#42846=CARTESIAN_POINT('Ctrl Pts',(5.47919091794798,-0.363184819889405,
3.76316768886851));
#42847=CARTESIAN_POINT('Ctrl Pts',(5.5030488359794,-0.205303779432806,3.61810588490468));
#42848=CARTESIAN_POINT('Ctrl Pts',(5.52690675401082,0.00277962745745752,
3.56642759466814));
#42849=CARTESIAN_POINT('Ctrl Pts',(5.55076467204224,0.210183339719457,3.62076956781107));
#42850=CARTESIAN_POINT('Ctrl Pts',(5.57462259007365,0.36619150013966,3.76784371165257));
#42851=CARTESIAN_POINT('Ctrl Pts',(5.59848050810508,0.432655863921731,3.97168639180759));
#42852=CARTESIAN_POINT('Ctrl Pts',(5.62233842613649,0.393324083661671,4.18245252040861));
#42853=CARTESIAN_POINT('Ctrl Pts',(5.64619634416792,0.257813851021257,4.34860403787086));
#42854=CARTESIAN_POINT('Ctrl Pts',(5.66428375414861,0.107285005985459,4.40994309575933));
#42855=CARTESIAN_POINT('Ctrl Pts',(5.6744185247855,0.0190180158238588,4.41588401235146));
#42856=CARTESIAN_POINT('Ctrl Pts',(5.67660065607858,1.06631253201268E-5,
4.41586554077139));
#42857=CARTESIAN_POINT('Ctrl Pts',(5.4733993439214,-1.0901499259525E-5,
4.41587264340464));
#42858=CARTESIAN_POINT('Ctrl Pts',(5.47531673234419,-0.0167114040746605,
4.41588973972128));
#42859=CARTESIAN_POINT('Ctrl Pts',(5.48518676011079,-0.102669266038577,
4.41080986982701));
#42860=CARTESIAN_POINT('Ctrl Pts',(5.50300942722118,-0.251979671819092,
4.35284416104532));
#42861=CARTESIAN_POINT('Ctrl Pts',(5.52686734525261,-0.390234841353927,
4.18896964197264));
#42862=CARTESIAN_POINT('Ctrl Pts',(5.55072526328402,-0.433066962396004,
3.97888689800548));
#42863=CARTESIAN_POINT('Ctrl Pts',(5.57458318131544,-0.370002414621403,
3.77396688259));
#42864=CARTESIAN_POINT('Ctrl Pts',(5.59844109934686,-0.21646219781534,3.62431812139094));
#42865=CARTESIAN_POINT('Ctrl Pts',(5.62229901737828,-0.00999107731853999,
3.56653381289738));
#42866=CARTESIAN_POINT('Ctrl Pts',(5.64615693540971,0.198923133709572,3.61474379450078));
#42867=CARTESIAN_POINT('Ctrl Pts',(5.67001485344111,0.359195220034686,3.75715941257656));
#42868=CARTESIAN_POINT('Ctrl Pts',(5.69387277147254,0.431634290692432,3.95895616900985));
#42869=CARTESIAN_POINT('Ctrl Pts',(5.71773068950395,0.398527019959163,4.1707892603438));
#42870=CARTESIAN_POINT('Ctrl Pts',(5.74158860753538,0.267969036875697,4.34085972491723));
#42871=CARTESIAN_POINT('Ctrl Pts',(5.76014482567452,0.115458993192439,4.40830959117706));
#42872=CARTESIAN_POINT('Ctrl Pts',(5.77074840446986,0.0231018550196917,
4.41587281831976));
#42873=CARTESIAN_POINT('Ctrl Pts',(5.7733993439214,9.17748676073846E-6,
4.4158542849441));
#42874=CARTESIAN_POINT('Origin',(3.42660065607856,0.,4.));
#42875=CARTESIAN_POINT('',(5.07660065607859,8.10857529294212E-6,4.41589722116852));
#42876=CARTESIAN_POINT('',(5.1733993439214,1.02299162792543E-5,4.4158851107878));
#42877=CARTESIAN_POINT('',(3.42660065607856,4.87367679877478E-13,4.415875));
#42878=CARTESIAN_POINT('Ctrl Pts',(5.07660065607858,8.10857529294148E-6,
4.41589722116852));
#42879=CARTESIAN_POINT('Ctrl Pts',(5.08355518053415,-0.060555656273516,
4.41584370653314));
#42880=CARTESIAN_POINT('Ctrl Pts',(5.09846234433351,-0.190424342306974,
4.38715451669839));
#42881=CARTESIAN_POINT('Ctrl Pts',(5.1213221474767,-0.349282119693095,4.256894448863));
#42882=CARTESIAN_POINT('Ctrl Pts',(5.1451800655081,-0.4296670234643,4.05812921762123));
#42883=CARTESIAN_POINT('Ctrl Pts',(5.16903798353954,-0.404986636103755,
3.84514980926298));
#42884=CARTESIAN_POINT('Ctrl Pts',(5.19289590157095,-0.281275984601366,
3.67003549057442));
#42885=CARTESIAN_POINT('Ctrl Pts',(5.21675381960238,-0.0887856930599551,
3.5756064824932));
#42886=CARTESIAN_POINT('Ctrl Pts',(5.24061173763379,0.125415118908336,3.58495324968971));
#42887=CARTESIAN_POINT('Ctrl Pts',(5.26446965566521,0.308948518064291,3.69579025298356));
#42888=CARTESIAN_POINT('Ctrl Pts',(5.28832757369662,0.416935588964862,3.88101482593007));
#42889=CARTESIAN_POINT('Ctrl Pts',(5.31218549172805,0.422970551266107,4.09533451502773));
#42890=CARTESIAN_POINT('Ctrl Pts',(5.33604340975946,0.325577692296299,4.28634231834109));
#42891=CARTESIAN_POINT('Ctrl Pts',(5.35751513120965,0.166275769440666,4.39523064161658));
#42892=CARTESIAN_POINT('Ctrl Pts',(5.37103421331602,0.0484777907299229,
4.41581629730449));
#42893=CARTESIAN_POINT('Ctrl Pts',(5.37660065607859,-1.01751121954468E-5,
4.41586038335289));
#42894=CARTESIAN_POINT('Ctrl Pts',(5.1733993439214,1.02299162792474E-5,
4.4158851107878));
#42895=CARTESIAN_POINT('Ctrl Pts',(5.17988506021851,-0.0564756498766958,
4.41582730150705));
#42896=CARTESIAN_POINT('Ctrl Pts',(5.19432341585943,-0.182274442988225,
4.39002065289559));
#42897=CARTESIAN_POINT('Ctrl Pts',(5.21671441084416,-0.341564590845109,
4.26707000444592));
#42898=CARTESIAN_POINT('Ctrl Pts',(5.24057232887557,-0.427768622694993,
4.07075847957352));
#42899=CARTESIAN_POINT('Ctrl Pts',(5.264430246907,-0.409371574112622,3.85714457902312));
#42900=CARTESIAN_POINT('Ctrl Pts',(5.2882881649384,-0.290872024601924,3.6784627202051));
#42901=CARTESIAN_POINT('Ctrl Pts',(5.31214608296984,-0.101246341881189,
3.57840548479658));
#42902=CARTESIAN_POINT('Ctrl Pts',(5.33600400100125,0.113136829324483,3.58143959235932));
#42903=CARTESIAN_POINT('Ctrl Pts',(5.35986191903268,0.299854963974951,3.68682312094679));
#42904=CARTESIAN_POINT('Ctrl Pts',(5.38371983706408,0.413250392048343,3.8687869272297));
#42905=CARTESIAN_POINT('Ctrl Pts',(5.40757775509551,0.425594842551202,4.08283590397723));
#42906=CARTESIAN_POINT('Ctrl Pts',(5.43143567312693,0.333869761079625,4.27662924579771));
#42907=CARTESIAN_POINT('Ctrl Pts',(5.45337620273556,0.174437273907163,4.39264091290779));
#42908=CARTESIAN_POINT('Ctrl Pts',(5.46736409300038,0.0525562895569378,
4.41581883033293));
#42909=CARTESIAN_POINT('Ctrl Pts',(5.4733993439214,-1.0901499259525E-5,
4.41587264340464));
#42910=CARTESIAN_POINT('Origin',(3.42660065607856,0.,4.));
#42911=CARTESIAN_POINT('',(4.77660065607858,-3.27394476109793E-6,4.41584059078716));
#42912=CARTESIAN_POINT('',(4.8733993439214,-6.67049670156904E-6,4.4158459349409));
#42913=CARTESIAN_POINT('',(3.42660065607856,4.87367679877478E-13,4.415875));
#42914=CARTESIAN_POINT('Ctrl Pts',(4.77660065607858,-3.27394476113199E-6,
4.41584059078717));
#42915=CARTESIAN_POINT('Ctrl Pts',(4.78017086906467,-0.0311067951354469,
4.4158491206715));
#42916=CARTESIAN_POINT('Ctrl Pts',(4.79169372139456,-0.131487321212171,
4.40473555835468));
#42917=CARTESIAN_POINT('Ctrl Pts',(4.81116921306824,-0.287199161490599,
4.32482210305491));
#42918=CARTESIAN_POINT('Ctrl Pts',(4.83502713109967,-0.407721671464292,
4.14749845969467));
#42919=CARTESIAN_POINT('Ctrl Pts',(4.85888504913109,-0.42854512664958,3.93410742516172));
#42920=CARTESIAN_POINT('Ctrl Pts',(4.8827429671625,-0.344577625034195,3.73682892005441));
#42921=CARTESIAN_POINT('Ctrl Pts',(4.90660088519393,-0.176351507991885,
3.60390291263011));
#42922=CARTESIAN_POINT('Ctrl Pts',(4.93045880322534,0.0349973564730633,
3.56783343253575));
#42923=CARTESIAN_POINT('Ctrl Pts',(4.95431672125677,0.237788413971502,3.63744045016736));
#42924=CARTESIAN_POINT('Ctrl Pts',(4.97817463928818,0.382433727027559,3.79570315365689));
#42925=CARTESIAN_POINT('Ctrl Pts',(5.0020325573196,0.433563576539811,4.00392200101168));
#42926=CARTESIAN_POINT('Ctrl Pts',(5.02589047535102,0.378675321553375,4.21118181228595));
#42927=CARTESIAN_POINT('Ctrl Pts',(5.04974839338244,0.231190635538481,4.36680191797922));
#42928=CARTESIAN_POINT('Ctrl Pts',(5.0666517869583,0.086644022961884,4.4135113916189));
#42929=CARTESIAN_POINT('Ctrl Pts',(5.07560254119034,0.00870023350343714,
4.41590490160082));
#42930=CARTESIAN_POINT('Ctrl Pts',(5.07660065607858,8.10857529294148E-6,
4.41589722116852));
#42931=CARTESIAN_POINT('Ctrl Pts',(4.8733993439214,-6.67049670157252E-6,
4.41584593494091));
#42932=CARTESIAN_POINT('Ctrl Pts',(4.87650074874903,-0.0270249643080214,
4.41586127519519));
#42933=CARTESIAN_POINT('Ctrl Pts',(4.88755479292047,-0.123313358466266,
4.40662010077424));
#42934=CARTESIAN_POINT('Ctrl Pts',(4.90656147643571,-0.277507970732168,
4.33313973520738));
#42935=CARTESIAN_POINT('Ctrl Pts',(4.93041939446713,-0.403200703213916,
4.15944262266324));
#42936=CARTESIAN_POINT('Ctrl Pts',(4.95427731249855,-0.430299880793222,
3.94675744574809));
#42937=CARTESIAN_POINT('Ctrl Pts',(4.97813523052996,-0.352179016385168,
3.7470915236456));
#42938=CARTESIAN_POINT('Ctrl Pts',(5.00199314856139,-0.187940789307144,
3.60926861310034));
#42939=CARTESIAN_POINT('Ctrl Pts',(5.0258510665928,0.0222540801607904,3.56699016996131));
#42940=CARTESIAN_POINT('Ctrl Pts',(5.04970898462423,0.227007220840439,3.63059442521772));
#42941=CARTESIAN_POINT('Ctrl Pts',(5.07356690265564,0.376250912472057,3.7845284059142));
#42942=CARTESIAN_POINT('Ctrl Pts',(5.09742482068706,0.433491007135177,3.99115106069306));
#42943=CARTESIAN_POINT('Ctrl Pts',(5.12128273871848,0.384730742495793,4.19993752217271));
#42944=CARTESIAN_POINT('Ctrl Pts',(5.1451406567499,0.241893331461176,4.35983381329239));
#42945=CARTESIAN_POINT('Ctrl Pts',(5.16251285848421,0.0948160588051851,
4.41219316122439));
#42946=CARTESIAN_POINT('Ctrl Pts',(5.17193242087471,0.0127860645481494,
4.41589818594594));
#42947=CARTESIAN_POINT('Ctrl Pts',(5.1733993439214,1.02299162792474E-5,
4.4158851107878));
#42948=CARTESIAN_POINT('Origin',(3.42660065607856,0.,4.));
#42949=CARTESIAN_POINT('',(4.47660065607858,-1.72413508574122E-6,4.41591032029986));
#42950=CARTESIAN_POINT('',(4.5733993439214,2.6062779713001E-6,4.4159095790646));
#42951=CARTESIAN_POINT('',(3.42660065607856,4.87367679877478E-13,4.415875));
#42952=CARTESIAN_POINT('Ctrl Pts',(4.47660065607858,-1.72413508575881E-6,
4.41591032029986));
#42953=CARTESIAN_POINT('Ctrl Pts',(4.47678655759518,-0.00162050728124812,
4.41591069657345));
#42954=CARTESIAN_POINT('Ctrl Pts',(4.48492509845559,-0.0724886630755744,
4.4155056303295));
#42955=CARTESIAN_POINT('Ctrl Pts',(4.5010162786598,-0.212178818846594,4.37811758201071));
#42956=CARTESIAN_POINT('Ctrl Pts',(4.52487419669122,-0.367409789343613,
4.23022337776645));
#42957=CARTESIAN_POINT('Ctrl Pts',(4.54873211472264,-0.432799058467291,
4.02603328640456));
#42958=CARTESIAN_POINT('Ctrl Pts',(4.57259003275406,-0.392357168499796,
3.8154773474345));
#42959=CARTESIAN_POINT('Ctrl Pts',(4.59644795078547,-0.255973263285106,
3.65004222328625));
#42960=CARTESIAN_POINT('Ctrl Pts',(4.6203058688169,-0.0569969226013119,
3.57018130821703));
#42961=CARTESIAN_POINT('Ctrl Pts',(4.64416378684831,0.155916718210686,3.59542277130738));
#42962=CARTESIAN_POINT('Ctrl Pts',(4.66802170487973,0.330704474340828,3.71959438727947));
#42963=CARTESIAN_POINT('Ctrl Pts',(4.69187962291115,0.424625978282027,3.91233281365517));
#42964=CARTESIAN_POINT('Ctrl Pts',(4.71573754094257,0.41471486395576,4.1265082550995));
#42965=CARTESIAN_POINT('Ctrl Pts',(4.73959545897399,0.303394668785218,4.30974898215573));
#42966=CARTESIAN_POINT('Ctrl Pts',(4.75988316401932,0.145646585585232,4.40116103141851));
#42967=CARTESIAN_POINT('Ctrl Pts',(4.77221822972086,0.0381762104768988,
4.41583012037823));
#42968=CARTESIAN_POINT('Ctrl Pts',(4.77660065607858,-3.27394476113199E-6,
4.41584059078717));
#42969=CARTESIAN_POINT('Ctrl Pts',(4.5733993439214,2.60627797130011E-6,
4.4159095790646));
#42970=CARTESIAN_POINT('Ctrl Pts',(4.58106907662335,-0.0667838229435618,
4.4158868274511));
#42971=CARTESIAN_POINT('Ctrl Pts',(4.59669144866912,-0.202842099803805,
4.38250385602613));
#42972=CARTESIAN_POINT('Ctrl Pts',(4.62026646005868,-0.360469908510665,
4.24094439618412));
#42973=CARTESIAN_POINT('Ctrl Pts',(4.6441243780901,-0.431844582779732,4.03876871570463));
#42974=CARTESIAN_POINT('Ctrl Pts',(4.66798229612152,-0.397621493350665,
3.82711302819544));
#42975=CARTESIAN_POINT('Ctrl Pts',(4.69184021415294,-0.266169117804412,
3.65773291463971));
#42976=CARTESIAN_POINT('Ctrl Pts',(4.71569813218436,-0.0696311426542753,
3.57204642662242));
#42977=CARTESIAN_POINT('Ctrl Pts',(4.73955605021577,0.143933543589337,3.59100624451743));
#42978=CARTESIAN_POINT('Ctrl Pts',(4.76341396824719,0.322302557754209,3.70997617639404));
#42979=CARTESIAN_POINT('Ctrl Pts',(4.78727188627862,0.421859817202848,3.8998648332327));
#42980=CARTESIAN_POINT('Ctrl Pts',(4.81112980431003,0.41826086011465,4.11423926597311));
#42981=CARTESIAN_POINT('Ctrl Pts',(4.83498772234146,0.312385729531365,4.30067908636799));
#42982=CARTESIAN_POINT('Ctrl Pts',(4.85574423554524,0.15381688120809,4.39891624198015));
#42983=CARTESIAN_POINT('Ctrl Pts',(4.86854810940522,0.04225549351942,4.41582193963064));
#42984=CARTESIAN_POINT('Ctrl Pts',(4.8733993439214,-6.67049670157252E-6,
4.41584593494091));
#42985=CARTESIAN_POINT('Origin',(3.42660065607856,0.,4.));
#42986=CARTESIAN_POINT('',(4.17660065607858,5.88453344125852E-6,4.41584444980552));
#42987=CARTESIAN_POINT('',(4.2733993439214,2.51014653358805E-6,4.41583996132385));
#42988=CARTESIAN_POINT('',(3.42660065607856,4.87367679877478E-13,4.415875));
#42989=CARTESIAN_POINT('Ctrl Pts',(4.17660065607858,5.88453344126799E-6,
4.41584444980552));
#42990=CARTESIAN_POINT('Ctrl Pts',(4.18135488546951,-0.0414115481342504,
4.41582334930757));
#42991=CARTESIAN_POINT('Ctrl Pts',(4.19406175420423,-0.152126265423154,
4.3993918905015));
#42992=CARTESIAN_POINT('Ctrl Pts',(4.21472126228278,-0.310547447266788,
4.30257739619942));
#42993=CARTESIAN_POINT('Ctrl Pts',(4.23857918031418,-0.417556725585918,
4.11678647978038));
#42994=CARTESIAN_POINT('Ctrl Pts',(4.26243709834561,-0.422462345057068,
3.90243789311793));
#42995=CARTESIAN_POINT('Ctrl Pts',(4.28629501637703,-0.324064236326554,
3.71194600226016));
#42996=CARTESIAN_POINT('Ctrl Pts',(4.31015293440845,-0.146423688323203,
3.59189110566319));
#42997=CARTESIAN_POINT('Ctrl Pts',(4.33401085243986,0.0670214896752265,
3.5716299793216));
#42998=CARTESIAN_POINT('Ctrl Pts',(4.35786877047129,0.264078061498623,3.65611697628114));
#42999=CARTESIAN_POINT('Ctrl Pts',(4.38172668850271,0.396560367883193,3.82469274783887));
#43000=CARTESIAN_POINT('Ctrl Pts',(4.40558460653412,0.432072854850341,4.03613591352675));
#43001=CARTESIAN_POINT('Ctrl Pts',(4.42944252456555,0.361931763288092,4.23874286631049));
#43002=CARTESIAN_POINT('Ctrl Pts',(4.45311454108036,0.204524647174786,4.38184685695289));
#43003=CARTESIAN_POINT('Ctrl Pts',(4.46883391825138,0.0676290543833733,
4.4158946000499));
#43004=CARTESIAN_POINT('Ctrl Pts',(4.47660065607858,-1.72413508575881E-6,
4.41591032029986));
#43005=CARTESIAN_POINT('Ctrl Pts',(4.2733993439214,2.51014653359152E-6,
4.41583996132385));
#43006=CARTESIAN_POINT('Ctrl Pts',(4.27768476515387,-0.0373320337329404,
4.41583213221101));
#43007=CARTESIAN_POINT('Ctrl Pts',(4.28992282573015,-0.143955736965383,
4.40160880992953));
#43008=CARTESIAN_POINT('Ctrl Pts',(4.31011352565024,-0.301501118270308,
4.3115924136571));
#43009=CARTESIAN_POINT('Ctrl Pts',(4.33397144368164,-0.413936097932681,
4.12903358037428));
#43010=CARTESIAN_POINT('Ctrl Pts',(4.35782936171308,-0.425152419412173,
3.91492252699502));
#43011=CARTESIAN_POINT('Ctrl Pts',(4.38168727974448,-0.332407397051365,
3.72161523052345));
#43012=CARTESIAN_POINT('Ctrl Pts',(4.40554519777592,-0.158379709595794,
3.5963805946708));
#43013=CARTESIAN_POINT('Ctrl Pts',(4.42940311580732,0.0543761300157755,
3.56984189703405));
#43014=CARTESIAN_POINT('Ctrl Pts',(4.45326103383876,0.25383552520097,3.64848857324589));
#43015=CARTESIAN_POINT('Ctrl Pts',(4.47711895187016,0.39122521984844,3.81308936806525));
#43016=CARTESIAN_POINT('Ctrl Pts',(4.50097686990159,0.432949691632991,4.02339490384879));
#43017=CARTESIAN_POINT('Ctrl Pts',(4.524834787933,0.368806170420464,4.22797974831721));
#43018=CARTESIAN_POINT('Ctrl Pts',(4.54869270596443,0.214479494504121,4.37681733431002));
#43019=CARTESIAN_POINT('Ctrl Pts',(4.56488089129389,0.0741790848482271,
4.4152866170047));
#43020=CARTESIAN_POINT('Ctrl Pts',(4.57311643727954,0.0024660981813593,
4.41591041828323));
#43021=CARTESIAN_POINT('Ctrl Pts',(4.5733993439214,2.60627797130011E-6,
4.4159095790646));
#43022=CARTESIAN_POINT('Origin',(4.,0.,4.));
#43023=CARTESIAN_POINT('',(4.,-7.34788079488412E-17,4.6));
#43024=CARTESIAN_POINT('Origin',(4.,0.,4.));
#43025=CARTESIAN_POINT('',(4.,-0.219892372742957,4.3529863453938));
#43026=CARTESIAN_POINT('Ctrl Pts',(4.,-0.219914231356238,4.35301468169996));
#43027=CARTESIAN_POINT('Ctrl Pts',(4.,-0.219843051329574,4.3531167999744));
#43028=CARTESIAN_POINT('Ctrl Pts',(4.,-0.219771822781512,4.35321888245988));
#43029=CARTESIAN_POINT('Ctrl Pts',(4.,-0.21970054575756,4.3533209291203));
#43030=CARTESIAN_POINT('Ctrl Pts',(4.,-0.207925336055227,4.3701793886806));
#43031=CARTESIAN_POINT('Ctrl Pts',(4.,-0.194831304039315,4.38605734350833));
#43032=CARTESIAN_POINT('Ctrl Pts',(4.,-0.18064579384139,4.40088380688851));
#43033=CARTESIAN_POINT('Ctrl Pts',(4.,-0.168975273508986,4.41308164397169));
#43034=CARTESIAN_POINT('Ctrl Pts',(4.,-0.156565051628872,4.42456888924957));
#43035=CARTESIAN_POINT('Ctrl Pts',(4.,-0.143515931303371,4.43531683418355));
#43036=CARTESIAN_POINT('Ctrl Pts',(4.,-0.133182439541062,4.44382804395605));
#43037=CARTESIAN_POINT('Ctrl Pts',(4.,-0.122447811630206,4.45187590303098));
#43038=CARTESIAN_POINT('Ctrl Pts',(4.,-0.111352162047151,4.45944712768208));
#43039=CARTESIAN_POINT('Ctrl Pts',(4.,-0.105068105051177,4.46373511522897));
#43040=CARTESIAN_POINT('Ctrl Pts',(4.,-0.0986661212125077,4.46787107983396));
#43041=CARTESIAN_POINT('Ctrl Pts',(4.,-0.0921733602714696,4.47184061613108));
#43042=CARTESIAN_POINT('Ctrl Pts',(4.,-0.0718171345235072,4.48428598070136));
#43043=CARTESIAN_POINT('Ctrl Pts',(4.,-0.0505350523745213,4.49512244469223));
#43044=CARTESIAN_POINT('Ctrl Pts',(4.,-0.0285775088988711,4.50429938857761));
#43045=CARTESIAN_POINT('Ctrl Pts',(4.,-0.00645956782426854,4.51354336909515));
#43046=CARTESIAN_POINT('Ctrl Pts',(4.,0.0163444141029789,4.52110543571878));
#43047=CARTESIAN_POINT('Ctrl Pts',(4.,0.0396343143342583,4.52702898180467));
#43048=CARTESIAN_POINT('Ctrl Pts',(4.,0.0479455316904685,4.52914285427945));
#43049=CARTESIAN_POINT('Ctrl Pts',(4.,0.0563191235587283,4.53104786585874));
#43050=CARTESIAN_POINT('Ctrl Pts',(4.,0.0647475081636451,4.53274519105122));
#43051=CARTESIAN_POINT('Ctrl Pts',(4.,0.0709442475001029,4.53399310299165));
#43052=CARTESIAN_POINT('Ctrl Pts',(4.,0.0771669940275102,4.53512789739638));
#43053=CARTESIAN_POINT('Ctrl Pts',(4.,0.0834037601527001,4.53614909266968));
#43054=CARTESIAN_POINT('Ctrl Pts',(4.,0.108500755516298,4.54025842313435));
#43055=CARTESIAN_POINT('Ctrl Pts',(4.,0.133859781029961,4.54253781872753));
#43056=CARTESIAN_POINT('Ctrl Pts',(3.99999999999999,0.159256593756596,4.54305292380224));
#43057=CARTESIAN_POINT('Ctrl Pts',(3.99999999999999,0.185497795908202,4.5435851550133));
#43058=CARTESIAN_POINT('Ctrl Pts',(3.99999999999998,0.211780221987087,4.54223483664603));
#43059=CARTESIAN_POINT('Ctrl Pts',(3.99999999999998,0.237902321580844,4.5390442708621));
#43060=CARTESIAN_POINT('Ctrl Pts',(3.99999999999998,0.243507595489062,4.53835964001621));
#43061=CARTESIAN_POINT('Ctrl Pts',(3.99999999999998,0.249105619801251,4.53759013757336));
#43062=CARTESIAN_POINT('Ctrl Pts',(3.99999999999998,0.254694598474614,4.53673594206822));
#43063=CARTESIAN_POINT('',(4.,-0.219892372743086,3.64701365460628));
#43064=CARTESIAN_POINT('Ctrl Pts',(4.,0.254721014554616,3.46322028700966));
#43065=CARTESIAN_POINT('Ctrl Pts',(4.,0.254552373521139,3.46319452321125));
#43066=CARTESIAN_POINT('Ctrl Pts',(4.,0.254383724765285,3.46316883668624));
#43067=CARTESIAN_POINT('Ctrl Pts',(4.,0.254215068323085,3.46314322746093));
#43068=CARTESIAN_POINT('Ctrl Pts',(4.,0.228435861761457,3.4592288468388));
#43069=CARTESIAN_POINT('Ctrl Pts',(4.,0.202474691352968,3.45711700011808));
#43070=CARTESIAN_POINT('Ctrl Pts',(4.,0.176517231963435,3.45683380906617));
#43071=CARTESIAN_POINT('Ctrl Pts',(4.,0.151199179447316,3.45655759382427));
#43072=CARTESIAN_POINT('Ctrl Pts',(4.,0.125883695414598,3.45802192769867));
#43073=CARTESIAN_POINT('Ctrl Pts',(4.,0.1007794950383,3.46128259448669));
#43074=CARTESIAN_POINT('Ctrl Pts',(4.,0.0854593772715275,3.46327245269535));
#43075=CARTESIAN_POINT('Ctrl Pts',(4.,0.0702187270328167,3.46593187194604));
#43076=CARTESIAN_POINT('Ctrl Pts',(4.,0.0551140352340102,3.4692772918897));
#43077=CARTESIAN_POINT('Ctrl Pts',(4.,0.0468842919617017,3.47110003330284));
#43078=CARTESIAN_POINT('Ctrl Pts',(4.,0.0386923719445779,3.47312744960567));
#43079=CARTESIAN_POINT('Ctrl Pts',(4.,0.0305707631998946,3.47535548770785));
#43080=CARTESIAN_POINT('Ctrl Pts',(4.,0.0102648423897012,3.48092610391051));
#43081=CARTESIAN_POINT('Ctrl Pts',(4.,-0.00963556638195036,3.48775588581666));
#43082=CARTESIAN_POINT('Ctrl Pts',(4.,-0.0289965775380143,3.49587186612014));
#43083=CARTESIAN_POINT('Ctrl Pts',(4.,-0.047965755796229,3.50382359322137));
#43084=CARTESIAN_POINT('Ctrl Pts',(4.,-0.0664174073931304,3.51301096346156));
#43085=CARTESIAN_POINT('Ctrl Pts',(4.,-0.0841982143338667,3.52340033683134));
#43086=CARTESIAN_POINT('Ctrl Pts',(4.,-0.0930898199841631,3.5285957259532));
#43087=CARTESIAN_POINT('Ctrl Pts',(4.,-0.101813128894432,3.53409169793663));
#43088=CARTESIAN_POINT('Ctrl Pts',(4.,-0.110345561972859,3.53988353361915));
#43089=CARTESIAN_POINT('Ctrl Pts',(4.,-0.11586100642067,3.5436274303089));
#43090=CARTESIAN_POINT('Ctrl Pts',(4.,-0.121288652521606,3.54748953413154));
#43091=CARTESIAN_POINT('Ctrl Pts',(4.,-0.126621987542688,3.55146681430013));
#43092=CARTESIAN_POINT('Ctrl Pts',(4.,-0.143297831161627,3.56390265451229));
#43093=CARTESIAN_POINT('Ctrl Pts',(4.,-0.159061930875806,3.57746928852925));
#43094=CARTESIAN_POINT('Ctrl Pts',(4.,-0.173743808224101,3.59211536896244));
#43095=CARTESIAN_POINT('Ctrl Pts',(4.,-0.187864697165731,3.60620182877415));
#43096=CARTESIAN_POINT('Ctrl Pts',(4.,-0.200984288190684,3.62128798311348));
#43097=CARTESIAN_POINT('Ctrl Pts',(4.,-0.212904831975564,3.63731335989365));
#43098=CARTESIAN_POINT('Ctrl Pts',(4.,-0.21528245268753,3.64050971304978));
#43099=CARTESIAN_POINT('Ctrl Pts',(4.,-0.217612227418936,3.64374335030505));
#43100=CARTESIAN_POINT('Ctrl Pts',(4.,-0.219892372743211,3.64701365460636));
#43101=CARTESIAN_POINT('Origin',(4.,0.,4.));
#43102=CARTESIAN_POINT('Origin',(2.,0.,4.));
#43103=CARTESIAN_POINT('',(2.,-7.34788079488412E-17,4.6));
#43104=CARTESIAN_POINT('',(2.,-7.34788079488412E-17,4.6));
#43105=CARTESIAN_POINT('Origin',(2.,0.,4.));
#43106=CARTESIAN_POINT('Origin',(2.,0.,4.));
#43107=CARTESIAN_POINT('Ctrl Pts',(3.95224475517895,0.178288362465424,4.37571967666652));
#43108=CARTESIAN_POINT('Ctrl Pts',(3.96019739452275,0.115708609995841,4.40541533085819));
#43109=CARTESIAN_POINT('Ctrl Pts',(3.97610267321037,-0.0245105356436035,
4.43290545314371));
#43110=CARTESIAN_POINT('Ctrl Pts',(3.99996059124178,-0.228962993402626,
4.36819499612132));
#43111=CARTESIAN_POINT('Ctrl Pts',(4.0238185092732,-0.377374743411151,4.21349068386271));
#43112=CARTESIAN_POINT('Ctrl Pts',(4.04767642730463,-0.433534992178268,
4.00656196868444));
#43113=CARTESIAN_POINT('Ctrl Pts',(4.07153434533603,-0.383670022685343,
3.79803920418254));
#43114=CARTESIAN_POINT('Ctrl Pts',(4.09539226336747,-0.239994733226421,
3.63889579340969));
#43115=CARTESIAN_POINT('Ctrl Pts',(4.11925018139887,-0.0376302499649443,
3.56805514133307));
#43116=CARTESIAN_POINT('Ctrl Pts',(4.1431080994303,0.173933765839147,3.60283521426327));
#43117=CARTESIAN_POINT('Ctrl Pts',(4.16696601746172,0.342967344134064,3.73473372141871));
#43118=CARTESIAN_POINT('Ctrl Pts',(4.19082393549313,0.428135478754777,3.93149662217858));
#43119=CARTESIAN_POINT('Ctrl Pts',(4.21468185352456,0.40861313688017,4.1450106963618));
#43120=CARTESIAN_POINT('Ctrl Pts',(4.23853977155597,0.289173588337559,4.32306558264197));
#43121=CARTESIAN_POINT('Ctrl Pts',(4.2623976895874,0.0990233075312312,4.42212219878201));
#43122=CARTESIAN_POINT('Ctrl Pts',(4.28625560761881,-0.115340915390822,
4.41795840454656));
#43123=CARTESIAN_POINT('Ctrl Pts',(4.31011352565024,-0.301501118270308,
4.3115924136571));
#43124=CARTESIAN_POINT('Ctrl Pts',(4.33397144368164,-0.413936097932681,
4.12903358037428));
#43125=CARTESIAN_POINT('Ctrl Pts',(4.35782936171308,-0.425152419412173,
3.91492252699502));
#43126=CARTESIAN_POINT('Ctrl Pts',(4.38168727974448,-0.332407397051365,
3.72161523052345));
#43127=CARTESIAN_POINT('Ctrl Pts',(4.40554519777592,-0.158379709595794,
3.5963805946708));
#43128=CARTESIAN_POINT('Ctrl Pts',(4.42940311580732,0.0543761300157755,
3.56984189703405));
#43129=CARTESIAN_POINT('Ctrl Pts',(4.45326103383876,0.25383552520097,3.64848857324589));
#43130=CARTESIAN_POINT('Ctrl Pts',(4.47711895187016,0.39122521984844,3.81308936806525));
#43131=CARTESIAN_POINT('Ctrl Pts',(4.50097686990159,0.432949691632991,4.02339490384879));
#43132=CARTESIAN_POINT('Ctrl Pts',(4.524834787933,0.368806170420464,4.22797974831721));
#43133=CARTESIAN_POINT('Ctrl Pts',(4.54869270596443,0.214479494504121,4.37681733431002));
#43134=CARTESIAN_POINT('Ctrl Pts',(4.57255062399584,0.00770673985495463,
4.4335128177492));
#43135=CARTESIAN_POINT('Ctrl Pts',(4.59640854202726,-0.200950522604244,
4.38420260860549));
#43136=CARTESIAN_POINT('Ctrl Pts',(4.62026646005868,-0.360469908510665,
4.24094439618412));
#43137=CARTESIAN_POINT('Ctrl Pts',(4.6441243780901,-0.431844582779732,4.03876871570463));
#43138=CARTESIAN_POINT('Ctrl Pts',(4.66798229612152,-0.397621493350665,
3.82711302819544));
#43139=CARTESIAN_POINT('Ctrl Pts',(4.69184021415294,-0.266169117804412,
3.65773291463971));
#43140=CARTESIAN_POINT('Ctrl Pts',(4.71569813218436,-0.0696311426542753,
3.57204642662242));
#43141=CARTESIAN_POINT('Ctrl Pts',(4.73955605021577,0.143933543589337,3.59100624451743));
#43142=CARTESIAN_POINT('Ctrl Pts',(4.76341396824719,0.322302557754209,3.70997617639404));
#43143=CARTESIAN_POINT('Ctrl Pts',(4.78727188627862,0.421859817202848,3.8998648332327));
#43144=CARTESIAN_POINT('Ctrl Pts',(4.81112980431003,0.41826086011465,4.11423926597311));
#43145=CARTESIAN_POINT('Ctrl Pts',(4.83498772234146,0.312385729531365,4.30067908636799));
#43146=CARTESIAN_POINT('Ctrl Pts',(4.85884564037287,0.130123778861223,4.41359467981201));
#43147=CARTESIAN_POINT('Ctrl Pts',(4.88270355840429,-0.0839569802410516,
4.42537510794913));
#43148=CARTESIAN_POINT('Ctrl Pts',(4.90656147643571,-0.277507970732168,
4.33313973520738));
#43149=CARTESIAN_POINT('Ctrl Pts',(4.93041939446713,-0.403200703213916,
4.15944262266324));
#43150=CARTESIAN_POINT('Ctrl Pts',(4.95427731249855,-0.430299880793222,
3.94675744574809));
#43151=CARTESIAN_POINT('Ctrl Pts',(4.97813523052996,-0.352179016385168,
3.7470915236456));
#43152=CARTESIAN_POINT('Ctrl Pts',(5.00199314856139,-0.187940789307144,
3.60926861310034));
#43153=CARTESIAN_POINT('Ctrl Pts',(5.0258510665928,0.0222540801607904,3.56699016996131));
#43154=CARTESIAN_POINT('Ctrl Pts',(5.04970898462423,0.227007220840439,3.63059442521772));
#43155=CARTESIAN_POINT('Ctrl Pts',(5.07356690265564,0.376250912472057,3.7845284059142));
#43156=CARTESIAN_POINT('Ctrl Pts',(5.09742482068706,0.433491007135177,3.99115106069306));
#43157=CARTESIAN_POINT('Ctrl Pts',(5.12128273871848,0.384730742495793,4.19993752217271));
#43158=CARTESIAN_POINT('Ctrl Pts',(5.1451406567499,0.241893331461176,4.35983381329239));
#43159=CARTESIAN_POINT('Ctrl Pts',(5.16899857478132,0.0399064118422473,
4.43174093538579));
#43160=CARTESIAN_POINT('Ctrl Pts',(5.19285649281273,-0.171838712500945,
4.39807563839043));
#43161=CARTESIAN_POINT('Ctrl Pts',(5.21671441084416,-0.341564590845109,
4.26707000444592));
#43162=CARTESIAN_POINT('Ctrl Pts',(5.24057232887557,-0.427768622694993,
4.07075847957352));
#43163=CARTESIAN_POINT('Ctrl Pts',(5.264430246907,-0.409371574112622,3.85714457902312));
#43164=CARTESIAN_POINT('Ctrl Pts',(5.2882881649384,-0.290872024601924,3.6784627202051));
#43165=CARTESIAN_POINT('Ctrl Pts',(5.31214608296984,-0.101246341881189,
3.57840548479658));
#43166=CARTESIAN_POINT('Ctrl Pts',(5.33600400100125,0.113136829324483,3.58143959235932));
#43167=CARTESIAN_POINT('Ctrl Pts',(5.35986191903268,0.299854963974951,3.68682312094679));
#43168=CARTESIAN_POINT('Ctrl Pts',(5.38371983706408,0.413250392048343,3.8687869272297));
#43169=CARTESIAN_POINT('Ctrl Pts',(5.40757775509551,0.425594842551202,4.08283590397723));
#43170=CARTESIAN_POINT('Ctrl Pts',(5.43143567312693,0.333869761079625,4.27662924579771));
#43171=CARTESIAN_POINT('Ctrl Pts',(5.45529359115834,0.160504428594232,4.4027792017911));
#43172=CARTESIAN_POINT('Ctrl Pts',(5.47915150918977,-0.0521086087350157,
4.43043867146175));
#43173=CARTESIAN_POINT('Ctrl Pts',(5.50300942722118,-0.251979671819092,
4.35284416104532));
#43174=CARTESIAN_POINT('Ctrl Pts',(5.52686734525261,-0.390234841353927,
4.18896964197264));
#43175=CARTESIAN_POINT('Ctrl Pts',(5.55072526328402,-0.433066962396004,
3.97888689800548));
#43176=CARTESIAN_POINT('Ctrl Pts',(5.57458318131544,-0.370002414621403,
3.77396688259));
#43177=CARTESIAN_POINT('Ctrl Pts',(5.59844109934686,-0.21646219781534,3.62431812139094));
#43178=CARTESIAN_POINT('Ctrl Pts',(5.62229901737828,-0.00999107731853999,
3.56653381289738));
#43179=CARTESIAN_POINT('Ctrl Pts',(5.64615693540971,0.198923133709572,3.61474379450078));
#43180=CARTESIAN_POINT('Ctrl Pts',(5.67001485344111,0.359195220034686,3.75715941257656));
#43181=CARTESIAN_POINT('Ctrl Pts',(5.69387277147254,0.431634290692432,3.95895616900985));
#43182=CARTESIAN_POINT('Ctrl Pts',(5.71773068950395,0.398527019959163,4.1707892603438));
#43183=CARTESIAN_POINT('Ctrl Pts',(5.74158860753538,0.267969036875697,4.34085972491723));
#43184=CARTESIAN_POINT('Ctrl Pts',(5.76544652556679,0.0718853255354575,
4.42758070267197));
#43185=CARTESIAN_POINT('Ctrl Pts',(5.78930444359821,-0.141776307127955,
4.40974655013133));
#43186=CARTESIAN_POINT('Ctrl Pts',(5.81316236162963,-0.320769768688322,
4.29171820750724));
#43187=CARTESIAN_POINT('Ctrl Pts',(5.83702027966105,-0.421326288178809,
4.10235681181338));
#43188=CARTESIAN_POINT('Ctrl Pts',(5.86087819769247,-0.418857046020503,
3.88796639709818));
#43189=CARTESIAN_POINT('Ctrl Pts',(5.88473611572389,-0.313965860818636,
3.70097123187977));
#43190=CARTESIAN_POINT('Ctrl Pts',(5.90859403375531,-0.132301443679057,
3.58709678011166));
#43191=CARTESIAN_POINT('Ctrl Pts',(5.93245195178673,0.0817142298265842,
3.57418834816524));
#43192=CARTESIAN_POINT('Ctrl Pts',(5.95630986981814,0.275748643515392,3.66540258613358));
#43193=CARTESIAN_POINT('Ctrl Pts',(5.98016778784957,0.402354822815078,3.83843477537114));
#43194=CARTESIAN_POINT('Ctrl Pts',(6.00402570588098,0.430574627524036,4.05097449853386));
#43195=CARTESIAN_POINT('Ctrl Pts',(6.02788362391241,0.353506566116634,4.25104874587108));
#43196=CARTESIAN_POINT('Ctrl Pts',(6.05174154194382,0.189997730437525,4.38973628930191));
#43197=CARTESIAN_POINT('Ctrl Pts',(6.07559945997525,-0.0199730113800777,
4.43311976162365));
#43198=CARTESIAN_POINT('Ctrl Pts',(6.09945737800665,-0.2250554921608,4.3705991908187));
#43199=CARTESIAN_POINT('Ctrl Pts',(6.12331529603809,-0.375113923638194,
4.21744656883549));
#43200=CARTESIAN_POINT('Ctrl Pts',(6.1471732140695,-0.433431396087355,4.01114207710762));
#43201=CARTESIAN_POINT('Ctrl Pts',(6.17103113210093,-0.385792139046387,
3.80207577201042));
#43202=CARTESIAN_POINT('Ctrl Pts',(6.19488905013233,-0.243761337718234,
3.64147770828707));
#43203=CARTESIAN_POINT('Ctrl Pts',(6.21874696816376,-0.042227823444436,
3.56841523311022));
#43204=CARTESIAN_POINT('Ctrl Pts',(6.24260488619517,0.16982704650124,3.60113783246665));
#43205=CARTESIAN_POINT('Ctrl Pts',(6.2664628042266,0.339985970990829,3.73091992247201));
#43206=CARTESIAN_POINT('Ctrl Pts',(6.29032072225801,0.427700638223926,3.92738904240251));
#43207=CARTESIAN_POINT('Ctrl Pts',(6.31417864028943,0.409561128158778,4.13996490148311));
#43208=CARTESIAN_POINT('Ctrl Pts',(6.34598919766466,0.254661277208374,4.38159318714805));
#43209=CARTESIAN_POINT('Ctrl Pts',(6.38575239438369,-0.125272905304917,
4.47558432627151));
#43210=CARTESIAN_POINT('Ctrl Pts',(6.43346823044653,-0.468271923807345,
4.15124960425567));
#43211=CARTESIAN_POINT('Ctrl Pts',(6.48118406650937,-0.380227249479543,
3.6882349865083));
#43212=CARTESIAN_POINT('Ctrl Pts',(6.52889990257221,0.0564566449812287,
3.51140415777354));
#43213=CARTESIAN_POINT('Ctrl Pts',(6.57661573863504,0.441574375138847,3.78331933667001));
#43214=CARTESIAN_POINT('Ctrl Pts',(6.62433157469789,0.421040068198854,4.25418342072721));
#43215=CARTESIAN_POINT('Ctrl Pts',(6.67204741076071,0.0139362792425842,
4.49164405688148));
#43216=CARTESIAN_POINT('Ctrl Pts',(6.71976324682356,-0.406006764042365,
4.27761133505345));
#43217=CARTESIAN_POINT('Ctrl Pts',(6.76747908288639,-0.453085647428837,
3.80864864857145));
#43218=CARTESIAN_POINT('Ctrl Pts',(6.81519491894923,-0.0841006081168706,
3.51540431248109));
#43219=CARTESIAN_POINT('Ctrl Pts',(6.86291075501207,0.362121456530253,3.66717299786736));
#43220=CARTESIAN_POINT('Ctrl Pts',(6.91062659107491,0.475798562415156,4.124581128109));
#43221=CARTESIAN_POINT('Ctrl Pts',(6.95834242713775,0.152544250279933,4.46758486877347));
#43222=CARTESIAN_POINT('Ctrl Pts',(7.00605826320058,-0.310794706562241,
4.38119802990972));
#43223=CARTESIAN_POINT('Ctrl Pts',(7.05377409926342,-0.488725618924084,
3.94475128051735));
#43224=CARTESIAN_POINT('Ctrl Pts',(7.10148993532626,-0.21785253135038,3.55904022429238));
#43225=CARTESIAN_POINT('Ctrl Pts',(7.14920577138909,0.253078023397415,3.57826934481931));
#43226=CARTESIAN_POINT('Ctrl Pts',(7.19692160745195,0.491603063369337,3.98478019943955));
#43227=CARTESIAN_POINT('Ctrl Pts',(7.24463744351477,0.278681483980911,4.40526763942622));
#43228=CARTESIAN_POINT('Ctrl Pts',(7.29235327957762,-0.190157610347023,
4.45359156587464));
#43229=CARTESIAN_POINT('Ctrl Pts',(7.34006911564044,-0.484372034479295,
4.08537538031203));
#43230=CARTESIAN_POINT('Ctrl Pts',(7.3877849517033,-0.333780171974684,3.63875766810317));
#43231=CARTESIAN_POINT('Ctrl Pts',(7.43550078776612,0.123327161313159,3.52387434835784));
#43232=CARTESIAN_POINT('Ctrl Pts',(7.48321662382897,0.467181263150904,3.84622454030349));
#43233=CARTESIAN_POINT('Ctrl Pts',(7.5309324598918,0.382015623368301,4.30978910321172));
#43234=CARTESIAN_POINT('Ctrl Pts',(7.57864829595465,-0.0539608418635878,
4.4888695658253));
#43235=CARTESIAN_POINT('Ctrl Pts',(7.62636413201748,-0.440384235482588,
4.21901358396786));
#43236=CARTESIAN_POINT('Ctrl Pts',(7.67407996808031,-0.422396009600076,
3.7480340579683));
#43237=CARTESIAN_POINT('Ctrl Pts',(7.72179580414317,-0.0165150286377962,
3.50843873354525));
#43238=CARTESIAN_POINT('Ctrl Pts',(7.76951164020598,0.404531957204003,3.72025168374225));
#43239=CARTESIAN_POINT('Ctrl Pts',(7.81722747626884,0.454091022239626,4.18896181724392));
#43240=CARTESIAN_POINT('Ctrl Pts',(7.86494331233166,0.0866513144543145,
4.48414540641706));
#43241=CARTESIAN_POINT('Ctrl Pts',(7.91265914839452,-0.360361628691054,
4.33473081934393));
#43242=CARTESIAN_POINT('Ctrl Pts',(7.96037498445733,-0.476448943335793,
3.87792777037096));
#43243=CARTESIAN_POINT('Ctrl Pts',(8.0080908205202,-0.1550058622045,3.53322552818936));
#43244=CARTESIAN_POINT('Ctrl Pts',(8.05580665658301,0.308781487260178,3.61716946571973));
#43245=CARTESIAN_POINT('Ctrl Pts',(8.10352249264587,0.489010045760349,4.0526725734847));
#43246=CARTESIAN_POINT('Ctrl Pts',(8.1512383287087,0.220173154851853,4.43980564654689));
#43247=CARTESIAN_POINT('Ctrl Pts',(8.19895416477154,-0.250852131956433,
4.4230584271054));
#43248=CARTESIAN_POINT('Ctrl Pts',(8.24667000083438,-0.491516046133,4.01781014446235));
#43249=CARTESIAN_POINT('Ctrl Pts',(8.29438583689722,-0.280813212199106,
3.59620653211525));
#43250=CARTESIAN_POINT('Ctrl Pts',(8.34210167296004,0.187764715363875,3.54541267448783));
#43251=CARTESIAN_POINT('Ctrl Pts',(8.38981750902289,0.483915415676709,3.91207335260334));
#43252=CARTESIAN_POINT('Ctrl Pts',(8.43753334508573,0.335679143777854,4.35947842394856));
#43253=CARTESIAN_POINT('Ctrl Pts',(8.48524918114857,-0.120816450939738,
4.4767689272953));
#43254=CARTESIAN_POINT('Ctrl Pts',(8.5329650172114,-0.466364439759318,4.15623518867385));
#43255=CARTESIAN_POINT('Ctrl Pts',(8.58068085327425,-0.383642787608637,
3.69222827230584));
#43256=CARTESIAN_POINT('Ctrl Pts',(8.62839668933707,0.0513839395061145,
3.51085286915611));
#43257=CARTESIAN_POINT('Ctrl Pts',(8.67611252539993,0.439224004328866,3.77866880275638));
#43258=CARTESIAN_POINT('Ctrl Pts',(8.72382836146275,0.42371790764641,4.24973658040369));
#43259=CARTESIAN_POINT('Ctrl Pts',(8.7715441975256,0.0191051366342138,4.49146741357506));
#43260=CARTESIAN_POINT('Ctrl Pts',(8.81926003358843,-0.403052175319494,
4.28187615866228));
#43261=CARTESIAN_POINT('Ctrl Pts',(8.86697586965126,-0.455080472922433,
3.81343369002772));
#43262=CARTESIAN_POINT('Ctrl Pts',(8.91469170571412,-0.0892013699275644,
3.51631793453238));
#43263=CARTESIAN_POINT('Ctrl Pts',(8.96240754177693,0.358592723611288,3.66337486216116));
#43264=CARTESIAN_POINT('Ctrl Pts',(9.0101233778398,0.477085601399612,4.11955983351088));
#43265=CARTESIAN_POINT('Ctrl Pts',(9.05783921390261,0.157463430517111,4.46595117008304));
#43266=CARTESIAN_POINT('Ctrl Pts',(9.10555504996547,-0.306759831495564,
4.38445237758765));
#43267=CARTESIAN_POINT('Ctrl Pts',(9.1532708860283,-0.489280820139143,3.94990505119329));
#43268=CARTESIAN_POINT('Ctrl Pts',(9.20098672209113,-0.222487703095825,
3.56136068709803));
#43269=CARTESIAN_POINT('Ctrl Pts',(9.24870255815399,0.248619295113741,3.57562555337399));
#43270=CARTESIAN_POINT('Ctrl Pts',(9.29641839421681,0.49141536912078,3.97960000382683));
#43271=CARTESIAN_POINT('Ctrl Pts',(9.34413423027966,0.282937148266828,4.40230808465976));
#43272=CARTESIAN_POINT('Ctrl Pts',(9.39185006634249,-0.185366609388173,
4.45557046104408));
#43273=CARTESIAN_POINT('Ctrl Pts',(9.43956590240532,-0.483445357410111,
4.09047547319903));
#43274=CARTESIAN_POINT('Ctrl Pts',(9.48728173846818,-0.337568794959357,
3.64229546617122));
#43275=CARTESIAN_POINT('Ctrl Pts',(9.53499757453099,0.118302386066128,3.5226010365501));
#43276=CARTESIAN_POINT('Ctrl Pts',(9.58271341059386,0.465534665650901,3.84130942079228));
#43277=CARTESIAN_POINT('Ctrl Pts',(9.63042924665667,0.385259298596883,4.30574580568933));
#43278=CARTESIAN_POINT('Ctrl Pts',(9.67814508271952,-0.0488056103349303,
4.48941111271794));
#43279=CARTESIAN_POINT('Ctrl Pts',(9.72586091878235,-0.438051576325333,
4.22364266437974));
#43280=CARTESIAN_POINT('Ctrl Pts',(9.77357675484519,-0.425028039486299,
3.75249971615691));
#43281=CARTESIAN_POINT('Ctrl Pts',(9.82129259090803,-0.0216947140899849,
3.50864008686857));
#43282=CARTESIAN_POINT('Ctrl Pts',(9.86900842697087,0.401561201071248,3.7160038263529));
#43283=CARTESIAN_POINT('Ctrl Pts',(9.91672426303371,0.456057286475463,4.18416562194019));
#43284=CARTESIAN_POINT('Ctrl Pts',(9.96444009909655,0.0917489483659128,
4.48320529314746));
#43285=CARTESIAN_POINT('Ctrl Pts',(10.0121559351594,-0.356813860767086,
4.3385101085883));
#43286=CARTESIAN_POINT('Ctrl Pts',(10.0598717712222,-0.477709011270712,
3.88295588266498));
#43287=CARTESIAN_POINT('Ctrl Pts',(10.1075876072851,-0.159916626226494,
3.53488507064564));
#43288=CARTESIAN_POINT('Ctrl Pts',(10.1553034433479,0.304729657315094,3.61393645496551));
#43289=CARTESIAN_POINT('Ctrl Pts',(10.2030192794107,0.489538007675758,4.04751593304174));
#43290=CARTESIAN_POINT('Ctrl Pts',(10.2507351154736,0.224796073077312,4.43746079867915));
#43291=CARTESIAN_POINT('Ctrl Pts',(10.2984509515364,-0.246379554360218,
4.42567868168988));
#43292=CARTESIAN_POINT('Ctrl Pts',(10.3461667875993,-0.491301045992024,
4.02298928139638));
#43293=CARTESIAN_POINT('Ctrl Pts',(10.3938826236621,-0.285053227451061,
3.599188470261));
#43294=CARTESIAN_POINT('Ctrl Pts',(10.4415984597249,0.182963355965895,3.54345905416307));
#43295=CARTESIAN_POINT('Ctrl Pts',(10.4893142957878,0.482961874346273,3.9069782134126));
#43296=CARTESIAN_POINT('Ctrl Pts',(10.5370301318506,0.339449072190825,4.35592071060949));
#43297=CARTESIAN_POINT('Ctrl Pts',(10.5847459679134,-0.115785036052801,
4.47801574270962));
#43298=CARTESIAN_POINT('Ctrl Pts',(10.6324618039763,-0.464691964107356,
4.16114156306187));
#43299=CARTESIAN_POINT('Ctrl Pts',(10.6801776400391,-0.386865111317189,
3.69628860657276));
#43300=CARTESIAN_POINT('Ctrl Pts',(10.7278934761019,0.0462259258804368,
3.51033849586834));
#43301=CARTESIAN_POINT('Ctrl Pts',(10.7756093121648,0.436866984064762,3.77405207881873));
#43302=CARTESIAN_POINT('Ctrl Pts',(10.8233251482276,0.426326368719826,4.24525711444552));
#43303=CARTESIAN_POINT('Ctrl Pts',(10.8710409842905,0.0242836891050981,
4.49123876811122));
#43304=CARTESIAN_POINT('Ctrl Pts',(10.9187568203533,-0.400059075867425,
4.28610830234036));
#43305=CARTESIAN_POINT('Ctrl Pts',(10.9664726564161,-0.45702143577077,3.81824018018824));
#43306=CARTESIAN_POINT('Ctrl Pts',(11.014188492479,-0.0942939790271268,
3.51728489730359));
#43307=CARTESIAN_POINT('Ctrl Pts',(11.0619043285418,0.355025089556487,3.65961432075161));
#43308=CARTESIAN_POINT('Ctrl Pts',(11.1096201646047,0.478319155637209,4.11452515096033));
#43309=CARTESIAN_POINT('Ctrl Pts',(11.1573360006675,0.16236538121005,4.46426577284621));
#43310=CARTESIAN_POINT('Ctrl Pts',(11.2050518367304,-0.302691021094817,
4.38766399188028));
#43311=CARTESIAN_POINT('Ctrl Pts',(11.2527676727932,-0.489781601228288,
3.95506440219344));
#43312=CARTESIAN_POINT('Ctrl Pts',(11.300483508856,-0.227098200695192,3.56372986339542));
#43313=CARTESIAN_POINT('Ctrl Pts',(11.3481993449188,0.244132971891272,3.57302890392028));
#43314=CARTESIAN_POINT('Ctrl Pts',(11.3959151809817,0.491173079921361,3.97442207176994));
#43315=CARTESIAN_POINT('Ctrl Pts',(11.4436310170445,0.287161390990383,4.39930384468027));
#43316=CARTESIAN_POINT('Ctrl Pts',(11.4913468531074,-0.180555021833016,
4.45749875294131));
#43317=CARTESIAN_POINT('Ctrl Pts',(11.5390626891702,-0.482464979911041,
4.09556551685319));
#43318=CARTESIAN_POINT('Ctrl Pts',(11.586778525233,-0.341319923258817,3.64587299617429));
#43319=CARTESIAN_POINT('Ctrl Pts',(11.6344943612959,0.113264470804062,3.5213807520529));
#43320=CARTESIAN_POINT('Ctrl Pts',(11.6822101973587,0.463836358529674,3.83641192782507));
#43321=CARTESIAN_POINT('Ctrl Pts',(11.7299260334216,0.38846018117773,4.30166854740152));
#43322=CARTESIAN_POINT('Ctrl Pts',(11.7776418694844,-0.0436449577779122,
4.48989829813191));
#43323=CARTESIAN_POINT('Ctrl Pts',(11.8253577055472,-0.435670260442099,
4.22824690363353));
#43324=CARTESIAN_POINT('Ctrl Pts',(11.8730735416101,-0.427612859293677,
3.75699286549843));
#43325=CARTESIAN_POINT('Ctrl Pts',(11.9207893776729,-0.0268719897862959,
3.50889601812151));
#43326=CARTESIAN_POINT('Ctrl Pts',(11.9685052137357,0.398545841420554,3.71178751390968));
#43327=CARTESIAN_POINT('Ctrl Pts',(12.0162210497986,0.457972894034889,4.17934897039372));
#43328=CARTESIAN_POINT('Ctrl Pts',(12.0639368858614,0.0968363912382316,
4.48221150772657));
#43329=CARTESIAN_POINT('Ctrl Pts',(12.1116527219243,-0.353226459651896,
4.34225179773635));
#43330=CARTESIAN_POINT('Ctrl Pts',(12.1593685579871,-0.478916017555994,
3.88799699566402));
#43331=CARTESIAN_POINT('Ctrl Pts',(12.2070843940499,-0.164809627468288,
3.53659627586117));
#43332=CARTESIAN_POINT('Ctrl Pts',(12.2548002301128,0.300643979445627,3.61074632631782));
#43333=CARTESIAN_POINT('Ctrl Pts',(12.3025160661756,0.490011594032383,4.04235401475446));
#43334=CARTESIAN_POINT('Ctrl Pts',(12.3502319022385,0.229394022021679,4.43506735974179));
#43335=CARTESIAN_POINT('Ctrl Pts',(12.3979477383013,-0.241879610092261,
4.42825165390643));
#43336=CARTESIAN_POINT('Ctrl Pts',(12.4456635743641,-0.491031474462283,
4.0281658647901));
#43337=CARTESIAN_POINT('Ctrl Pts',(12.493379410427,-0.289261580343189,3.60221492864948));
#43338=CARTESIAN_POINT('Ctrl Pts',(12.5410952464898,0.178141673866572,3.54155614424011));
#43339=CARTESIAN_POINT('Ctrl Pts',(12.5888110825527,0.481954687902679,3.90189340664049));
#43340=CARTESIAN_POINT('Ctrl Pts',(12.6365269186155,0.343181296211668,4.35232346328687));
#43341=CARTESIAN_POINT('Ctrl Pts',(12.6842427546783,-0.110740760313508,
4.47920946240362));
#43342=CARTESIAN_POINT('Ctrl Pts',(12.7319585907412,-0.462967872677167,
4.16603003860975));
#43343=CARTESIAN_POINT('Ctrl Pts',(12.779674426804,-0.390044463885,3.70038267566003));
#43344=CARTESIAN_POINT('Ctrl Pts',(12.8273902628668,0.0410627776982723,
3.50987851185683));
#43345=CARTESIAN_POINT('Ctrl Pts',(12.8751060989297,0.434461438689172,3.76946045210395));
#43346=CARTESIAN_POINT('Ctrl Pts',(12.9228219349925,0.42888747548329,4.24075040649094));
#43347=CARTESIAN_POINT('Ctrl Pts',(12.9705377710553,0.0294595442590321,
4.49095555817611));
#43348=CARTESIAN_POINT('Ctrl Pts',(13.0182536071182,-0.397021539751646,
4.29030866646591));
#43349=CARTESIAN_POINT('Ctrl Pts',(13.065969443181,-0.458911634846768,3.82306685936703));
#43350=CARTESIAN_POINT('Ctrl Pts',(13.1136852792439,-0.0993761143989603,
3.51830547777773));
#43351=CARTESIAN_POINT('Ctrl Pts',(13.1614011153067,0.351418020999476,3.65589158776806));
#43352=CARTESIAN_POINT('Ctrl Pts',(13.2091169513695,0.479499580452807,4.10947774749948));
#43353=CARTESIAN_POINT('Ctrl Pts',(13.2568327874324,0.167249297126924,4.46252880717046));
#43354=CARTESIAN_POINT('Ctrl Pts',(13.3045486234952,-0.298588589211839,
4.39083254629632));
#43355=CARTESIAN_POINT('Ctrl Pts',(13.352264459558,-0.490227979701372,3.96022874442655));
#43356=CARTESIAN_POINT('Ctrl Pts',(13.3999802956209,-0.23168347330409,3.56614749850931));
#43357=CARTESIAN_POINT('Ctrl Pts',(13.4476961316837,0.239619531536799,3.57047968038978));
#43358=CARTESIAN_POINT('Ctrl Pts',(13.4954119677466,0.490876233547033,3.96924698078795));
#43359=CARTESIAN_POINT('Ctrl Pts',(13.5431278038094,0.291353737189313,4.39625525192456));
#43360=CARTESIAN_POINT('Ctrl Pts',(13.5908436398722,-0.175723379082843,
4.45937622804808));
#43361=CARTESIAN_POINT('Ctrl Pts',(13.6385594759351,-0.481431012491488,
4.10064494554323));
#43362=CARTESIAN_POINT('Ctrl Pts',(13.6862753119979,-0.345033139360895,
3.64948986092447));
#43363=CARTESIAN_POINT('Ctrl Pts',(13.7339911480608,0.108213974662067,3.52021363031051));
#43364=CARTESIAN_POINT('Ctrl Pts',(13.7817069841236,0.462086530666827,3.83153260544464));
#43365=CARTESIAN_POINT('Ctrl Pts',(13.8294228201864,0.391617915445045,4.297557781203));
#43366=CARTESIAN_POINT('Ctrl Pts',(13.8771386562493,-0.0384794573460961,
4.49033106796769));
#43367=CARTESIAN_POINT('Ctrl Pts',(13.9248544923121,-0.433240552373761,
4.23282579030437));
#43368=CARTESIAN_POINT('Ctrl Pts',(13.9725703283749,-0.430150181893835,
3.76151300691929));
#43369=CARTESIAN_POINT('Ctrl Pts',(14.0202861644378,-0.032046280669499,
3.50920649887429));
#43370=CARTESIAN_POINT('Ctrl Pts',(14.0680020005006,0.39548621318905,3.70760321474174));
#43371=CARTESIAN_POINT('Ctrl Pts',(14.1157178365634,0.459837632138507,4.1745123976147));
#43372=CARTESIAN_POINT('Ctrl Pts',(14.1634336726263,0.101913077983734,4.48116416053968));
#43373=CARTESIAN_POINT('Ctrl Pts',(14.2111495086891,-0.349599823817769,
4.34595547117883));
#43374=CARTESIAN_POINT('Ctrl Pts',(14.258865344752,-0.480069828122688,3.8930505494253));
#43375=CARTESIAN_POINT('Ctrl Pts',(14.3065811808148,-0.169684322438749,
3.53835895376334));
#43376=CARTESIAN_POINT('Ctrl Pts',(14.3542970168777,0.296524907469595,3.60759943412104));
#43377=CARTESIAN_POINT('Ctrl Pts',(14.4020128529405,0.49043075222644,4.0371873919842));
#43378=CARTESIAN_POINT('Ctrl Pts',(14.4497286890033,0.233966490966644,4.43262559558668));
#43379=CARTESIAN_POINT('Ctrl Pts',(14.4974445250662,-0.237352798985028,
4.43077705796148));
#43380=CARTESIAN_POINT('Ctrl Pts',(14.545160361129,-0.490707361486496,4.03333931965322));
#43381=CARTESIAN_POINT('Ctrl Pts',(14.5928761971918,-0.293437803431633,
3.60528557111603));
#43382=CARTESIAN_POINT('Ctrl Pts',(14.6405920332547,0.173300204635467,3.53970415608515));
#43383=CARTESIAN_POINT('Ctrl Pts',(14.6883078693175,0.480893968219416,3.89681949708321));
#43384=CARTESIAN_POINT('Ctrl Pts',(14.7360237053804,0.346875401282657,4.34868708154587));
#43385=CARTESIAN_POINT('Ctrl Pts',(14.7837395414432,-0.10568418401607,4.48034995378457));
#43386=CARTESIAN_POINT('Ctrl Pts',(14.831455377506,-0.461192356972643,4.17090007232882));
#43387=CARTESIAN_POINT('Ctrl Pts',(14.8791712135689,-0.393180492164677,
3.7045100248179));
#43388=CARTESIAN_POINT('Ctrl Pts',(14.9268870496317,0.0358950684576197,
3.50947296821438));
#43389=CARTESIAN_POINT('Ctrl Pts',(14.9746028856945,0.432007635398663,3.76489443262817));
#43390=CARTESIAN_POINT('Ctrl Pts',(15.0223187217574,0.431400943461215,4.23621695712364));
#43391=CARTESIAN_POINT('Ctrl Pts',(15.0700345578202,0.0346321271865876,
4.4906178152274));
#43392=CARTESIAN_POINT('Ctrl Pts',(15.1177503938831,-0.393939904367254,
4.2944767844824));
#43393=CARTESIAN_POINT('Ctrl Pts',(15.1654662299459,-0.46075086019608,3.82791319143947));
#43394=CARTESIAN_POINT('Ctrl Pts',(15.2131820660087,-0.104447211543591,
3.51937956259357));
#43395=CARTESIAN_POINT('Ctrl Pts',(15.2608979020716,0.347771918596306,3.652207076714));
#43396=CARTESIAN_POINT('Ctrl Pts',(15.3086137381344,0.480626744730421,4.10441818376995));
#43397=CARTESIAN_POINT('Ctrl Pts',(15.3563295741973,0.172114635785536,4.46074046598969));
#43398=CARTESIAN_POINT('Ctrl Pts',(15.4040454102601,-0.294452991525291,
4.39395768888776));
#43399=CARTESIAN_POINT('Ctrl Pts',(15.4517612463229,-0.490619905976795,
3.96539750426199));
#43400=CARTESIAN_POINT('Ctrl Pts',(15.4994770823858,-0.236243011612202,
3.56861332390027));
#43401=CARTESIAN_POINT('Ctrl Pts',(15.5471929184486,0.235079475381852,3.56797816593814));
#43402=CARTESIAN_POINT('Ctrl Pts',(15.5949087545115,0.490524862970081,3.9640753057054));
#43403=CARTESIAN_POINT('Ctrl Pts',(15.6426245905743,0.295513721197704,4.39316264501585));
#43404=CARTESIAN_POINT('Ctrl Pts',(15.6903404266371,-0.170872217813597,
4.46120267782338));
#43405=CARTESIAN_POINT('Ctrl Pts',(15.7380562626999,-0.480343569999647,
4.1057131950703));
#43406=CARTESIAN_POINT('Ctrl Pts',(15.7857720987628,-0.348708030819167,
3.6531456586776));
#43407=CARTESIAN_POINT('Ctrl Pts',(15.8334879348256,0.103151458625294,3.5190998009613));
#43408=CARTESIAN_POINT('Ctrl Pts',(15.8812037708885,0.460285376424935,3.82667199562295));
#43409=CARTESIAN_POINT('Ctrl Pts',(15.9289196069513,0.39473215065269,4.29341396369818));
#43410=CARTESIAN_POINT('Ctrl Pts',(15.9766354430142,-0.033309682798763,
4.49070937415524));
#43411=CARTESIAN_POINT('Ctrl Pts',(16.024351279077,-0.430762722000766,4.23737881579128));
#43412=CARTESIAN_POINT('Ctrl Pts',(16.0720671151398,-0.432639725453012,
3.76605963834362));
#43413=CARTESIAN_POINT('Ctrl Pts',(16.1197829512026,-0.0372170120039125,
3.50957149464017));
#43414=CARTESIAN_POINT('Ctrl Pts',(16.1674987872655,0.392382656225717,3.70345139362117));
#43415=CARTESIAN_POINT('Ctrl Pts',(16.2152146233283,0.461651293660056,4.16965644082667));
#43416=CARTESIAN_POINT('Ctrl Pts',(16.2629304593912,0.106978444708158,4.48006336792116));
#43417=CARTESIAN_POINT('Ctrl Pts',(16.310646295454,-0.345934356094203,4.34962071752925));
#43418=CARTESIAN_POINT('Ctrl Pts',(16.3583621315169,-0.481170314810987,
3.89811598262401));
#43419=CARTESIAN_POINT('Ctrl Pts',(16.4060779675797,-0.174540169679895,
3.54017290856226));
#43420=CARTESIAN_POINT('Ctrl Pts',(16.4537938036425,0.292372898913969,3.60449612791703));
#43421=CARTESIAN_POINT('Ctrl Pts',(16.5015096397054,0.490795435699827,4.0320166386149));
#43422=CARTESIAN_POINT('Ctrl Pts',(16.5492254757682,0.238512972024049,4.4301357774334));
#43423=CARTESIAN_POINT('Ctrl Pts',(16.596941311831,-0.23279962385521,4.43325461334514));
#43424=CARTESIAN_POINT('Ctrl Pts',(16.6446571478939,-0.490328743065594,
4.03850907134293));
#43425=CARTESIAN_POINT('Ctrl Pts',(16.6923729839567,-0.297581432841348,
3.60840005658827));
#43426=CARTESIAN_POINT('Ctrl Pts',(16.7400888200196,0.168439486040012,3.53790329540825));
#43427=CARTESIAN_POINT('Ctrl Pts',(16.7878046560824,0.479779833116189,3.89175704832657));
#43428=CARTESIAN_POINT('Ctrl Pts',(16.8355204921452,0.350530977080134,4.3450119692985));
#43429=CARTESIAN_POINT('Ctrl Pts',(16.8832363282081,-0.100615868820984,
4.4814370901721));
#43430=CARTESIAN_POINT('Ctrl Pts',(16.9309521642709,-0.459365614209645,
4.17575112327883));
#43431=CARTESIAN_POINT('Ctrl Pts',(16.9786680003337,-0.396272847821079,
3.70867019559999));
#43432=CARTESIAN_POINT('Ctrl Pts',(17.0263838363966,0.0307233721630972,
3.5091219099869));
#43433=CARTESIAN_POINT('Ctrl Pts',(17.0740996724594,0.429505846750062,3.76035452756312));
#43434=CARTESIAN_POINT('Ctrl Pts',(17.1218155085223,0.433866493469502,4.23165726989771));
#43435=CARTESIAN_POINT('Ctrl Pts',(17.1695313445851,0.039800863341802,4.49022557677993));
#43436=CARTESIAN_POINT('Ctrl Pts',(17.217247180648,-0.390814512007675,4.29861219341511));
#43437=CARTESIAN_POINT('Ctrl Pts',(17.2649630167107,-0.462538907526291,
3.83277863809798));
#43438=CARTESIAN_POINT('Ctrl Pts',(17.3126788527736,-0.109506707187599,
3.52050703244687));
#43439=CARTESIAN_POINT('Ctrl Pts',(17.3603946888365,0.344087187338735,3.64856119684745));
#43440=CARTESIAN_POINT('Ctrl Pts',(17.4081105248993,0.481700523269991,4.09934702176407));
#43441=CARTESIAN_POINT('Ctrl Pts',(17.4558263609621,0.176960856767158,4.45890094794434));
#43442=CARTESIAN_POINT('Ctrl Pts',(17.503542197025,-0.290284687397741,4.39703907252861));
#43443=CARTESIAN_POINT('Ctrl Pts',(17.5512580330878,-0.490957336521241,
3.97057010757845));
#43444=CARTESIAN_POINT('Ctrl Pts',(17.5989738691507,-0.240776309167652,
3.57112706567612));
#43445=CARTESIAN_POINT('Ctrl Pts',(17.6466897052135,0.230513307714322,3.56552463842171));
#43446=CARTESIAN_POINT('Ctrl Pts',(17.6944055412763,0.490119007219086,3.95890762096741));
#43447=CARTESIAN_POINT('Ctrl Pts',(17.7421213773392,0.299640880944266,4.39002636746625));
#43448=CARTESIAN_POINT('Ctrl Pts',(17.789837213402,-0.166002076869247,4.46297789939377));
#43449=CARTESIAN_POINT('Ctrl Pts',(17.8375530494648,-0.479202773223469,
4.11076970247734));
#43450=CARTESIAN_POINT('Ctrl Pts',(17.8852688855277,-0.352344189444135,
3.65683998336499));
#43451=CARTESIAN_POINT('Ctrl Pts',(17.9329847215905,0.0980774850139738,
3.51803938772416));
#43452=CARTESIAN_POINT('Ctrl Pts',(17.9807005576534,0.458433095867658,3.82183063825345));
#43453=CARTESIAN_POINT('Ctrl Pts',(18.0284163937162,0.397802540886209,4.28923755516265));
#43454=CARTESIAN_POINT('Ctrl Pts',(18.076132229779,-0.0281362083699241,
4.49103317467411));
#43455=CARTESIAN_POINT('Ctrl Pts',(18.1238480658419,-0.428237044548737,
4.24190547436581));
#43456=CARTESIAN_POINT('Ctrl Pts',(18.1715639019047,-0.435081213444543,
3.7706322547532));
#43457=CARTESIAN_POINT('Ctrl Pts',(18.2192797379675,-0.0423836094492617,
3.50999096487715));
#43458=CARTESIAN_POINT('Ctrl Pts',(18.2669955740304,0.389235515258945,3.69933251171255));
#43459=CARTESIAN_POINT('Ctrl Pts',(18.3147114100932,0.463413677146622,4.16478163940629));
#43460=CARTESIAN_POINT('Ctrl Pts',(18.3624272461561,0.112031928774586,4.4789092521418));
#43461=CARTESIAN_POINT('Ctrl Pts',(18.4101430822189,-0.342230463623947,
4.35324712966946));
#43462=CARTESIAN_POINT('Ctrl Pts',(18.4578589182817,-0.482217355384067,
3.90319273261591));
#43463=CARTESIAN_POINT('Ctrl Pts',(18.5055747543446,-0.179376629827252,
3.54203793877243));
#43464=CARTESIAN_POINT('Ctrl Pts',(18.5532905904074,0.288188414964166,3.60143675240633));
#43465=CARTESIAN_POINT('Ctrl Pts',(18.6010064264702,0.491105603945206,4.02684232898929));
#43466=CARTESIAN_POINT('Ctrl Pts',(18.6487222625331,0.243032960192409,4.42759818183915));
#43467=CARTESIAN_POINT('Ctrl Pts',(18.6964380985959,-0.228220590447982,
4.43568404486223));
#43468=CARTESIAN_POINT('Ctrl Pts',(18.7441539346588,-0.489895661254576,
4.0436745456279));
#43469=CARTESIAN_POINT('Ctrl Pts',(18.7918697707216,-0.301692008317894,
3.6115580391236));
#43470=CARTESIAN_POINT('Ctrl Pts',(18.8395856067845,0.163560057986223,3.53615376224111));
#43471=CARTESIAN_POINT('Ctrl Pts',(18.8873014428472,0.478612406344963,3.88670662268212));
#43472=CARTESIAN_POINT('Ctrl Pts',(18.9350172789101,0.35414761756175,4.34129853476112));
#43473=CARTESIAN_POINT('Ctrl Pts',(18.982733114973,-0.0955363776958117,
4.48247075080787));
#43474=CARTESIAN_POINT('Ctrl Pts',(19.0304489510358,-0.457487847288108,
4.18058265263639));
#43475=CARTESIAN_POINT('Ctrl Pts',(19.0781647870987,-0.399321187381313,
3.71286272589862));
#43476=CARTESIAN_POINT('Ctrl Pts',(19.1258806231614,0.0255482632835279,
3.50882537619781));
#43477=CARTESIAN_POINT('Ctrl Pts',(19.1735964592243,0.426956350589889,3.75584124112414));
#43478=CARTESIAN_POINT('Ctrl Pts',(19.2213122952871,0.436283851722622,4.22707185138688));
#43479=CARTESIAN_POINT('Ctrl Pts',(19.26902813135,0.0449651784623906,4.48977888620274));
#43480=CARTESIAN_POINT('Ctrl Pts',(19.3167439674128,-0.387645709555542,
4.3027144342981));
#43481=CARTESIAN_POINT('Ctrl Pts',(19.3644598034757,-0.464275578741542,
3.8376626582024));
#43482=CARTESIAN_POINT('Ctrl Pts',(19.4121756395385,-0.114554038379521,
3.52168776344319));
#43483=CARTESIAN_POINT('Ctrl Pts',(19.4598914756013,0.340364234683876,3.64495435060606));
#43484=CARTESIAN_POINT('Ctrl Pts',(19.5076073116642,0.482720800247919,4.09426482953845));
#43485=CARTESIAN_POINT('Ctrl Pts',(19.555323147727,0.181787415268628,4.45701044834135));
#43486=CARTESIAN_POINT('Ctrl Pts',(19.6030389837899,-0.28608412753634,4.40007637198121));
#43487=CARTESIAN_POINT('Ctrl Pts',(19.6507548198527,-0.491240257057309,
3.97574594767572));
#43488=CARTESIAN_POINT('Ctrl Pts',(19.6984706559155,-0.245282818621706,
3.57368850533185));
#43489=CARTESIAN_POINT('Ctrl Pts',(19.7461864919783,0.225921452997342,3.56311925573479));
#43490=CARTESIAN_POINT('Ctrl Pts',(19.7939023280412,0.489658867576397,3.95374471702426));
#43491=CARTESIAN_POINT('Ctrl Pts',(19.841618164104,0.303734463062876,4.38684635894002));
#43492=CARTESIAN_POINT('Ctrl Pts',(19.8893340001669,-0.161112940293692,
4.46470246728215));
#43493=CARTESIAN_POINT('Ctrl Pts',(19.9370498362297,-0.47800980043334,4.11581244897344));
#43494=CARTESIAN_POINT('Ctrl Pts',(19.9847656722926,-0.355939225796451,
3.66057517601247));
#43495=CARTESIAN_POINT('Ctrl Pts',(20.0324815083554,0.0929888682922082,
3.51702731322357));
#43496=CARTESIAN_POINT('Ctrl Pts',(20.0801973444182,0.456536973876988,3.81701888067549));
#43497=CARTESIAN_POINT('Ctrl Pts',(20.1279131804811,0.400815378068436,4.28501049648274));
#43498=CARTESIAN_POINT('Ctrl Pts',(20.1756290165439,-0.022934367574535,
4.49133741301101));
#43499=CARTESIAN_POINT('Ctrl Pts',(20.2233448526067,-0.425711472830213,
4.24633918020534));
#43500=CARTESIAN_POINT('Ctrl Pts',(20.2710606886696,-0.437384262562023,
3.77535541015343));
#43501=CARTESIAN_POINT('Ctrl Pts',(20.3187765247324,-0.0477164433392854,
3.51022640082505));
#43502=CARTESIAN_POINT('Ctrl Pts',(20.3664923607953,0.386374384143037,3.69571627142296));
#43503=CARTESIAN_POINT('Ctrl Pts',(20.4062555575143,0.45143962727185,4.08165775845481));
#43504=CARTESIAN_POINT('Ctrl Pts',(20.4380661148895,0.291471375703242,4.31996082336987));
#43505=CARTESIAN_POINT('Ctrl Pts',(20.461924032921,0.103697252552815,4.42124466395835));
#43506=CARTESIAN_POINT('Ctrl Pts',(20.4857819509523,-0.111451542568667,
4.41901444157942));
#43507=CARTESIAN_POINT('Ctrl Pts',(20.5096398689838,-0.298255971346869,
4.31460392554555));
#43508=CARTESIAN_POINT('Ctrl Pts',(20.5334977870152,-0.412709509332759,
4.13311446574462));
#43509=CARTESIAN_POINT('Ctrl Pts',(20.5573557050466,-0.425936384696969,
3.91915434697803));
#43510=CARTESIAN_POINT('Ctrl Pts',(20.581213623078,-0.335173342752607,3.72492109335083));
#43511=CARTESIAN_POINT('Ctrl Pts',(20.6050715411095,-0.162364888615448,
3.59797442377207));
#43512=CARTESIAN_POINT('Ctrl Pts',(20.6289294591408,0.0501004451364318,
3.56932214892951));
#43513=CARTESIAN_POINT('Ctrl Pts',(20.6527873771723,0.250339089241223,3.64598859455508));
#43514=CARTESIAN_POINT('Ctrl Pts',(20.6766452952037,0.389350172549011,3.80921715950176));
#43515=CARTESIAN_POINT('Ctrl Pts',(20.7005032132352,0.433161330121289,4.01909908002448));
#43516=CARTESIAN_POINT('Ctrl Pts',(20.7243611312665,0.371049143609512,4.22430982617278));
#43517=CARTESIAN_POINT('Ctrl Pts',(20.748219049298,0.218207240773441,4.37467120177868));
#43518=CARTESIAN_POINT('Ctrl Pts',(20.7720769673293,0.01200671405148,4.43341500212799));
#43519=CARTESIAN_POINT('Ctrl Pts',(20.7959348853608,-0.197129246586683,
4.38617716647524));
#43520=CARTESIAN_POINT('Ctrl Pts',(20.8197928033922,-0.358062019934396,
4.24450842127602));
#43521=CARTESIAN_POINT('Ctrl Pts',(20.8436507214237,-0.431438726014498,
4.04305074550709));
#43522=CARTESIAN_POINT('Ctrl Pts',(20.867508639455,-0.399316990859146,3.83106596928302));
#43523=CARTESIAN_POINT('Ctrl Pts',(20.8913665574865,-0.269551332195825,
3.66039017609669));
#43524=CARTESIAN_POINT('Ctrl Pts',(20.9152244755179,-0.0738730526583281,
3.57275822989076));
#43525=CARTESIAN_POINT('Ctrl Pts',(20.9390823935493,0.139869212314499,3.58959853735383));
#43526=CARTESIAN_POINT('Ctrl Pts',(20.9629403115807,0.319409638666883,3.70679317993256));
#43527=CARTESIAN_POINT('Ctrl Pts',(20.9867982296122,0.420845711130686,3.8956848776653));
#43528=CARTESIAN_POINT('Ctrl Pts',(21.0106561476436,0.419373541863394,4.11008446384341));
#43529=CARTESIAN_POINT('Ctrl Pts',(21.034514065675,0.315353119032788,4.29756540021079));
#43530=CARTESIAN_POINT('Ctrl Pts',(21.0583719837064,0.134220268060588,4.41228349058099));
#43531=CARTESIAN_POINT('Ctrl Pts',(21.0822299017379,-0.079733094278782,
4.42618703719455));
#43532=CARTESIAN_POINT('Ctrl Pts',(21.1060878197692,-0.274189543318984,
4.33587624407661));
#43533=CARTESIAN_POINT('Ctrl Pts',(21.1299457378007,-0.401599180171465,
4.16343456021562));
#43534=CARTESIAN_POINT('Ctrl Pts',(21.1538036558321,-0.430806878168669,
3.95102867450389));
#43535=CARTESIAN_POINT('Ctrl Pts',(21.1776615738635,-0.354670559489406,
3.75059761183336));
#43536=CARTESIAN_POINT('Ctrl Pts',(21.2015194918949,-0.191807627993766,
3.61115222665144));
#43537=CARTESIAN_POINT('Ctrl Pts',(21.2253774099264,0.0179574932869785,
3.56679071405539));
#43538=CARTESIAN_POINT('Ctrl Pts',(21.2492353279577,0.223331518303719,3.62836067225603));
#43539=CARTESIAN_POINT('Ctrl Pts',(21.2730932459892,0.374094903668402,3.78080656934254));
#43540=CARTESIAN_POINT('Ctrl Pts',(21.2969511640206,0.433381894944723,3.98685123093373));
#43541=CARTESIAN_POINT('Ctrl Pts',(21.320809082052,0.386695207821707,4.19611112472705));
#43542=CARTESIAN_POINT('Ctrl Pts',(21.3446670000834,0.245451009020076,4.35741650656472));
#43543=CARTESIAN_POINT('Ctrl Pts',(21.3685249181149,0.0441873525619181,
4.43132381671722));
#43544=CARTESIAN_POINT('Ctrl Pts',(21.3923828361462,-0.167881315237013,
4.39976070465745));
#43545=CARTESIAN_POINT('Ctrl Pts',(21.4162407541777,-0.338898428465248,
4.27044521104599));
#43546=CARTESIAN_POINT('Ctrl Pts',(21.4400986722091,-0.427045644525908,
4.07499849655415));
#43547=CARTESIAN_POINT('Ctrl Pts',(21.4639565902406,-0.410768568010174,
3.86121260673678));
#43548=CARTESIAN_POINT('Ctrl Pts',(21.4878145082719,-0.294047387504818,
3.68136401506497));
#43549=CARTESIAN_POINT('Ctrl Pts',(21.5116724263034,-0.105423611064507,
3.57943060117972));
#43550=CARTESIAN_POINT('Ctrl Pts',(21.5355303443348,0.108979109962582,3.58033786138646));
#43551=CARTESIAN_POINT('Ctrl Pts',(21.5593882623662,0.296733470072461,3.68386394585134));
#43552=CARTESIAN_POINT('Ctrl Pts',(21.5832461803976,0.411928413892185,3.86469390692879));
#43553=CARTESIAN_POINT('Ctrl Pts',(21.6071040984291,0.426395639810567,4.07860989342611));
#43554=CARTESIAN_POINT('Ctrl Pts',(21.6309620164605,0.33659751701124,4.27330361969026));
#43555=CARTESIAN_POINT('Ctrl Pts',(21.6548199344919,0.164492132570386,4.401167166299));
#43556=CARTESIAN_POINT('Ctrl Pts',(21.6786778525233,-0.0478360589596606,
4.43093441317345));
#43557=CARTESIAN_POINT('Ctrl Pts',(21.7025357705547,-0.248467031045983,
4.35532645760922));
#43558=CARTESIAN_POINT('Ctrl Pts',(21.7263936885861,-0.388341045935521,
4.1928315042612));
#43559=CARTESIAN_POINT('Ctrl Pts',(21.7502516066176,-0.433255096896122,
3.98318399549658));
#43560=CARTESIAN_POINT('Ctrl Pts',(21.774109524649,-0.372226475033738,3.77764845789182));
#43561=CARTESIAN_POINT('Ctrl Pts',(21.7979674426804,-0.220178340780001,
3.62648392906691));
#43562=CARTESIAN_POINT('Ctrl Pts',(21.8218253607118,-0.0142906046679706,
3.56665425395863));
#43563=CARTESIAN_POINT('Ctrl Pts',(21.8456832787432,0.195091573553633,3.61278941785858));
#43564=CARTESIAN_POINT('Ctrl Pts',(21.8695411967747,0.356768547853618,3.75360811649661));
#43565=CARTESIAN_POINT('Ctrl Pts',(21.8933991148061,0.431205894023261,3.95467634223136));
#43566=CARTESIAN_POINT('Ctrl Pts',(21.9172570328375,0.400201653291494,4.16682743688221));
#43567=CARTESIAN_POINT('Ctrl Pts',(21.941114950869,0.271337207055788,4.33818467892719));
#43568=CARTESIAN_POINT('Ctrl Pts',(21.9649728689003,0.0761234226178432,
4.4268465550088));
#43569=CARTESIAN_POINT('Ctrl Pts',(21.9888307869318,-0.137704612210607,
4.41113282132402));
#43570=CARTESIAN_POINT('Ctrl Pts',(22.0126887049632,-0.317860118355158,
4.29488591379237));
#43571=CARTESIAN_POINT('Ctrl Pts',(22.0365466229946,-0.420290167226249,
4.10653136780738));
#43572=CARTESIAN_POINT('Ctrl Pts',(22.060404541026,-0.419947821735935,3.89212700053744));
#43573=CARTESIAN_POINT('Ctrl Pts',(22.0842624590574,-0.316916794682727,
3.70410052003731));
#43574=CARTESIAN_POINT('Ctrl Pts',(22.1081203770888,-0.136390978688423,
3.58842952252864));
#43575=CARTESIAN_POINT('Ctrl Pts',(22.1319782951203,0.0774861468089536,
3.57339871771534));
#43576=CARTESIAN_POINT('Ctrl Pts',(22.1558362131517,0.27241579873489,3.66268354680831));
#43577=CARTESIAN_POINT('Ctrl Pts',(22.1796941311831,0.400732367405962,3.83445143701846));
#43578=CARTESIAN_POINT('Ctrl Pts',(22.2035520492145,0.431058956528623,4.04670046033727));
#43579=CARTESIAN_POINT('Ctrl Pts',(22.227409967246,0.355979888945518,4.24752994899471));
#43580=CARTESIAN_POINT('Ctrl Pts',(22.2512678852773,0.193854041863619,4.38783162256878));
#43581=CARTESIAN_POINT('Ctrl Pts',(22.2751258033088,-0.0156743990186396,
4.43329790005389));
#43582=CARTESIAN_POINT('Ctrl Pts',(22.2989837213402,-0.221370022215225,
4.37281103827166));
#43583=CARTESIAN_POINT('Ctrl Pts',(22.3228416393716,-0.372934645290675,
4.22116172228637));
#43584=CARTESIAN_POINT('Ctrl Pts',(22.346699557403,-0.43330658847365,4.01543234121164));
#43585=CARTESIAN_POINT('Ctrl Pts',(22.3705574754345,-0.387723268841402,
3.80592933171158));
#43586=CARTESIAN_POINT('Ctrl Pts',(22.3944153934659,-0.247331046528593,
3.64388188817752));
#43587=CARTESIAN_POINT('Ctrl Pts',(22.4182733114973,-0.0464596501027702,
3.56891502119853));
#43588=CARTESIAN_POINT('Ctrl Pts',(22.4421312295287,0.165772403721094,3.59936017830047));
#43589=CARTESIAN_POINT('Ctrl Pts',(22.4659891475602,0.337468575289321,3.7277726770023));
#43590=CARTESIAN_POINT('Ctrl Pts',(22.4898470655915,0.426644514167594,3.92275218663495));
#43591=CARTESIAN_POINT('Ctrl Pts',(22.513704983623,0.411494197867752,4.13662086224655));
#43592=CARTESIAN_POINT('Ctrl Pts',(22.5375629016544,0.295722435535401,4.31708206952049));
#43593=CARTESIAN_POINT('Ctrl Pts',(22.5614208196858,0.107638304484935,4.42000797176855));
#43594=CARTESIAN_POINT('Ctrl Pts',(22.5852787377172,-0.106765988085903,
4.42023067651324));
#43595=CARTESIAN_POINT('Ctrl Pts',(22.6091366557487,-0.295063722636797,
4.31769517074077));
#43596=CARTESIAN_POINT('Ctrl Pts',(22.6329945737801,-0.411209141905604,
4.13747522778479));
#43597=CARTESIAN_POINT('Ctrl Pts',(22.6568524918115,-0.426804986482714,
3.92363755172126));
#43598=CARTESIAN_POINT('Ctrl Pts',(22.6807104098429,-0.33803111495158,3.72847502015617));
#43599=CARTESIAN_POINT('Ctrl Pts',(22.7045683278743,-0.16660749730952,3.59970312177549));
#43600=CARTESIAN_POINT('Ctrl Pts',(22.7284262459057,0.0455714674079685,
3.56882345794434));
#43601=CARTESIAN_POINT('Ctrl Pts',(22.7522841639372,0.246577802732478,3.64336153500176));
#43602=CARTESIAN_POINT('Ctrl Pts',(22.7761420819686,0.387346815298129,3.80514019809748));
#43603=CARTESIAN_POINT('Ctrl Pts',(22.7920473606562,0.417963038852713,3.94471011778788));
#43604=CARTESIAN_POINT('Ctrl Pts',(22.8,0.415641328671541,4.01393920819689));
#43605=CARTESIAN_POINT('Ctrl Pts',(3.96816317011929,0.203757107801821,4.42939176513376));
#43606=CARTESIAN_POINT('Ctrl Pts',(3.9761158094631,0.132237748973037,4.46332948562603));
#43607=CARTESIAN_POINT('Ctrl Pts',(3.99202108815071,-0.0280119004087947,
4.49474661085258));
#43608=CARTESIAN_POINT('Ctrl Pts',(4.01587900618213,-0.261670681609628,
4.42079217330492));
#43609=CARTESIAN_POINT('Ctrl Pts',(4.03973692421355,-0.431283260509235,
4.24398813071681));
#43610=CARTESIAN_POINT('Ctrl Pts',(4.06359484224497,-0.495466080430727,
4.00749935521381));
#43611=CARTESIAN_POINT('Ctrl Pts',(4.08745276027639,-0.438477829352452,
3.76918881818141));
#43612=CARTESIAN_POINT('Ctrl Pts',(4.11131067830781,-0.274278321106756,
3.5873115455631));
#43613=CARTESIAN_POINT('Ctrl Pts',(4.13516859633923,-0.0430057845205295,
3.50635120590702));
#43614=CARTESIAN_POINT('Ctrl Pts',(4.15902651437064,0.198780450874126,3.54609966156282));
#43615=CARTESIAN_POINT('Ctrl Pts',(4.18288443240206,0.391960715466274,3.69684005745713));
#43616=CARTESIAN_POINT('Ctrl Pts',(4.20674235043348,0.489295238859844,3.92171081754005));
#43617=CARTESIAN_POINT('Ctrl Pts',(4.2306002684649,0.466984102771714,4.16572567991789));
#43618=CARTESIAN_POINT('Ctrl Pts',(4.25445818649632,0.330482445391075,4.36921595913043));
#43619=CARTESIAN_POINT('Ctrl Pts',(4.27831610452774,0.113168927396708,4.48242295331799));
#43620=CARTESIAN_POINT('Ctrl Pts',(4.30217402255916,-0.131817528672551,
4.47766435517297));
#43621=CARTESIAN_POINT('Ctrl Pts',(4.32603194059057,-0.344570980451485,
4.35610383169054));
#43622=CARTESIAN_POINT('Ctrl Pts',(4.349889858622,-0.473067456356951,4.14746621026076));
#43623=CARTESIAN_POINT('Ctrl Pts',(4.37374777665341,-0.485886045261059,
3.9027690893624));
#43624=CARTESIAN_POINT('Ctrl Pts',(4.39760569468484,-0.379892264971952,
3.68184757153936));
#43625=CARTESIAN_POINT('Ctrl Pts',(4.42146361271625,-0.181004475645389,
3.53872299041084));
#43626=CARTESIAN_POINT('Ctrl Pts',(4.44532153074767,0.0621438372772935,
3.50839320219298));
#43627=CARTESIAN_POINT('Ctrl Pts',(4.46917944877909,0.290096289836991,3.5982746675986));
#43628=CARTESIAN_POINT('Ctrl Pts',(4.49303736681051,0.447112297141319,3.78638891931142));
#43629=CARTESIAN_POINT('Ctrl Pts',(4.51689528484194,0.494797168872773,4.02673689903048));
#43630=CARTESIAN_POINT('Ctrl Pts',(4.54075320287334,0.421490654719143,4.26054697856981));
#43631=CARTESIAN_POINT('Ctrl Pts',(4.56461112090478,0.245118194360182,4.43064622472778));
#43632=CARTESIAN_POINT('Ctrl Pts',(4.58846903893618,0.00880765856895839,
4.49544073835303));
#43633=CARTESIAN_POINT('Ctrl Pts',(4.61232695696761,-0.229656589644598,
4.43908649592634));
#43634=CARTESIAN_POINT('Ctrl Pts',(4.63618487499902,-0.411963545977342,
4.2753636447643));
#43635=CARTESIAN_POINT('Ctrl Pts',(4.66004279303045,-0.493534193653132,
4.04430688170513));
#43636=CARTESIAN_POINT('Ctrl Pts',(4.68390071106186,-0.454422287381232,
3.80241587917234));
#43637=CARTESIAN_POINT('Ctrl Pts',(4.70775862909328,-0.304191753628974,
3.60883957626609));
#43638=CARTESIAN_POINT('Ctrl Pts',(4.7316165471247,-0.0795780500979935,
3.51091265195837));
#43639=CARTESIAN_POINT('Ctrl Pts',(4.75547446515612,0.164494654344808,3.53258090671894));
#43640=CARTESIAN_POINT('Ctrl Pts',(4.77933238318754,0.368343935055725,3.66854586202706));
#43641=CARTESIAN_POINT('Ctrl Pts',(4.80319030121895,0.482123090158262,3.88556038269908));
#43642=CARTESIAN_POINT('Ctrl Pts',(4.82704821925038,0.478010016947761,4.13055850707372));
#43643=CARTESIAN_POINT('Ctrl Pts',(4.85090613728179,0.357010473862124,4.34363152012653));
#43644=CARTESIAN_POINT('Ctrl Pts',(4.87476405531322,0.14871214514713,4.47267726617372));
#43645=CARTESIAN_POINT('Ctrl Pts',(4.89862197334463,-0.0959503538938319,
4.48614054517122));
#43646=CARTESIAN_POINT('Ctrl Pts',(4.92247989137606,-0.317150377772593,
4.38072921867179));
#43647=CARTESIAN_POINT('Ctrl Pts',(4.94633780940747,-0.460798495283114,
4.1822192273514));
#43648=CARTESIAN_POINT('Ctrl Pts',(4.97019572743889,-0.49176882879792,3.93915167139151));
#43649=CARTESIAN_POINT('Ctrl Pts',(4.99405364547031,-0.40248828815769,3.71096318925158));
#43650=CARTESIAN_POINT('Ctrl Pts',(5.01791156350173,-0.214788397502062,
3.55345208054429));
#43651=CARTESIAN_POINT('Ctrl Pts',(5.04176948153314,0.0254331070612992,
3.50513410186502));
#43652=CARTESIAN_POINT('Ctrl Pts',(5.06562739956457,0.259435524164246,3.57782431515618));
#43653=CARTESIAN_POINT('Ctrl Pts',(5.08948531759598,0.429998888727244,3.75374798322641));
#43654=CARTESIAN_POINT('Ctrl Pts',(5.11334323562741,0.495415812061873,3.98988697716804));
#43655=CARTESIAN_POINT('Ctrl Pts',(5.13720115365882,0.439690074491602,4.2284988806653));
#43656=CARTESIAN_POINT('Ctrl Pts',(5.16105907169025,0.276448136790977,4.41123658365534));
#43657=CARTESIAN_POINT('Ctrl Pts',(5.18491698972166,0.0456070993489057,
4.49341574008204));
#43658=CARTESIAN_POINT('Ctrl Pts',(5.20877490775308,-0.196386116196418,
4.45494130768376));
#43659=CARTESIAN_POINT('Ctrl Pts',(5.2326328257845,-0.390357576881318,4.3052213332044));
#43660=CARTESIAN_POINT('Ctrl Pts',(5.25649074381592,-0.488875976891831,
4.08086642869437));
#43661=CARTESIAN_POINT('Ctrl Pts',(5.28034866184734,-0.467850883838054,
3.83673747961128));
#43662=CARTESIAN_POINT('Ctrl Pts',(5.30420657987876,-0.332423505683668,
3.632530663945));
#43663=CARTESIAN_POINT('Ctrl Pts',(5.32806449791017,-0.115709525355139,
3.5181801106079));
#43664=CARTESIAN_POINT('Ctrl Pts',(5.3519224159416,0.129298585786916,3.52164764473745));
#43665=CARTESIAN_POINT('Ctrl Pts',(5.37578033397301,0.342689670681295,3.64208535978523));
#43666=CARTESIAN_POINT('Ctrl Pts',(5.39963825200445,0.472283796414913,3.85004295376459));
#43667=CARTESIAN_POINT('Ctrl Pts',(5.42349617003584,0.48639166917272,4.09466913029638));
#43668=CARTESIAN_POINT('Ctrl Pts',(5.44735408806728,0.381563529774833,4.31614612573549));
#43669=CARTESIAN_POINT('Ctrl Pts',(5.47121200609869,0.183432713764955,4.46031678178449));
#43670=CARTESIAN_POINT('Ctrl Pts',(5.49506992413012,-0.059552397366927,
4.49192744591021));
#43671=CARTESIAN_POINT('Ctrl Pts',(5.51892784216153,-0.287975325168481,
4.40324844967551));
#43672=CARTESIAN_POINT('Ctrl Pts',(5.54278576019295,-0.445980441674811,
4.21596422322942));
#43673=CARTESIAN_POINT('Ctrl Pts',(5.56664367822437,-0.494931191930538,
3.97587086145358));
#43674=CARTESIAN_POINT('Ctrl Pts',(5.59050159625579,-0.422857784100094,
3.74167773132221));
#43675=CARTESIAN_POINT('Ctrl Pts',(5.61435951428721,-0.247384129650275,
3.57065143242979));
#43676=CARTESIAN_POINT('Ctrl Pts',(5.63821743231862,-0.0114183168777074,
3.50461255354752));
#43677=CARTESIAN_POINT('Ctrl Pts',(5.66207535035005,0.227339585372105,3.55970939936999));
#43678=CARTESIAN_POINT('Ctrl Pts',(5.68593326838146,0.410506766445453,3.72246929038963));
#43679=CARTESIAN_POINT('Ctrl Pts',(5.70979118641288,0.493293861043031,3.9530929995654));
#43680=CARTESIAN_POINT('Ctrl Pts',(5.73364910444431,0.455457169749513,4.19518674831082));
#43681=CARTESIAN_POINT('Ctrl Pts',(5.75750702247572,0.306248793691327,4.38955201985635));
#43682=CARTESIAN_POINT('Ctrl Pts',(5.78136494050715,0.0821542461994931,
4.48866121222712));
#43683=CARTESIAN_POINT('Ctrl Pts',(5.80522285853855,-0.162029253596618,
4.46827942571263));
#43684=CARTESIAN_POINT('Ctrl Pts',(5.82908077656998,-0.366592184898752,
4.33339056701663));
#43685=CARTESIAN_POINT('Ctrl Pts',(5.85293869460139,-0.481513345756758,
4.11697862749145));
#43686=CARTESIAN_POINT('Ctrl Pts',(5.87679661263282,-0.478691368855474,
3.87196223809426));
#43687=CARTESIAN_POINT('Ctrl Pts',(5.90065453066423,-0.358816329143926,
3.65825454842257));
#43688=CARTESIAN_POINT('Ctrl Pts',(5.92451244869565,-0.151200892471453,
3.52811296978032));
#43689=CARTESIAN_POINT('Ctrl Pts',(5.94837036672708,0.093387223403125,3.5133605500302));
#43690=CARTESIAN_POINT('Ctrl Pts',(5.97222828475848,0.315139728168714,3.61760487120619));
#43691=CARTESIAN_POINT('Ctrl Pts',(5.99608620278992,0.459831779670103,3.81535495398299));
#43692=CARTESIAN_POINT('Ctrl Pts',(6.01994412082132,0.492082823488737,4.05825627791571));
#43693=CARTESIAN_POINT('Ctrl Pts',(6.04380203885276,0.404005480250355,4.28691141512903));
#43694=CARTESIAN_POINT('Ctrl Pts',(6.06765995688416,0.21713917558903,4.44541067075535));
#43695=CARTESIAN_POINT('Ctrl Pts',(6.09151787491559,-0.0228261843714051,
4.49499153360272));
#43696=CARTESIAN_POINT('Ctrl Pts',(6.11537579294701,-0.257204988275768,
4.42353981062321));
#43697=CARTESIAN_POINT('Ctrl Pts',(6.13923371097843,-0.428699479426561,
4.24850911946619));
#43698=CARTESIAN_POINT('Ctrl Pts',(6.16309162900984,-0.49534768549136,4.01273373861842));
#43699=CARTESIAN_POINT('Ctrl Pts',(6.18694954704127,-0.440903093044182,
3.77380201544612));
#43700=CARTESIAN_POINT('Ctrl Pts',(6.21080746507268,-0.278582990390117,
3.59026229064107));
#43701=CARTESIAN_POINT('Ctrl Pts',(6.23466538310411,-0.048260127889517,
3.50676273730504));
#43702=CARTESIAN_POINT('Ctrl Pts',(6.25852330113552,0.194087080856728,3.5441598063702));
#43703=CARTESIAN_POINT('Ctrl Pts',(6.28238121916694,0.388553448942855,3.69248145192407));
#43704=CARTESIAN_POINT('Ctrl Pts',(6.30623913719837,0.488798280742691,3.9170164641697));
#43705=CARTESIAN_POINT('Ctrl Pts',(6.33009705522977,0.468067515948433,4.15995908608738));
#43706=CARTESIAN_POINT('Ctrl Pts',(6.36190761260502,0.291040001689194,4.43610431491443));
#43707=CARTESIAN_POINT('Ctrl Pts',(6.40167080932402,-0.143168317426403,
4.54352222151223));
#43708=CARTESIAN_POINT('Ctrl Pts',(6.44938664538688,-0.535165231989368,
4.17285582464912));
#43709=CARTESIAN_POINT('Ctrl Pts',(6.49710248144971,-0.434543251113388,
3.64369891234367));
#43710=CARTESIAN_POINT('Ctrl Pts',(6.54481831751255,0.0645215567551043,
3.4416075490323));
#43711=CARTESIAN_POINT('Ctrl Pts',(6.59253415357539,0.504653900644641,3.75236619672659));
#43712=CARTESIAN_POINT('Ctrl Pts',(6.64024998963822,0.481186238846835,4.29049388273239));
#43713=CARTESIAN_POINT('Ctrl Pts',(6.68796582570107,0.01592709648968,4.56187610740764));
#43714=CARTESIAN_POINT('Ctrl Pts',(6.7356816617639,-0.464005405879062,4.31726850783359));
#43715=CARTESIAN_POINT('Ctrl Pts',(6.78339749782674,-0.517809574500644,
3.78131383674221));
#43716=CARTESIAN_POINT('Ctrl Pts',(6.83111333388957,-0.0961144992151805,
3.44617913151078));
#43717=CARTESIAN_POINT('Ctrl Pts',(6.87882916995242,0.413851019972934,3.61962818876606));
#43718=CARTESIAN_POINT('Ctrl Pts',(6.92654500601525,0.543767061592725,4.14237771887731));
#43719=CARTESIAN_POINT('Ctrl Pts',(6.97426084207809,0.174335412693353,4.53438003016987));
#43720=CARTESIAN_POINT('Ctrl Pts',(7.02197667814094,-0.355192171006393,
4.43565270890428));
#43721=CARTESIAN_POINT('Ctrl Pts',(7.06969251420376,-0.558540766450571,
3.93685892261342));
#43722=CARTESIAN_POINT('Ctrl Pts',(7.11740835026661,-0.248973074301851,
3.49604849518665));
#43723=CARTESIAN_POINT('Ctrl Pts',(7.16512418632944,0.289230577826905,3.51802452284194));
#43724=CARTESIAN_POINT('Ctrl Pts',(7.21284002239229,0.561829257914175,3.98260602935256));
#43725=CARTESIAN_POINT('Ctrl Pts',(7.26055585845511,0.318491529052478,4.46316069626365));
#43726=CARTESIAN_POINT('Ctrl Pts',(7.30827169451797,-0.217321894570402,
4.51838776411367));
#43727=CARTESIAN_POINT('Ctrl Pts',(7.35598753058078,-0.553565266295818,
4.09757137442565));
#43728=CARTESIAN_POINT('Ctrl Pts',(7.40370336664365,-0.381461142739227,
3.58715368886071));
#43729=CARTESIAN_POINT('Ctrl Pts',(7.45141920270646,0.140944621146953,3.45585912402047));
#43730=CARTESIAN_POINT('Ctrl Pts',(7.49913503876933,0.533918768911932,3.82425749787944));
#43731=CARTESIAN_POINT('Ctrl Pts',(7.54685087483214,0.436587096747522,4.3540429157916));
#43732=CARTESIAN_POINT('Ctrl Pts',(7.594566710895,-0.0616692246238245,4.5587052763707));
#43733=CARTESIAN_POINT('Ctrl Pts',(7.64228254695782,-0.503293747851232,
4.25029998493175));
#43734=CARTESIAN_POINT('Ctrl Pts',(7.68999838302067,-0.482735878399531,
3.7120403659385));
#43735=CARTESIAN_POINT('Ctrl Pts',(7.7377142190835,-0.0188742238918736,
3.43821850974892));
#43736=CARTESIAN_POINT('Ctrl Pts',(7.78543005514633,0.462319920793015,3.6802892401675));
#43737=CARTESIAN_POINT('Ctrl Pts',(7.83314589120918,0.518958568528469,4.21595528072725));
#43738=CARTESIAN_POINT('Ctrl Pts',(7.88086172727202,0.099029577569048,4.55330626409362));
#43739=CARTESIAN_POINT('Ctrl Pts',(7.92857756333485,-0.411839798232008,
4.38254759143289));
#43740=CARTESIAN_POINT('Ctrl Pts',(7.9762933993977,-0.544510350349916,3.86048957930736));
#43741=CARTESIAN_POINT('Ctrl Pts',(8.02400923546053,-0.177148669371157,
3.466546133148));
#43742=CARTESIAN_POINT('Ctrl Pts',(8.07172507152338,0.352891360472903,3.56248158116143));
#43743=CARTESIAN_POINT('Ctrl Pts',(8.1194409075862,0.558865824063627,4.06019692528064));
#43744=CARTESIAN_POINT('Ctrl Pts',(8.16715674364906,0.251625202160443,4.50263250666582));
#43745=CARTESIAN_POINT('Ctrl Pts',(8.21487257971187,-0.286686714637947,
4.48349292318459));
#43746=CARTESIAN_POINT('Ctrl Pts',(8.26258841577472,-0.561729810142263,
4.02035434884804));
#43747=CARTESIAN_POINT('Ctrl Pts',(8.31030425183756,-0.32092777766878,3.53852406277244));
#43748=CARTESIAN_POINT('Ctrl Pts',(8.3580200879004,0.21458717114652,3.4804742305729));
#43749=CARTESIAN_POINT('Ctrl Pts',(8.40573592396324,0.553043418849938,3.89951290636976));
#43750=CARTESIAN_POINT('Ctrl Pts',(8.45345176002607,0.383631385356639,4.41083042643994));
#43751=CARTESIAN_POINT('Ctrl Pts',(8.50116759608892,-0.13807525223727,4.54487604447167));
#43752=CARTESIAN_POINT('Ctrl Pts',(8.54888343215175,-0.532985261140852,
4.17855360686946));
#43753=CARTESIAN_POINT('Ctrl Pts',(8.59659926821459,-0.43844670370641,3.64826264467864));
#43754=CARTESIAN_POINT('Ctrl Pts',(8.64431510427743,0.0587242081113278,
3.4409775080543));
#43755=CARTESIAN_POINT('Ctrl Pts',(8.69203094034026,0.501967776032349,3.74705132745037));
#43756=CARTESIAN_POINT('Ctrl Pts',(8.73974677640311,0.484246611455832,4.28541180496438));
#43757=CARTESIAN_POINT('Ctrl Pts',(8.78746261246592,0.021834332487559,4.56167423035448));
#43758=CARTESIAN_POINT('Ctrl Pts',(8.83517844852879,-0.460628749968427,
4.32214256754115));
#43759=CARTESIAN_POINT('Ctrl Pts',(8.88289428459161,-0.520089363644054,
3.78678242815423));
#43760=CARTESIAN_POINT('Ctrl Pts',(8.93061012065447,-0.101943912081849,
3.44722326576734));
#43761=CARTESIAN_POINT('Ctrl Pts',(8.97832595671729,0.409818202553832,3.61528748398963));
#43762=CARTESIAN_POINT('Ctrl Pts',(9.02604179278014,0.545237955920739,4.1366391252272));
#43763=CARTESIAN_POINT('Ctrl Pts',(9.07375762884296,0.179957304801303,4.53251295530543));
#43764=CARTESIAN_POINT('Ctrl Pts',(9.12147346490582,-0.350580908316224,
4.43937194476168));
#43765=CARTESIAN_POINT('Ctrl Pts',(9.16918930096864,-0.559175278946307,
3.94274891673689));
#43766=CARTESIAN_POINT('Ctrl Pts',(9.21690513703149,-0.254270386902387,
3.49870043939378));
#43767=CARTESIAN_POINT('Ctrl Pts',(9.26462097309432,0.284134913886797,3.51500306204057));
#43768=CARTESIAN_POINT('Ctrl Pts',(9.31233680915716,0.56161475127612,3.97668583545263));
#43769=CARTESIAN_POINT('Ctrl Pts',(9.36005264522,0.323355121014866,4.45977836490307));
#43770=CARTESIAN_POINT('Ctrl Pts',(9.40776848128284,-0.211846492332409,
4.52064934726353));
#43771=CARTESIAN_POINT('Ctrl Pts',(9.45548431734568,-0.552506212093558,
4.10340002281193));
#43772=CARTESIAN_POINT('Ctrl Pts',(9.50320015340851,-0.385790975888367,
3.59119686639829));
#43773=CARTESIAN_POINT('Ctrl Pts',(9.55091598947136,0.135202049632292,3.45440391781584));
#43774=CARTESIAN_POINT('Ctrl Pts',(9.59863182553417,0.532036952624682,3.81864024657791));
#43775=CARTESIAN_POINT('Ctrl Pts',(9.64634766159704,0.440294135581046,4.34942202748599));
#43776=CARTESIAN_POINT('Ctrl Pts',(9.69406349765985,-0.0557775609627595,
4.55932418400469));
#43777=CARTESIAN_POINT('Ctrl Pts',(9.74177933372271,-0.500627865026369,
4.25559033604309));
#43778=CARTESIAN_POINT('Ctrl Pts',(9.78949516978553,-0.485743897486414,
3.71714394973028));
#43779=CARTESIAN_POINT('Ctrl Pts',(9.83721100584839,-0.0247938347541151,
3.43844862667992));
#43780=CARTESIAN_POINT('Ctrl Pts',(9.88492684191122,0.458924787935076,3.67543457032792));
#43781=CARTESIAN_POINT('Ctrl Pts',(9.93264267797406,0.521205716397956,4.21047394212484));
#43782=CARTESIAN_POINT('Ctrl Pts',(9.98035851403688,0.104855415711801,4.55223185431066));
#43783=CARTESIAN_POINT('Ctrl Pts',(10.0280743500997,-0.407785226630454,
4.3868667575037));
#43784=CARTESIAN_POINT('Ctrl Pts',(10.0757901861625,-0.54595042077573,3.86623596457089));
#43785=CARTESIAN_POINT('Ctrl Pts',(10.1235060222254,-0.182760942995651,
3.46844274359687));
#43786=CARTESIAN_POINT('Ctrl Pts',(10.1712218582882,0.34826072087591,3.55878673023755));
#43787=CARTESIAN_POINT('Ctrl Pts',(10.2189376943511,0.559469206087141,4.05430365143988));
#43788=CARTESIAN_POINT('Ctrl Pts',(10.2666535304139,0.256908510808291,4.49995269395588));
#43789=CARTESIAN_POINT('Ctrl Pts',(10.3143693664768,-0.281575222991369,
4.4864874848512));
#43790=CARTESIAN_POINT('Ctrl Pts',(10.3620852025396,-0.561484096926345,
4.02627333283551));
#43791=CARTESIAN_POINT('Ctrl Pts',(10.4098010386024,-0.325773485110519,
3.5419319750098));
#43792=CARTESIAN_POINT('Ctrl Pts',(10.4575168746653,0.209099930751681,3.47824153281512));
#43793=CARTESIAN_POINT('Ctrl Pts',(10.5052327107281,0.55195366278862,3.89368991932227));
#43794=CARTESIAN_POINT('Ctrl Pts',(10.552948546791,0.387939853388008,4.40676448870664));
#43795=CARTESIAN_POINT('Ctrl Pts',(10.6006643828538,-0.13232509260073,4.54630096923553));
#43796=CARTESIAN_POINT('Ctrl Pts',(10.6483802189166,-0.531073869970951,
4.18416086379456));
#43797=CARTESIAN_POINT('Ctrl Pts',(10.6960960549795,-0.442129340924997,
3.6529030034519));
#43798=CARTESIAN_POINT('Ctrl Pts',(10.7438118910423,0.0528293649267388,
3.44038965581316));
#43799=CARTESIAN_POINT('Ctrl Pts',(10.7915277271051,0.499274052081986,3.74177509795313));
#43800=CARTESIAN_POINT('Ctrl Pts',(10.839243563168,0.487227694891584,4.28029244094358));
#43801=CARTESIAN_POINT('Ctrl Pts',(10.8869593992308,0.0277526485205102,
4.56141292256198));
#43802=CARTESIAN_POINT('Ctrl Pts',(10.9346752352937,-0.457208082016334,
4.32697927894352));
#43803=CARTESIAN_POINT('Ctrl Pts',(10.9823910713565,-0.522307595786967,
3.79227553224832));
#43804=CARTESIAN_POINT('Ctrl Pts',(11.0301069074193,-0.107764007611043,
3.44832836054127));
#43805=CARTESIAN_POINT('Ctrl Pts',(11.0778227434822,0.405740926916492,3.61098974390844));
#43806=CARTESIAN_POINT('Ctrl Pts',(11.125538579545,0.54664772512998,4.13088523113667));
#43807=CARTESIAN_POINT('Ctrl Pts',(11.1732544156078,0.185559506100192,4.53058679668394));
#43808=CARTESIAN_POINT('Ctrl Pts',(11.2209702516707,-0.345930862581405,
4.4430423427091));
#43809=CARTESIAN_POINT('Ctrl Pts',(11.2686860877335,-0.559747597323992,
3.94864528834179));
#43810=CARTESIAN_POINT('Ctrl Pts',(11.3164019237964,-0.259539500620097,
3.50140805588402));
#43811=CARTESIAN_POINT('Ctrl Pts',(11.3641177598592,0.279007713031768,3.51203547753114));
#43812=CARTESIAN_POINT('Ctrl Pts',(11.411833595922,0.561337850721073,3.97076822846069));
#43813=CARTESIAN_POINT('Ctrl Pts',(11.4595494319849,0.328182802800164,4.45634496498341));
#43814=CARTESIAN_POINT('Ctrl Pts',(11.5072652680477,-0.206347562673641,
4.52285309839201));
#43815=CARTESIAN_POINT('Ctrl Pts',(11.5549811041106,-0.551385786278872,
4.10921718641821));
#43816=CARTESIAN_POINT('Ctrl Pts',(11.6026969401734,-0.390077958183356,
3.59528545163414));
#43817=CARTESIAN_POINT('Ctrl Pts',(11.6504127762362,0.129444461032819,3.45300931394821));
#43818=CARTESIAN_POINT('Ctrl Pts',(11.6981286122991,0.530096039923511,3.8130431397972));
#43819=CARTESIAN_POINT('Ctrl Pts',(11.7458444483619,0.443952268776438,4.34476232707146));
#43820=CARTESIAN_POINT('Ctrl Pts',(11.7935602844247,-0.0498797018717475,
4.55988096454574));
#43821=CARTESIAN_POINT('Ctrl Pts',(11.8412761204876,-0.497906374793238,
4.26085229740167));
#43822=CARTESIAN_POINT('Ctrl Pts',(11.8889919565504,-0.48869796246776,3.72227895182515));
#43823=CARTESIAN_POINT('Ctrl Pts',(11.9367077926133,-0.0307106916234339,
3.43874111807518));
#43824=CARTESIAN_POINT('Ctrl Pts',(11.9844236286761,0.455478679883424,3.67061595167475));
#43825=CARTESIAN_POINT('Ctrl Pts',(12.0321394647389,0.523394971212992,4.20496922507643));
#43826=CARTESIAN_POINT('Ctrl Pts',(12.0798553008018,0.110669607010866,4.5510961052335));
#43827=CARTESIAN_POINT('Ctrl Pts',(12.1275711368646,-0.403685360180124,
4.39114295225112));
#43828=CARTESIAN_POINT('Ctrl Pts',(12.1752869729274,-0.547329849620031,
3.8719972077086));
#43829=CARTESIAN_POINT('Ctrl Pts',(12.2230028089903,-0.188352916401613,
3.4703983969034));
#43830=CARTESIAN_POINT('Ctrl Pts',(12.2707186450531,0.34359139813055,3.55514088718992));
#43831=CARTESIAN_POINT('Ctrl Pts',(12.318434481116,0.560010444926212,4.04840434580723));
#43832=CARTESIAN_POINT('Ctrl Pts',(12.3661503171788,0.262163283277844,4.49721734887317));
#43833=CARTESIAN_POINT('Ctrl Pts',(12.4138661532417,-0.276432455305192,
4.48942800979656));
#43834=CARTESIAN_POINT('Ctrl Pts',(12.4615819893045,-0.561176016721412,
4.03218939850585));
#43835=CARTESIAN_POINT('Ctrl Pts',(12.5092978253673,-0.330583007179444,
3.54539076726965));
#43836=CARTESIAN_POINT('Ctrl Pts',(12.5570136614301,0.203589464528802,3.47606678951191));
#43837=CARTESIAN_POINT('Ctrl Pts',(12.604729497493,0.550802598333678,3.88787874069406));
#43838=CARTESIAN_POINT('Ctrl Pts',(12.6524453335558,0.392205230901379,4.40265336950419));
#43839=CARTESIAN_POINT('Ctrl Pts',(12.7001611696187,-0.126560234920843,
4.54766521348015));
#43840=CARTESIAN_POINT('Ctrl Pts',(12.7478770056815,-0.529103489635726,
4.18974766500481));
#43841=CARTESIAN_POINT('Ctrl Pts',(12.7955928417443,-0.44576286851447,3.65758191611243));
#43842=CARTESIAN_POINT('Ctrl Pts',(12.8433086778072,0.0469286537069902,
3.43986396243348));
#43843=CARTESIAN_POINT('Ctrl Pts',(12.89102451387,0.496524871139168,3.73652755085263));
#43844=CARTESIAN_POINT('Ctrl Pts',(12.9387403499328,0.490154659387074,4.27514194336855));
#43845=CARTESIAN_POINT('Ctrl Pts',(12.9864561859957,0.0336678819209607,
4.56108925568614));
#43846=CARTESIAN_POINT('Ctrl Pts',(13.0341720220585,-0.45373662956012,4.33177967103923));
#43847=CARTESIAN_POINT('Ctrl Pts',(13.0818878581214,-0.524467812480695,
3.79779170939055));
#43848=CARTESIAN_POINT('Ctrl Pts',(13.1296036941842,-0.113572133225654,
3.44949473238301));
#43849=CARTESIAN_POINT('Ctrl Pts',(13.177319530247,0.401618583502394,3.60673521324049));
#43850=CARTESIAN_POINT('Ctrl Pts',(13.2250353663099,0.547996775303968,4.12511679893576));
#43851=CARTESIAN_POINT('Ctrl Pts',(13.2727512023727,0.191141096329688,4.52860170299893));
#43852=CARTESIAN_POINT('Ctrl Pts',(13.3204670384356,-0.341242392487953,
4.4466635296155));
#43853=CARTESIAN_POINT('Ctrl Pts',(13.3681828744984,-0.560257741594785,
3.95454736418435));
#43854=CARTESIAN_POINT('Ctrl Pts',(13.4158987105612,-0.264779785921688,
3.5041710536014));
#43855=CARTESIAN_POINT('Ctrl Pts',(13.4636145466241,0.273849521323983,3.50912209380529));
#43856=CARTESIAN_POINT('Ctrl Pts',(13.5113303826869,0.560998599421335,3.96485386839523));
#43857=CARTESIAN_POINT('Ctrl Pts',(13.5590462187498,0.332974031597074,4.45286087643057));
#43858=CARTESIAN_POINT('Ctrl Pts',(13.6067620548126,-0.200825712906817,
4.52499877347948));
#43859=CARTESIAN_POINT('Ctrl Pts',(13.6544778908754,-0.550204115147588,
4.11502221869768));
#43860=CARTESIAN_POINT('Ctrl Pts',(13.7021937269383,-0.394321612469819,
3.5994189906415));
#43861=CARTESIAN_POINT('Ctrl Pts',(13.7499095630011,0.123672494356884,3.45167546721031));
#43862=CARTESIAN_POINT('Ctrl Pts',(13.7976253990639,0.528096246669736,3.80746679929733));
#43863=CARTESIAN_POINT('Ctrl Pts',(13.8453412351268,0.44756108986054,4.34006433209368));
#43864=CARTESIAN_POINT('Ctrl Pts',(13.8930570711896,-0.0439763023801491,
4.56037555616609));
#43865=CARTESIAN_POINT('Ctrl Pts',(13.9407729072525,-0.495129579482757,
4.26608528452492));
#43866=CARTESIAN_POINT('Ctrl Pts',(13.9884887433153,-0.491597745198497,
3.72744480185615));
#43867=CARTESIAN_POINT('Ctrl Pts',(14.0362045793781,-0.0366241372948624,
3.43909595144367));
#43868=CARTESIAN_POINT('Ctrl Pts',(14.083920415441,0.451981979421435,3.66583391943861));
#43869=CARTESIAN_POINT('Ctrl Pts',(14.1316362515038,0.525526089798339,4.19944174101915));
#43870=CARTESIAN_POINT('Ctrl Pts',(14.1793520875667,0.11647150565515,4.54989914301615));
#43871=CARTESIAN_POINT('Ctrl Pts',(14.2270679236295,-0.399540654275635,
4.39537570069553));
#43872=CARTESIAN_POINT('Ctrl Pts',(14.2747837596924,-0.548648483661927,
3.87777266878906));
#43873=CARTESIAN_POINT('Ctrl Pts',(14.3224995957551,-0.193923968459428,
3.47241287584284));
#43874=CARTESIAN_POINT('Ctrl Pts',(14.370215431818,0.338883910883161,3.5515444569815));
#43875=CARTESIAN_POINT('Ctrl Pts',(14.4179312678808,0.560489480462528,4.04249966364955));
#43876=CARTESIAN_POINT('Ctrl Pts',(14.4656471039437,0.267388935893957,4.49442677524682));
#43877=CARTESIAN_POINT('Ctrl Pts',(14.5133629400065,-0.271258982813659,
4.49231417140114));
#43878=CARTESIAN_POINT('Ctrl Pts',(14.5610787760694,-0.560805603747543,
4.03810188873054));
#43879=CARTESIAN_POINT('Ctrl Pts',(14.6087946121322,-0.335355809656676,
3.54890005536578));
#43880=CARTESIAN_POINT('Ctrl Pts',(14.656510448195,0.198056384554314,3.47395024222346));
#43881=CARTESIAN_POINT('Ctrl Pts',(14.7042262842579,0.549590353339887,3.88208001596329));
#43882=CARTESIAN_POINT('Ctrl Pts',(14.7519421203207,0.396427044118869,4.3984975254762));
#43883=CARTESIAN_POINT('Ctrl Pts',(14.7996579563836,-0.120781319530639,
4.54896862567174));
#43884=CARTESIAN_POINT('Ctrl Pts',(14.8473737924464,-0.527074338995675,
4.19531338994486));
#43885=CARTESIAN_POINT('Ctrl Pts',(14.8950896285092,-0.449346882879826,
3.66229886294881));
#43886=CARTESIAN_POINT('Ctrl Pts',(14.9428054645721,0.041022729875082,3.43940048630678));
#43887=CARTESIAN_POINT('Ctrl Pts',(14.9905213006349,0.493720538569869,3.73130926902151));
#43888=CARTESIAN_POINT('Ctrl Pts',(15.0382371366977,0.493027179828974,4.2699608843321));
#43889=CARTESIAN_POINT('Ctrl Pts',(15.0859529727606,0.0395793756528551,
4.56070326567839));
#43890=CARTESIAN_POINT('Ctrl Pts',(15.1336688088234,-0.450214778192253,
4.33654321062351));
#43891=CARTESIAN_POINT('Ctrl Pts',(15.1813846448863,-0.526569773778615,
3.80333034687015));
#43892=CARTESIAN_POINT('Ctrl Pts',(15.2291004809491,-0.119367643786657,
3.45072225173751));
#43893=CARTESIAN_POINT('Ctrl Pts',(15.2768163170119,0.397451630201876,3.60252436455885));
#43894=CARTESIAN_POINT('Ctrl Pts',(15.3245321530748,0.549284956596614,4.11933446935456));
#43895=CARTESIAN_POINT('Ctrl Pts',(15.3722479891376,0.196701455513243,4.52655789474516));
#43896=CARTESIAN_POINT('Ctrl Pts',(15.4199638252005,-0.336516018808871,
4.45023510325662));
#43897=CARTESIAN_POINT('Ctrl Pts',(15.4676796612633,-0.560705655094284,
3.96045448869));
#43898=CARTESIAN_POINT('Ctrl Pts',(15.5153954973261,-0.269990660741143,
3.50698912564524));
#43899=CARTESIAN_POINT('Ctrl Pts',(15.5631113333889,0.268660911710894,3.50626323446785));
#43900=CARTESIAN_POINT('Ctrl Pts',(15.6108271694518,0.560597035059331,3.95894341219528));
#43901=CARTESIAN_POINT('Ctrl Pts',(15.6585430055146,0.337728275218647,4.44932648624059));
#43902=CARTESIAN_POINT('Ctrl Pts',(15.7062588415775,-0.1952815563728,4.52708613419449));
#43903=CARTESIAN_POINT('Ctrl Pts',(15.7539746776403,-0.548961329954127,
4.12081447485494));
#43904=CARTESIAN_POINT('Ctrl Pts',(15.8016905137031,-0.398521467382777,
3.60359702428645));
#43905=CARTESIAN_POINT('Ctrl Pts',(15.849406349766,0.117886790727162,3.4504025257595));
#43906=CARTESIAN_POINT('Ctrl Pts',(15.8971221858288,0.526037794990907,3.80191184447176));
#43907=CARTESIAN_POINT('Ctrl Pts',(15.9448380218916,0.451120197982628,4.33532856438364));
#43908=CARTESIAN_POINT('Ctrl Pts',(15.9925538579545,-0.0380680182095728,
4.56080790392885));
#43909=CARTESIAN_POINT('Ctrl Pts',(16.0402696940173,-0.492297787528177,
4.27128871615743));
#43910=CARTESIAN_POINT('Ctrl Pts',(16.0879855300802,-0.494442923584513,
3.73264092602517));
#43911=CARTESIAN_POINT('Ctrl Pts',(16.135701366143,-0.0425335149309099,
3.43951308737216));
#43912=CARTESIAN_POINT('Ctrl Pts',(16.1834172022058,0.448435074945997,3.66108900478495));
#43913=CARTESIAN_POINT('Ctrl Pts',(16.2311330382687,0.52759883543946,4.19389210391969));
#43914=CARTESIAN_POINT('Ctrl Pts',(16.2788488743315,0.122260467197297,4.54864110061148));
#43915=CARTESIAN_POINT('Ctrl Pts',(16.3265647103944,-0.395351569291248,
4.39956453268331));
#43916=CARTESIAN_POINT('Ctrl Pts',(16.3742805464572,-0.549906176433804,
3.88356170630145));
#43917=CARTESIAN_POINT('Ctrl Pts',(16.42199638252,-0.199473480363076,3.47448595665642));
#43918=CARTESIAN_POINT('Ctrl Pts',(16.4697122185829,0.334138782019088,3.54799783908671));
#43919=CARTESIAN_POINT('Ctrl Pts',(16.5174280546457,0.560906259487099,4.0365902608309));
#43920=CARTESIAN_POINT('Ctrl Pts',(16.5651438907085,0.272584888215931,4.49158128304055));
#43921=CARTESIAN_POINT('Ctrl Pts',(16.6128597267714,-0.26605538016154,4.49514564908375));
#43922=CARTESIAN_POINT('Ctrl Pts',(16.6605755628342,-0.560372899148451,
4.04401014677825));
#43923=CARTESIAN_POINT('Ctrl Pts',(16.7082913988971,-0.340091362401967,
3.55245944950311));
#43924=CARTESIAN_POINT('Ctrl Pts',(16.7560072349599,0.19250130541649,3.4718921260458));
#43925=CARTESIAN_POINT('Ctrl Pts',(16.8037230710227,0.548317062457662,3.87629438922476));
#43926=CARTESIAN_POINT('Ctrl Pts',(16.8514389070856,0.400604824101502,4.39429741823411));
#43927=CARTESIAN_POINT('Ctrl Pts',(16.8991547431484,-0.114988988324618,
4.55021106103346));
#43928=CARTESIAN_POINT('Ctrl Pts',(16.9468705792113,-0.524986643439221,
4.20085742040038));
#43929=CARTESIAN_POINT('Ctrl Pts',(16.9945864152741,-0.45288098592576,3.66705332002498));
#43930=CARTESIAN_POINT('Ctrl Pts',(17.0423022513369,0.0351122494330066,
3.4389992789138));
#43931=CARTESIAN_POINT('Ctrl Pts',(17.0900180873998,0.490861365866046,3.72612083208173));
#43932=CARTESIAN_POINT('Ctrl Pts',(17.1377339234626,0.49584493715134,4.26474983932169));
#43933=CARTESIAN_POINT('Ctrl Pts',(17.1854497595254,0.0454864730955262,
4.56025499541263));
#43934=CARTESIAN_POINT('Ctrl Pts',(17.2331655955883,-0.446642919103261,
4.34126936858499));
#43935=CARTESIAN_POINT('Ctrl Pts',(17.2808814316511,-0.528613246204851,
3.80889082948154));
#43936=CARTESIAN_POINT('Ctrl Pts',(17.328597267714,-0.125149895556227,3.45201078225777));
#43937=CARTESIAN_POINT('Ctrl Pts',(17.3763131037768,0.393240529860342,3.59835766558462));
#43938=CARTESIAN_POINT('Ctrl Pts',(17.4240289398397,0.55051212592285,4.1135388846668));
#43939=CARTESIAN_POINT('Ctrl Pts',(17.4717447759024,0.202239966032548,4.52445559893916));
#43940=CARTESIAN_POINT('Ctrl Pts',(17.5194606119653,-0.331752266527324,
4.45375666691904));
#43941=CARTESIAN_POINT('Ctrl Pts',(17.5671764480281,-0.561091288070378,
3.96636600572338));
#43942=CARTESIAN_POINT('Ctrl Pts',(17.614892284091,-0.275171546279217,3.50986195899749));
#43943=CARTESIAN_POINT('Ctrl Pts',(17.6626081201538,0.263442460518632,3.50345921706735));
#43944=CARTESIAN_POINT('Ctrl Pts',(17.7103239562167,0.560133202238927,3.95303751636628));
#43945=CARTESIAN_POINT('Ctrl Pts',(17.7580397922795,0.342445005586054,4.44574218699675));
#43946=CARTESIAN_POINT('Ctrl Pts',(17.8057556283423,-0.189715708890181,
4.52911494868296));
#43947=CARTESIAN_POINT('Ctrl Pts',(17.8534714644052,-0.547657568741173,
4.12659331151364));
#43948=CARTESIAN_POINT('Ctrl Pts',(17.901187300468,-0.402677056422281,3.60781908849286));
#43949=CARTESIAN_POINT('Ctrl Pts',(17.9489031365308,0.112087992792125,3.44919063098808));
#43950=CARTESIAN_POINT('Ctrl Pts',(17.9966189725937,0.523920913530056,3.79637889233847));
#43951=CARTESIAN_POINT('Ctrl Pts',(18.0443348086565,0.454629197813879,4.33055554996792));
#43952=CARTESIAN_POINT('Ctrl Pts',(18.0920506447194,-0.0321555056241734,
4.56117795981091));
#43953=CARTESIAN_POINT('Ctrl Pts',(18.1397664807822,-0.489411313471489,
4.27646201432672));
#43954=CARTESIAN_POINT('Ctrl Pts',(18.1874823168451,-0.497233181596917,
3.73786674717144));
#43955=CARTESIAN_POINT('Ctrl Pts',(18.2351981529079,-0.0484381681459794,
3.43999247952716));
#43956=CARTESIAN_POINT('Ctrl Pts',(18.2829139889707,0.444838360430441,3.65638173475637));
#43957=CARTESIAN_POINT('Ctrl Pts',(18.3306298250336,0.529612977905601,4.18832093020544));
#43958=CARTESIAN_POINT('Ctrl Pts',(18.3783456610964,0.128035848626906,4.54732211775687));
#43959=CARTESIAN_POINT('Ctrl Pts',(18.4260614971592,-0.391118570530631,
4.40370898293889));
#43960=CARTESIAN_POINT('Ctrl Pts',(18.4737773332221,-0.551102788237131,
3.88936367722697));
#43961=CARTESIAN_POINT('Ctrl Pts',(18.5214931692849,-0.205000835699102,
3.47661740907615));
#43962=CARTESIAN_POINT('Ctrl Pts',(18.5692090053478,0.329356538604741,3.54450142744705));
#43963=CARTESIAN_POINT('Ctrl Pts',(18.6169248414106,0.561260735706054,4.03067679373969));
#43964=CARTESIAN_POINT('Ctrl Pts',(18.6646406774734,0.2777505631021,4.48868118831814));
#43965=CARTESIAN_POINT('Ctrl Pts',(18.7123565135363,-0.260822225340423,
4.49792212833724));
#43966=CARTESIAN_POINT('Ctrl Pts',(18.7600723495991,-0.559877950986752,
4.04991351638789));
#43967=CARTESIAN_POINT('Ctrl Pts',(18.8077881856619,-0.344789139412875,
3.55606855432066));
#43968=CARTESIAN_POINT('Ctrl Pts',(18.8555040217248,0.186924844147682,3.46989266958543));
#43969=CARTESIAN_POINT('Ctrl Pts',(18.9032198577876,0.546982867117114,3.87052250311704));
#43970=CARTESIAN_POINT('Ctrl Pts',(18.9509356938504,0.404738106803207,4.39005351430856));
#43971=CARTESIAN_POINT('Ctrl Pts',(18.9986515299133,-0.109183884691052,
4.55139238155646));
#43972=CARTESIAN_POINT('Ctrl Pts',(19.0463673659761,-0.522840634850846,
4.20637914057629));
#43973=CARTESIAN_POINT('Ctrl Pts',(19.094083202039,-0.456364785113784,3.67184475922049));
#43974=CARTESIAN_POINT('Ctrl Pts',(19.1417990381018,0.029197868913272,3.43866038485254));
#43975=CARTESIAN_POINT('Ctrl Pts',(19.1895148741647,0.487947670564988,3.72096281627648));
#43976=CARTESIAN_POINT('Ctrl Pts',(19.2372307102275,0.498607618457993,4.25950938727589));
#43977=CARTESIAN_POINT('Ctrl Pts',(19.2849465462903,0.0513885179525073,
4.55974449445321));
#43978=CARTESIAN_POINT('Ctrl Pts',(19.3326623823531,-0.44302144872845,4.34595762039384));
#43979=CARTESIAN_POINT('Ctrl Pts',(19.380378218416,-0.530598003365269,3.81447253878192));
#43980=CARTESIAN_POINT('Ctrl Pts',(19.4280940544788,-0.130918245164485,
3.45336018235082));
#43981=CARTESIAN_POINT('Ctrl Pts',(19.4758098905417,0.38898574814073,3.59423557624425));
#43982=CARTESIAN_POINT('Ctrl Pts',(19.5235257266045,0.551678150913516,4.10773069407674));
#43983=CARTESIAN_POINT('Ctrl Pts',(19.5712415626673,0.207756005258534,4.52229503878775));
#43984=CARTESIAN_POINT('Ctrl Pts',(19.6189573987302,-0.326951650734615,
4.4572278489044));
#43985=CARTESIAN_POINT('Ctrl Pts',(19.666673234793,-0.561414624206118,3.9722812219163));
#43986=CARTESIAN_POINT('Ctrl Pts',(19.7143890708559,-0.280321816997631,
3.51278930393937));
#43987=CARTESIAN_POINT('Ctrl Pts',(19.7621049069187,0.258194652845487,3.5007102220535));
#43988=CARTESIAN_POINT('Ctrl Pts',(19.8098207429815,0.559607330995945,3.94713708427543));
#43989=CARTESIAN_POINT('Ctrl Pts',(19.8575365790444,0.347123361713752,4.44210790974427));
#43990=CARTESIAN_POINT('Ctrl Pts',(19.9052524151072,-0.184128152223511,
4.53108587353909));
#43991=CARTESIAN_POINT('Ctrl Pts',(19.9529682511701,-0.546294178096705,
4.13235642149579));
#43992=CARTESIAN_POINT('Ctrl Pts',(20.0006840872329,-0.406785648814185,
3.61208785870539));
#43993=CARTESIAN_POINT('Ctrl Pts',(20.0483999232957,0.106272459957556,3.44803398021027));
#43994=CARTESIAN_POINT('Ctrl Pts',(20.0961157593586,0.5217539278249,3.7908797683689));
#43995=CARTESIAN_POINT('Ctrl Pts',(20.1438315954214,0.458072423058868,4.32572464996293));
#43996=CARTESIAN_POINT('Ctrl Pts',(20.1915474314842,-0.0262105744965466,
4.56152565902554));
#43997=CARTESIAN_POINT('Ctrl Pts',(20.2392632675471,-0.486524960252488,
4.28152908133109));
#43998=CARTESIAN_POINT('Ctrl Pts',(20.2869791036099,-0.499865224545849,
3.74326461201656));
#43999=CARTESIAN_POINT('Ctrl Pts',(20.3346949396728,-0.0545328049175168,
3.440261547834));
#44000=CARTESIAN_POINT('Ctrl Pts',(20.3824107757356,0.441568512678419,3.6522489094147));
#44001=CARTESIAN_POINT('Ctrl Pts',(20.4221739724547,0.515928418030698,4.09332268501583));
#44002=CARTESIAN_POINT('Ctrl Pts',(20.4539845298298,0.333108474939506,4.36566768059473));
#44003=CARTESIAN_POINT('Ctrl Pts',(20.4778424478613,0.118510552090848,4.48142006140068));
#44004=CARTESIAN_POINT('Ctrl Pts',(20.5017003658927,-0.127372553428812,
4.47887124859312));
#44005=CARTESIAN_POINT('Ctrl Pts',(20.5255582839241,-0.340862259689409,
4.35954554232165));
#44006=CARTESIAN_POINT('Ctrl Pts',(20.5494162019555,-0.471665647836603,
4.15213005589169));
#44007=CARTESIAN_POINT('Ctrl Pts',(20.5732741199869,-0.486782001098211,
3.90760543082941));
#44008=CARTESIAN_POINT('Ctrl Pts',(20.5971320380184,-0.38305332993788,3.68562568155832));
#44009=CARTESIAN_POINT('Ctrl Pts',(20.6209899560498,-0.185558943137764,
3.54054450025879));
#44010=CARTESIAN_POINT('Ctrl Pts',(20.6448478740812,0.0572573647513246,
3.50779920733485));
#44011=CARTESIAN_POINT('Ctrl Pts',(20.6687057921126,0.28610038304352,3.59541756340761));
#44012=CARTESIAN_POINT('Ctrl Pts',(20.6925637101441,0.444969396676924,3.78196356026503));
#44013=CARTESIAN_POINT('Ctrl Pts',(20.7164216281754,0.495039040219165,4.02182741068269));
#44014=CARTESIAN_POINT('Ctrl Pts',(20.7402795462069,0.424054039808096,4.25635280284423));
#44015=CARTESIAN_POINT('Ctrl Pts',(20.7641374642383,0.249378454468877,4.42819351412177));
#44016=CARTESIAN_POINT('Ctrl Pts',(20.7879953822697,0.0137218901755031,
4.49532894963167));
#44017=CARTESIAN_POINT('Ctrl Pts',(20.8118533003011,-0.22528943893053,4.44134312218709));
#44018=CARTESIAN_POINT('Ctrl Pts',(20.8357112183326,-0.409211687104306,
4.27943679589328));
#44019=CARTESIAN_POINT('Ctrl Pts',(20.859569136364,-0.493070359673604,4.04920060553547));
#44020=CARTESIAN_POINT('Ctrl Pts',(20.8834270543954,-0.456359989112496,
3.80693350349834));
#44021=CARTESIAN_POINT('Ctrl Pts',(20.9072849724268,-0.308057122141145,
3.61187643128937));
#44022=CARTESIAN_POINT('Ctrl Pts',(20.9311428904583,-0.0844259229598539,
3.51172613733272));
#44023=CARTESIAN_POINT('Ctrl Pts',(20.9550008084896,0.159849727585384,3.53097210659131));
#44024=CARTESIAN_POINT('Ctrl Pts',(20.9788587265211,0.365037758375503,3.66490817000854));
#44025=CARTESIAN_POINT('Ctrl Pts',(21.0027166445525,0.480964117596,3.88078331455297));
#44026=CARTESIAN_POINT('Ctrl Pts',(21.026574562584,0.479281646861755,4.12581018556955));
#44027=CARTESIAN_POINT('Ctrl Pts',(21.0504324806153,0.360401759160676,4.34007303948752));
#44028=CARTESIAN_POINT('Ctrl Pts',(21.0742903986468,0.153393823636192,4.47117877170218));
#44029=CARTESIAN_POINT('Ctrl Pts',(21.0981483166782,-0.0911230798336762,
4.48706845966041));
#44030=CARTESIAN_POINT('Ctrl Pts',(21.1220062347096,-0.313357908298923,
4.38385664171252));
#44031=CARTESIAN_POINT('Ctrl Pts',(21.145864152741,-0.458968192403581,4.18678141884249));
#44032=CARTESIAN_POINT('Ctrl Pts',(21.1697220707724,-0.492348251467217,
3.94403305123036));
#44033=CARTESIAN_POINT('Ctrl Pts',(21.1935799888039,-0.405335751726616,
3.71497012710753));
#44034=CARTESIAN_POINT('Ctrl Pts',(21.2174379068353,-0.21920761957706,3.55560477096155));
#44035=CARTESIAN_POINT('Ctrl Pts',(21.2412958248667,0.0205227466613194,
3.50490615340017));
#44036=CARTESIAN_POINT('Ctrl Pts',(21.2651537428981,0.255234742309135,3.57527146741714));
#44037=CARTESIAN_POINT('Ctrl Pts',(21.2890116609295,0.427534891009427,3.74949447702405));
#44038=CARTESIAN_POINT('Ctrl Pts',(21.312869578961,0.495291113040325,3.98497291063177));
#44039=CARTESIAN_POINT('Ctrl Pts',(21.3367274969923,0.441935166474334,4.22412587691986));
#44040=CARTESIAN_POINT('Ctrl Pts',(21.3605854150238,0.280514033632862,4.40847396123464));
#44041=CARTESIAN_POINT('Ctrl Pts',(21.3844433330552,0.0504995785194436,
4.49293903542029));
#44042=CARTESIAN_POINT('Ctrl Pts',(21.4083012510867,-0.191863399122956,
4.45686708805594));
#44043=CARTESIAN_POINT('Ctrl Pts',(21.432159169118,-0.387310549425693,4.3090786928523));
#44044=CARTESIAN_POINT('Ctrl Pts',(21.4560170871495,-0.488049720266331,
4.08571213811173));
#44045=CARTESIAN_POINT('Ctrl Pts',(21.4798750051809,-0.469447440294381,
3.84138663085107));
#44046=CARTESIAN_POINT('Ctrl Pts',(21.5037329232123,-0.336052473678932,
3.63584641288874));
#44047=CARTESIAN_POINT('Ctrl Pts',(21.5275908412437,-0.120483523363382,
3.51935166631968));
#44048=CARTESIAN_POINT('Ctrl Pts',(21.5514487592752,0.124546930319796,3.5203885299332));
#44049=CARTESIAN_POINT('Ctrl Pts',(21.5753066773065,0.339122266949511,3.63870346233219));
#44050=CARTESIAN_POINT('Ctrl Pts',(21.599164595338,0.470772971804989,3.84536523971104));
#44051=CARTESIAN_POINT('Ctrl Pts',(21.6230225133694,0.487306861455871,4.08983942814686));
#44052=CARTESIAN_POINT('Ctrl Pts',(21.6468804314008,0.384680949508402,4.31234542922385));
#44053=CARTESIAN_POINT('Ctrl Pts',(21.6707383494323,0.187990066907445,4.45847446473699));
#44054=CARTESIAN_POINT('Ctrl Pts',(21.6945962674636,-0.0546695077989956,
4.49249400502822));
#44055=CARTESIAN_POINT('Ctrl Pts',(21.7184541854951,-0.283960898681086,
4.40608534582272));
#44056=CARTESIAN_POINT('Ctrl Pts',(21.7423121035264,-0.443816114896065,
4.22037775802082));
#44057=CARTESIAN_POINT('Ctrl Pts',(21.766170021558,-0.495146201710716,3.98078180541326));
#44058=CARTESIAN_POINT('Ctrl Pts',(21.7900279395893,-0.425399554695369,
3.74588522487523));
#44059=CARTESIAN_POINT('Ctrl Pts',(21.8138858576208,-0.25163112890579,3.57312662880273));
#44060=CARTESIAN_POINT('Ctrl Pts',(21.8377437756521,-0.0163320378044167,
3.50475019978512));
#44061=CARTESIAN_POINT('Ctrl Pts',(21.8616016936836,0.222960681415914,3.55747583725374));
#44062=CARTESIAN_POINT('Ctrl Pts',(21.885459611715,0.407733440703041,3.71841068663001));
#44063=CARTESIAN_POINT('Ctrl Pts',(21.9093175297464,0.492804267302335,3.94820179346412));
#44064=CARTESIAN_POINT('Ctrl Pts',(21.9331754477779,0.457371026827486,4.19065897275109));
#44065=CARTESIAN_POINT('Ctrl Pts',(21.9570333658092,0.310098111756678,4.38649483975425));
#44066=CARTESIAN_POINT('Ctrl Pts',(21.9808912838407,0.0869977614584207,
4.48782219052945));
#44067=CARTESIAN_POINT('Ctrl Pts',(22.0047492018721,-0.15737591128791,4.46986372771052));
#44068=CARTESIAN_POINT('Ctrl Pts',(22.0286071199035,-0.363266886890503,
4.33701078463543));
#44069=CARTESIAN_POINT('Ctrl Pts',(22.0524650379349,-0.480329213457224,
4.12174952472744));
#44070=CARTESIAN_POINT('Ctrl Pts',(22.0763229559664,-0.479937963428243,
3.87671718963328));
#44071=CARTESIAN_POINT('Ctrl Pts',(22.1001808739978,-0.362188808094022,
3.66183085982978));
#44072=CARTESIAN_POINT('Ctrl Pts',(22.1240387920292,-0.155874623354616,
3.529636096341));
#44073=CARTESIAN_POINT('Ctrl Pts',(22.1478967100606,0.0885551527323001,
3.51245811975107));
#44074=CARTESIAN_POINT('Ctrl Pts',(22.1717546280921,0.311330781786364,3.61449741325855));
#44075=CARTESIAN_POINT('Ctrl Pts',(22.1956125461234,0.457977554205651,3.81080259009947));
#44076=CARTESIAN_POINT('Ctrl Pts',(22.2194704641549,0.492636339578261,4.05337168730347));
#44077=CARTESIAN_POINT('Ctrl Pts',(22.2433283821863,0.406832120751761,4.28288995313029));
#44078=CARTESIAN_POINT('Ctrl Pts',(22.2671863002177,0.22154636656941,4.44323391967918));
#44079=CARTESIAN_POINT('Ctrl Pts',(22.2910442182491,-0.0179135091400202,
4.49519511936025));
#44080=CARTESIAN_POINT('Ctrl Pts',(22.3149021362805,-0.2529930437236,4.42606762362056));
#44081=CARTESIAN_POINT('Ctrl Pts',(22.338760054312,-0.426208888077552,4.25275498785448));
#44082=CARTESIAN_POINT('Ctrl Pts',(22.3626179723434,-0.495205048933098,
4.01763687303198));
#44083=CARTESIAN_POINT('Ctrl Pts',(22.3864758903748,-0.443110087468167,
3.77820606161377));
#44084=CARTESIAN_POINT('Ctrl Pts',(22.4103338084062,-0.282662637164788,
3.59300991103726));
#44085=CARTESIAN_POINT('Ctrl Pts',(22.4341917264377,-0.0530964769854286,
3.50733392083031));
#44086=CARTESIAN_POINT('Ctrl Pts',(22.458049644469,0.189453226607198,3.5421282117862));
#44087=CARTESIAN_POINT('Ctrl Pts',(22.4819075625005,0.385676439696491,3.6888846179772));
#44088=CARTESIAN_POINT('Ctrl Pts',(22.5057654805319,0.487591287867653,3.9117172269821));
#44089=CARTESIAN_POINT('Ctrl Pts',(22.5296233985634,0.470276727405835,4.15613734610506));
#44090=CARTESIAN_POINT('Ctrl Pts',(22.5534813165947,0.337966804695391,4.36237769267677));
#44091=CARTESIAN_POINT('Ctrl Pts',(22.5773392346262,0.123014588878675,4.48000670597833));
#44092=CARTESIAN_POINT('Ctrl Pts',(22.6011971526576,-0.122017660845505,
4.48026122441149));
#44093=CARTESIAN_POINT('Ctrl Pts',(22.625055070689,-0.337213993725473,4.36307837627545));
#44094=CARTESIAN_POINT('Ctrl Pts',(22.6489129887204,-0.469950950795418,
4.15711375897153));
#44095=CARTESIAN_POINT('Ctrl Pts',(22.6727709067518,-0.487774683880463,
3.912729067726));
#44096=CARTESIAN_POINT('Ctrl Pts',(22.6966288247832,-0.386319338946922,
3.6896872918462));
#44097=CARTESIAN_POINT('Ctrl Pts',(22.7204867428147,-0.190407614498503,
3.54252014522276));
#44098=CARTESIAN_POINT('Ctrl Pts',(22.7443446608461,0.0520814161336476,
3.50722927763546));
#44099=CARTESIAN_POINT('Ctrl Pts',(22.7682025788775,0.281801791424649,3.59241522467272));
#44100=CARTESIAN_POINT('Ctrl Pts',(22.7920604969089,0.442679857002608,3.77730419914427));
#44101=CARTESIAN_POINT('Ctrl Pts',(22.8079657755965,0.477669651496365,3.93681187972983));
#44102=CARTESIAN_POINT('Ctrl Pts',(22.8159184149403,0.475016281724327,4.01593044384941));
#44103=CARTESIAN_POINT('Ctrl Pts',(3.98408158505964,0.229225853138217,4.48306385360099));
#44104=CARTESIAN_POINT('Ctrl Pts',(3.99203422440344,0.148766887950233,4.52124364039387));
#44105=CARTESIAN_POINT('Ctrl Pts',(4.00793950309106,-0.0315132651739855,
4.55658776856145));
#44106=CARTESIAN_POINT('Ctrl Pts',(4.03179742112247,-0.29437836981663,4.47338935048851));
#44107=CARTESIAN_POINT('Ctrl Pts',(4.0556553391539,-0.485191777607318,4.27448557757091));
#44108=CARTESIAN_POINT('Ctrl Pts',(4.07951325718531,-0.557397168683185,
4.00843674174317));
#44109=CARTESIAN_POINT('Ctrl Pts',(4.10337117521674,-0.493285636019562,
3.74033843218029));
#44110=CARTESIAN_POINT('Ctrl Pts',(4.12722909324815,-0.308561908987092,
3.53572729771651));
#44111=CARTESIAN_POINT('Ctrl Pts',(4.15108701127957,-0.0483813190761145,
3.44464727048097));
#44112=CARTESIAN_POINT('Ctrl Pts',(4.17494492931099,0.223627135909104,3.48936410886239));
#44113=CARTESIAN_POINT('Ctrl Pts',(4.19880284734241,0.440954086798485,3.65894639349553));
#44114=CARTESIAN_POINT('Ctrl Pts',(4.22266076537383,0.55045499896491,3.91192501290154));
#44115=CARTESIAN_POINT('Ctrl Pts',(4.24651868340524,0.525355068663259,4.18644066347397));
#44116=CARTESIAN_POINT('Ctrl Pts',(4.27037660143667,0.371791302444591,4.41536633561891));
#44117=CARTESIAN_POINT('Ctrl Pts',(4.29423451946808,0.127314547262185,4.54272370785395));
#44118=CARTESIAN_POINT('Ctrl Pts',(4.31809243749951,-0.14829414195428,4.5373703057994));
#44119=CARTESIAN_POINT('Ctrl Pts',(4.34195035553092,-0.387640842632661,
4.40061524972397));
#44120=CARTESIAN_POINT('Ctrl Pts',(4.36580827356235,-0.53219881478122,4.16589884014724));
#44121=CARTESIAN_POINT('Ctrl Pts',(4.38966619159376,-0.546619671109945,
3.89061565172978));
#44122=CARTESIAN_POINT('Ctrl Pts',(4.41352410962518,-0.427377132892538,
3.64207991255526));
#44123=CARTESIAN_POINT('Ctrl Pts',(4.4373820276566,-0.203629241694984,3.48106538615089));
#44124=CARTESIAN_POINT('Ctrl Pts',(4.46123994568802,0.0699115445388116,
3.44694450735191));
#44125=CARTESIAN_POINT('Ctrl Pts',(4.48509786371944,0.326357054473012,3.54806076195131));
#44126=CARTESIAN_POINT('Ctrl Pts',(4.50895578175085,0.502999374434197,3.7596884705576));
#44127=CARTESIAN_POINT('Ctrl Pts',(4.53281369978229,0.556644646112557,4.03007889421215));
#44128=CARTESIAN_POINT('Ctrl Pts',(4.55667161781369,0.474175139017821,4.29311420882242));
#44129=CARTESIAN_POINT('Ctrl Pts',(4.58052953584512,0.275756894216243,4.48447511514554));
#44130=CARTESIAN_POINT('Ctrl Pts',(4.60438745387653,0.00990857728296194,
4.55736865895685));
#44131=CARTESIAN_POINT('Ctrl Pts',(4.62824537190795,-0.258362656684952,
4.49397038324719));
#44132=CARTESIAN_POINT('Ctrl Pts',(4.65210328993938,-0.463457183444019,
4.30978289334447));
#44133=CARTESIAN_POINT('Ctrl Pts',(4.67596120797079,-0.555223804526532,
4.04984504770563));
#44134=CARTESIAN_POINT('Ctrl Pts',(4.69981912600221,-0.511223081411799,
3.77771873014923));
#44135=CARTESIAN_POINT('Ctrl Pts',(4.72367704403363,-0.342214389453536,
3.55994623789246));
#44136=CARTESIAN_POINT('Ctrl Pts',(4.74753496206505,-0.0895249575417115,
3.44977887729433));
#44137=CARTESIAN_POINT('Ctrl Pts',(4.77139288009647,0.185055765100279,3.47415556892044));
#44138=CARTESIAN_POINT('Ctrl Pts',(4.79525079812788,0.414385312357242,3.62711554766008));
#44139=CARTESIAN_POINT('Ctrl Pts',(4.81910871615931,0.542386363113676,3.87125593216545));
#44140=CARTESIAN_POINT('Ctrl Pts',(4.84296663419071,0.537759173780872,4.14687774817434));
#44141=CARTESIAN_POINT('Ctrl Pts',(4.86682455222215,0.401635218192884,4.38658395388507));
#44142=CARTESIAN_POINT('Ctrl Pts',(4.89068247025356,0.167300511433038,4.53175985253543));
#44143=CARTESIAN_POINT('Ctrl Pts',(4.91454038828499,-0.107943727546613,
4.54690598239331));
#44144=CARTESIAN_POINT('Ctrl Pts',(4.9383983063164,-0.356792784813018,4.42831870213619));
#44145=CARTESIAN_POINT('Ctrl Pts',(4.96225622434782,-0.518396287352312,
4.20499583203957));
#44146=CARTESIAN_POINT('Ctrl Pts',(4.98611414237924,-0.553237776802617,
3.93154589703492));
#44147=CARTESIAN_POINT('Ctrl Pts',(5.00997206041066,-0.452797559930213,
3.67483485485756));
#44148=CARTESIAN_POINT('Ctrl Pts',(5.03382997844208,-0.241636005696979,
3.49763554798826));
#44149=CARTESIAN_POINT('Ctrl Pts',(5.05768789647349,0.0286121339618079,
3.44327803376872));
#44150=CARTESIAN_POINT('Ctrl Pts',(5.08154581450492,0.291863827488053,3.52505420509465));
#44151=CARTESIAN_POINT('Ctrl Pts',(5.10540373253633,0.48374686498243,3.72296756053861));
#44152=CARTESIAN_POINT('Ctrl Pts',(5.12926165056775,0.557340616988569,3.98862289364304));
#44153=CARTESIAN_POINT('Ctrl Pts',(5.15311956859917,0.49464940648741,4.25706023915787));
#44154=CARTESIAN_POINT('Ctrl Pts',(5.17697748663059,0.311002942120779,4.46263935401832));
#44155=CARTESIAN_POINT('Ctrl Pts',(5.20083540466201,0.0513077868555636,
4.55509054477827));
#44156=CARTESIAN_POINT('Ctrl Pts',(5.22469332269342,-0.22093351989189,4.5118069769771));
#44157=CARTESIAN_POINT('Ctrl Pts',(5.24855124072485,-0.439150562917527,
4.34337266196288));
#44158=CARTESIAN_POINT('Ctrl Pts',(5.27240915875626,-0.549983331088669,
4.09097437781523));
#44159=CARTESIAN_POINT('Ctrl Pts',(5.29626707678769,-0.526330193563486,
3.81633038019944));
#44160=CARTESIAN_POINT('Ctrl Pts',(5.32012499481911,-0.373974986765411,
3.5865986076849));
#44161=CARTESIAN_POINT('Ctrl Pts',(5.34398291285052,-0.130172708829089,
3.45795473641922));
#44162=CARTESIAN_POINT('Ctrl Pts',(5.36784083088195,0.145460342249349,3.46185569711558));
#44163=CARTESIAN_POINT('Ctrl Pts',(5.39169874891335,0.385524377387638,3.59734759862366));
#44164=CARTESIAN_POINT('Ctrl Pts',(5.41555666694479,0.531317200781484,3.83129898029949));
#44165=CARTESIAN_POINT('Ctrl Pts',(5.4394145849762,0.547188495794237,4.10650235661553));
#44166=CARTESIAN_POINT('Ctrl Pts',(5.46327250300762,0.42925729847004,4.35566300567327));
#44167=CARTESIAN_POINT('Ctrl Pts',(5.48713042103904,0.206360998935678,4.51785436177788));
#44168=CARTESIAN_POINT('Ctrl Pts',(5.51098833907045,-0.0669961859988386,
4.55341622035867));
#44169=CARTESIAN_POINT('Ctrl Pts',(5.53484625710188,-0.323970978517869,
4.45365273830571));
#44170=CARTESIAN_POINT('Ctrl Pts',(5.55870417513329,-0.501726041995696,
4.2429588044862));
#44171=CARTESIAN_POINT('Ctrl Pts',(5.58256209316472,-0.556795421465071,
3.97285482490167));
#44172=CARTESIAN_POINT('Ctrl Pts',(5.60642001119613,-0.475713153578786,
3.70938858005442));
#44173=CARTESIAN_POINT('Ctrl Pts',(5.63027792922756,-0.27830606148521,3.51698474346866));
#44174=CARTESIAN_POINT('Ctrl Pts',(5.65413584725897,-0.0128455564368745,
3.44269129419766));
#44175=CARTESIAN_POINT('Ctrl Pts',(5.67799376529039,0.255756037034639,3.5046750042392));
#44176=CARTESIAN_POINT('Ctrl Pts',(5.70185168332181,0.46181831285622,3.68777916820271));
#44177=CARTESIAN_POINT('Ctrl Pts',(5.72570960135323,0.554953431393631,3.94722983012095));
#44178=CARTESIAN_POINT('Ctrl Pts',(5.74956751938465,0.512387319539865,4.21958423627784));
#44179=CARTESIAN_POINT('Ctrl Pts',(5.77342543741606,0.344528550506956,4.43824431479549));
#44180=CARTESIAN_POINT('Ctrl Pts',(5.79728335544749,0.0924231668635294,
4.54974172178225));
#44181=CARTESIAN_POINT('Ctrl Pts',(5.82114127347891,-0.182282200065281,
4.52681230129395));
#44182=CARTESIAN_POINT('Ctrl Pts',(5.84499919151032,-0.412414601109181,
4.37506292652603));
#44183=CARTESIAN_POINT('Ctrl Pts',(5.86885710954175,-0.541700403334708,
4.13160044316952));
#44184=CARTESIAN_POINT('Ctrl Pts',(5.89271502757316,-0.538525691690445,
3.85595807909033));
#44185=CARTESIAN_POINT('Ctrl Pts',(5.91657294560459,-0.403666797469215,
3.61553786496538));
#44186=CARTESIAN_POINT('Ctrl Pts',(5.94043086363599,-0.170100341263849,
3.46912915944898));
#44187=CARTESIAN_POINT('Ctrl Pts',(5.96428878166742,0.105060216979666,3.45253275189516));
#44188=CARTESIAN_POINT('Ctrl Pts',(5.98814669969884,0.354530812822036,3.5698071562788));
#44189=CARTESIAN_POINT('Ctrl Pts',(6.01200461773026,0.517308736525128,3.79227513259484));
#44190=CARTESIAN_POINT('Ctrl Pts',(6.03586253576167,0.553591019453439,4.06553805729756));
#44191=CARTESIAN_POINT('Ctrl Pts',(6.0597204537931,0.454504394384077,4.32277408438697));
#44192=CARTESIAN_POINT('Ctrl Pts',(6.08357837182452,0.244280620740535,4.50108505220882));
#44193=CARTESIAN_POINT('Ctrl Pts',(6.10743628985593,-0.0256793573627324,
4.55686330558177));
#44194=CARTESIAN_POINT('Ctrl Pts',(6.13129420788736,-0.289354484390735,
4.47648043042773));
#44195=CARTESIAN_POINT('Ctrl Pts',(6.15515212591877,-0.482285035214929,
4.27957167009689));
#44196=CARTESIAN_POINT('Ctrl Pts',(6.17901004395019,-0.557263974895364,
4.01432540012922));
#44197=CARTESIAN_POINT('Ctrl Pts',(6.20286796198161,-0.496014047041978,
3.74552825888183));
#44198=CARTESIAN_POINT('Ctrl Pts',(6.22672588001303,-0.313404643062,3.53904687299508));
#44199=CARTESIAN_POINT('Ctrl Pts',(6.25058379804445,-0.0542924323345977,
3.44511024149985));
#44200=CARTESIAN_POINT('Ctrl Pts',(6.27444171607587,0.218347115212216,3.48718178027374));
#44201=CARTESIAN_POINT('Ctrl Pts',(6.29829963410728,0.437120926894882,3.65404298137615));
#44202=CARTESIAN_POINT('Ctrl Pts',(6.32215755213871,0.549895923261456,3.90664388593688));
#44203=CARTESIAN_POINT('Ctrl Pts',(6.34601547017011,0.526573903738089,4.17995327069166));
#44204=CARTESIAN_POINT('Ctrl Pts',(6.37782602754536,0.327418726170013,4.4906154426808));
#44205=CARTESIAN_POINT('Ctrl Pts',(6.41758922426438,-0.161063729547888,
4.61146011675295));
#44206=CARTESIAN_POINT('Ctrl Pts',(6.46530506032721,-0.60205854017139,4.19446204504257));
#44207=CARTESIAN_POINT('Ctrl Pts',(6.51302089639007,-0.488859252747234,
3.59916283817905));
#44208=CARTESIAN_POINT('Ctrl Pts',(6.56073673245289,0.0725864685289804,
3.37181094029106));
#44209=CARTESIAN_POINT('Ctrl Pts',(6.60845256851574,0.567733426150434,3.72141305678318));
#44210=CARTESIAN_POINT('Ctrl Pts',(6.65616840457857,0.541332409494817,4.32680434473755));
#44211=CARTESIAN_POINT('Ctrl Pts',(6.70388424064141,0.0179179137367747,
4.6321081579338));
#44212=CARTESIAN_POINT('Ctrl Pts',(6.75160007670425,-0.522004047715759,
4.35692568061372));
#44213=CARTESIAN_POINT('Ctrl Pts',(6.79931591276708,-0.582533501572452,
3.75397902491298));
#44214=CARTESIAN_POINT('Ctrl Pts',(6.84703174882993,-0.10812839031349,3.37695395054049));
#44215=CARTESIAN_POINT('Ctrl Pts',(6.89474758489276,0.465580583415614,3.57208337966475));
#44216=CARTESIAN_POINT('Ctrl Pts',(6.9424634209556,0.611735560770294,4.16017430964564));
#44217=CARTESIAN_POINT('Ctrl Pts',(6.99017925701844,0.196126575106773,4.60117519156627));
#44218=CARTESIAN_POINT('Ctrl Pts',(7.03789509308127,-0.399589635450545,
4.49010738789885));
#44219=CARTESIAN_POINT('Ctrl Pts',(7.08561092914412,-0.628355913977057,
3.92896656470948));
#44220=CARTESIAN_POINT('Ctrl Pts',(7.13332676520695,-0.280093617253323,
3.43305676608093));
#44221=CARTESIAN_POINT('Ctrl Pts',(7.1810426012698,0.325383132256395,3.45777970086456));
#44222=CARTESIAN_POINT('Ctrl Pts',(7.22875843733263,0.632055452459012,3.98043185926557));
#44223=CARTESIAN_POINT('Ctrl Pts',(7.27647427339546,0.358301574124045,4.52105375310108));
#44224=CARTESIAN_POINT('Ctrl Pts',(7.32419010945831,-0.244486178793781,
4.58318396235269));
#44225=CARTESIAN_POINT('Ctrl Pts',(7.37190594552114,-0.622758498112341,
4.10976736853928));
#44226=CARTESIAN_POINT('Ctrl Pts',(7.41962178158399,-0.42914211350377,3.53554970961824));
#44227=CARTESIAN_POINT('Ctrl Pts',(7.46733761764681,0.158562080980748,3.38784389968312));
#44228=CARTESIAN_POINT('Ctrl Pts',(7.51505345370967,0.600656274672958,3.80229045545538));
#44229=CARTESIAN_POINT('Ctrl Pts',(7.56276928977248,0.491158570126743,4.3982967283715));
#44230=CARTESIAN_POINT('Ctrl Pts',(7.61048512583535,-0.0693776073840611,
4.62854098691609));
#44231=CARTESIAN_POINT('Ctrl Pts',(7.65820096189817,-0.566203260219877,
4.28158638589565));
#44232=CARTESIAN_POINT('Ctrl Pts',(7.70591679796101,-0.543075747198986,
3.67604667390869));
#44233=CARTESIAN_POINT('Ctrl Pts',(7.75363263402386,-0.0212334191459514,
3.36799828595259));
#44234=CARTESIAN_POINT('Ctrl Pts',(7.80134847008666,0.520107884382028,3.64032679659274));
#44235=CARTESIAN_POINT('Ctrl Pts',(7.84906430614954,0.583826114817312,4.24294874421058));
#44236=CARTESIAN_POINT('Ctrl Pts',(7.89678014221235,0.111407840683781,4.62246712177016));
#44237=CARTESIAN_POINT('Ctrl Pts',(7.94449597827521,-0.463317967772962,
4.43036436352186));
#44238=CARTESIAN_POINT('Ctrl Pts',(7.99221181433803,-0.612571757364041,
3.84305138824375));
#44239=CARTESIAN_POINT('Ctrl Pts',(8.03992765040088,-0.199291476537812,
3.39986673810663));
#44240=CARTESIAN_POINT('Ctrl Pts',(8.08764348646372,0.397001233685627,3.50779369660314));
#44241=CARTESIAN_POINT('Ctrl Pts',(8.13535932252656,0.628721602366905,4.06772127707659));
#44242=CARTESIAN_POINT('Ctrl Pts',(8.18307515858938,0.283077249469033,4.56545936678474));
#44243=CARTESIAN_POINT('Ctrl Pts',(8.23079099465223,-0.32252129731946,4.54392741926377));
#44244=CARTESIAN_POINT('Ctrl Pts',(8.27850683071506,-0.631943574151527,
4.02289855323374));
#44245=CARTESIAN_POINT('Ctrl Pts',(8.32622266677791,-0.361042343138453,
3.48084159342964));
#44246=CARTESIAN_POINT('Ctrl Pts',(8.37393850284074,0.241409626929164,3.41553578665797));
#44247=CARTESIAN_POINT('Ctrl Pts',(8.42165433890358,0.622171422023167,3.88695246013618));
#44248=CARTESIAN_POINT('Ctrl Pts',(8.46937017496642,0.431583626935426,4.46218242893131));
#44249=CARTESIAN_POINT('Ctrl Pts',(8.51708601102927,-0.155334053534803,
4.61298316164806));
#44250=CARTESIAN_POINT('Ctrl Pts',(8.56480184709209,-0.599606082522386,
4.20087202506506));
#44251=CARTESIAN_POINT('Ctrl Pts',(8.61251768315494,-0.493250619804184,
3.60429701705146));
#44252=CARTESIAN_POINT('Ctrl Pts',(8.66023351921777,0.0660644767165412,
3.37110214695249));
#44253=CARTESIAN_POINT('Ctrl Pts',(8.70794935528061,0.564711547735832,3.71543385214437));
#44254=CARTESIAN_POINT('Ctrl Pts',(8.75566519134344,0.544775315265253,4.32108702952508));
#44255=CARTESIAN_POINT('Ctrl Pts',(8.80338102740629,0.0245635283409047,
4.6318810471339));
#44256=CARTESIAN_POINT('Ctrl Pts',(8.85109686346912,-0.518205324617361,
4.36240897642002));
#44257=CARTESIAN_POINT('Ctrl Pts',(8.89881269953197,-0.585098254365674,
3.76013116628075));
#44258=CARTESIAN_POINT('Ctrl Pts',(8.9465285355948,-0.114686454236133,3.3781285970023));
#44259=CARTESIAN_POINT('Ctrl Pts',(8.99424437165764,0.461043681496376,3.56720010581811));
#44260=CARTESIAN_POINT('Ctrl Pts',(9.04196020772047,0.613390310441866,4.15371841694351));
#44261=CARTESIAN_POINT('Ctrl Pts',(9.08967604378332,0.202451179085494,4.59907474052783));
#44262=CARTESIAN_POINT('Ctrl Pts',(9.13739187984615,-0.394401985136886,
4.49429151193569));
#44263=CARTESIAN_POINT('Ctrl Pts',(9.18510771590899,-0.629069737753471,
3.93559278228048));
#44264=CARTESIAN_POINT('Ctrl Pts',(9.23282355197184,-0.28605307070895,3.43604019168954));
#44265=CARTESIAN_POINT('Ctrl Pts',(9.28053938803466,0.319650532659854,3.45438057070715));
#44266=CARTESIAN_POINT('Ctrl Pts',(9.32825522409751,0.631814133431458,3.97377166707843));
#44267=CARTESIAN_POINT('Ctrl Pts',(9.37597106016033,0.363773093762905,4.51724864514637));
#44268=CARTESIAN_POINT('Ctrl Pts',(9.4236868962232,-0.238326375276645,4.58572823348297));
#44269=CARTESIAN_POINT('Ctrl Pts',(9.47140273228601,-0.621567066777005,
4.11632457242483));
#44270=CARTESIAN_POINT('Ctrl Pts',(9.51911856834886,-0.434013156817378,
3.54009826662536));
#44271=CARTESIAN_POINT('Ctrl Pts',(9.5668344044117,0.152101713198456,3.38620679908157));
#44272=CARTESIAN_POINT('Ctrl Pts',(9.61455024047453,0.598539239598464,3.79597107236355));
#44273=CARTESIAN_POINT('Ctrl Pts',(9.66226607653739,0.495328972565208,4.39309824928265));
#44274=CARTESIAN_POINT('Ctrl Pts',(9.7099819126002,-0.0627495115905886,
4.62923725529147));
#44275=CARTESIAN_POINT('Ctrl Pts',(9.75769774866305,-0.563204153727404,
4.28753800770644));
#44276=CARTESIAN_POINT('Ctrl Pts',(9.80541358472588,-0.54645975548653,3.68178818330365));
#44277=CARTESIAN_POINT('Ctrl Pts',(9.85312942078873,-0.027892955418244,
3.36825716649128));
#44278=CARTESIAN_POINT('Ctrl Pts',(9.90084525685157,0.516288374798902,3.63486531430293));
#44279=CARTESIAN_POINT('Ctrl Pts',(9.9485610929144,0.58635414632045,4.2367822623095));
#44280=CARTESIAN_POINT('Ctrl Pts',(9.99627692897723,0.117961883057689,4.62125841547385));
#44281=CARTESIAN_POINT('Ctrl Pts',(10.0439927650401,-0.458756592493822,
4.4352234064191));
#44282=CARTESIAN_POINT('Ctrl Pts',(10.0917086011029,-0.614191830280748,
3.8495160464768));
#44283=CARTESIAN_POINT('Ctrl Pts',(10.1394244371658,-0.205605259764808,
3.40200041654811));
#44284=CARTESIAN_POINT('Ctrl Pts',(10.1871402732286,0.391791784436726,3.5036370055096));
#44285=CARTESIAN_POINT('Ctrl Pts',(10.2348561092915,0.629400404498524,4.06109136983801));
#44286=CARTESIAN_POINT('Ctrl Pts',(10.2825719453542,0.289020948539269,4.56244458923262));
#44287=CARTESIAN_POINT('Ctrl Pts',(10.3302877814171,-0.316770891622519,
4.54729628801251));
#44288=CARTESIAN_POINT('Ctrl Pts',(10.3780036174799,-0.631667147860668,
4.02955738427466));
#44289=CARTESIAN_POINT('Ctrl Pts',(10.4257194535428,-0.366493742769977,
3.48467547975859));
#44290=CARTESIAN_POINT('Ctrl Pts',(10.4734352896056,0.235236505537468,3.41302401146715));
#44291=CARTESIAN_POINT('Ctrl Pts',(10.5211511256685,0.620945451230968,3.88040162523195));
#44292=CARTESIAN_POINT('Ctrl Pts',(10.5688669617313,0.436430634585191,4.45760826680378));
#44293=CARTESIAN_POINT('Ctrl Pts',(10.6165827977941,-0.148865149148659,
4.61458619576145));
#44294=CARTESIAN_POINT('Ctrl Pts',(10.664298633857,-0.597455775834545,4.20718016452724));
#44295=CARTESIAN_POINT('Ctrl Pts',(10.7120144699198,-0.497393570532806,
3.60951740033105));
#44296=CARTESIAN_POINT('Ctrl Pts',(10.7597303059826,0.059432803973042,3.37044081575797));
#44297=CARTESIAN_POINT('Ctrl Pts',(10.8074461420455,0.56168112009921,3.70949811708754));
#44298=CARTESIAN_POINT('Ctrl Pts',(10.8551619781083,0.548129021063343,4.31532776744164));
#44299=CARTESIAN_POINT('Ctrl Pts',(10.9028778141712,0.0312216079359222,
4.63158707701274));
#44300=CARTESIAN_POINT('Ctrl Pts',(10.950593650234,-0.514357088165242,4.36785025554668));
#44301=CARTESIAN_POINT('Ctrl Pts',(10.9983094862968,-0.587593755803164,
3.7663108843084));
#44302=CARTESIAN_POINT('Ctrl Pts',(11.0460253223597,-0.12123403619496,3.37937182377895));
#44303=CARTESIAN_POINT('Ctrl Pts',(11.0937411584225,0.456456764276497,3.56236516706526));
#44304=CARTESIAN_POINT('Ctrl Pts',(11.1414569944854,0.61497629462275,4.14724531131301));
#44305=CARTESIAN_POINT('Ctrl Pts',(11.1891728305482,0.208753630990335,4.59690782052167));
#44306=CARTESIAN_POINT('Ctrl Pts',(11.236888666611,-0.389170704067994,4.49842069353791));
#44307=CARTESIAN_POINT('Ctrl Pts',(11.2846045026739,-0.629713593419695,
3.94222617449013));
#44308=CARTESIAN_POINT('Ctrl Pts',(11.3323203387367,-0.291980800545002,
3.43908624837263));
#44309=CARTESIAN_POINT('Ctrl Pts',(11.3800361747996,0.313882454172263,3.45104205114199));
#44310=CARTESIAN_POINT('Ctrl Pts',(11.4277520108624,0.631502621520784,3.96711438515144));
#44311=CARTESIAN_POINT('Ctrl Pts',(11.4754678469252,0.369204214609944,4.51338608528654));
#44312=CARTESIAN_POINT('Ctrl Pts',(11.5231836829881,-0.232140103514266,
4.58820744384271));
#44313=CARTESIAN_POINT('Ctrl Pts',(11.5708995190509,-0.620306592646703,
4.12286885598323));
#44314=CARTESIAN_POINT('Ctrl Pts',(11.6186153551137,-0.438835993107895,
3.54469790709399));
#44315=CARTESIAN_POINT('Ctrl Pts',(11.6663311911766,0.145624451261577,3.38463787584353));
#44316=CARTESIAN_POINT('Ctrl Pts',(11.7140470272394,0.596355721317347,3.78967435176932));
#44317=CARTESIAN_POINT('Ctrl Pts',(11.7617628633022,0.499444356375145,4.38785610674141));
#44318=CARTESIAN_POINT('Ctrl Pts',(11.8094786993651,-0.0561144459655822,
4.62986363095956));
#44319=CARTESIAN_POINT('Ctrl Pts',(11.8571945354279,-0.560142489144378,
4.29345769116983));
#44320=CARTESIAN_POINT('Ctrl Pts',(11.9049103714908,-0.549783065641843,
3.68756503815187));
#44321=CARTESIAN_POINT('Ctrl Pts',(11.9526262075536,-0.0345493934605723,
3.36858621802886));
#44322=CARTESIAN_POINT('Ctrl Pts',(12.0003420436164,0.512411518346294,3.62944438943981));
#44323=CARTESIAN_POINT('Ctrl Pts',(12.0480578796793,0.588817048391095,4.23058947975914));
#44324=CARTESIAN_POINT('Ctrl Pts',(12.0957737157421,0.1245028227835,4.61998070274044));
#44325=CARTESIAN_POINT('Ctrl Pts',(12.1434895518049,-0.454144260708352,
4.44003410676589));
#44326=CARTESIAN_POINT('Ctrl Pts',(12.1912053878678,-0.615743681684068,
3.85599741975318));
#44327=CARTESIAN_POINT('Ctrl Pts',(12.2389212239306,-0.211896205334937,
3.40420051794564));
#44328=CARTESIAN_POINT('Ctrl Pts',(12.2866370599935,0.386538816815474,3.49953544806202));
#44329=CARTESIAN_POINT('Ctrl Pts',(12.3343528960563,0.63000929582004,4.05445467686));
#44330=CARTESIAN_POINT('Ctrl Pts',(12.3820687321191,0.294932544534008,4.55936733800455));
#44331=CARTESIAN_POINT('Ctrl Pts',(12.429784568182,-0.310985300518122,4.55060436568669));
#44332=CARTESIAN_POINT('Ctrl Pts',(12.4775004042448,-0.631320558980542,
4.0362129322216));
#44333=CARTESIAN_POINT('Ctrl Pts',(12.5252162403077,-0.371904434015698,
3.48856660588983));
#44334=CARTESIAN_POINT('Ctrl Pts',(12.5729320763705,0.229037255191033,3.41057743478371));
#44335=CARTESIAN_POINT('Ctrl Pts',(12.6206479124333,0.619650508764677,3.87386407474765));
#44336=CARTESIAN_POINT('Ctrl Pts',(12.6683637484962,0.44122916559109,4.4529832757215));
#44337=CARTESIAN_POINT('Ctrl Pts',(12.716079584559,-0.142379709528176,4.61612096455669));
#44338=CARTESIAN_POINT('Ctrl Pts',(12.7637954206218,-0.595239106594286,
4.21346529139986));
#44339=CARTESIAN_POINT('Ctrl Pts',(12.8115112566847,-0.501481273143938,
3.61478115656484));
#44340=CARTESIAN_POINT('Ctrl Pts',(12.8592270927475,0.0527945297157079,
3.36984941301012));
#44341=CARTESIAN_POINT('Ctrl Pts',(12.9069429288104,0.558588303589165,3.70359464960132));
#44342=CARTESIAN_POINT('Ctrl Pts',(12.9546587648732,0.551421843290858,4.30953348024615));
#44343=CARTESIAN_POINT('Ctrl Pts',(13.002374600936,0.0378762195828894,4.63122295319618));
#44344=CARTESIAN_POINT('Ctrl Pts',(13.0500904369989,-0.510451719368595,
4.37325067561256));
#44345=CARTESIAN_POINT('Ctrl Pts',(13.0978062730617,-0.590023990114621,
3.77251655941407));
#44346=CARTESIAN_POINT('Ctrl Pts',(13.1455221091246,-0.127768152052348,
3.38068398698829));
#44347=CARTESIAN_POINT('Ctrl Pts',(13.1932379451874,0.451819146005312,3.55757883871291));
#44348=CARTESIAN_POINT('Ctrl Pts',(13.2409537812502,0.616493970155128,4.14075585037205));
#44349=CARTESIAN_POINT('Ctrl Pts',(13.2886696173131,0.215032895532453,4.59467459882739));
#44350=CARTESIAN_POINT('Ctrl Pts',(13.3363854533759,-0.383896195764066,
4.50249451293469));
#44351=CARTESIAN_POINT('Ctrl Pts',(13.3841012894387,-0.630287503488198,
3.94886598394213));
#44352=CARTESIAN_POINT('Ctrl Pts',(13.4318171255016,-0.297876098539286,
3.4421946086935));
#44353=CARTESIAN_POINT('Ctrl Pts',(13.4795329615644,0.308079511111167,3.44776450722078));
#44354=CARTESIAN_POINT('Ctrl Pts',(13.5272487976272,0.631120965295637,3.96046075600252));
#44355=CARTESIAN_POINT('Ctrl Pts',(13.5749646336901,0.374594326004835,4.50946650093658));
#44356=CARTESIAN_POINT('Ctrl Pts',(13.6226804697529,-0.225928046730791,
4.59062131891086));
#44357=CARTESIAN_POINT('Ctrl Pts',(13.6703963058158,-0.618977217803688,
4.12939949185215));
#44358=CARTESIAN_POINT('Ctrl Pts',(13.7181121418786,-0.443610085578744,
3.54934812035851));
#44359=CARTESIAN_POINT('Ctrl Pts',(13.7658279779415,0.139131014051702,3.38313730411011));
#44360=CARTESIAN_POINT('Ctrl Pts',(13.8135438140043,0.594105962672646,3.78340099315002));
#44361=CARTESIAN_POINT('Ctrl Pts',(13.8612596500671,0.503504264276035,4.38257088298437));
#44362=CARTESIAN_POINT('Ctrl Pts',(13.90897548613,-0.0494731474142026,4.63042004436449));
#44363=CARTESIAN_POINT('Ctrl Pts',(13.9566913221928,-0.557018606591754,
4.29934477874546));
#44364=CARTESIAN_POINT('Ctrl Pts',(14.0044071582556,-0.553045308503159,
3.69337659679301));
#44365=CARTESIAN_POINT('Ctrl Pts',(14.0521229943185,-0.0412019939202257,
3.36898540401303));
#44366=CARTESIAN_POINT('Ctrl Pts',(14.0998388303813,0.50847774565382,3.62406462413548));
#44367=CARTESIAN_POINT('Ctrl Pts',(14.1475546664442,0.591214547458171,4.22437108442359));
#44368=CARTESIAN_POINT('Ctrl Pts',(14.195270502507,0.131029933326566,4.61863412549262));
#44369=CARTESIAN_POINT('Ctrl Pts',(14.2429863385698,-0.4494814847335,4.44479593021223));
#44370=CARTESIAN_POINT('Ctrl Pts',(14.2907021746327,-0.617227139201166,
3.86249478815283));
#44371=CARTESIAN_POINT('Ctrl Pts',(14.3384180106955,-0.218163614480107,
3.40646679792233));
#44372=CARTESIAN_POINT('Ctrl Pts',(14.3861338467583,0.381242914296727,3.49548947984197));
#44373=CARTESIAN_POINT('Ctrl Pts',(14.4338496828212,0.630548208698617,4.0478119353149));
#44374=CARTESIAN_POINT('Ctrl Pts',(14.481565518884,0.300811380821271,4.55622795490698));
#44375=CARTESIAN_POINT('Ctrl Pts',(14.5292813549469,-0.305165166642291,
4.55385128484077));
#44376=CARTESIAN_POINT('Ctrl Pts',(14.5769971910097,-0.630903846008588,
4.04286445780787));
#44377=CARTESIAN_POINT('Ctrl Pts',(14.6247130270726,-0.37727381588172,3.49251453961553));
#44378=CARTESIAN_POINT('Ctrl Pts',(14.6724288631354,0.222812564473163,3.40819632836178));
#44379=CARTESIAN_POINT('Ctrl Pts',(14.7201446991982,0.618286738460357,3.86734053484336));
#44380=CARTESIAN_POINT('Ctrl Pts',(14.7678605352611,0.44597868695508,4.44830796940654));
#44381=CARTESIAN_POINT('Ctrl Pts',(14.8155763713239,-0.135878455045208,
4.6175872975589));
#44382=CARTESIAN_POINT('Ctrl Pts',(14.8632922073867,-0.592956321018707,
4.2197267075609));
#44383=CARTESIAN_POINT('Ctrl Pts',(14.9110080434496,-0.505513273594975,
3.62008770107973));
#44384=CARTESIAN_POINT('Ctrl Pts',(14.9587238795124,0.0461503912925444,
3.36932800439917));
#44385=CARTESIAN_POINT('Ctrl Pts',(15.0064397155752,0.555433441741075,3.69772410541485));
#44386=CARTESIAN_POINT('Ctrl Pts',(15.0541555516381,0.554653416196733,4.30370481154056));
#44387=CARTESIAN_POINT('Ctrl Pts',(15.1018713877009,0.0445266241191229,
4.63078871612938));
#44388=CARTESIAN_POINT('Ctrl Pts',(15.1495872237638,-0.506489652017253,
4.37860963676461));
#44389=CARTESIAN_POINT('Ctrl Pts',(15.1973030598266,-0.592388687361149,
3.77874750230084));
#44390=CARTESIAN_POINT('Ctrl Pts',(15.2450188958894,-0.134288076029725,
3.38206494088146));
#44391=CARTESIAN_POINT('Ctrl Pts',(15.2927347319523,0.447131341807447,3.5528416524037));
#44392=CARTESIAN_POINT('Ctrl Pts',(15.3404505680151,0.617943168462805,4.13425075493917));
#44393=CARTESIAN_POINT('Ctrl Pts',(15.3881664040779,0.221288275240951,4.59237532350063));
#44394=CARTESIAN_POINT('Ctrl Pts',(15.4358822401408,-0.378579046092452,
4.50651251762549));
#44395=CARTESIAN_POINT('Ctrl Pts',(15.4835980762036,-0.630791404211772,
3.95551147311801));
#44396=CARTESIAN_POINT('Ctrl Pts',(15.5313139122665,-0.303738309870084,
3.44536492739022));
#44397=CARTESIAN_POINT('Ctrl Pts',(15.5790297483293,0.302242348039936,3.44454830299756));
#44398=CARTESIAN_POINT('Ctrl Pts',(15.6267455843921,0.630669207148581,3.95381151868517));
#44399=CARTESIAN_POINT('Ctrl Pts',(15.674461420455,0.379942829239589,4.50549032746533));
#44400=CARTESIAN_POINT('Ctrl Pts',(15.7221772565178,-0.219690894932002,
4.59296959056563));
#44401=CARTESIAN_POINT('Ctrl Pts',(15.7698930925806,-0.617579089908608,
4.13591575463957));
#44402=CARTESIAN_POINT('Ctrl Pts',(15.8176089286435,-0.448334903946386,
3.5540483898953));
#44403=CARTESIAN_POINT('Ctrl Pts',(15.8653247647063,0.13262212282903,3.3817052505577));
#44404=CARTESIAN_POINT('Ctrl Pts',(15.9130406007692,0.591790213556878,3.77715169332057));
#44405=CARTESIAN_POINT('Ctrl Pts',(15.960756436832,0.507508245312566,4.37724316506909));
#44406=CARTESIAN_POINT('Ctrl Pts',(16.0084722728949,-0.0428263536203826,
4.63090643370248));
#44407=CARTESIAN_POINT('Ctrl Pts',(16.0561881089577,-0.553832853055588,
4.30519861652357));
#44408=CARTESIAN_POINT('Ctrl Pts',(16.1039039450205,-0.556246121716014,
3.69922221370673));
#44409=CARTESIAN_POINT('Ctrl Pts',(16.1516197810833,-0.0478500178579074,
3.36945468010413));
#44410=CARTESIAN_POINT('Ctrl Pts',(16.1993356171462,0.504487493666278,3.61872661594874));
#44411=CARTESIAN_POINT('Ctrl Pts',(16.247051453209,0.593546377218863,4.21812776701271));
#44412=CARTESIAN_POINT('Ctrl Pts',(16.2947672892719,0.137542489686435,4.61721883330181));
#44413=CARTESIAN_POINT('Ctrl Pts',(16.3424831253347,-0.444768782488292,
4.44950834783736));
#44414=CARTESIAN_POINT('Ctrl Pts',(16.3901989613976,-0.618642038056621,
3.86900742997889));
#44415=CARTESIAN_POINT('Ctrl Pts',(16.4379147974604,-0.224406791046256,
3.40879900475058));
#44416=CARTESIAN_POINT('Ctrl Pts',(16.4856306335233,0.375904665124208,3.49149955025639));
#44417=CARTESIAN_POINT('Ctrl Pts',(16.533346469586,0.631017083274371,4.04116388304691));
#44418=CARTESIAN_POINT('Ctrl Pts',(16.5810623056489,0.306656804407812,4.55302678864769));
#44419=CARTESIAN_POINT('Ctrl Pts',(16.6287781417117,-0.29931113646787,4.55703668482238));
#44420=CARTESIAN_POINT('Ctrl Pts',(16.6764939777746,-0.630417055231307,
4.04951122221356));
#44421=CARTESIAN_POINT('Ctrl Pts',(16.7242098138374,-0.382601291962586,
3.49651884241796));
#44422=CARTESIAN_POINT('Ctrl Pts',(16.7719256499003,0.216563124792967,3.40588095668335));
#44423=CARTESIAN_POINT('Ctrl Pts',(16.8196414859631,0.616854291799135,3.86083173012294));
#44424=CARTESIAN_POINT('Ctrl Pts',(16.8673573220259,0.450678671122871,4.44358286716973));
#44425=CARTESIAN_POINT('Ctrl Pts',(16.9150731580887,-0.129362107828251,
4.61898503189482));
#44426=CARTESIAN_POINT('Ctrl Pts',(16.9627889941516,-0.590607672668797,
4.22596371752193));
#44427=CARTESIAN_POINT('Ctrl Pts',(17.0105048302144,-0.509489124030439,
3.62543644444997));
#44428=CARTESIAN_POINT('Ctrl Pts',(17.0582206662773,0.0395011267029154,
3.3688766478407));
#44429=CARTESIAN_POINT('Ctrl Pts',(17.1059365023401,0.552216884982031,3.69188713660034));
#44430=CARTESIAN_POINT('Ctrl Pts',(17.153652338403,0.557823380833178,4.29784240874569));
#44431=CARTESIAN_POINT('Ctrl Pts',(17.2013681744658,0.0511720828492506,
4.63028441404532));
#44432=CARTESIAN_POINT('Ctrl Pts',(17.2490840105287,-0.502471326198846,
4.38392654375487));
#44433=CARTESIAN_POINT('Ctrl Pts',(17.2967998465914,-0.594687584883411,
3.78500302086511));
#44434=CARTESIAN_POINT('Ctrl Pts',(17.3445156826543,-0.140793083924855,
3.38351453206865));
#44435=CARTESIAN_POINT('Ctrl Pts',(17.3922315187171,0.442393872381948,3.5481541343218));
#44436=CARTESIAN_POINT('Ctrl Pts',(17.43994735478,0.61932372857571,4.1277307475695));
#44437=CARTESIAN_POINT('Ctrl Pts',(17.4876631908428,0.227519075297936,4.590010249934));
#44438=CARTESIAN_POINT('Ctrl Pts',(17.5353790269057,-0.373219845656906,
4.51047426130944));
#44439=CARTESIAN_POINT('Ctrl Pts',(17.5830948629685,-0.631225239619516,
3.96216190386831));
#44440=CARTESIAN_POINT('Ctrl Pts',(17.6308106990313,-0.309566783390781,
3.44859685231885));
#44441=CARTESIAN_POINT('Ctrl Pts',(17.6785265350942,0.29637161332294,3.44139379571298));
#44442=CARTESIAN_POINT('Ctrl Pts',(17.726242371157,0.630147397258769,3.94716741176515));
#44443=CARTESIAN_POINT('Ctrl Pts',(17.7739582072198,0.385249130227842,4.50145800652724));
#44444=CARTESIAN_POINT('Ctrl Pts',(17.8216740432827,-0.213429340911116,
4.59525199797214));
#44445=CARTESIAN_POINT('Ctrl Pts',(17.8693898793456,-0.616112364258878,
4.14241692054995));
#44446=CARTESIAN_POINT('Ctrl Pts',(17.9171057154084,-0.453009923400427,
3.55879819362073));
#44447=CARTESIAN_POINT('Ctrl Pts',(17.9648215514712,0.126098500570276,3.38034187425201));
#44448=CARTESIAN_POINT('Ctrl Pts',(18.012537387534,0.589408731192455,3.77092714642348));
#44449=CARTESIAN_POINT('Ctrl Pts',(18.0602532235969,0.511455854741549,4.3718735447732));
#44450=CARTESIAN_POINT('Ctrl Pts',(18.1079690596597,-0.0361748028784226,
4.6313227449477));
#44451=CARTESIAN_POINT('Ctrl Pts',(18.1556848957226,-0.55058558239424,4.31101855428765));
#44452=CARTESIAN_POINT('Ctrl Pts',(18.2034007317854,-0.559385149749292,
3.70510123958967));
#44453=CARTESIAN_POINT('Ctrl Pts',(18.2511165678482,-0.0544927268426965,
3.36999399417717));
#44454=CARTESIAN_POINT('Ctrl Pts',(18.2988324039111,0.500441205601937,3.6134309578002));
#44455=CARTESIAN_POINT('Ctrl Pts',(18.3465482399739,0.595812278664582,4.21186022100458));
#44456=CARTESIAN_POINT('Ctrl Pts',(18.3942640760367,0.144039768479226,4.61573498337195));
#44457=CARTESIAN_POINT('Ctrl Pts',(18.4419799120996,-0.440006677437314,
4.4541708362083));
#44458=CARTESIAN_POINT('Ctrl Pts',(18.4896957481624,-0.619988221090196,
3.87553462183804));
#44459=CARTESIAN_POINT('Ctrl Pts',(18.5374115842252,-0.230625041570952,
3.41119687937986));
#44460=CARTESIAN_POINT('Ctrl Pts',(18.5851274202881,0.370524662245315,3.48756610248778));
#44461=CARTESIAN_POINT('Ctrl Pts',(18.6328432563509,0.631415867466904,4.03451125849008));
#44462=CARTESIAN_POINT('Ctrl Pts',(18.6805590924138,0.31246816601179,4.54976419479712));
#44463=CARTESIAN_POINT('Ctrl Pts',(18.7282749284766,-0.293423860232864,
4.56016021181225));
#44464=CARTESIAN_POINT('Ctrl Pts',(18.7759907645394,-0.629860240718928,
4.05615248714788));
#44465=CARTESIAN_POINT('Ctrl Pts',(18.8237066006023,-0.387886270507855,
3.50057906951772));
#44466=CARTESIAN_POINT('Ctrl Pts',(18.8714224366651,0.210289630309142,3.40363157692976));
#44467=CARTESIAN_POINT('Ctrl Pts',(18.919138272728,0.615353327889266,3.85433838355196));
#44468=CARTESIAN_POINT('Ctrl Pts',(18.9668541087908,0.455328596044662,4.43880849385601));
#44469=CARTESIAN_POINT('Ctrl Pts',(19.0145699448537,-0.122831391686292,
4.62031401230505));
#44470=CARTESIAN_POINT('Ctrl Pts',(19.0622857809165,-0.588193422413584,
4.2321756285162));
#44471=CARTESIAN_POINT('Ctrl Pts',(19.1100016169793,-0.513408382846255,
3.63082679254236));
#44472=CARTESIAN_POINT('Ctrl Pts',(19.1577174530421,0.0328474745430158,
3.36849539350727));
#44473=CARTESIAN_POINT('Ctrl Pts',(19.205433289105,0.548938990540088,3.68608439142882));
#44474=CARTESIAN_POINT('Ctrl Pts',(19.2531491251678,0.560931385193363,4.2919469231649));
#44475=CARTESIAN_POINT('Ctrl Pts',(19.3008649612307,0.0578118574426247,
4.62971010270368));
#44476=CARTESIAN_POINT('Ctrl Pts',(19.3485807972935,-0.498397187901359,
4.38920080648958));
#44477=CARTESIAN_POINT('Ctrl Pts',(19.3962966333563,-0.596920427988996,
3.79128241936144));
#44478=CARTESIAN_POINT('Ctrl Pts',(19.4440124694192,-0.147282451949449,
3.38503260125846));
#44479=CARTESIAN_POINT('Ctrl Pts',(19.491728305482,0.437607261597584,3.54351680188243));
#44480=CARTESIAN_POINT('Ctrl Pts',(19.5394441415449,0.620635501579114,4.12119655861503));
#44481=CARTESIAN_POINT('Ctrl Pts',(19.5871599776077,0.233724595248439,4.58757962923414));
#44482=CARTESIAN_POINT('Ctrl Pts',(19.6348758136705,-0.367819173932889,
4.51437932582758));
#44483=CARTESIAN_POINT('Ctrl Pts',(19.6825916497334,-0.631588991354928,
3.96881649615688));
#44484=CARTESIAN_POINT('Ctrl Pts',(19.7303074857962,-0.315360815373557,
3.4518901025469));
#44485=CARTESIAN_POINT('Ctrl Pts',(19.778023321859,0.290467852693633,3.43830118837221));
#44486=CARTESIAN_POINT('Ctrl Pts',(19.8257391579219,0.629555794415491,3.94052945152661));
#44487=CARTESIAN_POINT('Ctrl Pts',(19.8734549939847,0.390512260364629,4.49736946054851));
#44488=CARTESIAN_POINT('Ctrl Pts',(19.9211708300476,-0.207143364153331,
4.59746927979605));
#44489=CARTESIAN_POINT('Ctrl Pts',(19.9688866661104,-0.61457855576007,4.14890039401813));
#44490=CARTESIAN_POINT('Ctrl Pts',(20.0166025021732,-0.45763207183192,3.5636005413983));
#44491=CARTESIAN_POINT('Ctrl Pts',(20.0643183382361,0.119556051622903,3.37904064719698));
#44492=CARTESIAN_POINT('Ctrl Pts',(20.1120341742989,0.586970881772813,3.7647406560623));
#44493=CARTESIAN_POINT('Ctrl Pts',(20.1597500103618,0.515329468049299,4.36643880344312));
#44494=CARTESIAN_POINT('Ctrl Pts',(20.2074658464246,-0.029486781418557,
4.63171390504007));
#44495=CARTESIAN_POINT('Ctrl Pts',(20.2551816824874,-0.547338447674763,
4.31671898245684));
#44496=CARTESIAN_POINT('Ctrl Pts',(20.3028975185503,-0.562346186529673,
3.71117381387971));
#44497=CARTESIAN_POINT('Ctrl Pts',(20.3506133546131,-0.0613491664957494,
3.37029669484294));
#44498=CARTESIAN_POINT('Ctrl Pts',(20.398329190676,0.496762641213801,3.60878154740643));
#44499=CARTESIAN_POINT('Ctrl Pts',(20.4380923873949,0.580417208789547,4.10498761157686));
#44500=CARTESIAN_POINT('Ctrl Pts',(20.4699029447702,0.374745574175769,4.41137453781958));
#44501=CARTESIAN_POINT('Ctrl Pts',(20.4937608628016,0.13332385162888,4.54159545884303));
#44502=CARTESIAN_POINT('Ctrl Pts',(20.517618780833,-0.143293564288956,4.53872805560682));
#44503=CARTESIAN_POINT('Ctrl Pts',(20.5414766988645,-0.38346854803195,4.40448715909776));
#44504=CARTESIAN_POINT('Ctrl Pts',(20.5653346168959,-0.530621786340447,
4.17114564603877));
#44505=CARTESIAN_POINT('Ctrl Pts',(20.5891925349273,-0.547627617499454,
3.89605651468078));
#44506=CARTESIAN_POINT('Ctrl Pts',(20.6130504529587,-0.430933317123153,
3.64633026976583));
#44507=CARTESIAN_POINT('Ctrl Pts',(20.6369083709901,-0.208752997660079,
3.48311457674551));
#44508=CARTESIAN_POINT('Ctrl Pts',(20.6607662890215,0.0644142843662171,
3.4462762657402));
#44509=CARTESIAN_POINT('Ctrl Pts',(20.684624207053,0.321861676845817,3.54484653226013));
#44510=CARTESIAN_POINT('Ctrl Pts',(20.7084821250844,0.500588620804837,3.75470996102831));
#44511=CARTESIAN_POINT('Ctrl Pts',(20.7323400431158,0.556916750317041,4.02455574134091));
#44512=CARTESIAN_POINT('Ctrl Pts',(20.7561979611472,0.47705893600668,4.28839577951569));
#44513=CARTESIAN_POINT('Ctrl Pts',(20.7800558791787,0.280549668164313,4.48171582646486));
#44514=CARTESIAN_POINT('Ctrl Pts',(20.8039137972101,0.0154370662995263,
4.55724289713534));
#44515=CARTESIAN_POINT('Ctrl Pts',(20.8277717152415,-0.253449631274377,
4.49650907789895));
#44516=CARTESIAN_POINT('Ctrl Pts',(20.8516296332729,-0.460361354274216,
4.31436517051053));
#44517=CARTESIAN_POINT('Ctrl Pts',(20.8754875513043,-0.554701993332711,
4.05535046556385));
#44518=CARTESIAN_POINT('Ctrl Pts',(20.8993454693358,-0.513402987365846,
3.78280103771366));
#44519=CARTESIAN_POINT('Ctrl Pts',(20.9232033873672,-0.346562912086465,
3.56336268648205));
#44520=CARTESIAN_POINT('Ctrl Pts',(20.9470613053986,-0.0949787932613798,
3.45069404477467));
#44521=CARTESIAN_POINT('Ctrl Pts',(20.97091922343,0.179830242856268,3.47234567582879));
#44522=CARTESIAN_POINT('Ctrl Pts',(20.9947771414614,0.410665878084123,3.62302316008453));
#44523=CARTESIAN_POINT('Ctrl Pts',(21.0186350594928,0.541082524061315,3.86588175144064));
#44524=CARTESIAN_POINT('Ctrl Pts',(21.0424929775243,0.539189751860116,4.14153590729571));
#44525=CARTESIAN_POINT('Ctrl Pts',(21.0663508955557,0.405450399288564,4.38258067876424));
#44526=CARTESIAN_POINT('Ctrl Pts',(21.0902088135871,0.172567379211795,4.53007405282339));
#44527=CARTESIAN_POINT('Ctrl Pts',(21.1140667316185,-0.102513065388571,
4.54794988212627));
#44528=CARTESIAN_POINT('Ctrl Pts',(21.1379246496499,-0.352526273278862,
4.43183703934844));
#44529=CARTESIAN_POINT('Ctrl Pts',(21.1617825676814,-0.516337204635697,
4.21012827746935));
#44530=CARTESIAN_POINT('Ctrl Pts',(21.1856404857128,-0.553889624765765,
3.93703742795684));
#44531=CARTESIAN_POINT('Ctrl Pts',(21.2094984037442,-0.456000943963824,
3.67934264238169));
#44532=CARTESIAN_POINT('Ctrl Pts',(21.2333563217756,-0.246607611160355,
3.50005731527167));
#44533=CARTESIAN_POINT('Ctrl Pts',(21.257214239807,0.0230880000356606,3.44302159274494));
#44534=CARTESIAN_POINT('Ctrl Pts',(21.2810721578385,0.287137966314551,3.52218226257825));
#44535=CARTESIAN_POINT('Ctrl Pts',(21.3049300758698,0.480974878350452,3.71818238470557));
#44536=CARTESIAN_POINT('Ctrl Pts',(21.3287879939013,0.557200331135927,3.9830945903298));
#44537=CARTESIAN_POINT('Ctrl Pts',(21.3526459119327,0.497175125126959,4.25214062911267));
#44538=CARTESIAN_POINT('Ctrl Pts',(21.3765038299641,0.31557705824565,4.45953141590455));
#44539=CARTESIAN_POINT('Ctrl Pts',(21.4003617479955,0.0568118044769688,
4.55455425412338));
#44540=CARTESIAN_POINT('Ctrl Pts',(21.424219666027,-0.215845483008899,4.51397347145443));
#44541=CARTESIAN_POINT('Ctrl Pts',(21.4480775840584,-0.435722670386138,
4.34771217465862));
#44542=CARTESIAN_POINT('Ctrl Pts',(21.4719355020898,-0.549053796006754,
4.0964257796693));
#44543=CARTESIAN_POINT('Ctrl Pts',(21.4957934201212,-0.528126312578589,
3.82156065496534));
#44544=CARTESIAN_POINT('Ctrl Pts',(21.5196513381527,-0.378057559853047,
3.59032881071252));
#44545=CARTESIAN_POINT('Ctrl Pts',(21.543509256184,-0.135543435662257,3.45927273145963));
#44546=CARTESIAN_POINT('Ctrl Pts',(21.5673671742155,0.14011475067701,3.46043919847993));
#44547=CARTESIAN_POINT('Ctrl Pts',(21.5912250922469,0.381511063826562,3.59354297881304));
#44548=CARTESIAN_POINT('Ctrl Pts',(21.6150830102783,0.529617529717794,3.8260365724933));
#44549=CARTESIAN_POINT('Ctrl Pts',(21.6389409283097,0.548218083101175,4.10106896286759));
#44550=CARTESIAN_POINT('Ctrl Pts',(21.6627988463412,0.432764382005563,4.35138723875747));
#44551=CARTESIAN_POINT('Ctrl Pts',(21.6866567643726,0.211488001244504,4.51578176317496));
#44552=CARTESIAN_POINT('Ctrl Pts',(21.710514682404,-0.0615029566383307,
4.55405359688301));
#44553=CARTESIAN_POINT('Ctrl Pts',(21.7343726004354,-0.319454766316188,
4.4568442340362));
#44554=CARTESIAN_POINT('Ctrl Pts',(21.7582305184669,-0.499291183856609,
4.24792401178047));
#44555=CARTESIAN_POINT('Ctrl Pts',(21.7820884364982,-0.557037306525311,
3.97837961532992));
#44556=CARTESIAN_POINT('Ctrl Pts',(21.8059463545297,-0.478572634356998,
3.71412199185867));
#44557=CARTESIAN_POINT('Ctrl Pts',(21.8298042725611,-0.283083917031579,
3.51976932853855));
#44558=CARTESIAN_POINT('Ctrl Pts',(21.8536621905926,-0.018373470940863,
3.44284614561161));
#44559=CARTESIAN_POINT('Ctrl Pts',(21.8775201086239,0.250829789278194,3.5021622566489));
#44560=CARTESIAN_POINT('Ctrl Pts',(21.9013780266554,0.458698333552465,3.68321325676341));
#44561=CARTESIAN_POINT('Ctrl Pts',(21.9252359446868,0.55440264058141,3.94172724469688));
#44562=CARTESIAN_POINT('Ctrl Pts',(21.9490938627182,0.514540400363477,4.21449050861997));
#44563=CARTESIAN_POINT('Ctrl Pts',(21.9729517807496,0.348859016457567,4.4348050005813));
#44564=CARTESIAN_POINT('Ctrl Pts',(21.996809698781,0.0978721002989983,4.54879782605011));
#44565=CARTESIAN_POINT('Ctrl Pts',(22.0206676168125,-0.177047210365213,
4.52859463409701));
#44566=CARTESIAN_POINT('Ctrl Pts',(22.0445255348439,-0.408673655425848,
4.3791356554785));
#44567=CARTESIAN_POINT('Ctrl Pts',(22.0683834528753,-0.540368259688198,
4.13696768164748));
#44568=CARTESIAN_POINT('Ctrl Pts',(22.0922413709067,-0.53992810512055,3.86130737872913));
#44569=CARTESIAN_POINT('Ctrl Pts',(22.1160992889381,-0.407460821505317,
3.61956119962225));
#44570=CARTESIAN_POINT('Ctrl Pts',(22.1399572069695,-0.175358268020808,
3.47084267015335));
#44571=CARTESIAN_POINT('Ctrl Pts',(22.163815125001,0.0996241586556461,3.45151752178681));
#44572=CARTESIAN_POINT('Ctrl Pts',(22.1876730430324,0.350245764837839,3.56631127970877));
#44573=CARTESIAN_POINT('Ctrl Pts',(22.2115309610638,0.51522274100534,3.78715374318048));
#44574=CARTESIAN_POINT('Ctrl Pts',(22.2353888790952,0.554213722627899,4.06004291426965));
#44575=CARTESIAN_POINT('Ctrl Pts',(22.2592467971266,0.457684352558003,4.31824995726588));
#44576=CARTESIAN_POINT('Ctrl Pts',(22.2831047151581,0.249238691275201,4.49863621678958));
#44577=CARTESIAN_POINT('Ctrl Pts',(22.3069626331895,-0.0201526192614011,
4.55709233866662));
#44578=CARTESIAN_POINT('Ctrl Pts',(22.3308205512209,-0.284616065231974,
4.47932420896945));
#44579=CARTESIAN_POINT('Ctrl Pts',(22.3546784692523,-0.479483130864429,
4.28434825342259));
#44580=CARTESIAN_POINT('Ctrl Pts',(22.3785363872838,-0.557103509392546,
4.01984140485232));
#44581=CARTESIAN_POINT('Ctrl Pts',(22.4023943053151,-0.498496906094933,
3.75048279151596));
#44582=CARTESIAN_POINT('Ctrl Pts',(22.4262522233466,-0.317994227800984,
3.542137933897));
#44583=CARTESIAN_POINT('Ctrl Pts',(22.450110141378,-0.0597333038680864,
3.44575282046209));
#44584=CARTESIAN_POINT('Ctrl Pts',(22.4739680594094,0.213134049493302,3.48489624527193));
#44585=CARTESIAN_POINT('Ctrl Pts',(22.4978259774408,0.433884304103661,3.6499965589521));
#44586=CARTESIAN_POINT('Ctrl Pts',(22.5216838954723,0.548538061567711,3.90068226732924));
#44587=CARTESIAN_POINT('Ctrl Pts',(22.5455418135037,0.529059256943919,4.17565382996358));
#44588=CARTESIAN_POINT('Ctrl Pts',(22.5693997315351,0.380211173855379,4.40767331583304));
#44589=CARTESIAN_POINT('Ctrl Pts',(22.5932576495665,0.138390873272415,4.54000544018811));
#44590=CARTESIAN_POINT('Ctrl Pts',(22.6171155675979,-0.137269333605106,
4.54029177230974));
#44591=CARTESIAN_POINT('Ctrl Pts',(22.6409734856293,-0.379364264814148,
4.40846158181013));
#44592=CARTESIAN_POINT('Ctrl Pts',(22.6648314036608,-0.528692759685234,
4.17675229015827));
#44593=CARTESIAN_POINT('Ctrl Pts',(22.6886893216921,-0.54874438127821,3.90182058373076));
#44594=CARTESIAN_POINT('Ctrl Pts',(22.7125472397236,-0.434607562942265,
3.65089956353622));
#44595=CARTESIAN_POINT('Ctrl Pts',(22.736405157755,-0.214207731687487,3.48533716867003));
#44596=CARTESIAN_POINT('Ctrl Pts',(22.7602630757864,0.0585913648593265,
3.44563509732658));
#44597=CARTESIAN_POINT('Ctrl Pts',(22.7841209938179,0.31702578011682,3.5414689143437));
#44598=CARTESIAN_POINT('Ctrl Pts',(22.8079789118493,0.498012898707086,3.74946820019106));
#44599=CARTESIAN_POINT('Ctrl Pts',(22.8238841905369,0.537376264140017,3.92891364167179));
#44600=CARTESIAN_POINT('Ctrl Pts',(22.8318368298807,0.534391234777113,4.01792167950194));
#44601=CARTESIAN_POINT('Ctrl Pts',(3.99999999999998,0.254694598474614,4.53673594206822));
#44602=CARTESIAN_POINT('Ctrl Pts',(4.00795263934379,0.165296026927429,4.57915779516171));
#44603=CARTESIAN_POINT('Ctrl Pts',(4.0238579180314,-0.0350146299391769,
4.61842892627033));
#44604=CARTESIAN_POINT('Ctrl Pts',(4.04771583606282,-0.327086058023631,
4.5259865276721));
#44605=CARTESIAN_POINT('Ctrl Pts',(4.07157375409423,-0.539100294705402,
4.30498302442502));
#44606=CARTESIAN_POINT('Ctrl Pts',(4.09543167212566,-0.619328256935644,
4.00937412827253));
#44607=CARTESIAN_POINT('Ctrl Pts',(4.11928959015708,-0.548093442686671,
3.71148804617917));
#44608=CARTESIAN_POINT('Ctrl Pts',(4.1431475081885,-0.342845496867427,3.48414304986991));
#44609=CARTESIAN_POINT('Ctrl Pts',(4.16700542621991,-0.0537568536316998,
3.38294333505492));
#44610=CARTESIAN_POINT('Ctrl Pts',(4.19086334425134,0.248473820944083,3.43262855616194));
#44611=CARTESIAN_POINT('Ctrl Pts',(4.21472126228276,0.489947458130694,3.62105272953394));
#44612=CARTESIAN_POINT('Ctrl Pts',(4.23857918031417,0.611614759069978,3.90213920826301));
#44613=CARTESIAN_POINT('Ctrl Pts',(4.26243709834559,0.583726034554802,4.20715564703007));
#44614=CARTESIAN_POINT('Ctrl Pts',(4.28629501637702,0.413100159498109,4.46151671210738));
#44615=CARTESIAN_POINT('Ctrl Pts',(4.31015293440843,0.141460167127662,4.60302446238992));
#44616=CARTESIAN_POINT('Ctrl Pts',(4.33401085243986,-0.164770755236008,
4.59707625642582));
#44617=CARTESIAN_POINT('Ctrl Pts',(4.35786877047126,-0.430710704813839,
4.44512666775742));
#44618=CARTESIAN_POINT('Ctrl Pts',(4.38172668850269,-0.59133017320549,4.18433147003372));
#44619=CARTESIAN_POINT('Ctrl Pts',(4.40558460653411,-0.607353296958831,
3.87846221409715));
#44620=CARTESIAN_POINT('Ctrl Pts',(4.42944252456553,-0.474862000813124,
3.60231225357117));
#44621=CARTESIAN_POINT('Ctrl Pts',(4.45330044259694,-0.226254007744579,
3.42340778189093));
#44622=CARTESIAN_POINT('Ctrl Pts',(4.47715836062837,0.0776792518003291,
3.38549581251083));
#44623=CARTESIAN_POINT('Ctrl Pts',(4.50101627865978,0.362617819109035,3.49784685630402));
#44624=CARTESIAN_POINT('Ctrl Pts',(4.5248741966912,0.558886451727075,3.73298802180378));
#44625=CARTESIAN_POINT('Ctrl Pts',(4.54873211472262,0.618492123352341,4.03342088939383));
#44626=CARTESIAN_POINT('Ctrl Pts',(4.57259003275404,0.5268596233165,4.32568143907503));
#44627=CARTESIAN_POINT('Ctrl Pts',(4.59644795078546,0.306395594072305,4.5383040055633));
#44628=CARTESIAN_POINT('Ctrl Pts',(4.62030586881688,0.0110094959969652,
4.61929657956068));
#44629=CARTESIAN_POINT('Ctrl Pts',(4.6441637868483,-0.287068723725306,4.54885427056805));
#44630=CARTESIAN_POINT('Ctrl Pts',(4.66802170487971,-0.514950820910697,
4.34420214192463));
#44631=CARTESIAN_POINT('Ctrl Pts',(4.69187962291114,-0.616913415399932,
4.05538321370614));
#44632=CARTESIAN_POINT('Ctrl Pts',(4.71573754094255,-0.568023875442366,
3.75302158112612));
#44633=CARTESIAN_POINT('Ctrl Pts',(4.73959545897398,-0.380237025278099,
3.51105289951885));
#44634=CARTESIAN_POINT('Ctrl Pts',(4.76345337700539,-0.0994718649854296,
3.38864510263028));
#44635=CARTESIAN_POINT('Ctrl Pts',(4.78731129503681,0.205616875855751,3.41573023112194));
#44636=CARTESIAN_POINT('Ctrl Pts',(4.81116921306823,0.460426689658758,3.5856852332931));
#44637=CARTESIAN_POINT('Ctrl Pts',(4.83502713109965,0.60264963606909,3.85695148163183));
#44638=CARTESIAN_POINT('Ctrl Pts',(4.85888504913107,0.597508330613982,4.16319698927494));
#44639=CARTESIAN_POINT('Ctrl Pts',(4.88274296716248,0.446259962523644,4.42953638764361));
#44640=CARTESIAN_POINT('Ctrl Pts',(4.90660088519391,0.185888877718945,4.59084243889714));
#44641=CARTESIAN_POINT('Ctrl Pts',(4.93045880322533,-0.119937101199393,
4.60767141961541));
#44642=CARTESIAN_POINT('Ctrl Pts',(4.95431672125674,-0.396435191853442,
4.47590818560059));
#44643=CARTESIAN_POINT('Ctrl Pts',(4.97817463928816,-0.575994079421511,
4.22777243672773));
#44644=CARTESIAN_POINT('Ctrl Pts',(5.00203255731958,-0.614706724807315,
3.92394012267834));
#44645=CARTESIAN_POINT('Ctrl Pts',(5.025890475351,-0.503106831702736,3.63870652046354));
#44646=CARTESIAN_POINT('Ctrl Pts',(5.04974839338242,-0.268483613891896,
3.44181901543221));
#44647=CARTESIAN_POINT('Ctrl Pts',(5.07360631141384,0.0317911608623165,
3.38142196567243));
#44648=CARTESIAN_POINT('Ctrl Pts',(5.09746422944526,0.32429213081186,3.47228409503311));
#44649=CARTESIAN_POINT('Ctrl Pts',(5.12132214747667,0.537494841237617,3.69218713785082));
#44650=CARTESIAN_POINT('Ctrl Pts',(5.1451800655081,0.619265421915264,3.98735881011802));
#44651=CARTESIAN_POINT('Ctrl Pts',(5.16903798353952,0.549608738483219,4.28562159765047));
#44652=CARTESIAN_POINT('Ctrl Pts',(5.19289590157094,0.34555774745058,4.51404212438126));
#44653=CARTESIAN_POINT('Ctrl Pts',(5.21675381960235,0.0570084743622218,
4.61676534947452));
#44654=CARTESIAN_POINT('Ctrl Pts',(5.24061173763377,-0.245480923587363,
4.56867264627043));
#44655=CARTESIAN_POINT('Ctrl Pts',(5.26446965566519,-0.487943548953736,
4.38152399072137));
#44656=CARTESIAN_POINT('Ctrl Pts',(5.28832757369661,-0.611090685285508,
4.10108232693608));
#44657=CARTESIAN_POINT('Ctrl Pts',(5.31218549172803,-0.584809503288917,
3.79592328078761));
#44658=CARTESIAN_POINT('Ctrl Pts',(5.33604340975945,-0.415526467847156,
3.5406665514248));
#44659=CARTESIAN_POINT('Ctrl Pts',(5.35990132779088,-0.144635892303038,
3.39772936223054));
#44660=CARTESIAN_POINT('Ctrl Pts',(5.38375924582228,0.161622098711782,3.40206374949372));
#44661=CARTESIAN_POINT('Ctrl Pts',(5.40761716385371,0.428359084093981,3.55260983746209));
#44662=CARTESIAN_POINT('Ctrl Pts',(5.43147508188512,0.590350605148055,3.81255500683439));
#44663=CARTESIAN_POINT('Ctrl Pts',(5.45533299991655,0.607985322415754,4.11833558293467));
#44664=CARTESIAN_POINT('Ctrl Pts',(5.47919091794796,0.476951067165249,4.39517988561105));
#44665=CARTESIAN_POINT('Ctrl Pts',(5.50304883597938,0.2292892841064,4.57539194177126));
#44666=CARTESIAN_POINT('Ctrl Pts',(5.5269067540108,-0.0744399746307492,
4.61490499480714));
#44667=CARTESIAN_POINT('Ctrl Pts',(5.55076467204222,-0.359966631867259,
4.5040570269359));
#44668=CARTESIAN_POINT('Ctrl Pts',(5.57462259007364,-0.55747164231658,4.26995338574299));
#44669=CARTESIAN_POINT('Ctrl Pts',(5.59848050810506,-0.618659650999605,
3.96983878834977));
#44670=CARTESIAN_POINT('Ctrl Pts',(5.62233842613648,-0.528568523057477,
3.67709942878664));
#44671=CARTESIAN_POINT('Ctrl Pts',(5.6461963441679,-0.309227993320144,3.46331805450751));
#44672=CARTESIAN_POINT('Ctrl Pts',(5.67005426219932,-0.0142727959960426,
3.38077003484781));
#44673=CARTESIAN_POINT('Ctrl Pts',(5.69391218023074,0.284172488697173,3.4496406091084));
#44674=CARTESIAN_POINT('Ctrl Pts',(5.71777009826216,0.513129859266986,3.65308904601577));
#44675=CARTESIAN_POINT('Ctrl Pts',(5.74162801629357,0.616613001744231,3.94136666067651));
#44676=CARTESIAN_POINT('Ctrl Pts',(5.765485934325,0.569317469330215,4.24398172424487));
#44677=CARTESIAN_POINT('Ctrl Pts',(5.78934385235641,0.382808307322586,4.48693660973462));
#44678=CARTESIAN_POINT('Ctrl Pts',(5.81320177038783,0.102692087527565,4.61082223133738));
#44679=CARTESIAN_POINT('Ctrl Pts',(5.83705968841925,-0.202535146533943,
4.58534517687525));
#44680=CARTESIAN_POINT('Ctrl Pts',(5.86091760645067,-0.458237017319611,
4.41673528603543));
#44681=CARTESIAN_POINT('Ctrl Pts',(5.88477552448209,-0.601887460912657,
4.14622225884759));
#44682=CARTESIAN_POINT('Ctrl Pts',(5.9086334425135,-0.598360014525416,3.83995392008642));
#44683=CARTESIAN_POINT('Ctrl Pts',(5.93249136054493,-0.448517265794504,
3.57282118150817));
#44684=CARTESIAN_POINT('Ctrl Pts',(5.95634927857635,-0.188999790056246,
3.41014534911766));
#44685=CARTESIAN_POINT('Ctrl Pts',(5.98020719660777,0.116733210556207,3.39170495376011));
#44686=CARTESIAN_POINT('Ctrl Pts',(6.00406511463918,0.393921897475357,3.52200944135141));
#44687=CARTESIAN_POINT('Ctrl Pts',(6.02792303267061,0.574785693380153,3.76919531120668));
#44688=CARTESIAN_POINT('Ctrl Pts',(6.05178095070201,0.61509921541814,4.07281983667942));
#44689=CARTESIAN_POINT('Ctrl Pts',(6.07563886873346,0.505003308517799,4.35863675364492));
#44690=CARTESIAN_POINT('Ctrl Pts',(6.09949678676485,0.27142206589204,4.55675943366228));
#44691=CARTESIAN_POINT('Ctrl Pts',(6.12335470479629,-0.0285325303540597,
4.61873507756083));
#44692=CARTESIAN_POINT('Ctrl Pts',(6.14721262282769,-0.321503980505702,
4.52942105023226));
#44693=CARTESIAN_POINT('Ctrl Pts',(6.17107054085913,-0.535870591003297,
4.31063422072759));
#44694=CARTESIAN_POINT('Ctrl Pts',(6.19492845889052,-0.619180264299368,
4.01591706164003));
#44695=CARTESIAN_POINT('Ctrl Pts',(6.21878637692196,-0.551125001039776,
3.71725450231754));
#44696=CARTESIAN_POINT('Ctrl Pts',(6.24264429495337,-0.348226295733882,
3.48783145534908));
#44697=CARTESIAN_POINT('Ctrl Pts',(6.2665022129848,-0.0603247367796791,
3.38345774569467));
#44698=CARTESIAN_POINT('Ctrl Pts',(6.29036013101621,0.242607149567705,3.43020375417728));
#44699=CARTESIAN_POINT('Ctrl Pts',(6.31421804904763,0.485688404846908,3.61560451082823));
#44700=CARTESIAN_POINT('Ctrl Pts',(6.33807596707905,0.61099356578022,3.89627130770405));
#44701=CARTESIAN_POINT('Ctrl Pts',(6.36193388511046,0.585080291527744,4.19994745529594));
#44702=CARTESIAN_POINT('Ctrl Pts',(6.3937444424857,0.363797450650833,4.54512657044717));
#44703=CARTESIAN_POINT('Ctrl Pts',(6.43350763920472,-0.178959141669374,
4.67939801199369));
#44704=CARTESIAN_POINT('Ctrl Pts',(6.48122347526757,-0.668951848353412,
4.21606826543601));
#44705=CARTESIAN_POINT('Ctrl Pts',(6.5289393113304,-0.543175254381078,3.55462676401443));
#44706=CARTESIAN_POINT('Ctrl Pts',(6.57665514739324,0.0806513803028556,
3.30201433154981));
#44707=CARTESIAN_POINT('Ctrl Pts',(6.62437098345608,0.630812951656228,3.69045991683978));
#44708=CARTESIAN_POINT('Ctrl Pts',(6.67208681951892,0.601478580142798,4.36311480674272));
#44709=CARTESIAN_POINT('Ctrl Pts',(6.71980265558175,0.0199087309838695,
4.70234020845997));
#44710=CARTESIAN_POINT('Ctrl Pts',(6.76751849164459,-0.580002689552455,
4.39658285339385));
#44711=CARTESIAN_POINT('Ctrl Pts',(6.81523432770743,-0.64725742864426,3.72664421308375));
#44712=CARTESIAN_POINT('Ctrl Pts',(6.86295016377027,-0.120142281411799,
3.30772876957018));
#44713=CARTESIAN_POINT('Ctrl Pts',(6.91066599983311,0.517310146858294,3.52453857056345));
#44714=CARTESIAN_POINT('Ctrl Pts',(6.95838183589594,0.679704059947864,4.17797090041396));
#44715=CARTESIAN_POINT('Ctrl Pts',(7.00609767195879,0.217917737520193,4.66797035296266));
#44716=CARTESIAN_POINT('Ctrl Pts',(7.05381350802161,-0.443987099894697,
4.54456206689342));
#44717=CARTESIAN_POINT('Ctrl Pts',(7.10152934408447,-0.698171061503544,
3.92107420680554));
#44718=CARTESIAN_POINT('Ctrl Pts',(7.14924518014729,-0.311214160204793,
3.3700650369752));
#44719=CARTESIAN_POINT('Ctrl Pts',(7.19696101621015,0.361535686685884,3.39753487888718));
#44720=CARTESIAN_POINT('Ctrl Pts',(7.24467685227297,0.702281647003851,3.97825768917858));
#44721=CARTESIAN_POINT('Ctrl Pts',(7.29239268833582,0.398111619195611,4.5789468099385));
#44722=CARTESIAN_POINT('Ctrl Pts',(7.34010852439865,-0.271650463017158,
4.64798016059173));
#44723=CARTESIAN_POINT('Ctrl Pts',(7.38782436046149,-0.691951729928866,
4.1219633626529));
#44724=CARTESIAN_POINT('Ctrl Pts',(7.43554019652432,-0.476823084268312,
3.48394573037578));
#44725=CARTESIAN_POINT('Ctrl Pts',(7.48325603258717,0.17617954081454,3.31982867534575));
#44726=CARTESIAN_POINT('Ctrl Pts',(7.53097186865001,0.667393780433987,3.78032341303133));
#44727=CARTESIAN_POINT('Ctrl Pts',(7.57868770471284,0.545730043505963,4.44255054095139));
#44728=CARTESIAN_POINT('Ctrl Pts',(7.62640354077568,-0.077085990144297,
4.69837669746149));
#44729=CARTESIAN_POINT('Ctrl Pts',(7.67411937683852,-0.629112772588521,
4.31287278685955));
#44730=CARTESIAN_POINT('Ctrl Pts',(7.72183521290136,-0.603415615998442,
3.64005298187887));
#44731=CARTESIAN_POINT('Ctrl Pts',(7.76955104896419,-0.0235926144000291,
3.29777806215626));
#44732=CARTESIAN_POINT('Ctrl Pts',(7.81726688502703,0.577895847971041,3.60036435301798));
#44733=CARTESIAN_POINT('Ctrl Pts',(7.86498272108987,0.648693661106154,4.26994220769392));
#44734=CARTESIAN_POINT('Ctrl Pts',(7.9126985571527,0.123786103798515,4.6916279794467));
#44735=CARTESIAN_POINT('Ctrl Pts',(7.96041439321555,-0.514796137313916,
4.47818113561083));
#44736=CARTESIAN_POINT('Ctrl Pts',(8.00813022927838,-0.680633164378164,
3.82561319718015));
#44737=CARTESIAN_POINT('Ctrl Pts',(8.05584606534123,-0.221434283704469,
3.33318734306526));
#44738=CARTESIAN_POINT('Ctrl Pts',(8.10356190140405,0.441111106898351,3.45310581204486));
#44739=CARTESIAN_POINT('Ctrl Pts',(8.1512777374669,0.698577380670183,4.07524562887252));
#44740=CARTESIAN_POINT('Ctrl Pts',(8.19899357352974,0.314529296777622,4.62828622690367));
#44741=CARTESIAN_POINT('Ctrl Pts',(8.24670940959258,-0.358355880000973,
4.60436191534297));
#44742=CARTESIAN_POINT('Ctrl Pts',(8.29442524565541,-0.70215733816079,4.02544275761943));
#44743=CARTESIAN_POINT('Ctrl Pts',(8.34214108171825,-0.401156908608127,
3.42315912408683));
#44744=CARTESIAN_POINT('Ctrl Pts',(8.3898569177811,0.268232082711808,3.35059734274305));
#44745=CARTESIAN_POINT('Ctrl Pts',(8.43757275384392,0.691299425196396,3.8743920139026));
#44746=CARTESIAN_POINT('Ctrl Pts',(8.48528858990677,0.479535868514212,4.51353443142269));
#44747=CARTESIAN_POINT('Ctrl Pts',(8.53300442596961,-0.172592854832336,
4.68109027882443));
#44748=CARTESIAN_POINT('Ctrl Pts',(8.58072026203244,-0.66622690390392,4.22319044326068));
#44749=CARTESIAN_POINT('Ctrl Pts',(8.62843609809529,-0.548054535901959,
3.56033138942427));
#44750=CARTESIAN_POINT('Ctrl Pts',(8.67615193415812,0.0734047453217555,
3.30122678585069));
#44751=CARTESIAN_POINT('Ctrl Pts',(8.72386777022095,0.627455319439314,3.68381637683837));
#44752=CARTESIAN_POINT('Ctrl Pts',(8.7715836062838,0.605304019074675,4.35676225408577));
#44753=CARTESIAN_POINT('Ctrl Pts',(8.81929944234663,0.0272927241942496,
4.70208786391332));
#44754=CARTESIAN_POINT('Ctrl Pts',(8.86701527840948,-0.575781899266294,
4.40267538529889));
#44755=CARTESIAN_POINT('Ctrl Pts',(8.9147311144723,-0.650107145087294,3.73347990440727));
#44756=CARTESIAN_POINT('Ctrl Pts',(8.96244695053515,-0.127428996390418,
3.30903392823725));
#44757=CARTESIAN_POINT('Ctrl Pts',(9.01016278659798,0.512269160438921,3.51911272764658));
#44758=CARTESIAN_POINT('Ctrl Pts',(9.05787862266082,0.681542664962993,4.17079770865984));
#44759=CARTESIAN_POINT('Ctrl Pts',(9.10559445872366,0.224945053369686,4.66563652575022));
#44760=CARTESIAN_POINT('Ctrl Pts',(9.1533102947865,-0.438223061957547,4.54921107910972));
#44761=CARTESIAN_POINT('Ctrl Pts',(9.20102613084934,-0.698964196560635,
3.92843664782408));
#44762=CARTESIAN_POINT('Ctrl Pts',(9.24874196691217,-0.317835754515511,
3.3733799439853));
#44763=CARTESIAN_POINT('Ctrl Pts',(9.29645780297501,0.355166151432911,3.39375807937372));
#44764=CARTESIAN_POINT('Ctrl Pts',(9.34417363903786,0.702013515586798,3.97085749870423));
#44765=CARTESIAN_POINT('Ctrl Pts',(9.39188947510068,0.404191066510942,4.57471892538967));
#44766=CARTESIAN_POINT('Ctrl Pts',(9.43960531116354,-0.264806258220881,
4.65080711970243));
#44767=CARTESIAN_POINT('Ctrl Pts',(9.48732114722635,-0.690627921460452,
4.12924912203773));
#44768=CARTESIAN_POINT('Ctrl Pts',(9.53503698328922,-0.482235337746388,
3.48899966685243));
#44769=CARTESIAN_POINT('Ctrl Pts',(9.58275281935202,0.169001376764621,3.31800968034731));
#44770=CARTESIAN_POINT('Ctrl Pts',(9.63046865541491,0.665041526572246,3.77330189814918));
#44771=CARTESIAN_POINT('Ctrl Pts',(9.6781844914777,0.550363809549371,4.43677447107931));
#44772=CARTESIAN_POINT('Ctrl Pts',(9.72590032754056,-0.0697214622184181,
4.69915032657822));
#44773=CARTESIAN_POINT('Ctrl Pts',(9.7736161636034,-0.625780442428439,4.31948567936979));
#44774=CARTESIAN_POINT('Ctrl Pts',(9.82133199966623,-0.607175613486645,
3.64643241687702));
#44775=CARTESIAN_POINT('Ctrl Pts',(9.86904783572907,-0.030992076082374,
3.29806570630264));
#44776=CARTESIAN_POINT('Ctrl Pts',(9.91676367179191,0.573651961662729,3.59429605827795));
#44777=CARTESIAN_POINT('Ctrl Pts',(9.96447950785474,0.651502576242943,4.26309058249416));
#44778=CARTESIAN_POINT('Ctrl Pts',(10.0121953439176,0.131068350403577,4.69028497663703));
#44779=CARTESIAN_POINT('Ctrl Pts',(10.0599111799804,-0.50972795835719,4.48358005533451));
#44780=CARTESIAN_POINT('Ctrl Pts',(10.1076270160433,-0.682433239785766,
3.83279612838271));
#44781=CARTESIAN_POINT('Ctrl Pts',(10.1553428521061,-0.228449576533966,
3.33555808949935));
#44782=CARTESIAN_POINT('Ctrl Pts',(10.2030586881689,0.435322847997542,3.44848728078164));
#44783=CARTESIAN_POINT('Ctrl Pts',(10.2507745242318,0.699331602909907,4.06787908823615));
#44784=CARTESIAN_POINT('Ctrl Pts',(10.2984903602946,0.321133386270249,4.62493648450936));
#44785=CARTESIAN_POINT('Ctrl Pts',(10.3462061963575,-0.351966560253669,
4.60810509117381));
#44786=CARTESIAN_POINT('Ctrl Pts',(10.3939220324203,-0.701850198794989,
4.03284143571381));
#44787=CARTESIAN_POINT('Ctrl Pts',(10.4416378684831,-0.407214000429435,
3.42741898450738));
#44788=CARTESIAN_POINT('Ctrl Pts',(10.489353704546,0.261373080323254,3.34780649011919));
#44789=CARTESIAN_POINT('Ctrl Pts',(10.5370695406088,0.689937239673316,3.86711333114163));
#44790=CARTESIAN_POINT('Ctrl Pts',(10.5847853766716,0.484921415782374,4.50845204490092));
#44791=CARTESIAN_POINT('Ctrl Pts',(10.6325012127345,-0.165405205696588,
4.68287142228737));
#44792=CARTESIAN_POINT('Ctrl Pts',(10.6802170487973,-0.66383768169814,4.23019946525991));
#44793=CARTESIAN_POINT('Ctrl Pts',(10.7279328848602,-0.552657800140614,
3.5661317972102));
#44794=CARTESIAN_POINT('Ctrl Pts',(10.775648720923,0.0660362430193439,3.30049197570278));
#44795=CARTESIAN_POINT('Ctrl Pts',(10.8233645569858,0.624088188116435,3.67722113622194));
#44796=CARTESIAN_POINT('Ctrl Pts',(10.8710803930487,0.609030347235101,4.3503630939397));
#44797=CARTESIAN_POINT('Ctrl Pts',(10.9187962291115,0.0346905673513346,
4.70176123146349));
#44798=CARTESIAN_POINT('Ctrl Pts',(10.9665120651743,-0.57150609431415,4.40872123214985));
#44799=CARTESIAN_POINT('Ctrl Pts',(11.0142279012372,-0.65287991581936,3.74034623636848));
#44800=CARTESIAN_POINT('Ctrl Pts',(11.0619437373,-0.134704064778877,3.31041528701663));
#44801=CARTESIAN_POINT('Ctrl Pts',(11.1096595733629,0.507172601636502,3.51374059022208));
#44802=CARTESIAN_POINT('Ctrl Pts',(11.1573754094257,0.68330486411552,4.16360539148934));
#44803=CARTESIAN_POINT('Ctrl Pts',(11.2050912454885,0.231947755880478,4.66322884435941));
#44804=CARTESIAN_POINT('Ctrl Pts',(11.2528070815514,-0.432410545554582,
4.55379904436673));
#44805=CARTESIAN_POINT('Ctrl Pts',(11.3005229176142,-0.699679589515398,
3.93580706063847));
#44806=CARTESIAN_POINT('Ctrl Pts',(11.348238753677,-0.324422100469907,3.37676444086124));
#44807=CARTESIAN_POINT('Ctrl Pts',(11.3959545897399,0.348757195312759,3.39004862475285));
#44808=CARTESIAN_POINT('Ctrl Pts',(11.4436704258027,0.701667392320496,3.9634605418422));
#44809=CARTESIAN_POINT('Ctrl Pts',(11.4913862618656,0.410225626419724,4.57042720558968));
#44810=CARTESIAN_POINT('Ctrl Pts',(11.5391020979284,-0.257932644354891,
4.65356178929341));
#44811=CARTESIAN_POINT('Ctrl Pts',(11.5868179339912,-0.689227399014534,
4.13652052554825));
#44812=CARTESIAN_POINT('Ctrl Pts',(11.6345337700541,-0.487594028032435,
3.49411036255383));
#44813=CARTESIAN_POINT('Ctrl Pts',(11.6822496061169,0.161804441490335,3.31626643773886));
#44814=CARTESIAN_POINT('Ctrl Pts',(11.7299654421798,0.662615402711184,3.76630556374144));
#44815=CARTESIAN_POINT('Ctrl Pts',(11.7776812782426,0.554936443973853,4.43094988641136));
#44816=CARTESIAN_POINT('Ctrl Pts',(11.8253971143054,-0.062349190059417,
4.69984629737339));
#44817=CARTESIAN_POINT('Ctrl Pts',(11.8731129503683,-0.622378603495518,
4.32606308493799));
#44818=CARTESIAN_POINT('Ctrl Pts',(11.9208287864311,-0.610868168815925,
3.65285112447858));
#44819=CARTESIAN_POINT('Ctrl Pts',(11.9685446224939,-0.0383880952977111,
3.29843131798253));
#44820=CARTESIAN_POINT('Ctrl Pts',(12.0162604585568,0.569344356809164,3.58827282720487));
#44821=CARTESIAN_POINT('Ctrl Pts',(12.0639762946196,0.654239125569198,4.25620973444184));
#44822=CARTESIAN_POINT('Ctrl Pts',(12.1116921306825,0.138336038556134,4.68886530024737));
#44823=CARTESIAN_POINT('Ctrl Pts',(12.1594079667453,-0.50460316123658,4.48892526128066));
#44824=CARTESIAN_POINT('Ctrl Pts',(12.2071238028081,-0.684157513748105,
3.83999763179777));
#44825=CARTESIAN_POINT('Ctrl Pts',(12.254839638871,-0.235439494268261,3.33800263898788));
#44826=CARTESIAN_POINT('Ctrl Pts',(12.3025554749338,0.429486235500398,3.44393000893412));
#44827=CARTESIAN_POINT('Ctrl Pts',(12.3502713109967,0.700008146713868,4.06050500791278));
#44828=CARTESIAN_POINT('Ctrl Pts',(12.3979871470595,0.327701805790174,4.62151732713591));
#44829=CARTESIAN_POINT('Ctrl Pts',(12.4457029831223,-0.345538145731053,
4.61178072157682));
#44830=CARTESIAN_POINT('Ctrl Pts',(12.4934188191852,-0.701465101239671,
4.04023646593735));
#44831=CARTESIAN_POINT('Ctrl Pts',(12.541134655248,-0.413225860851952,3.43174244451));
#44832=CARTESIAN_POINT('Ctrl Pts',(12.5888504913108,0.254485045853264,3.34508808005552));
#44833=CARTESIAN_POINT('Ctrl Pts',(12.6365663273737,0.688498419195676,3.85984940880123));
#44834=CARTESIAN_POINT('Ctrl Pts',(12.6842821634365,0.490253100280801,4.50331318193882));
#44835=CARTESIAN_POINT('Ctrl Pts',(12.7319979994994,-0.158199184135511,
4.68457671563321));
#44836=CARTESIAN_POINT('Ctrl Pts',(12.7797138355622,-0.661374723552845,
4.23718291779492));
#44837=CARTESIAN_POINT('Ctrl Pts',(12.827429671625,-0.557199677773407,3.57198039701723));
#44838=CARTESIAN_POINT('Ctrl Pts',(12.8751455076879,0.058660405724426,3.29983486358678));
#44839=CARTESIAN_POINT('Ctrl Pts',(12.9228613437507,0.62065173603916,3.67066174834999));
#44840=CARTESIAN_POINT('Ctrl Pts',(12.9705771798135,0.612689027194643,4.34392501712378));
#44841=CARTESIAN_POINT('Ctrl Pts',(13.0182930158764,0.0420845572448178,
4.7013566507062));
#44842=CARTESIAN_POINT('Ctrl Pts',(13.0660088519392,-0.567166809177069,
4.4147216801859));
#44843=CARTESIAN_POINT('Ctrl Pts',(13.1137246880021,-0.655580167748548,
3.74724140943759));
#44844=CARTESIAN_POINT('Ctrl Pts',(13.1614405240649,-0.141964170879043,
3.31187324159358));
#44845=CARTESIAN_POINT('Ctrl Pts',(13.2091563601277,0.502019708508231,3.50842246418533));
#44846=CARTESIAN_POINT('Ctrl Pts',(13.2568721961906,0.684991165006287,4.15639490180834));
#44847=CARTESIAN_POINT('Ctrl Pts',(13.3045880322534,0.238924694735218,4.66074749465585));
#44848=CARTESIAN_POINT('Ctrl Pts',(13.3523038683163,-0.426549999040181,
4.55832549625387));
#44849=CARTESIAN_POINT('Ctrl Pts',(13.4000197043791,-0.700317265381609,
3.94318460369993));
#44850=CARTESIAN_POINT('Ctrl Pts',(13.4477355404419,-0.330972411156884,
3.38021816378559));
#44851=CARTESIAN_POINT('Ctrl Pts',(13.4954513765048,0.342309500898352,3.3864069206363));
#44852=CARTESIAN_POINT('Ctrl Pts',(13.5431672125676,0.70124333116994,3.95606764360979));
#44853=CARTESIAN_POINT('Ctrl Pts',(13.5908830486304,0.416214620412595,4.5660721254426));
#44854=CARTESIAN_POINT('Ctrl Pts',(13.6385988846933,-0.251030380554765,
4.65624386434224));
#44855=CARTESIAN_POINT('Ctrl Pts',(13.6863147207561,-0.687750320459788,
4.14377676500662));
#44856=CARTESIAN_POINT('Ctrl Pts',(13.734030556819,-0.492898558687668,3.49927725007553));
#44857=CARTESIAN_POINT('Ctrl Pts',(13.7817463928818,0.15458953374652,3.31459914100992));
#44858=CARTESIAN_POINT('Ctrl Pts',(13.8294622289446,0.660115678675556,3.75933518700271));
#44859=CARTESIAN_POINT('Ctrl Pts',(13.8771780650075,0.559447438691528,4.42507743387505));
#44860=CARTESIAN_POINT('Ctrl Pts',(13.9248939010703,-0.0549699924482557,
4.7004645325629));
#44861=CARTESIAN_POINT('Ctrl Pts',(13.9726097371331,-0.61890763370075,4.33260427296601));
#44862=CARTESIAN_POINT('Ctrl Pts',(14.020325573196,-0.614492871807821,3.65930839172987));
#44863=CARTESIAN_POINT('Ctrl Pts',(14.0680414092588,-0.0457798505455885,
3.29887485658241));
#44864=CARTESIAN_POINT('Ctrl Pts',(14.1157572453217,0.564973511886205,3.58229532883235));
#44865=CARTESIAN_POINT('Ctrl Pts',(14.1634730813845,0.656903005118004,4.24930042782804));
#44866=CARTESIAN_POINT('Ctrl Pts',(14.2111889174473,0.145588360997982,4.6873691079691));
#44867=CARTESIAN_POINT('Ctrl Pts',(14.2589047535102,-0.499422315191365,
4.49421615972892));
#44868=CARTESIAN_POINT('Ctrl Pts',(14.306620589573,-0.685805794740406,3.8472169075166));
#44869=CARTESIAN_POINT('Ctrl Pts',(14.3543364256359,-0.242403260500786,
3.34052072000184));
#44870=CARTESIAN_POINT('Ctrl Pts',(14.4020522616987,0.423601917710294,3.43943450270243));
#44871=CARTESIAN_POINT('Ctrl Pts',(14.4497680977615,0.700606936934704,4.05312420698026));
#44872=CARTESIAN_POINT('Ctrl Pts',(14.4974839338244,0.334233825748585,4.61802913456711));
#44873=CARTESIAN_POINT('Ctrl Pts',(14.5451997698872,-0.339071350470923,
4.61538839828042));
#44874=CARTESIAN_POINT('Ctrl Pts',(14.59291560595,-0.701002088269634,4.04762702688518));
#44875=CARTESIAN_POINT('Ctrl Pts',(14.6406314420129,-0.419191822106764,
3.43612902386528));
#44876=CARTESIAN_POINT('Ctrl Pts',(14.6883472780757,0.24756874439201,3.34244241450009));
#44877=CARTESIAN_POINT('Ctrl Pts',(14.7360631141386,0.686983123580828,3.85260105372344));
#44878=CARTESIAN_POINT('Ctrl Pts',(14.7837789502014,0.495530329791292,4.49811841333687));
#44879=CARTESIAN_POINT('Ctrl Pts',(14.8314947862642,-0.150975590559777,
4.68620596944608));
#44880=CARTESIAN_POINT('Ctrl Pts',(14.8792106223271,-0.658838303041738,
4.24414002517693));
#44881=CARTESIAN_POINT('Ctrl Pts',(14.9269264583899,-0.561679664310124,
3.57787653921065));
#44882=CARTESIAN_POINT('Ctrl Pts',(14.9746422944528,0.0512780527100071,
3.29925552249156));
#44883=CARTESIAN_POINT('Ctrl Pts',(15.0223581305156,0.617146344912281,3.6641389418082));
#44884=CARTESIAN_POINT('Ctrl Pts',(15.0700739665784,0.616279652564493,4.337448738749));
#44885=CARTESIAN_POINT('Ctrl Pts',(15.1177898026413,0.0494738725853903,
4.70087416658037));
#44886=CARTESIAN_POINT('Ctrl Pts',(15.1655056387041,-0.562764525842253,
4.42067606290572));
#44887=CARTESIAN_POINT('Ctrl Pts',(15.2132214747669,-0.658207600943685,
3.75416465773151));
#44888=CARTESIAN_POINT('Ctrl Pts',(15.2609373108298,-0.14920850827279,3.31340763002542));
#44889=CARTESIAN_POINT('Ctrl Pts',(15.3086531468926,0.496811053413015,3.50315894024854));
#44890=CARTESIAN_POINT('Ctrl Pts',(15.3563689829554,0.686601380328997,4.14916704052379));
#44891=CARTESIAN_POINT('Ctrl Pts',(15.4040848190183,0.245875094968658,4.6581927522561));
#44892=CARTESIAN_POINT('Ctrl Pts',(15.4518006550811,-0.420642073376032,
4.56278993199436));
#44893=CARTESIAN_POINT('Ctrl Pts',(15.499516491144,-0.700877153329261,3.95056845754601));
#44894=CARTESIAN_POINT('Ctrl Pts',(15.5472323272068,-0.337485958999024,
3.3837407291352));
#44895=CARTESIAN_POINT('Ctrl Pts',(15.5949481632696,0.335823784368978,3.38283337152726));
#44896=CARTESIAN_POINT('Ctrl Pts',(15.6426639993325,0.70074137923783,3.94867962517506));
#44897=CARTESIAN_POINT('Ctrl Pts',(15.6903798353953,0.422157383260532,4.56165416869007));
#44898=CARTESIAN_POINT('Ctrl Pts',(15.7380956714582,-0.244100233491204,
4.65885304693675));
#44899=CARTESIAN_POINT('Ctrl Pts',(15.785811507521,-0.686196849863089,4.15101703442422));
#44900=CARTESIAN_POINT('Ctrl Pts',(15.8335273435838,-0.498148340509996,
3.50449975550414));
#44901=CARTESIAN_POINT('Ctrl Pts',(15.8812431796467,0.147357454930898,3.3130079753559));
#44902=CARTESIAN_POINT('Ctrl Pts',(15.9289590157095,0.657542632122849,3.75239154216938));
#44903=CARTESIAN_POINT('Ctrl Pts',(15.9766748517723,0.563896292642505,4.41915776575455));
#44904=CARTESIAN_POINT('Ctrl Pts',(16.0243906878352,-0.0475846890311933,
4.70100496347609));
#44905=CARTESIAN_POINT('Ctrl Pts',(16.072106523898,-0.615367918582998,4.33910851688972));
#44906=CARTESIAN_POINT('Ctrl Pts',(16.1198223599609,-0.618049319847516,
3.66580350138828));
#44907=CARTESIAN_POINT('Ctrl Pts',(16.1675381960237,-0.0531665207849041,
3.29939627283611));
#44908=CARTESIAN_POINT('Ctrl Pts',(16.2152540320865,0.560539912386559,3.57636422711252));
#44909=CARTESIAN_POINT('Ctrl Pts',(16.2629698681494,0.659493918998266,4.24236343010572));
#44910=CARTESIAN_POINT('Ctrl Pts',(16.3106857042122,0.152824512175573,4.68579656599215));
#44911=CARTESIAN_POINT('Ctrl Pts',(16.358401540275,-0.494185995685336,4.49945216299141));
#44912=CARTESIAN_POINT('Ctrl Pts',(16.4061173763379,-0.687377899679438,
3.85445315365633));
#44913=CARTESIAN_POINT('Ctrl Pts',(16.4538332124007,-0.249340101729437,
3.34311205284473));
#44914=CARTESIAN_POINT('Ctrl Pts',(16.5015490484636,0.417670548229327,3.43500126142608));
#44915=CARTESIAN_POINT('Ctrl Pts',(16.5492648845264,0.701127907061643,4.04573750526291));
#44916=CARTESIAN_POINT('Ctrl Pts',(16.5969807205892,0.340728720599694,4.61447229425484));
#44917=CARTESIAN_POINT('Ctrl Pts',(16.6446965566521,-0.3325668927742,4.61892772056098));
#44918=CARTESIAN_POINT('Ctrl Pts',(16.6924123927149,-0.700461211314163,
4.05501229764889));
#44919=CARTESIAN_POINT('Ctrl Pts',(16.7401282287777,-0.425111221523205,
3.4405782353328));
#44920=CARTESIAN_POINT('Ctrl Pts',(16.7878440648406,0.240624944169445,3.3398697873209));
#44921=CARTESIAN_POINT('Ctrl Pts',(16.8355599009034,0.685391521140609,3.84536907102113));
#44922=CARTESIAN_POINT('Ctrl Pts',(16.8832757369663,0.500752518144239,4.49286831610534));
#44923=CARTESIAN_POINT('Ctrl Pts',(16.9309915730291,-0.143735227331884,
4.68775900275617));
#44924=CARTESIAN_POINT('Ctrl Pts',(16.978707409092,-0.656228701898373,4.25107001464348));
#44925=CARTESIAN_POINT('Ctrl Pts',(17.0264232451548,-0.566097262135119,
3.58381956887496));
#44926=CARTESIAN_POINT('Ctrl Pts',(17.0741390812176,0.0438900039728252,
3.29875401676759));
#44927=CARTESIAN_POINT('Ctrl Pts',(17.1218549172805,0.613572404098014,3.65765344111895));
#44928=CARTESIAN_POINT('Ctrl Pts',(17.1695707533433,0.619801824515016,4.33093497816967));
#44929=CARTESIAN_POINT('Ctrl Pts',(17.2172865894061,0.0568576926029748,
4.70031383267802));
#44930=CARTESIAN_POINT('Ctrl Pts',(17.265002425469,-0.558299733294432,4.42658371892475));
#44931=CARTESIAN_POINT('Ctrl Pts',(17.3127182615318,-0.66076192356197,3.76111521224867));
#44932=CARTESIAN_POINT('Ctrl Pts',(17.3604340975947,-0.156436272293483,
3.31501828187956));
#44933=CARTESIAN_POINT('Ctrl Pts',(17.4081499336575,0.491547214903555,3.49795060305896));
#44934=CARTESIAN_POINT('Ctrl Pts',(17.4558657697204,0.688135331228569,4.14192261047223));
#44935=CARTESIAN_POINT('Ctrl Pts',(17.5035816057831,0.252798184563325,4.65556490092881));
#44936=CARTESIAN_POINT('Ctrl Pts',(17.551297441846,-0.414687424786488,4.56719185569987));
#44937=CARTESIAN_POINT('Ctrl Pts',(17.5990132779088,-0.701359191168653,
3.95795780201324));
#44938=CARTESIAN_POINT('Ctrl Pts',(17.6467291139717,-0.343962020502345,
3.38733174564023));
#44939=CARTESIAN_POINT('Ctrl Pts',(17.6944449500345,0.329300766127249,3.37932837435862));
#44940=CARTESIAN_POINT('Ctrl Pts',(17.7421607860974,0.700161592278611,3.94129730716402));
#44941=CARTESIAN_POINT('Ctrl Pts',(17.7898766221602,0.428053254869629,4.55717382605774));
#44942=CARTESIAN_POINT('Ctrl Pts',(17.837592458223,-0.23714297293205,4.66138904726133));
#44943=CARTESIAN_POINT('Ctrl Pts',(17.8853082942859,-0.684567159776581,
4.15824052958626));
#44944=CARTESIAN_POINT('Ctrl Pts',(17.9330241303487,-0.503342790378573,
3.50977729874859));
#44945=CARTESIAN_POINT('Ctrl Pts',(17.9807399664116,0.140109008348428,3.31149311751593));
#44946=CARTESIAN_POINT('Ctrl Pts',(18.0284558024744,0.654896548854854,3.7454754005085));
#44947=CARTESIAN_POINT('Ctrl Pts',(18.0761716385372,0.568282511669218,4.41319153957849));
#44948=CARTESIAN_POINT('Ctrl Pts',(18.1238874746001,-0.040194100132671,
4.70146753008449));
#44949=CARTESIAN_POINT('Ctrl Pts',(18.1716033106629,-0.611759851316993,
4.34557509424858));
#44950=CARTESIAN_POINT('Ctrl Pts',(18.2193191467258,-0.621537117901666,
3.67233573200791));
#44951=CARTESIAN_POINT('Ctrl Pts',(18.2670349827885,-0.0605472855394143,
3.29999550882718));
#44952=CARTESIAN_POINT('Ctrl Pts',(18.3147508188514,0.556044050773433,3.57048018084402));
#44953=CARTESIAN_POINT('Ctrl Pts',(18.3624666549143,0.662011579423562,4.23539951180373));
#44954=CARTESIAN_POINT('Ctrl Pts',(18.4101824909771,0.160043688331546,4.684147848987));
#44955=CARTESIAN_POINT('Ctrl Pts',(18.4578983270399,-0.488894784343999,
4.50463268947774));
#44956=CARTESIAN_POINT('Ctrl Pts',(18.5056141631028,-0.68887365394326,3.86170556644909));
#44957=CARTESIAN_POINT('Ctrl Pts',(18.5533299991656,-0.256249247442801,
3.34577634968359));
#44958=CARTESIAN_POINT('Ctrl Pts',(18.6010458352284,0.41169278588589,3.4306307775285));
#44959=CARTESIAN_POINT('Ctrl Pts',(18.6487616712913,0.701570999227752,4.03834572324048));
#44960=CARTESIAN_POINT('Ctrl Pts',(18.6964775073541,0.347185768921481,4.6108472012761));
#44961=CARTESIAN_POINT('Ctrl Pts',(18.744193343417,-0.326025495125306,4.62239829528727));
#44962=CARTESIAN_POINT('Ctrl Pts',(18.7919091794798,-0.699842530451103,
4.06239145790787));
#44963=CARTESIAN_POINT('Ctrl Pts',(18.8396250155426,-0.430983401602837,
3.44508958471478));
#44964=CARTESIAN_POINT('Ctrl Pts',(18.8873408516055,0.233654416470602,3.33737048427408));
#44965=CARTESIAN_POINT('Ctrl Pts',(18.9350566876683,0.683723788661416,3.83815426398688));
#44966=CARTESIAN_POINT('Ctrl Pts',(18.9827725237312,0.505919085286118,4.48756347340344));
#44967=CARTESIAN_POINT('Ctrl Pts',(19.030488359794,-0.136478898681533,4.68923564305365));
#44968=CARTESIAN_POINT('Ctrl Pts',(19.0782041958568,-0.653546209976322,
4.2579721164561));
#44969=CARTESIAN_POINT('Ctrl Pts',(19.1259200319197,-0.570451980578726,
3.58980882586423));
#44970=CARTESIAN_POINT('Ctrl Pts',(19.1736358679825,0.0364970801727598,
3.29833040216201));
#44971=CARTESIAN_POINT('Ctrl Pts',(19.2213517040453,0.609930310515188,3.65120596658116));
#44972=CARTESIAN_POINT('Ctrl Pts',(19.2690675401082,0.623255151928734,4.32438445905389));
#44973=CARTESIAN_POINT('Ctrl Pts',(19.316783376171,0.0642351969327414,4.69967571095415));
#44974=CARTESIAN_POINT('Ctrl Pts',(19.3644992122339,-0.553772927074266,
4.43244399258532));
#44975=CARTESIAN_POINT('Ctrl Pts',(19.4122150482967,-0.663242852612724,
3.76809229994096));
#44976=CARTESIAN_POINT('Ctrl Pts',(19.4599308843595,-0.163646658734412,
3.3167050201661));
#44977=CARTESIAN_POINT('Ctrl Pts',(19.5076467204224,0.486228775054438,3.49279802752061));
#44978=CARTESIAN_POINT('Ctrl Pts',(19.5553625564852,0.689592852244711,4.13466242315333));
#44979=CARTESIAN_POINT('Ctrl Pts',(19.6030783925481,0.259693185238344,4.65286421968052));
#44980=CARTESIAN_POINT('Ctrl Pts',(19.6507942286109,-0.408686697131164,
4.57153080275077));
#44981=CARTESIAN_POINT('Ctrl Pts',(19.6985100646738,-0.701763358503738,
3.96535177039745));
#44982=CARTESIAN_POINT('Ctrl Pts',(19.7462259007365,-0.350399813749482,
3.39099090115443));
#44983=CARTESIAN_POINT('Ctrl Pts',(19.7939417367994,0.322741052541778,3.37589215469092));
#44984=CARTESIAN_POINT('Ctrl Pts',(19.8416575728622,0.699504257835039,3.93392181877779));
#44985=CARTESIAN_POINT('Ctrl Pts',(19.8893734089251,0.433901159015506,4.55263101135276));
#44986=CARTESIAN_POINT('Ctrl Pts',(19.9370892449879,-0.23015857608315,4.663852686053));
#44987=CARTESIAN_POINT('Ctrl Pts',(19.9848050810507,-0.682862933423436,
4.16544436654047));
#44988=CARTESIAN_POINT('Ctrl Pts',(20.0325209171136,-0.508478494849655,
3.51511322409123));
#44989=CARTESIAN_POINT('Ctrl Pts',(20.0802367531764,0.132839643288252,3.31004731418368));
#44990=CARTESIAN_POINT('Ctrl Pts',(20.1279525892393,0.652187835720725,3.73860154375571));
#44991=CARTESIAN_POINT('Ctrl Pts',(20.1756684253021,0.572586513039731,4.4071529569233));
#44992=CARTESIAN_POINT('Ctrl Pts',(20.2233842613649,-0.0327629883405684,
4.70190215105461));
#44993=CARTESIAN_POINT('Ctrl Pts',(20.2711000974278,-0.608151935097038,
4.35190888358257));
#44994=CARTESIAN_POINT('Ctrl Pts',(20.3188159334906,-0.624827148513498,
3.67908301574286));
#44995=CARTESIAN_POINT('Ctrl Pts',(20.3665317695535,-0.0681655280739813,
3.30033184185188));
#44996=CARTESIAN_POINT('Ctrl Pts',(20.4142476056163,0.551956769749184,3.56531418539817));
#44997=CARTESIAN_POINT('Ctrl Pts',(20.4540108023353,0.644905999548395,4.11665253813788));
#44998=CARTESIAN_POINT('Ctrl Pts',(20.4858213597105,0.416382673412033,4.45708139504444));
#44999=CARTESIAN_POINT('Ctrl Pts',(20.509679277742,0.148137151166912,4.60177085628536));
#45000=CARTESIAN_POINT('Ctrl Pts',(20.5335371957734,-0.159214575149101,
4.59858486262053));
#45001=CARTESIAN_POINT('Ctrl Pts',(20.5573951138048,-0.426074836374489,
4.44942877587387));
#45002=CARTESIAN_POINT('Ctrl Pts',(20.5812530318362,-0.589577924844292,
4.19016123618585));
#45003=CARTESIAN_POINT('Ctrl Pts',(20.6051109498677,-0.608473233900696,
3.88450759853215));
#45004=CARTESIAN_POINT('Ctrl Pts',(20.6289688678991,-0.478813304308425,
3.60703485797333));
#45005=CARTESIAN_POINT('Ctrl Pts',(20.6528267859305,-0.231947052182395,
3.42568465323223));
#45006=CARTESIAN_POINT('Ctrl Pts',(20.6766847039619,0.0715712039811096,
3.38475332414555));
#45007=CARTESIAN_POINT('Ctrl Pts',(20.7005426219933,0.357622970648114,3.49427550111266));
#45008=CARTESIAN_POINT('Ctrl Pts',(20.7244005400248,0.556207844932749,3.72745636179159));
#45009=CARTESIAN_POINT('Ctrl Pts',(20.7482584580561,0.618794460414918,4.02728407199912));
#45010=CARTESIAN_POINT('Ctrl Pts',(20.7721163760876,0.530063832205264,4.32043875618714));
#45011=CARTESIAN_POINT('Ctrl Pts',(20.7959742941189,0.311720881859749,4.53523813880796));
#45012=CARTESIAN_POINT('Ctrl Pts',(20.8198322121505,0.01715224242355,4.619156844639));
#45013=CARTESIAN_POINT('Ctrl Pts',(20.8436901301818,-0.281609823618225,
4.55167503361081));
#45014=CARTESIAN_POINT('Ctrl Pts',(20.8675480482133,-0.511511021444125,
4.34929354512778));
#45015=CARTESIAN_POINT('Ctrl Pts',(20.8914059662447,-0.616333626991818,
4.06150032559224));
#45016=CARTESIAN_POINT('Ctrl Pts',(20.9152638842761,-0.570445985619195,
3.75866857192897));
#45017=CARTESIAN_POINT('Ctrl Pts',(20.9391218023075,-0.385068702031786,
3.51484894167474));
#45018=CARTESIAN_POINT('Ctrl Pts',(20.9629797203389,-0.105531663562905,
3.38966195221662));
#45019=CARTESIAN_POINT('Ctrl Pts',(20.9868376383704,0.199810758127152,3.41371924506628));
#45020=CARTESIAN_POINT('Ctrl Pts',(21.0106955564018,0.456293997792742,3.58113815016051));
#45021=CARTESIAN_POINT('Ctrl Pts',(21.0345534744332,0.60120093052663,3.85098018832832));
#45022=CARTESIAN_POINT('Ctrl Pts',(21.0584113924646,0.599097856858477,4.15726162902184));
#45023=CARTESIAN_POINT('Ctrl Pts',(21.082269310496,0.450499039416452,4.42508831804098));
#45024=CARTESIAN_POINT('Ctrl Pts',(21.1061272285275,0.191740934787398,4.58896933394457));
#45025=CARTESIAN_POINT('Ctrl Pts',(21.1299851465589,-0.113903050943465,
4.60883130459215));
#45026=CARTESIAN_POINT('Ctrl Pts',(21.1538430645903,-0.391694638258801,
4.47981743698434));
#45027=CARTESIAN_POINT('Ctrl Pts',(21.1777009826217,-0.573706216867813,
4.23347513609622));
#45028=CARTESIAN_POINT('Ctrl Pts',(21.2015589006531,-0.615430998064313,
3.9300418046833));
#45029=CARTESIAN_POINT('Ctrl Pts',(21.2254168186846,-0.506666136201032,
3.64371515765586));
#45030=CARTESIAN_POINT('Ctrl Pts',(21.2492747367159,-0.27400760274365,3.44450985958179));
#45031=CARTESIAN_POINT('Ctrl Pts',(21.2731326547474,0.0256532534100022,
3.38113703208972));
#45032=CARTESIAN_POINT('Ctrl Pts',(21.2969905727788,0.319041190319967,3.46909305773936));
#45033=CARTESIAN_POINT('Ctrl Pts',(21.3208484908102,0.534414865691478,3.68687029238709));
#45034=CARTESIAN_POINT('Ctrl Pts',(21.3447064088416,0.619109549231529,3.98121627002784));
#45035=CARTESIAN_POINT('Ctrl Pts',(21.3685643268731,0.552415083779586,4.28015538130547));
#45036=CARTESIAN_POINT('Ctrl Pts',(21.3924222449044,0.350640082858436,4.51058887057447));
#45037=CARTESIAN_POINT('Ctrl Pts',(21.4162801629359,0.0631240304344945,
4.61616947282646));
#45038=CARTESIAN_POINT('Ctrl Pts',(21.4401380809673,-0.239827566894842,
4.57107985485291));
#45039=CARTESIAN_POINT('Ctrl Pts',(21.4639959989987,-0.484134791346583,
4.38634565646493));
#45040=CARTESIAN_POINT('Ctrl Pts',(21.4878539170302,-0.610057871747176,
4.10713942122688));
#45041=CARTESIAN_POINT('Ctrl Pts',(21.5117118350615,-0.586805184862796,
3.80173467907963));
#45042=CARTESIAN_POINT('Ctrl Pts',(21.535569753093,-0.420062646027161,3.5448112085363));
#45043=CARTESIAN_POINT('Ctrl Pts',(21.5594276711244,-0.150603347961132,
3.39919379659958));
#45044=CARTESIAN_POINT('Ctrl Pts',(21.5832855891558,0.155682571034224,3.40048986702667));
#45045=CARTESIAN_POINT('Ctrl Pts',(21.6071435071872,0.423899860703612,3.54838249529388));
#45046=CARTESIAN_POINT('Ctrl Pts',(21.6310014252187,0.588462087630599,3.80670790527556));
#45047=CARTESIAN_POINT('Ctrl Pts',(21.6548593432501,0.609129304746478,4.11229849758833));
#45048=CARTESIAN_POINT('Ctrl Pts',(21.6787172612815,0.480847814502724,4.39042904829107));
#45049=CARTESIAN_POINT('Ctrl Pts',(21.7025751793129,0.234985935581564,4.57308906161293));
#45050=CARTESIAN_POINT('Ctrl Pts',(21.7264330973443,-0.0683364054776661,
4.61561318873779));
#45051=CARTESIAN_POINT('Ctrl Pts',(21.7502910153758,-0.35494863395129,4.5076031222497));
#45052=CARTESIAN_POINT('Ctrl Pts',(21.7741489334072,-0.554766252817153,
4.2754702655401));
#45053=CARTESIAN_POINT('Ctrl Pts',(21.7980068514386,-0.618928411339905,
3.9759774252466));
#45054=CARTESIAN_POINT('Ctrl Pts',(21.82186476947,-0.531745714018629,3.68235875884208));
#45055=CARTESIAN_POINT('Ctrl Pts',(21.8457226875014,-0.314536705157368,
3.46641202827438));
#45056=CARTESIAN_POINT('Ctrl Pts',(21.8695806055329,-0.0204149040773093,
3.3809420914381));
#45057=CARTESIAN_POINT('Ctrl Pts',(21.8934385235643,0.278698897140474,3.44684867604406));
#45058=CARTESIAN_POINT('Ctrl Pts',(21.9172964415957,0.509663226401888,3.6480158268968));
#45059=CARTESIAN_POINT('Ctrl Pts',(21.9411543596271,0.616001013860485,3.93525269592965));
#45060=CARTESIAN_POINT('Ctrl Pts',(21.9650122776585,0.571709773899469,4.23832204448885));
#45061=CARTESIAN_POINT('Ctrl Pts',(21.98887019569,0.387619921158457,4.48311516140836));
#45062=CARTESIAN_POINT('Ctrl Pts',(22.0127281137213,0.108746439139576,4.60977346157076));
#45063=CARTESIAN_POINT('Ctrl Pts',(22.0365860317528,-0.196718509442517,
4.5873255404835));
#45064=CARTESIAN_POINT('Ctrl Pts',(22.0604439497842,-0.454080423961193,
4.42126052632156));
#45065=CARTESIAN_POINT('Ctrl Pts',(22.0843018678156,-0.600407305919173,
4.15218583856754));
#45066=CARTESIAN_POINT('Ctrl Pts',(22.1081597858471,-0.599918246812857,
3.84589756782496));
#45067=CARTESIAN_POINT('Ctrl Pts',(22.1320177038785,-0.452732834916613,
3.57729153941473));
#45068=CARTESIAN_POINT('Ctrl Pts',(22.1558756219099,-0.194841912687001,
3.41204924396571));
#45069=CARTESIAN_POINT('Ctrl Pts',(22.1797335399413,0.110693164578993,3.39057692382254));
#45070=CARTESIAN_POINT('Ctrl Pts',(22.2035914579728,0.389160747889314,3.51812514615901));
#45071=CARTESIAN_POINT('Ctrl Pts',(22.2274493760041,0.572467927805029,3.76350489626149));
#45072=CARTESIAN_POINT('Ctrl Pts',(22.2513072940356,0.615791105677536,4.06671414123586));
#45073=CARTESIAN_POINT('Ctrl Pts',(22.2751652120669,0.508536584364246,4.35360996140145));
#45074=CARTESIAN_POINT('Ctrl Pts',(22.2990231300984,0.276931015980992,4.55403851389998));
#45075=CARTESIAN_POINT('Ctrl Pts',(22.3228810481298,-0.0223917293827815,
4.61898955797298));
#45076=CARTESIAN_POINT('Ctrl Pts',(22.3467389661613,-0.31623908674035,4.53258079431836));
#45077=CARTESIAN_POINT('Ctrl Pts',(22.3705968841927,-0.532757373651304,
4.31594151899069));
#45078=CARTESIAN_POINT('Ctrl Pts',(22.3944548022241,-0.619001969851995,
4.02204593667267));
#45079=CARTESIAN_POINT('Ctrl Pts',(22.4183127202555,-0.553883724721699,
3.72275952141814));
#45080=CARTESIAN_POINT('Ctrl Pts',(22.4421706382869,-0.35332581843718,3.49126595675675));
#45081=CARTESIAN_POINT('Ctrl Pts',(22.4660285563184,-0.0663701307507445,
3.38417172009386));
#45082=CARTESIAN_POINT('Ctrl Pts',(22.4898864743497,0.236814872379406,3.42766427875767));
#45083=CARTESIAN_POINT('Ctrl Pts',(22.5137443923812,0.482092168510832,3.61110849992699));
#45084=CARTESIAN_POINT('Ctrl Pts',(22.5376023104126,0.609484835267769,3.88964730767638));
#45085=CARTESIAN_POINT('Ctrl Pts',(22.561460228444,0.587841786482003,4.19517031382209));
#45086=CARTESIAN_POINT('Ctrl Pts',(22.5853181464754,0.422455543015367,4.45296893898932));
#45087=CARTESIAN_POINT('Ctrl Pts',(22.6091760645069,0.153767157666155,4.60000417439789));
#45088=CARTESIAN_POINT('Ctrl Pts',(22.6330339825383,-0.152521006364708,
4.60032232020799));
#45089=CARTESIAN_POINT('Ctrl Pts',(22.6568919005697,-0.421514535902825,
4.45384478734481));
#45090=CARTESIAN_POINT('Ctrl Pts',(22.6807498186011,-0.587434568575047,
4.19639082134502));
#45091=CARTESIAN_POINT('Ctrl Pts',(22.7046077366325,-0.60971407867596,3.89091209973551));
#45092=CARTESIAN_POINT('Ctrl Pts',(22.728465654664,-0.482895786937606,3.61211183522625));
#45093=CARTESIAN_POINT('Ctrl Pts',(22.7523235726954,-0.23800784887647,3.4281541921173));
#45094=CARTESIAN_POINT('Ctrl Pts',(22.7761814907268,0.0651013135850054,
3.38404091701771));
#45095=CARTESIAN_POINT('Ctrl Pts',(22.8000394087582,0.352249768808992,3.49052260401466));
#45096=CARTESIAN_POINT('Ctrl Pts',(22.8238973267896,0.553345940411564,3.72163220123786));
#45097=CARTESIAN_POINT('Ctrl Pts',(22.8398026054772,0.597082876783669,3.92101540361374));
#45098=CARTESIAN_POINT('Ctrl Pts',(22.847755244821,0.593766187829899,4.01991291515446));
#45099=CARTESIAN_POINT('',(22.8,0.337479661717902,3.51106003648017));
#45100=CARTESIAN_POINT('Ctrl Pts',(22.8,0.337504360408405,3.51101527402275));
#45101=CARTESIAN_POINT('Ctrl Pts',(22.8,0.337610992569967,3.51114843896934));
#45102=CARTESIAN_POINT('Ctrl Pts',(22.8,0.337717562131928,3.51128164981369));
#45103=CARTESIAN_POINT('Ctrl Pts',(22.8,0.337824069051012,3.51141490653789));
#45104=CARTESIAN_POINT('Ctrl Pts',(22.8,0.354145371784291,3.53183539523119));
#45105=CARTESIAN_POINT('Ctrl Pts',(22.8,0.368999739942303,3.55333386321799));
#45106=CARTESIAN_POINT('Ctrl Pts',(22.8,0.382262544471458,3.57576050230915));
#45107=CARTESIAN_POINT('Ctrl Pts',(22.8,0.395177725624396,3.59759933027929));
#45108=CARTESIAN_POINT('Ctrl Pts',(22.8,0.406583379369087,3.62031953557487));
#45109=CARTESIAN_POINT('Ctrl Pts',(22.8,0.416319965152677,3.64376476659274));
#45110=CARTESIAN_POINT('Ctrl Pts',(22.8,0.420499854003763,3.65382973822867));
#45111=CARTESIAN_POINT('Ctrl Pts',(22.8,0.424371599987778,3.66402799385056));
#45112=CARTESIAN_POINT('Ctrl Pts',(22.8,0.42792023461967,3.67434527679585));
#45113=CARTESIAN_POINT('Ctrl Pts',(22.8,0.430015882150509,3.68043815216119));
#45114=CARTESIAN_POINT('Ctrl Pts',(22.8,0.431995626466768,3.68656321156818));
#45115=CARTESIAN_POINT('Ctrl Pts',(22.8,0.433857425300493,3.69271766785326));
#45116=CARTESIAN_POINT('Ctrl Pts',(22.8,0.440667704273582,3.71523007009016));
#45117=CARTESIAN_POINT('Ctrl Pts',(22.8,0.445903532435623,3.73813926926309));
#45118=CARTESIAN_POINT('Ctrl Pts',(22.8,0.449441836754149,3.76130640751661));
#45119=CARTESIAN_POINT('Ctrl Pts',(22.8,0.450038513826676,3.76521316594877));
#45120=CARTESIAN_POINT('Ctrl Pts',(22.8,0.450586822418701,3.76912718643627));
#45121=CARTESIAN_POINT('Ctrl Pts',(22.8,0.451086059471329,3.77304770583064));
#45122=CARTESIAN_POINT('Ctrl Pts',(22.8,0.453684096906641,3.79345015011803));
#45123=CARTESIAN_POINT('Ctrl Pts',(22.8,0.454954433743694,3.81403106227893));
#45124=CARTESIAN_POINT('Ctrl Pts',(22.8,0.45484641916779,3.83463783350426));
#45125=CARTESIAN_POINT('Ctrl Pts',(22.8,0.454808390965019,3.84189276616533));
#45126=CARTESIAN_POINT('Ctrl Pts',(22.8,0.454599381710613,3.84915061719132));
#45127=CARTESIAN_POINT('Ctrl Pts',(22.8,0.454216814112443,3.8564037154462));
#45128=CARTESIAN_POINT('Ctrl Pts',(22.8,0.453866695925276,3.86304160538904));
#45129=CARTESIAN_POINT('Ctrl Pts',(22.8,0.453371644107099,3.86966645154658));
#45130=CARTESIAN_POINT('Ctrl Pts',(22.8,0.452731182295137,3.87626933737115));
#45131=CARTESIAN_POINT('Ctrl Pts',(22.8,0.450713457978438,3.89707120727158));
#45132=CARTESIAN_POINT('Ctrl Pts',(22.8,0.447253508643,3.9176725514372));
#45133=CARTESIAN_POINT('Ctrl Pts',(22.8,0.442312061254715,3.9379035771693));
#45134=CARTESIAN_POINT('Ctrl Pts',(22.8,0.437564183511961,3.95734209977996));
#45135=CARTESIAN_POINT('Ctrl Pts',(22.8,0.431447509288203,3.97643919003209));
#45136=CARTESIAN_POINT('Ctrl Pts',(22.8,0.423915075143768,3.9949978423605));
#45137=CARTESIAN_POINT('Ctrl Pts',(22.8,0.421325190817866,4.00137888225459));
#45138=CARTESIAN_POINT('Ctrl Pts',(22.8,0.418567902041021,4.00769582483512));
#45139=CARTESIAN_POINT('Ctrl Pts',(22.8,0.415641328671541,4.01393920819689));
#45140=CARTESIAN_POINT('Ctrl Pts',(22.6211545887425,-1.51173456864708E-7,
4.59404872180247));
#45141=CARTESIAN_POINT('Ctrl Pts',(22.6251143866744,-0.0492822808754852,
4.59404929162283));
#45142=CARTESIAN_POINT('Ctrl Pts',(22.6290741846063,-0.0985642856931001,
4.58798571459226));
#45143=CARTESIAN_POINT('Ctrl Pts',(22.6330339825383,-0.14630523394925,4.57585637376244));
#45144=CARTESIAN_POINT('Ctrl Pts',(22.6409866218821,-0.242185516210759,
4.55149647592026));
#45145=CARTESIAN_POINT('Ctrl Pts',(22.6489392612259,-0.331850026056775,
4.50267063163255));
#45146=CARTESIAN_POINT('Ctrl Pts',(22.6568919005697,-0.404335619758509,
4.43534871515538));
#45147=CARTESIAN_POINT('Ctrl Pts',(22.6648445399135,-0.476821213460227,
4.36802679867822));
#45148=CARTESIAN_POINT('Ctrl Pts',(22.6727971792573,-0.532127891017642,
4.28220881001161));
#45149=CARTESIAN_POINT('Ctrl Pts',(22.6807498186011,-0.563494481479829,
4.18838669541007));
#45150=CARTESIAN_POINT('Ctrl Pts',(22.6887024579449,-0.594861071942019,
4.09456458080851));
#45151=CARTESIAN_POINT('Ctrl Pts',(22.6966550972887,-0.602287575308989,
3.99273834027202));
#45152=CARTESIAN_POINT('Ctrl Pts',(22.7046077366325,-0.584864445036083,
3.89535850925222));
#45153=CARTESIAN_POINT('Ctrl Pts',(22.7125603759763,-0.567441314763176,
3.79797867823242));
#45154=CARTESIAN_POINT('Ctrl Pts',(22.7205130153201,-0.525168550850394,
3.70504525672934));
#45155=CARTESIAN_POINT('Ctrl Pts',(22.7284656546639,-0.463217512550482,
3.62791893879298));
#45156=CARTESIAN_POINT('Ctrl Pts',(22.7364182940078,-0.401266474250563,
3.5507926208566));
#45157=CARTESIAN_POINT('Ctrl Pts',(22.7443709333516,-0.319637161563486,
3.48947340648693));
#45158=CARTESIAN_POINT('Ctrl Pts',(22.7523235726954,-0.228304311476372,
3.45146158678551));
#45159=CARTESIAN_POINT('Ctrl Pts',(22.7602762120392,-0.136971461389268,
3.41344976708409));
#45160=CARTESIAN_POINT('Ctrl Pts',(22.768228851383,-0.0359350739021178,
3.3987453420509));
#45161=CARTESIAN_POINT('Ctrl Pts',(22.7761814907268,0.062441195712126,3.40914007736714));
#45162=CARTESIAN_POINT('Ctrl Pts',(22.7841209938178,0.160654966376612,3.41951764255099));
#45163=CARTESIAN_POINT('Ctrl Pts',(22.7920604969089,0.256217399931083,3.45491151845628));
#45164=CARTESIAN_POINT('Ctrl Pts',(22.8,0.337504360408238,3.51101527402264));
#45165=CARTESIAN_POINT('Ctrl Pts',(4.,-0.219914231356244,4.35301468169996));
#45166=CARTESIAN_POINT('Ctrl Pts',(4.00793950309107,-0.278596966840389,
4.31645650682028));
#45167=CARTESIAN_POINT('Ctrl Pts',(4.02383164552594,-0.377405665439666,
4.21337674819164));
#45168=CARTESIAN_POINT('Ctrl Pts',(4.04767642730463,-0.433534992178268,
4.00656196868444));
#45169=CARTESIAN_POINT('Ctrl Pts',(4.07153434533603,-0.383670022685343,
3.79803920418254));
#45170=CARTESIAN_POINT('Ctrl Pts',(4.09539226336747,-0.239994733226421,
3.63889579340969));
#45171=CARTESIAN_POINT('Ctrl Pts',(4.11925018139887,-0.0376302499649443,
3.56805514133307));
#45172=CARTESIAN_POINT('Ctrl Pts',(4.1431080994303,0.173933765839147,3.60283521426327));
#45173=CARTESIAN_POINT('Ctrl Pts',(4.16696601746172,0.342967344134064,3.73473372141871));
#45174=CARTESIAN_POINT('Ctrl Pts',(4.19082393549313,0.428135478754777,3.93149662217858));
#45175=CARTESIAN_POINT('Ctrl Pts',(4.21468185352456,0.40861313688017,4.1450106963618));
#45176=CARTESIAN_POINT('Ctrl Pts',(4.23853977155597,0.289173588337559,4.32306558264197));
#45177=CARTESIAN_POINT('Ctrl Pts',(4.25811226835493,0.13317859508208,4.40432939198872));
#45178=CARTESIAN_POINT('Ctrl Pts',(4.26973212581007,0.0319512750557707,
4.41584666103033));
#45179=CARTESIAN_POINT('Ctrl Pts',(4.2733993439214,2.51014653359152E-6,
4.41583996132385));
#45180=CARTESIAN_POINT('Origin',(3.42660065607856,0.,4.));
#45181=CARTESIAN_POINT('Ctrl Pts',(4.,-0.219892372743211,3.64701365460636));
#45182=CARTESIAN_POINT('Ctrl Pts',(4.00795263934381,-0.161099076858729,
3.61038844940468));
#45183=CARTESIAN_POINT('Ctrl Pts',(4.02385791803142,-0.0249198690254346,
3.56711791692558));
#45184=CARTESIAN_POINT('Ctrl Pts',(4.04771583606284,0.185569069288609,3.60813812632505));
#45185=CARTESIAN_POINT('Ctrl Pts',(4.07157375409426,0.350624105231944,3.74494568050885));
#45186=CARTESIAN_POINT('Ctrl Pts',(4.09543167212568,0.429971014252744,3.94413788601839));
#45187=CARTESIAN_POINT('Ctrl Pts',(4.1192895901571,0.40416308778273,4.15698104289539));
#45188=CARTESIAN_POINT('Ctrl Pts',(4.14314750818851,0.279534313346206,4.3314427366163));
#45189=CARTESIAN_POINT('Ctrl Pts',(4.16225119682902,0.125004509401131,4.40624063703925));
#45190=CARTESIAN_POINT('Ctrl Pts',(4.1734022461257,0.0278694809177792,4.41585864517498));
#45191=CARTESIAN_POINT('Ctrl Pts',(4.17660065607858,5.88453344126799E-6,
4.41584444980552));
#45192=CARTESIAN_POINT('Ctrl Pts',(3.95224475517896,-0.314128184302177,
3.49573985500833));
#45193=CARTESIAN_POINT('Ctrl Pts',(3.96019739452277,-0.230138771413741,
3.44341876234755));
#45194=CARTESIAN_POINT('Ctrl Pts',(3.97610267321038,-0.0355993848822847,
3.38160445914153));
#45195=CARTESIAN_POINT('Ctrl Pts',(3.9999605912418,0.265095483172694,3.44020405374152));
#45196=CARTESIAN_POINT('Ctrl Pts',(4.02381850927322,0.500885556761892,3.63564106712445));
#45197=CARTESIAN_POINT('Ctrl Pts',(4.04767642730465,0.614236921112272,3.92019793948569));
#45198=CARTESIAN_POINT('Ctrl Pts',(4.07153434533605,0.577368897990231,4.22425593648149));
#45199=CARTESIAN_POINT('Ctrl Pts',(4.09539226336749,0.399329932212592,4.47348393104611));
#45200=CARTESIAN_POINT('Ctrl Pts',(4.11925018139889,0.123637843932736,4.60692867011962));
#45201=CARTESIAN_POINT('Ctrl Pts',(4.14310809943032,-0.182283847264271,
4.59196468982869));
#45202=CARTESIAN_POINT('Ctrl Pts',(4.16696601746173,-0.443633876576525,
4.43224822622665));
#45203=CARTESIAN_POINT('Ctrl Pts',(4.19082393549315,-0.596502436238336,
4.16683582239239));
#45204=CARTESIAN_POINT('Ctrl Pts',(4.21468185352458,-0.603510379797736,
3.86062723727387));
#45205=CARTESIAN_POINT('Ctrl Pts',(4.23853977155598,-0.462943343075553,
3.58849923641164));
#45206=CARTESIAN_POINT('Ctrl Pts',(4.26239768958742,-0.209174182705692,
3.41699430327496));
#45207=CARTESIAN_POINT('Ctrl Pts',(4.28625560761882,0.0957438341235747,
3.38805018506757));
#45208=CARTESIAN_POINT('Ctrl Pts',(4.31011352565025,0.377249837899377,3.50874444390425));
#45209=CARTESIAN_POINT('Ctrl Pts',(4.33397144368167,0.566508000142931,3.7495640793295));
#45210=CARTESIAN_POINT('Ctrl Pts',(4.35782936171309,0.617239514437223,4.05162211295782));
#45211=CARTESIAN_POINT('Ctrl Pts',(4.3816872797445,0.517039159770137,4.34105713706075));
#45212=CARTESIAN_POINT('Ctrl Pts',(4.40554519777592,0.290408643717306,4.54709439922074));
#45213=CARTESIAN_POINT('Ctrl Pts',(4.42940311580735,-0.00723469473045889,
4.61935217913086));
#45214=CARTESIAN_POINT('Ctrl Pts',(4.45326103383876,-0.303108954077165,
4.54016147994594));
#45215=CARTESIAN_POINT('Ctrl Pts',(4.47711895187019,-0.524864817190473,
4.3288865854667));
#45216=CARTESIAN_POINT('Ctrl Pts',(4.5009768699016,-0.618276935702851,4.03718996201469));
#45217=CARTESIAN_POINT('Ctrl Pts',(4.52483478793302,-0.560503501787052,
3.7363993798876));
#45218=CARTESIAN_POINT('Ctrl Pts',(4.54869270596444,-0.365671693940747,
3.50006632967672));
#45219=CARTESIAN_POINT('Ctrl Pts',(4.57255062399586,-0.0814231961944085,
3.38598067979976));
#45220=CARTESIAN_POINT('Ctrl Pts',(4.59640854202727,0.222735490926488,3.42203947925158));
#45221=CARTESIAN_POINT('Ctrl Pts',(4.6202664600587,0.472429283332598,3.59942536936051));
#45222=CARTESIAN_POINT('Ctrl Pts',(4.64412437809011,0.606601247243452,3.87476266809168));
#45223=CARTESIAN_POINT('Ctrl Pts',(4.66798229612153,0.592442682719785,4.18072390587243));
#45224=CARTESIAN_POINT('Ctrl Pts',(4.69184021415295,0.433415744455024,4.44249322584619));
#45225=CARTESIAN_POINT('Ctrl Pts',(4.71569813218437,0.168406850663934,4.59606089882753));
#45226=CARTESIAN_POINT('Ctrl Pts',(4.7395560502158,-0.1377821054254,4.60387544567241));
#45227=CARTESIAN_POINT('Ctrl Pts',(4.7634139682472,-0.410279583628813,4.46402599681362));
#45228=CARTESIAN_POINT('Ctrl Pts',(4.78727188627863,-0.582452527843622,
4.21070955191949));
#45229=CARTESIAN_POINT('Ctrl Pts',(4.81112980431005,-0.612199963312297,
3.9058688819681));
#45230=CARTESIAN_POINT('Ctrl Pts',(4.83498772234147,-0.492247831758966,
3.62404583445569));
#45231=CARTESIAN_POINT('Ctrl Pts',(4.85884564037289,-0.251927696778831,
3.4341538212047));
#45232=CARTESIAN_POINT('Ctrl Pts',(4.88270355840431,0.0499956224363984,
3.38262661200963));
#45233=CARTESIAN_POINT('Ctrl Pts',(4.90656147643572,0.339693650112522,3.48206401309162));
#45234=CARTESIAN_POINT('Ctrl Pts',(4.93041939446714,0.546327327266884,3.70815087126575));
#45235=CARTESIAN_POINT('Ctrl Pts',(4.95427731249857,0.619369091246891,4.00560279122603));
#45236=CARTESIAN_POINT('Ctrl Pts',(4.97813523052998,0.540958241141728,4.3016846761146));
#45237=CARTESIAN_POINT('Ctrl Pts',(5.00199314856141,0.330268365670778,4.52399643996756));
#45238=CARTESIAN_POINT('Ctrl Pts',(5.02585106659282,0.0388188784636707,
4.61817680087201));
#45239=CARTESIAN_POINT('Ctrl Pts',(5.04970898462424,-0.262122881932824,
4.56119609516527));
#45240=CARTESIAN_POINT('Ctrl Pts',(5.07356690265566,-0.498968457612796,
4.36698765751594));
#45241=CARTESIAN_POINT('Ctrl Pts',(5.09742482068708,-0.613802653778546,
4.08304074106085));
#45242=CARTESIAN_POINT('Ctrl Pts',(5.12128273871849,-0.578545381446849,
3.77878810143205));
#45243=CARTESIAN_POINT('Ctrl Pts',(5.14514065674992,-0.40181800409162,3.52862779669421));
#45244=CARTESIAN_POINT('Ctrl Pts',(5.16899857478133,-0.126835179433317,
3.39373083558568));
#45245=CARTESIAN_POINT('Ctrl Pts',(5.19285649281276,0.179162301517353,3.4070831996169));
#45246=CARTESIAN_POINT('Ctrl Pts',(5.21671441084417,0.441349719463922,3.56541987207117));
#45247=CARTESIAN_POINT('Ctrl Pts',(5.24057232887559,0.595615108876583,3.83002322352904));
#45248=CARTESIAN_POINT('Ctrl Pts',(5.26443024690701,0.604236379939102,4.13619052690848));
#45249=CARTESIAN_POINT('Ctrl Pts',(5.28828816493843,0.465105397037983,4.40905553670335));
#45250=CARTESIAN_POINT('Ctrl Pts',(5.31214608296985,0.21224347534444,4.58189532532512));
#45251=CARTESIAN_POINT('Ctrl Pts',(5.33600400100126,-0.0925177574670201,
4.61244585639451));
#45252=CARTESIAN_POINT('Ctrl Pts',(5.35986191903269,-0.37465587844466,4.49323669288525));
#45253=CARTESIAN_POINT('Ctrl Pts',(5.3837198370641,-0.565180431721392,4.25341772246777));
#45254=CARTESIAN_POINT('Ctrl Pts',(5.40757775509553,-0.617502974236318,
3.95163121594683));
#45255=CARTESIAN_POINT('Ctrl Pts',(5.43143567312694,-0.518829219107294,
3.66167219466597));
#45256=CARTESIAN_POINT('Ctrl Pts',(5.45529359115837,-0.293287587282116,
3.45444353765392));
#45257=CARTESIAN_POINT('Ctrl Pts',(5.47915150918978,0.00397084862654925,
3.38061829634467));
#45258=CARTESIAN_POINT('Ctrl Pts',(5.50300942722121,0.300258303883157,3.45824875319892));
#45259=CARTESIAN_POINT('Ctrl Pts',(5.52686734525262,0.523124424966688,3.66835214690199));
#45260=CARTESIAN_POINT('Ctrl Pts',(5.55072526328404,0.618072374525773,3.95955247459688));
#45261=CARTESIAN_POINT('Ctrl Pts',(5.57458318131546,0.561884792553919,4.26064332401524));
#45262=CARTESIAN_POINT('Ctrl Pts',(5.59844109934688,0.368301073379394,4.49799978094171));
#45263=CARTESIAN_POINT('Ctrl Pts',(5.62229901737829,0.0846577094226282,
4.61358172616469));
#45264=CARTESIAN_POINT('Ctrl Pts',(5.64615693540972,-0.219686770477705,
4.57912622575047));
#45265=CARTESIAN_POINT('Ctrl Pts',(5.67001485344113,-0.470311850924231,
4.40305858798173));
#45266=CARTESIAN_POINT('Ctrl Pts',(5.69387277147256,-0.605932872639677,
4.12843214650112));
#45267=CARTESIAN_POINT('Ctrl Pts',(5.71773068950397,-0.593386801983745,
3.82240054650545));
#45268=CARTESIAN_POINT('Ctrl Pts',(5.74158860753539,-0.435741494202748,
3.55979685111874));
#45269=CARTESIAN_POINT('Ctrl Pts',(5.76544652556682,-0.171545522688555,
3.40483481554927));
#45270=CARTESIAN_POINT('Ctrl Pts',(5.78930444359822,0.134598003740687,3.39540688139736));
#45271=CARTESIAN_POINT('Ctrl Pts',(5.81316236162965,0.407828648458881,3.53381843004554));
#45272=CARTESIAN_POINT('Ctrl Pts',(5.83702027966106,0.58133408605803,3.78622407765735));
#45273=CARTESIAN_POINT('Ctrl Pts',(5.86087819769249,0.612687492198482,4.09090374899912));
#45274=CARTESIAN_POINT('Ctrl Pts',(5.8847361157239,0.494222140250734,4.3733550009975));
#45275=CARTESIAN_POINT('Ctrl Pts',(5.90859403375532,0.254905969192102,4.56451074097759));
#45276=CARTESIAN_POINT('Ctrl Pts',(5.93245195178675,-0.0467415727364197,
4.61762831145024));
#45277=CARTESIAN_POINT('Ctrl Pts',(5.95630986981815,-0.336959681931401,
4.51971877801409));
#45278=CARTESIAN_POINT('Ctrl Pts',(5.98016778784959,-0.544781677596122,
4.29472414464893));
#45279=CARTESIAN_POINT('Ctrl Pts',(6.00402570588099,-0.61939026621187,3.99766086682344));
#45280=CARTESIAN_POINT('Ctrl Pts',(6.02788362391242,-0.542540019317823,
3.70117063377655));
#45281=CARTESIAN_POINT('Ctrl Pts',(6.05174154194384,-0.333025929677459,
3.47775031355921));
#45282=CARTESIAN_POINT('Ctrl Pts',(6.07559945997526,-0.042074208138152,
3.38203805739984));
#45283=CARTESIAN_POINT('Ctrl Pts',(6.09945737800668,0.259158778028439,3.43742717299816));
#45284=CARTESIAN_POINT('Ctrl Pts',(6.12331529603809,0.497033648893269,3.63039418124561));
#45285=CARTESIAN_POINT('Ctrl Pts',(6.14717321406952,0.613345206175343,3.91371436613889));
#45286=CARTESIAN_POINT('Ctrl Pts',(6.17103113210093,0.579724447951105,4.21818191418763));
#45287=CARTESIAN_POINT('Ctrl Pts',(6.19488905013236,0.40425597056565,4.46920707734689));
#45288=CARTESIAN_POINT('Ctrl Pts',(6.21874696816377,0.13010450107023,4.60567007851858));
#45289=CARTESIAN_POINT('Ctrl Pts',(6.24260488619519,-0.176179318911185,
4.59370602015056));
#45290=CARTESIAN_POINT('Ctrl Pts',(6.26646280422661,-0.438782409775579,
4.43717629804221));
#45291=CARTESIAN_POINT('Ctrl Pts',(6.29032072225803,-0.595217424383659,
4.17259489198797));
#45292=CARTESIAN_POINT('Ctrl Pts',(6.31417864028945,-0.604035436411749,
3.86794272465182));
#45293=CARTESIAN_POINT('Ctrl Pts',(6.34598919766468,-0.423477061217623,
3.4998212904071));
#45294=CARTESIAN_POINT('Ctrl Pts',(6.3857523943837,0.100470573235224,3.30464850830547));
#45295=CARTESIAN_POINT('Ctrl Pts',(6.43346823044655,0.640013163212275,3.70919899990029));
#45296=CARTESIAN_POINT('Ctrl Pts',(6.48118406650937,0.590335835129396,4.3806576914582));
#45297=CARTESIAN_POINT('Ctrl Pts',(6.52889990257223,-0.000686065451295705,
4.70262946694599));
#45298=CARTESIAN_POINT('Ctrl Pts',(6.57661573863505,-0.591483599613884,
4.37932465573422));
#45299=CARTESIAN_POINT('Ctrl Pts',(6.6243315746979,-0.638898060441451,3.70770201230499));
#45300=CARTESIAN_POINT('Ctrl Pts',(6.67204741076074,-0.0997162142428727,
3.30448953810453));
#45301=CARTESIAN_POINT('Ctrl Pts',(6.71976324682356,0.531096731682035,3.53998115137447));
#45302=CARTESIAN_POINT('Ctrl Pts',(6.76747908288643,0.674163513320998,4.19791190586338));
#45303=CARTESIAN_POINT('Ctrl Pts',(6.81519491894923,0.19815244237474,4.67409883091767));
#45304=CARTESIAN_POINT('Ctrl Pts',(6.86291075501209,-0.459834002450772,
4.53124951681343));
#45305=CARTESIAN_POINT('Ctrl Pts',(6.91062659107492,-0.695543074258338,
3.90054607923755));
#45306=CARTESIAN_POINT('Ctrl Pts',(6.95834242713776,-0.292526745343327,
3.36117245204842));
#45307=CARTESIAN_POINT('Ctrl Pts',(7.00605826320061,0.379122722467859,3.40844412700009));
#45308=CARTESIAN_POINT('Ctrl Pts',(7.05377409926343,0.702617257610868,3.99895059076549));
#45309=CARTESIAN_POINT('Ctrl Pts',(7.10148993532628,0.380887926283931,4.59042078110798));
#45310=CARTESIAN_POINT('Ctrl Pts',(7.14920577138911,-0.290616845661789,
4.63969846327979));
#45311=CARTESIAN_POINT('Ctrl Pts',(7.19692160745196,-0.695243592084394,
4.10153121423426));
#45312=CARTESIAN_POINT('Ctrl Pts',(7.24463744351478,-0.461417505508394,
3.47012628326466));
#45313=CARTESIAN_POINT('Ctrl Pts',(7.29235327957764,0.196135405489393,3.32531254251214));
#45314=CARTESIAN_POINT('Ctrl Pts',(7.34006911564046,0.673574140181709,3.80007467379138));
#45315=CARTESIAN_POINT('Ctrl Pts',(7.38778495170331,0.532459385890787,4.45843130921146));
#45316=CARTESIAN_POINT('Ctrl Pts',(7.43550078776614,-0.0976210197556089,
4.69580341906706));
#45317=CARTESIAN_POINT('Ctrl Pts',(7.48321662382899,-0.638054538563543,
4.29420854311633));
#45318=CARTESIAN_POINT('Ctrl Pts',(7.53093245989182,-0.592552758097988,
3.62243743491725));
#45319=CARTESIAN_POINT('Ctrl Pts',(7.57864829595465,-0.00290066162856385,
3.29738783984629));
#45320=CARTESIAN_POINT('Ctrl Pts',(7.6263641320175,0.589415156704478,3.61755780248734));
#45321=CARTESIAN_POINT('Ctrl Pts',(7.67407996808033,0.64046196749915,4.28893031975233));
#45322=CARTESIAN_POINT('Ctrl Pts',(7.72179580414318,0.103362698669259,4.69497367861456));
#45323=CARTESIAN_POINT('Ctrl Pts',(7.769511640206,-0.528656126737314,4.46281201486565));
#45324=CARTESIAN_POINT('Ctrl Pts',(7.81722747626886,-0.675201896567852,
3.80564295658466));
#45325=CARTESIAN_POINT('Ctrl Pts',(7.86494331233168,-0.201699375449268,
3.32695496184095));
#45326=CARTESIAN_POINT('Ctrl Pts',(7.91265914839452,0.457026785680635,3.46633458176699));
#45327=CARTESIAN_POINT('Ctrl Pts',(7.96037498445737,0.696058217263005,4.09578736675475));
#45328=CARTESIAN_POINT('Ctrl Pts',(8.0080908205202,0.295888677698302,4.63727713897333));
#45329=CARTESIAN_POINT('Ctrl Pts',(8.05580665658303,-0.375999987428149,
4.59354550870361));
#45330=CARTESIAN_POINT('Ctrl Pts',(8.10352249264589,-0.702602078596463,
4.00475190491975));
#45331=CARTESIAN_POINT('Ctrl Pts',(8.1512383287087,-0.383993870066737,3.41159455373064));
#45332=CARTESIAN_POINT('Ctrl Pts',(8.19895416477156,0.287241817850264,3.35877897763223));
#45333=CARTESIAN_POINT('Ctrl Pts',(8.24667000083438,0.694698924651979,3.89480653282778));
#45334=CARTESIAN_POINT('Ctrl Pts',(8.29438583689724,0.464203319628796,4.52743486753713));
#45335=CARTESIAN_POINT('Ctrl Pts',(8.34210167296006,-0.192577336495663,
4.67571164775853));
#45336=CARTESIAN_POINT('Ctrl Pts',(8.3898175090229,-0.672511261332963,4.20347202468314));
#45337=CARTESIAN_POINT('Ctrl Pts',(8.43753334508575,-0.534867746972347,
3.54438091052171));
#45338=CARTESIAN_POINT('Ctrl Pts',(8.48524918114857,0.0939530494311211,
3.303691816829));
#45339=CARTESIAN_POINT('Ctrl Pts',(8.53296501721143,0.636495314888509,3.70243324182078));
#45340=CARTESIAN_POINT('Ctrl Pts',(8.58068085327425,0.594534138944492,4.37443479950165));
#45341=CARTESIAN_POINT('Ctrl Pts',(8.6283966893371,0.00660311512414562,
4.7025871193802));
#45342=CARTESIAN_POINT('Ctrl Pts',(8.67611252539993,-0.58739165091669,4.3855428768395));
#45343=CARTESIAN_POINT('Ctrl Pts',(8.72382836146277,-0.64197562573843,3.71444867815739));
#45344=CARTESIAN_POINT('Ctrl Pts',(8.77154419752561,-0.107023505379864,
3.30558065209521));
#45345=CARTESIAN_POINT('Ctrl Pts',(8.81926003358845,0.526209946737336,3.53440859822909));
#45346=CARTESIAN_POINT('Ctrl Pts',(8.86697586965128,0.676216707984864,4.19079629265377));
#45347=CARTESIAN_POINT('Ctrl Pts',(8.91469170571413,0.20524326135842,4.67197281575615));
#45348=CARTESIAN_POINT('Ctrl Pts',(8.96240754177695,-0.45420823024697,4.53606636251889));
#45349=CARTESIAN_POINT('Ctrl Pts',(9.0101233778398,-0.69655331512461,3.90788192013928));
#45350=CARTESIAN_POINT('Ctrl Pts',(9.05783921390263,-0.299242772872918,
3.36429092791464));
#45351=CARTESIAN_POINT('Ctrl Pts',(9.10555504996548,0.37286701214988,3.40448135822736));
#45352=CARTESIAN_POINT('Ctrl Pts',(9.15327088602831,0.702567282619003,3.99154572051203));
#45353=CARTESIAN_POINT('Ctrl Pts',(9.20098672209116,0.387089207071907,4.58637377773631));
#45354=CARTESIAN_POINT('Ctrl Pts',(9.24870255815397,-0.28385884346236,4.64272577234503));
#45355=CARTESIAN_POINT('Ctrl Pts',(9.29641839421684,-0.694134950315416,
4.10885280060212));
#45356=CARTESIAN_POINT('Ctrl Pts',(9.34413423027966,-0.46697625165475,3.47501862715065));
#45357=CARTESIAN_POINT('Ctrl Pts',(9.39185006634251,0.189013924253689,3.32328292626348));
#45358=CARTESIAN_POINT('Ctrl Pts',(9.43956590240535,0.671429705166911,3.79298692681914));
#45359=CARTESIAN_POINT('Ctrl Pts',(9.48728173846818,0.537261256551386,4.45279421778236));
#45360=CARTESIAN_POINT('Ctrl Pts',(9.53499757453101,-0.090282470782305,
4.69679361142145));
#45361=CARTESIAN_POINT('Ctrl Pts',(9.58271341059386,-0.634918416022234,
4.30091671014441));
#45362=CARTESIAN_POINT('Ctrl Pts',(9.63042924665669,-0.596499010353368,
3.62870336374299));
#45363=CARTESIAN_POINT('Ctrl Pts',(9.67814508271953,-0.0103053851599677,
3.29745743154951));
#45364=CARTESIAN_POINT('Ctrl Pts',(9.72586091878236,0.585351833794561,3.61136714997101));
#45365=CARTESIAN_POINT('Ctrl Pts',(9.77357675484522,0.643471456979869,4.28216439445919));
#45366=CARTESIAN_POINT('Ctrl Pts',(9.82129259090803,0.110681340139534,4.69384573385819));
#45367=CARTESIAN_POINT('Ctrl Pts',(9.8690084269709,-0.523749154402255,4.46835785966634));
#45368=CARTESIAN_POINT('Ctrl Pts',(9.91672426303372,-0.677212741539845,
3.81276975633088));
#45369=CARTESIAN_POINT('Ctrl Pts',(9.96444009909655,-0.208781447863971,
3.32911806666439));
#45370=CARTESIAN_POINT('Ctrl Pts',(10.0121559351594,0.451377061900895,3.4615475792254));
#45371=CARTESIAN_POINT('Ctrl Pts',(10.0598717712222,0.697029070393332,4.08844623493918));
#45372=CARTESIAN_POINT('Ctrl Pts',(10.1075876072851,0.302588558372737,4.63412335218805));
#45373=CARTESIAN_POINT('Ctrl Pts',(10.1553034433479,-0.369723682724971,
4.5974752378807));
#45374=CARTESIAN_POINT('Ctrl Pts',(10.2030192794108,-0.702512977046242,
4.01215641928927));
#45375=CARTESIAN_POINT('Ctrl Pts',(10.2507351154736,-0.390173794994359,
3.41567417381395));
#45376=CARTESIAN_POINT('Ctrl Pts',(10.2984509515364,0.280467986596366,3.3557873255338));
#45377=CARTESIAN_POINT('Ctrl Pts',(10.3461667875993,0.693551700540965,3.8874908887021));
#45378=CARTESIAN_POINT('Ctrl Pts',(10.3938826236621,0.469736216214169,4.52251329995044));
#45379=CARTESIAN_POINT('Ctrl Pts',(10.441598459725,-0.185445263282835,4.67770370795377));
#45380=CARTESIAN_POINT('Ctrl Pts',(10.4893142957878,-0.670329504065059,
4.21054837313121));
#45381=CARTESIAN_POINT('Ctrl Pts',(10.5370301318506,-0.539639846919137,
3.55004322755915));
#45382=CARTESIAN_POINT('Ctrl Pts',(10.5847459679134,0.0866093850789692,
3.30274030959437));
#45383=CARTESIAN_POINT('Ctrl Pts',(10.6324618039763,0.633323886102378,3.69574169404847));
#45384=CARTESIAN_POINT('Ctrl Pts',(10.6801776400391,0.598447317577389,4.36814816247366));
#45385=CARTESIAN_POINT('Ctrl Pts',(10.727893476102,0.0140073690254923,4.70247850861168));
#45386=CARTESIAN_POINT('Ctrl Pts',(10.7756093121648,-0.583295762033595,
4.39171203127037));
#45387=CARTESIAN_POINT('Ctrl Pts',(10.8233251482277,-0.644949419658282,
3.72123036834915));
#45388=CARTESIAN_POINT('Ctrl Pts',(10.8710409842905,-0.114336101388361,
3.30674714759503));
#45389=CARTESIAN_POINT('Ctrl Pts',(10.9187568203533,0.521273818073547,3.52888868827067));
#45390=CARTESIAN_POINT('Ctrl Pts',(10.9664726564162,0.678189969569843,4.18365899548663));
#45391=CARTESIAN_POINT('Ctrl Pts',(11.014188492479,0.212313836716152,4.66977242119035));
#45392=CARTESIAN_POINT('Ctrl Pts',(11.0619043285418,-0.44853335926228,4.54082352674158));
#45393=CARTESIAN_POINT('Ctrl Pts',(11.1096201646047,-0.697485469857315,
3.91522806604643));
#45394=CARTESIAN_POINT('Ctrl Pts',(11.1573360006675,-0.305925941288932,
3.36747997668469));
#45395=CARTESIAN_POINT('Ctrl Pts',(11.2050518367303,0.36657008644075,3.40058475730499));
#45396=CARTESIAN_POINT('Ctrl Pts',(11.2527676727932,0.702439163386103,3.98414177848112));
#45397=CARTESIAN_POINT('Ctrl Pts',(11.300483508856,0.393247548178179,4.58226164848818));
#45398=CARTESIAN_POINT('Ctrl Pts',(11.3481993449189,-0.277069341413063,
4.64568168744144));
#45399=CARTESIAN_POINT('Ctrl Pts',(11.3959151809817,-0.692949191524882,
4.11616229772746));
#45400=CARTESIAN_POINT('Ctrl Pts',(11.4436310170446,-0.47248313666557,3.47996928262364));
#45401=CARTESIAN_POINT('Ctrl Pts',(11.4913468531074,0.181871452681271,3.32132847698764));
#45402=CARTESIAN_POINT('Ctrl Pts',(11.5390626891702,0.669210688578896,3.78592217363756));
#45403=CARTESIAN_POINT('Ctrl Pts',(11.586778525233,0.54200345202451,4.44710683224685));
#45404=CARTESIAN_POINT('Ctrl Pts',(11.6344943612959,-0.082933894319074,
4.69770640718098));
#45405=CARTESIAN_POINT('Ctrl Pts',(11.6822101973587,-0.631711769407458,
4.30759145280778));
#45406=CARTESIAN_POINT('Ctrl Pts',(11.7299260334216,-0.600379006513997,
3.63501053441836));
#45407=CARTESIAN_POINT('Ctrl Pts',(11.7776418694844,-0.0177089639202829,
3.29760505835735));
#45408=CARTESIAN_POINT('Ctrl Pts',(11.8253577055473,0.581223492728864,3.60521966494218));
#45409=CARTESIAN_POINT('Ctrl Pts',(11.8730735416101,0.646409472732109,4.27536712768685));
#45410=CARTESIAN_POINT('Ctrl Pts',(11.9207893776729,0.11798768763725,4.69264072000881));
#45411=CARTESIAN_POINT('Ctrl Pts',(11.9685052137358,-0.518784006488825,
4.4738516814993));
#45412=CARTESIAN_POINT('Ctrl Pts',(12.0162210497986,-0.679148364938221,
3.81991735272367));
#45413=CARTESIAN_POINT('Ctrl Pts',(12.0639368858614,-0.215840329824027,
3.33135568986959));
#45414=CARTESIAN_POINT('Ctrl Pts',(12.1116527219243,0.445677201297934,3.45682038542343));
#45415=CARTESIAN_POINT('Ctrl Pts',(12.1593685579871,0.697922500842799,4.08109527893561));
#45416=CARTESIAN_POINT('Ctrl Pts',(12.2070843940499,0.309254828945687,4.63089912998995));
#45417=CARTESIAN_POINT('Ctrl Pts',(12.2548002301128,-0.36340631086944,4.60133860234362));
#45418=CARTESIAN_POINT('Ctrl Pts',(12.3025160661756,-0.702345843688318,
4.0195595833814));
#45419=CARTESIAN_POINT('Ctrl Pts',(12.3502319022385,-0.396310381268302,
3.41981869803717));
#45420=CARTESIAN_POINT('Ctrl Pts',(12.3979477383013,0.273663002289436,3.35286722952223));
#45421=CARTESIAN_POINT('Ctrl Pts',(12.4456635743641,0.69232743999824,3.88018774155459));
#45422=CARTESIAN_POINT('Ctrl Pts',(12.493379410427,0.475216936729713,4.51753369406595));
#45423=CARTESIAN_POINT('Ctrl Pts',(12.5410952464898,-0.178292591690169,
4.67962049203707));
#45424=CARTESIAN_POINT('Ctrl Pts',(12.5888110825527,-0.66807328977682,4.21760133486514));
#45425=CARTESIAN_POINT('Ctrl Pts',(12.6365269186155,-0.544352006232531,
3.55575552365962));
#45426=CARTESIAN_POINT('Ctrl Pts',(12.6842427546784,0.0792561005673328,
3.3018662506574));
#45427=CARTESIAN_POINT('Ctrl Pts',(12.7319585907411,0.630082110704352,3.68908394184497));
#45428=CARTESIAN_POINT('Ctrl Pts',(12.779674426804,0.60229402352211,4.36182063329482));
#45429=CARTESIAN_POINT('Ctrl Pts',(12.8273902628668,0.0214100670547408,
4.70229186986395));
#45430=CARTESIAN_POINT('Ctrl Pts',(12.8751060989297,-0.579135083425219,
4.39783767618763));
#45431=CARTESIAN_POINT('Ctrl Pts',(12.9228219349925,-0.647851575657132,
3.7280430229487));
#45432=CARTESIAN_POINT('Ctrl Pts',(12.9705377710554,-0.121635997485283,
3.30799064633195));
#45433=CARTESIAN_POINT('Ctrl Pts',(13.0182536071182,0.516279788787698,3.52342110712114));
#45434=CARTESIAN_POINT('Ctrl Pts',(13.065969443181,0.68008790103128,4.17650129834983));
#45435=CARTESIAN_POINT('Ctrl Pts',(13.1136852792439,0.219360829260397,4.66749763148232));
#45436=CARTESIAN_POINT('Ctrl Pts',(13.1614011153067,-0.44280866732052,4.54552061885334));
#45437=CARTESIAN_POINT('Ctrl Pts',(13.2091169513696,-0.698340151213866,
3.92258362801769));
#45438=CARTESIAN_POINT('Ctrl Pts',(13.2568327874324,-0.31257512890311,3.37073928277739));
#45439=CARTESIAN_POINT('Ctrl Pts',(13.3045486234952,0.36023244386594,3.39675473658331));
#45440=CARTESIAN_POINT('Ctrl Pts',(13.3522644595581,0.702233020544282,3.97673959790624));
#45441=CARTESIAN_POINT('Ctrl Pts',(13.3999802956209,0.39936220921291,4.57808484437918));
#45442=CARTESIAN_POINT('Ctrl Pts',(13.4476961316837,-0.270249063816132,
4.64856588328003));
#45443=CARTESIAN_POINT('Ctrl Pts',(13.4954119677466,-0.691686463226468,
4.123458892096));
#45444=CARTESIAN_POINT('Ctrl Pts',(13.5431278038094,-0.47793754049168,3.48497770064095));
#45445=CARTESIAN_POINT('Ctrl Pts',(13.5908436398723,0.174708779690948,3.31944941132403));
#45446=CARTESIAN_POINT('Ctrl Pts',(13.6385594759351,0.666917339243262,3.77888119920505));
#45447=CARTESIAN_POINT('Ctrl Pts',(13.6862753119979,0.54668544432619,4.44136978420615));
#45448=CARTESIAN_POINT('Ctrl Pts',(13.7339911480608,-0.075576105952426,
4.69854170502367));
#45449=CARTESIAN_POINT('Ctrl Pts',(13.7817069841236,-0.62843495524706,4.31423202967224));
#45450=CARTESIAN_POINT('Ctrl Pts',(13.8294228201864,-0.604192315423611,
3.64135824639153));
#45451=CARTESIAN_POINT('Ctrl Pts',(13.8771386562493,-0.025110575652917,
3.29783070386218));
#45452=CARTESIAN_POINT('Ctrl Pts',(13.9248544923121,0.577030592115723,3.59911603023956));
#45453=CARTESIAN_POINT('Ctrl Pts',(13.972570328375,0.649275688387581,4.26853927444071));
#45454=CARTESIAN_POINT('Ctrl Pts',(14.0202861644378,0.125280929622514,4.69135877091509));
#45455=CARTESIAN_POINT('Ctrl Pts',(14.0680020005006,-0.513761234509794,
4.47929287013608));
#45456=CARTESIAN_POINT('Ctrl Pts',(14.1157178365635,-0.681008551759042,
3.82708495184235));
#45457=CARTESIAN_POINT('Ctrl Pts',(14.1634336726263,-0.222875237264486,
3.33366758291179));
#45458=CARTESIAN_POINT('Ctrl Pts',(14.2111495086891,0.439927836986373,3.45215352543546));
#45459=CARTESIAN_POINT('Ctrl Pts',(14.258865344752,0.698738409372782,4.07373531525328));
#45460=CARTESIAN_POINT('Ctrl Pts',(14.3065811808148,0.315886748959774,4.62760483051036));
#45461=CARTESIAN_POINT('Ctrl Pts',(14.3542970168777,-0.357048573565392,
4.60513517296818));
#45462=CARTESIAN_POINT('Ctrl Pts',(14.4020128529405,-0.702100697086982,
4.02696057488784));
#45463=CARTESIAN_POINT('Ctrl Pts',(14.4497286890033,-0.402402947265751,
3.42402766604624));
#45464=CARTESIAN_POINT('Ctrl Pts',(14.4974445250662,0.266827620794843,3.35001901394789));
#45465=CARTESIAN_POINT('Ctrl Pts',(14.545160361129,0.691026279008849,3.87289790258421));
#45466=CARTESIAN_POINT('Ctrl Pts',(14.5928761971919,0.480644872403009,4.51249660299459));
#45467=CARTESIAN_POINT('Ctrl Pts',(14.6405920332547,-0.171120116202498,
4.6814617871012));
#45468=CARTESIAN_POINT('Ctrl Pts',(14.6883078693176,-0.665742869077823,
4.22463012647536));
#45469=CARTESIAN_POINT('Ctrl Pts',(14.7360237053803,-0.549003701508229,
3.56151716432844));
#45470=CARTESIAN_POINT('Ctrl Pts',(14.7837395414432,0.0718940126641393,
3.30106973710437));
#45471=CARTESIAN_POINT('Ctrl Pts',(14.831455377506,0.626770348775451,3.68246072472179));
#45472=CARTESIAN_POINT('Ctrl Pts',(14.8791712135689,0.606073829504824,4.35545291479698));
#45473=CARTESIAN_POINT('Ctrl Pts',(14.9268870496317,0.0288103869553486,
4.70202722386799));
#45474=CARTESIAN_POINT('Ctrl Pts',(14.9746028856946,-0.574910077240004,
4.4039191311837));
#45475=CARTESIAN_POINT('Ctrl Pts',(15.0223187217574,-0.650681771377263,
3.73488588523872));
#45476=CARTESIAN_POINT('Ctrl Pts',(15.0700345578202,-0.128922382832804,
3.30931101018402));
#45477=CARTESIAN_POINT('Ctrl Pts',(15.1177503938831,0.511228413592865,3.51800646209349));
#45478=CARTESIAN_POINT('Ctrl Pts',(15.1654662299459,0.681910291555949,4.16932399628639));
#45479=CARTESIAN_POINT('Ctrl Pts',(15.2131820660088,0.226383456244684,4.6651486993049));
#45480=CARTESIAN_POINT('Ctrl Pts',(15.2608979020716,-0.437034790293287,
4.55015711712348));
#45481=CARTESIAN_POINT('Ctrl Pts',(15.3086137381344,-0.699117264260319,
3.92994778903219));
#45482=CARTESIAN_POINT('Ctrl Pts',(15.3563295741972,-0.319189597155267,
3.37406848416447));
#45483=CARTESIAN_POINT('Ctrl Pts',(15.4040454102601,0.353854788380711,3.39299172148285));
#45484=CARTESIAN_POINT('Ctrl Pts',(15.4517612463229,0.70194887699091,3.96934000098645));
#45485=CARTESIAN_POINT('Ctrl Pts',(15.4994770823858,0.40543251098856,4.57384382934891));
#45486=CARTESIAN_POINT('Ctrl Pts',(15.5471929184486,-0.263398768235635,
4.65137803949801));
#45487=CARTESIAN_POINT('Ctrl Pts',(15.5949087545115,-0.690346905678043,
4.13074177323664));
#45488=CARTESIAN_POINT('Ctrl Pts',(15.6426245905743,-0.483338857283784,
3.4900433248913));
#45489=CARTESIAN_POINT('Ctrl Pts',(15.6903404266371,0.167526700878456,3.31764593799033));
#45490=CARTESIAN_POINT('Ctrl Pts',(15.7380562627,0.664549911894371,3.77186478559966));
#45491=CARTESIAN_POINT('Ctrl Pts',(15.7857720987628,0.551306713402943,4.43558371090429));
#45492=CARTESIAN_POINT('Ctrl Pts',(15.8334879348256,-0.0682099229505586,
4.69929941216862));
#45493=CARTESIAN_POINT('Ctrl Pts',(15.8812037708885,-0.625088337514006,
4.32083770313399));
#45494=CARTESIAN_POINT('Ctrl Pts',(15.9289196069513,-0.607938513517956,
3.64774579458877));
#45495=CARTESIAN_POINT('Ctrl Pts',(15.9766354430142,-0.0325093982219456,
3.29813434300035));
#45496=CARTESIAN_POINT('Ctrl Pts',(16.024351279077,0.572773597682653,3.59305692382598));
#45497=CARTESIAN_POINT('Ctrl Pts',(16.0720671151399,0.652069785580651,4.2616815931263));
#45498=CARTESIAN_POINT('Ctrl Pts',(16.1197829512026,0.132560255996602,4.69000002896988));
#45499=CARTESIAN_POINT('Ctrl Pts',(16.1674987872655,-0.508681396370837,
4.48468082119526));
#45500=CARTESIAN_POINT('Ctrl Pts',(16.2152146233283,-0.682793095381579,
3.83427175754402));
#45501=CARTESIAN_POINT('Ctrl Pts',(16.2629304593912,-0.229885388781225,
3.33605348899688));
#45502=CARTESIAN_POINT('Ctrl Pts',(16.310646295454,0.434129607578297,3.44754751763412));
#45503=CARTESIAN_POINT('Ctrl Pts',(16.3583621315168,0.699476705356048,4.06636716140204));
#45504=CARTESIAN_POINT('Ctrl Pts',(16.4060779675797,0.322483581772784,4.62424081966442));
#45505=CARTESIAN_POINT('Ctrl Pts',(16.4537938036425,-0.350651177000141,
4.60886452804932));
#45506=CARTESIAN_POINT('Ctrl Pts',(16.5015096397054,-0.701777564471952,
4.03435857174156));
#45507=CARTESIAN_POINT('Ctrl Pts',(16.5492254757682,-0.408450816253369,
3.42830061032894));
#45508=CARTESIAN_POINT('Ctrl Pts',(16.596941311831,0.259962601354342,3.34724299517707));
#45509=CARTESIAN_POINT('Ctrl Pts',(16.6446571478939,0.689648362099571,3.86562218151166));
#45510=CARTESIAN_POINT('Ctrl Pts',(16.6923729839567,0.486019420324727,4.50740258623259));
#45511=CARTESIAN_POINT('Ctrl Pts',(16.7400888200196,-0.163928633504336,
4.6832273886238));
#45512=CARTESIAN_POINT('Ctrl Pts',(16.7878046560824,-0.663338500820136,
4.23163396723712));
#45513=CARTESIAN_POINT('Ctrl Pts',(16.8355204921452,-0.553594416058007,
3.56732750958986));
#45514=CARTESIAN_POINT('Ctrl Pts',(16.8832363282081,0.064523939115192,3.30035085740826));
#45515=CARTESIAN_POINT('Ctrl Pts',(16.9309521642709,0.623388968170475,3.67587277835446));
#45516=CARTESIAN_POINT('Ctrl Pts',(16.9786680003338,0.609786315682611,4.34904571427615));
#45517=CARTESIAN_POINT('Ctrl Pts',(17.0263838363966,0.0362075067348799,
4.70168460001938));
#45518=CARTESIAN_POINT('Ctrl Pts',(17.0740996724594,-0.570621212771584,
4.40995572075944));
#45519=CARTESIAN_POINT('Ctrl Pts',(17.1218155085223,-0.653439692453966,
3.74175819514654));
#45520=CARTESIAN_POINT('Ctrl Pts',(17.1695313445851,-0.136194448093839,
3.31070809249149));
#45521=CARTESIAN_POINT('Ctrl Pts',(17.2172471806479,0.50612025357182,3.51264535462077));
#45522=CARTESIAN_POINT('Ctrl Pts',(17.2649630167108,0.683656938721366,4.16212788651693));
#45523=CARTESIAN_POINT('Ctrl Pts',(17.3126788527736,0.233380937628925,4.66272588556639));
#45524=CARTESIAN_POINT('Ctrl Pts',(17.3603946888365,-0.431212369515449,
4.55473250655174));
#45525=CARTESIAN_POINT('Ctrl Pts',(17.4081105248993,-0.699816722678643,
3.93731973111387));
#45526=CARTESIAN_POINT('Ctrl Pts',(17.4558263609621,-0.325768611341644,
3.37746721105403));
#45527=CARTESIAN_POINT('Ctrl Pts',(17.503542197025,0.347437828384778,3.38929612998149));
#45528=CARTESIAN_POINT('Ctrl Pts',(17.5512580330878,0.701586764287296,3.96194380963385));
#45529=CARTESIAN_POINT('Ctrl Pts',(17.5989738691507,0.411457779244836,4.56953907446917));
#45530=CARTESIAN_POINT('Ctrl Pts',(17.6466897052135,-0.256519215569882,
4.65411784373439));
#45531=CARTESIAN_POINT('Ctrl Pts',(17.6944055412764,-0.688930667671302,
4.13801013220155));
#45532=CARTESIAN_POINT('Ctrl Pts',(17.7421213773391,-0.488686487089258,
3.49516559270919));
#45533=CARTESIAN_POINT('Ctrl Pts',(17.789837213402,0.160326013994967,3.3159182573078));
#45534=CARTESIAN_POINT('Ctrl Pts',(17.8375530494648,0.662108669494809,3.76487371217125));
#45535=CARTESIAN_POINT('Ctrl Pts',(17.8852688855277,0.555866745946156,4.42974925503083));
#45536=CARTESIAN_POINT('Ctrl Pts',(17.9329847215905,-0.060836163514142,
4.69997944445332));
#45537=CARTESIAN_POINT('Ctrl Pts',(17.9807005576534,-0.621672287934692,
4.32740773946617));
#45538=CARTESIAN_POINT('Ctrl Pts',(18.0284163937162,-0.611617184687133,
3.65417246951162));
#45539=CARTESIAN_POINT('Ctrl Pts',(18.0761322297791,-0.0399046098013318,
3.29851594204507));
#45540=CARTESIAN_POINT('Ctrl Pts',(18.1238480658419,0.568452982276385,3.58704301871817));
#45541=CARTESIAN_POINT('Ctrl Pts',(18.1715639019047,0.65479145395626,4.25479484546229));
#45542=CARTESIAN_POINT('Ctrl Pts',(18.2192797379675,0.139824858206545,4.68856464509573));
#45543=CARTESIAN_POINT('Ctrl Pts',(18.2669955740304,-0.503545056316242,
4.49001493620888));
#45544=CARTESIAN_POINT('Ctrl Pts',(18.3147114100932,-0.684501797587214,
3.84147697155243));
#45545=CARTESIAN_POINT('Ctrl Pts',(18.3624272461561,-0.236870005719869,
3.33851314310973));
#45546=CARTESIAN_POINT('Ctrl Pts',(18.4101430822189,0.42828315711354,3.44300287363294));
#45547=CARTESIAN_POINT('Ctrl Pts',(18.4578589182817,0.70013730678616,4.05899163580144));
#45548=CARTESIAN_POINT('Ctrl Pts',(18.5055747543446,0.32904459463985,4.62080747111051));
#45549=CARTESIAN_POINT('Ctrl Pts',(18.5532905904074,-0.34421483176614,4.61252625334797));
#45550=CARTESIAN_POINT('Ctrl Pts',(18.6010064264702,-0.701376481735239,
4.0417527522082));
#45551=CARTESIAN_POINT('Ctrl Pts',(18.6487222625331,-0.414453316462639,
3.43263705626685));
#45552=CARTESIAN_POINT('Ctrl Pts',(18.6964380985959,0.253068706501803,3.34453948155689));
#45553=CARTESIAN_POINT('Ctrl Pts',(18.7441539346588,0.68819384232267,3.85836138648927));
#45554=CARTESIAN_POINT('Ctrl Pts',(18.7918697707216,0.491339983515996,4.50225220959958));
#45555=CARTESIAN_POINT('Ctrl Pts',(18.8395856067844,-0.156718942392259,
4.68491710048942));
#45556=CARTESIAN_POINT('Ctrl Pts',(18.8873014428473,-0.660860452068119,
4.23861207919858));
#45557=CARTESIAN_POINT('Ctrl Pts',(18.9350172789101,-0.558123639969822,
3.57318591405529));
#45558=CARTESIAN_POINT('Ctrl Pts',(18.9827331149729,0.0571466985584877,
3.29970969142451));
#45559=CARTESIAN_POINT('Ctrl Pts',(19.0304489510358,0.619938344467307,3.66932083449001));
#45560=CARTESIAN_POINT('Ctrl Pts',(19.0781647870986,0.613431069708698,4.3425997434341));
#45561=CARTESIAN_POINT('Ctrl Pts',(19.1258806231615,0.0436006047213211,
4.70126403633668));
#45562=CARTESIAN_POINT('Ctrl Pts',(19.1735964592243,-0.566268966340429,
4.41594677447179));
#45563=CARTESIAN_POINT('Ctrl Pts',(19.2213122952871,-0.656125032675529,
3.74865918919138));
#45564=CARTESIAN_POINT('Ctrl Pts',(19.26902813135,-0.143451385285705,3.31218173833215));
#45565=CARTESIAN_POINT('Ctrl Pts',(19.3167439674128,0.500955875668841,3.50733837970023));
#45566=CARTESIAN_POINT('Ctrl Pts',(19.3644598034757,0.68532764936022,4.15491376927485));
#45567=CARTESIAN_POINT('Ctrl Pts',(19.4121756395385,0.240352494576274,4.66022945763735));
#45568=CARTESIAN_POINT('Ctrl Pts',(19.4598914756013,-0.425342048711971,
4.55924628221868));
#45569=CARTESIAN_POINT('Ctrl Pts',(19.5076073116642,-0.700438454444525,
3.94469862920436));
#45570=CARTESIAN_POINT('Ctrl Pts',(19.555323147727,-0.332311429993836,3.3809350976725));
#45571=CARTESIAN_POINT('Ctrl Pts',(19.6030389837899,0.340982256434611,3.38566835039883));
#45572=CARTESIAN_POINT('Ctrl Pts',(19.6507548198527,0.701146760813864,3.95455188724214));
#45573=CARTESIAN_POINT('Ctrl Pts',(19.6984706559155,0.417437272672218,4.56517097885182));
#45574=CARTESIAN_POINT('Ctrl Pts',(19.7461864919784,-0.249611033919464,
4.6567851409082));
#45575=CARTESIAN_POINT('Ctrl Pts',(19.7939023280412,-0.687438163400574,
4.14526287985386));
#45576=CARTESIAN_POINT('Ctrl Pts',(19.841618164104,-0.493979350866992,3.5003444672369));
#45577=CARTESIAN_POINT('Ctrl Pts',(19.8893340001669,0.153106602982307,3.31426555646693));
#45578=CARTESIAN_POINT('Ctrl Pts',(19.9370498362297,0.659595612567133,3.75791065255607));
#45579=CARTESIAN_POINT('Ctrl Pts',(19.9847656722925,0.560361770063263,4.42386348253578));
#45580=CARTESIAN_POINT('Ctrl Pts',(20.0324815083554,-0.0534494809679074,
4.70058849011268));
#45581=CARTESIAN_POINT('Ctrl Pts',(20.0801973444182,-0.618198828117398,
4.33392863744107));
#45582=CARTESIAN_POINT('Ctrl Pts',(20.1279131804811,-0.615205937201001,
3.66066167313574));
#45583=CARTESIAN_POINT('Ctrl Pts',(20.1756290165439,-0.0473369003220797,
3.29892991724937));
#45584=CARTESIAN_POINT('Ctrl Pts',(20.2233448526068,0.564147630203746,3.58116102158214));
#45585=CARTESIAN_POINT('Ctrl Pts',(20.2710606886696,0.657292163719816,4.24771695100806));
#45586=CARTESIAN_POINT('Ctrl Pts',(20.3187765247324,0.147355317357748,4.68736342730055));
#45587=CARTESIAN_POINT('Ctrl Pts',(20.3664923607953,-0.498896366832293,
4.49468216892218));
#45588=CARTESIAN_POINT('Ctrl Pts',(20.4062555575143,-0.653992183610565,
3.9575054511282));
#45589=CARTESIAN_POINT('Ctrl Pts',(20.4380661148895,-0.465699721472375,
3.59327933193152));
#45590=CARTESIAN_POINT('Ctrl Pts',(20.461924032921,-0.215665100260693,3.41899970433759));
#45591=CARTESIAN_POINT('Ctrl Pts',(20.4857819509523,0.0900520562992202,
3.38718375849312));
#45592=CARTESIAN_POINT('Ctrl Pts',(20.5096398689838,0.372154449079436,3.50499792242313));
#45593=CARTESIAN_POINT('Ctrl Pts',(20.5334977870152,0.564103623124681,3.74397162737493));
#45594=CARTESIAN_POINT('Ctrl Pts',(20.5573557050466,0.61766411855396,4.04548854604559));
#45595=CARTESIAN_POINT('Ctrl Pts',(20.581213623078,0.520427284318709,4.33591550271974));
#45596=CARTESIAN_POINT('Ctrl Pts',(20.6050715411094,0.295805552416038,4.5441843692251));
#45597=CARTESIAN_POINT('Ctrl Pts',(20.6289294591409,-0.00108183093298003,
4.61939465531364));
#45598=CARTESIAN_POINT('Ctrl Pts',(20.6527873771723,-0.297740088546312,
4.543141139652));
#45599=CARTESIAN_POINT('Ctrl Pts',(20.6766452952037,-0.521574030203058,
4.33407743490148));
#45600=CARTESIAN_POINT('Ctrl Pts',(20.7005032132351,-0.617878846294169,
4.04332131262121));
#45601=CARTESIAN_POINT('Ctrl Pts',(20.7243611312665,-0.563090193646282,
3.74197268265107));
#45602=CARTESIAN_POINT('Ctrl Pts',(20.748219049298,-0.370613436173077,3.50371837193987));
#45603=CARTESIAN_POINT('Ctrl Pts',(20.7720769673294,-0.0875101228827464,
3.38681864340431));
#45604=CARTESIAN_POINT('Ctrl Pts',(20.7959348853608,0.216991017820888,3.41985835035499));
#45605=CARTESIAN_POINT('Ctrl Pts',(20.8197928033922,0.468432357761717,3.59475855107288));
#45606=CARTESIAN_POINT('Ctrl Pts',(20.8436507214236,0.605329007232586,3.86875129405724));
#45607=CARTESIAN_POINT('Ctrl Pts',(20.8675086394551,0.594206341669864,4.17483793696784));
#45608=CARTESIAN_POINT('Ctrl Pts',(20.8913665574864,0.437783978244149,4.43817193323088));
#45609=CARTESIAN_POINT('Ctrl Pts',(20.9152244755179,0.174311539695801,4.5943609607934));
#45610=CARTESIAN_POINT('Ctrl Pts',(20.9390823935493,-0.13178483570001,4.60521254097096));
#45611=CARTESIAN_POINT('Ctrl Pts',(20.9629403115808,-0.405656219889506,
4.46807317049539));
#45612=CARTESIAN_POINT('Ctrl Pts',(20.9867982296121,-0.580333613298163,
4.21647715910241));
#45613=CARTESIAN_POINT('Ctrl Pts',(21.0106561476436,-0.613103627724174,
3.91194658594648));
#45614=CARTESIAN_POINT('Ctrl Pts',(21.034514065675,-0.495953105920446,3.62894747086441));
#45615=CARTESIAN_POINT('Ctrl Pts',(21.0583719837064,-0.257528539509485,
3.43668080652407));
#45616=CARTESIAN_POINT('Ctrl Pts',(21.0822299017379,0.0438687693677006,
3.38216102944232));
#45617=CARTESIAN_POINT('Ctrl Pts',(21.1060878197692,0.334538969374667,3.47871971028568));
#45618=CARTESIAN_POINT('Ctrl Pts',(21.1299457378007,0.543405278604256,3.7027456213393));
#45619=CARTESIAN_POINT('Ctrl Pts',(21.153803655832,0.619394195209021,3.99945832503004));
#45620=CARTESIAN_POINT('Ctrl Pts',(21.1776615738635,0.543924359096133,4.29630348300169));
#45621=CARTESIAN_POINT('Ctrl Pts',(21.2015194918949,0.33545020099803,4.52069436823682));
#45622=CARTESIAN_POINT('Ctrl Pts',(21.2253774099264,0.0449493312674926,
4.61776129700707));
#45623=CARTESIAN_POINT('Ctrl Pts',(21.2492353279577,-0.256542874348706,
4.56376876117982));
#45624=CARTESIAN_POINT('Ctrl Pts',(21.2730932459892,-0.495303359101402,
4.37191940649105));
#45625=CARTESIAN_POINT('Ctrl Pts',(21.2969511640206,-0.612948680759938,
4.08912562603418));
#45626=CARTESIAN_POINT('Ctrl Pts',(21.320809082052,-0.580711353586496,3.78453820227854));
#45627=CARTESIAN_POINT('Ctrl Pts',(21.3446670000834,-0.406474282201139,
3.53263705712739));
#45628=CARTESIAN_POINT('Ctrl Pts',(21.3685249181149,-0.132843176680646,
3.39501888221951));
#45629=CARTESIAN_POINT('Ctrl Pts',(21.3923828361463,0.17327170411384,3.40533506996376));
#45630=CARTESIAN_POINT('Ctrl Pts',(21.4162407541777,0.437016933425986,3.56106303144932));
#45631=CARTESIAN_POINT('Ctrl Pts',(21.4400986722091,0.593899618413251,3.82412303814848));
#45632=CARTESIAN_POINT('Ctrl Pts',(21.4639565902405,0.605557669197671,4.13018975281259));
#45633=CARTESIAN_POINT('Ctrl Pts',(21.4878145082719,0.469140374803543,4.40442152661638));
#45634=CARTESIAN_POINT('Ctrl Pts',(21.5116724263034,0.218005479642704,4.57976122094124));
#45635=CARTESIAN_POINT('Ctrl Pts',(21.5355303443348,-0.0864376936408111,
4.61333350436739));
#45636=CARTESIAN_POINT('Ctrl Pts',(21.5593882623662,-0.369744496313637,
4.49692903910649));
#45637=CARTESIAN_POINT('Ctrl Pts',(21.5832461803976,-0.562638697999917,
4.2590118877088));
#45638=CARTESIAN_POINT('Ctrl Pts',(21.607104098429,-0.617952412054802,3.95775927442416));
#45639=CARTESIAN_POINT('Ctrl Pts',(21.6309620164605,-0.522159928676552,
3.66683566915707));
#45640=CARTESIAN_POINT('Ctrl Pts',(21.6548199344919,-0.298685119385998,
3.45737981799522));
#45641=CARTESIAN_POINT('Ctrl Pts',(21.6786778525233,-0.00217366238626178,
3.38060938201055));
#45642=CARTESIAN_POINT('Ctrl Pts',(21.7025357705547,0.294869314276287,3.45529682398599));
#45643=CARTESIAN_POINT('Ctrl Pts',(21.7263936885862,0.519808711519421,3.66317902991346));
#45644=CARTESIAN_POINT('Ctrl Pts',(21.7502516066175,0.617640719491047,3.95342313784609));
#45645=CARTESIAN_POINT('Ctrl Pts',(21.774109524649,0.564442747351711,4.25505655730362));
#45646=CARTESIAN_POINT('Ctrl Pts',(21.7979674426804,0.373223148373148,4.49432170089927));
#45647=CARTESIAN_POINT('Ctrl Pts',(21.8218253607118,0.0907403232229101,
4.61271172357229));
#45648=CARTESIAN_POINT('Ctrl Pts',(21.8456832787432,-0.213930982672105,
4.58127703989962));
#45649=CARTESIAN_POINT('Ctrl Pts',(21.8695411967746,-0.466290335940828,
4.40770428630285));
#45650=CARTESIAN_POINT('Ctrl Pts',(21.8933991148061,-0.604629000578284,
4.13443672906324));
#45651=CARTESIAN_POINT('Ctrl Pts',(21.9172570328375,-0.595119404811066,
3.82829572958469));
#45652=CARTESIAN_POINT('Ctrl Pts',(21.9411149508689,-0.440086903840403,
3.56414110135311));
#45653=CARTESIAN_POINT('Ctrl Pts',(21.9649728689003,-0.177441167154219,
3.40656584639871));
#45654=CARTESIAN_POINT('Ctrl Pts',(21.9888307869318,0.128593768301574,3.39410140682164));
#45655=CARTESIAN_POINT('Ctrl Pts',(22.0126887049631,0.403184024583593,3.52979567762293));
#45656=CARTESIAN_POINT('Ctrl Pts',(22.0365466229946,0.579184804342829,3.7804677133541));
#45657=CARTESIAN_POINT('Ctrl Pts',(22.060404541026,0.613559122762511,4.08482137310942));
#45658=CARTESIAN_POINT('Ctrl Pts',(22.0842624590574,0.497901522652627,4.36843389665204));
#45659=CARTESIAN_POINT('Ctrl Pts',(22.1081203770888,0.260493437687466,4.56195429652472));
#45660=CARTESIAN_POINT('Ctrl Pts',(22.1319782951203,-0.0406123884881684,
4.61806156357065));
#45661=CARTESIAN_POINT('Ctrl Pts',(22.1558362131517,-0.33178737942464,4.52303594266224));
#45662=CARTESIAN_POINT('Ctrl Pts',(22.1796941311831,-0.541831318374727,
4.30011378656432));
#45663=CARTESIAN_POINT('Ctrl Pts',(22.2035520492145,-0.619382740812877,
4.00380563470766));
#45664=CARTESIAN_POINT('Ctrl Pts',(22.2274099672459,-0.545478211438426,
3.70656690151735));
#45665=CARTESIAN_POINT('Ctrl Pts',(22.2512678852774,-0.338189400908512,
3.48108055383335));
#45666=CARTESIAN_POINT('Ctrl Pts',(22.2751258033088,-0.0482040696311437,
3.38248414587532));
#45667=CARTESIAN_POINT('Ctrl Pts',(22.2989837213402,0.253568469476171,3.43488718493857));
#45668=CARTESIAN_POINT('Ctrl Pts',(22.3228416393716,0.493336611197201,3.62547570084914));
#45669=CARTESIAN_POINT('Ctrl Pts',(22.346699557403,0.612470512379129,3.90764560936005));
#45670=CARTESIAN_POINT('Ctrl Pts',(22.3705574754344,0.581838691587799,4.21239868278141));
#45671=CARTESIAN_POINT('Ctrl Pts',(22.3944153934659,0.408931458591185,4.46521449128699));
#45672=CARTESIAN_POINT('Ctrl Pts',(22.4182733114973,0.13602935083686,4.60427268703701));
#45673=CARTESIAN_POINT('Ctrl Pts',(22.4421312295287,-0.170135649772668,
4.59556974592947));
#45674=CARTESIAN_POINT('Ctrl Pts',(22.4659891475601,-0.434697828443077,
4.44123378804823));
#45675=CARTESIAN_POINT('Ctrl Pts',(22.4898470655916,-0.592964587096883,
4.17900413283907));
#45676=CARTESIAN_POINT('Ctrl Pts',(22.513704983623,-0.606235276705168,3.87300312362118));
#45677=CARTESIAN_POINT('Ctrl Pts',(22.5375629016543,-0.471265070143009,
3.59805624874041));
#45678=CARTESIAN_POINT('Ctrl Pts',(22.5614208196858,-0.22105744785653,3.4213956854475));
#45679=CARTESIAN_POINT('Ctrl Pts',(22.5852787377172,0.0832042338527798,
3.38621941950615));
#45680=CARTESIAN_POINT('Ctrl Pts',(22.6091366557487,0.36712117327337,3.50112963696785));
#45681=CARTESIAN_POINT('Ctrl Pts',(22.63299457378,0.561265174232679,3.7380264683998));
#45682=CARTESIAN_POINT('Ctrl Pts',(22.6568524918115,0.618167971965146,4.03898443479498));
#45683=CARTESIAN_POINT('Ctrl Pts',(22.6807104098429,0.523905402647805,4.33040686810369));
#45684=CARTESIAN_POINT('Ctrl Pts',(22.7045683278744,0.301545895245711,4.54104106792393));
#45685=CARTESIAN_POINT('Ctrl Pts',(22.7284262459057,0.00542710047790416,
4.61936606261506));
#45686=CARTESIAN_POINT('Ctrl Pts',(22.7522841639372,-0.291974666000346,
4.54625809930836));
#45687=CARTESIAN_POINT('Ctrl Pts',(22.7761420819686,-0.518067845615496,
4.33953802216683));
#45688=CARTESIAN_POINT('Ctrl Pts',(22.7920473606562,-0.584213376873476,
4.14642833911731));
#45689=CARTESIAN_POINT('Ctrl Pts',(22.8,-0.592174260192535,4.04779597854866));
#45690=CARTESIAN_POINT('Ctrl Pts',(3.96816317011931,-0.282716247115855,
3.54616445487434));
#45691=CARTESIAN_POINT('Ctrl Pts',(3.97611580946312,-0.207125539895404,
3.49907532469992));
#45692=CARTESIAN_POINT('Ctrl Pts',(3.99202108815073,-0.0320395462633344,
3.44344227840288));
#45693=CARTESIAN_POINT('Ctrl Pts',(4.01587900618214,0.238586678544665,3.49618207793602));
#45694=CARTESIAN_POINT('Ctrl Pts',(4.03973692421357,0.450798406251909,3.67207593825259));
#45695=CARTESIAN_POINT('Ctrl Pts',(4.06359484224498,0.552814952159096,3.92817792166325));
#45696=CARTESIAN_POINT('Ctrl Pts',(4.0874527602764,0.519633627921064,4.20183097195279));
#45697=CARTESIAN_POINT('Ctrl Pts',(4.11131067830782,0.359398059257131,4.42613686623617));
#45698=CARTESIAN_POINT('Ctrl Pts',(4.13516859633924,0.11127440638865,4.54623750576341));
#45699=CARTESIAN_POINT('Ctrl Pts',(4.15902651437066,-0.164055973910312,
4.53276988152218));
#45700=CARTESIAN_POINT('Ctrl Pts',(4.18288443240208,-0.399271733473279,
4.38902461621758));
#45701=CARTESIAN_POINT('Ctrl Pts',(4.2067423504335,-0.536853866020863,4.15015270818839));
#45702=CARTESIAN_POINT('Ctrl Pts',(4.23060026846491,-0.543161034884179,
3.87456412255522));
#45703=CARTESIAN_POINT('Ctrl Pts',(4.25445818649634,-0.416650307492554,
3.62964815836115));
#45704=CARTESIAN_POINT('Ctrl Pts',(4.27831610452775,-0.188257351244862,
3.47529323740438));
#45705=CARTESIAN_POINT('Ctrl Pts',(4.30217402255918,0.0861697193074588,
3.44924344981891));
#45706=CARTESIAN_POINT('Ctrl Pts',(4.32603194059059,0.339525912432458,3.55786862136322));
#45707=CARTESIAN_POINT('Ctrl Pts',(4.34988985862202,0.509858789389686,3.77460696883261));
#45708=CARTESIAN_POINT('Ctrl Pts',(4.37374777665342,0.555517294574929,4.0464600464808));
#45709=CARTESIAN_POINT('Ctrl Pts',(4.39760569468486,0.465336694276122,4.30695238014399));
#45710=CARTESIAN_POINT('Ctrl Pts',(4.42146361271626,0.261368594047533,4.4923864940975));
#45711=CARTESIAN_POINT('Ctrl Pts',(4.4453215307477,-0.00651124555331369,
4.55741869872598));
#45712=CARTESIAN_POINT('Ctrl Pts',(4.4691794487791,-0.272798909000308,4.48614684730087));
#45713=CARTESIAN_POINT('Ctrl Pts',(4.49303736681053,-0.472379807908186,
4.29599884956661));
#45714=CARTESIAN_POINT('Ctrl Pts',(4.51689528484195,-0.55645097662433,4.03347107014466));
#45715=CARTESIAN_POINT('Ctrl Pts',(4.54075320287336,-0.504454724024634,
3.76275870240323));
#45716=CARTESIAN_POINT('Ctrl Pts',(4.56461112090479,-0.329105550388866,
3.55005829421323));
#45717=CARTESIAN_POINT('Ctrl Pts',(4.5884690389362,-0.0732811049967102,
3.44738088927219));
#45718=CARTESIAN_POINT('Ctrl Pts',(4.61232695696762,0.200462566687888,3.47983390993684));
#45719=CARTESIAN_POINT('Ctrl Pts',(4.63618487499904,0.425187680335341,3.63948170866684));
#45720=CARTESIAN_POINT('Ctrl Pts',(4.66004279303046,0.54594282425631,3.88728604994618));
#45721=CARTESIAN_POINT('Ctrl Pts',(4.68390071106188,0.533200076465109,4.16265202228146));
#45722=CARTESIAN_POINT('Ctrl Pts',(4.7077586290933,0.390075385898422,4.39824514461603));
#45723=CARTESIAN_POINT('Ctrl Pts',(4.73161654712472,0.151566638040082,4.53645648111246));
#45724=CARTESIAN_POINT('Ctrl Pts',(4.75547446515614,-0.124004281411749,
4.54348959519552));
#45725=CARTESIAN_POINT('Ctrl Pts',(4.77933238318755,-0.369252776249408,
4.41762469889406));
#45726=CARTESIAN_POINT('Ctrl Pts',(4.80319030121898,-0.524208909050512,
4.18963918784455));
#45727=CARTESIAN_POINT('Ctrl Pts',(4.82704821925039,-0.550981684424725,
3.91528172969931));
#45728=CARTESIAN_POINT('Ctrl Pts',(4.85090613728181,-0.443024429517375,
3.66164019632193));
#45729=CARTESIAN_POINT('Ctrl Pts',(4.87476405531323,-0.226735633849849,
3.49073685167984));
#45730=CARTESIAN_POINT('Ctrl Pts',(4.89862197334465,0.0449962004486201,
3.44436221885167));
#45731=CARTESIAN_POINT('Ctrl Pts',(4.92247989137607,0.305725238065515,3.53385615878353));
#45732=CARTESIAN_POINT('Ctrl Pts',(4.94633780940749,0.491696127187109,3.73733496539613));
#45733=CARTESIAN_POINT('Ctrl Pts',(4.9701957274389,0.557433919677865,4.00504252782125));
#45734=CARTESIAN_POINT('Ctrl Pts',(4.99405364547033,0.486863934612277,4.27151705483839));
#45735=CARTESIAN_POINT('Ctrl Pts',(5.01791156350174,0.297242455626679,4.47159826597145));
#45736=CARTESIAN_POINT('Ctrl Pts',(5.04176948153317,0.0349370995184326,
4.55636085499566));
#45737=CARTESIAN_POINT('Ctrl Pts',(5.06562739956458,-0.235911329089554,
4.505078060008));
#45738=CARTESIAN_POINT('Ctrl Pts',(5.08948531759601,-0.449073011639563,
4.33028992129829));
#45739=CARTESIAN_POINT('Ctrl Pts',(5.11334323562741,-0.552424110340463,
4.07473689991432));
#45740=CARTESIAN_POINT('Ctrl Pts',(5.13720115365885,-0.520692466332485,
3.80090867070902));
#45741=CARTESIAN_POINT('Ctrl Pts',(5.16105907169026,-0.361637330928202,
3.57576369465428));
#45742=CARTESIAN_POINT('Ctrl Pts',(5.18491698972168,-0.114152017308863,
3.45435605122152));
#45743=CARTESIAN_POINT('Ctrl Pts',(5.2087749077531,0.161246573981014,3.46637321630784));
#45744=CARTESIAN_POINT('Ctrl Pts',(5.23263282578452,0.397215985664045,3.60887666570863));
#45745=CARTESIAN_POINT('Ctrl Pts',(5.25649074381594,0.536055268906009,3.84702042432939));
#45746=CARTESIAN_POINT('Ctrl Pts',(5.28034866184735,0.543814437048104,4.12257185628156));
#45747=CARTESIAN_POINT('Ctrl Pts',(5.30420657987878,0.418596162124088,4.3681511305826));
#45748=CARTESIAN_POINT('Ctrl Pts',(5.32806449791019,0.191019723230217,4.5237074252207));
#45749=CARTESIAN_POINT('Ctrl Pts',(5.35192241594161,-0.0832662412662402,
4.55120298888854));
#45750=CARTESIAN_POINT('Ctrl Pts',(5.37578033397303,-0.337191341646214,
4.44391440730515));
#45751=CARTESIAN_POINT('Ctrl Pts',(5.39963825200445,-0.508663974085987,
4.22807666114996));
#45752=CARTESIAN_POINT('Ctrl Pts',(5.42349617003587,-0.555754409133215,
3.95646795866016));
#45753=CARTESIAN_POINT('Ctrl Pts',(5.4473540880673,-0.466947752701331,3.69550402606682));
#45754=CARTESIAN_POINT('Ctrl Pts',(5.47121200609871,-0.263959651332346,
3.50899765340418));
#45755=CARTESIAN_POINT('Ctrl Pts',(5.49506992413013,0.00357377490351851,
3.44255472911916));
#45756=CARTESIAN_POINT('Ctrl Pts',(5.51892784216155,0.270233315828591,3.51242235806964));
#45757=CARTESIAN_POINT('Ctrl Pts',(5.54278576019296,0.470813450024345,3.70151600181885));
#45758=CARTESIAN_POINT('Ctrl Pts',(5.56664367822439,0.556266870991092,3.96359711366712));
#45759=CARTESIAN_POINT('Ctrl Pts',(5.5905015962558,0.505697889589837,4.23457972281303));
#45760=CARTESIAN_POINT('Ctrl Pts',(5.61435951428722,0.331471999260015,4.4482011999181));
#45761=CARTESIAN_POINT('Ctrl Pts',(5.63821743231864,0.0761921759760934,
4.55222527486821));
#45762=CARTESIAN_POINT('Ctrl Pts',(5.66207535035006,-0.197718709731212,
4.52121522783523));
#45763=CARTESIAN_POINT('Ctrl Pts',(5.68593326838148,-0.423281985227643,
4.3627538599096));
#45764=CARTESIAN_POINT('Ctrl Pts',(5.70979118641289,-0.545341285237878,
4.11558929214995));
#45765=CARTESIAN_POINT('Ctrl Pts',(5.73364910444432,-0.534049786451273,
3.84015999362387));
#45766=CARTESIAN_POINT('Ctrl Pts',(5.75750702247573,-0.392168567195948,
3.6038159310769));
#45767=CARTESIAN_POINT('Ctrl Pts',(5.78136494050716,-0.154391451667357,
3.46434966433946));
#45768=CARTESIAN_POINT('Ctrl Pts',(5.80522285853857,0.121138580962943,3.45586449715393));
#45769=CARTESIAN_POINT('Ctrl Pts',(5.82908077656999,0.367046927720705,3.58043527923202));
#45770=CARTESIAN_POINT('Ctrl Pts',(5.85293869460141,0.523202308305842,3.80760107017232));
#45771=CARTESIAN_POINT('Ctrl Pts',(5.87679661263283,0.551420461789987,4.08181362911724));
#45772=CARTESIAN_POINT('Ctrl Pts',(5.90065453066425,0.44480131269862,4.33602054829434));
#45773=CARTESIAN_POINT('Ctrl Pts',(5.92451244869567,0.229416087376931,4.50806125053784));
#45774=CARTESIAN_POINT('Ctrl Pts',(5.94837036672709,-0.042067546589846,
4.55586721297736));
#45775=CARTESIAN_POINT('Ctrl Pts',(5.97222828475851,-0.30326465903273,4.46774835821298));
#45776=CARTESIAN_POINT('Ctrl Pts',(5.99608620278993,-0.490305038147314,
4.26525255699254));
#45777=CARTESIAN_POINT('Ctrl Pts',(6.01994412082133,-0.557452977205748,
3.99789477357902));
#45778=CARTESIAN_POINT('Ctrl Pts',(6.04380203885278,-0.488287539408226,
3.73105273207384));
#45779=CARTESIAN_POINT('Ctrl Pts',(6.06765995688417,-0.299724270968661,
3.52997381710292));
#45780=CARTESIAN_POINT('Ctrl Pts',(6.09151787491561,-0.0378669053578504,
3.44383251805177));
#45781=CARTESIAN_POINT('Ctrl Pts',(6.11537579294702,0.233243627260218,3.49368287747685));
#45782=CARTESIAN_POINT('Ctrl Pts',(6.13923371097844,0.447331678364145,3.6673537262422));
#45783=CARTESIAN_POINT('Ctrl Pts',(6.16309162900986,0.552012406214274,3.92234268746235));
#45784=CARTESIAN_POINT('Ctrl Pts',(6.18694954704127,0.521753629494025,4.19636433484848));
#45785=CARTESIAN_POINT('Ctrl Pts',(6.2108074650727,0.363831507594212,4.42228768590875));
#45786=CARTESIAN_POINT('Ctrl Pts',(6.23466538310411,0.117094415953721,4.54510476979165));
#45787=CARTESIAN_POINT('Ctrl Pts',(6.25852330113554,-0.158561881267111,
4.53433708369694));
#45788=CARTESIAN_POINT('Ctrl Pts',(6.28238121916695,-0.394905399742298,
4.39345989467659));
#45789=CARTESIAN_POINT('Ctrl Pts',(6.30623913719837,-0.535697351746728,
4.1553358869807));
#45790=CARTESIAN_POINT('Ctrl Pts',(6.33009705522979,-0.543633587309765,
3.88114808171798));
#45791=CARTESIAN_POINT('Ctrl Pts',(6.36190761260502,-0.381130543103143,
3.54983775818315));
#45792=CARTESIAN_POINT('Ctrl Pts',(6.40167080932404,0.0904237977681596,
3.37418170676098));
#45793=CARTESIAN_POINT('Ctrl Pts',(6.4493866453869,0.576013642360818,3.73827828410759));
#45794=CARTESIAN_POINT('Ctrl Pts',(6.49710248144972,0.531303907723303,4.34259299019566));
#45795=CARTESIAN_POINT('Ctrl Pts',(6.54481831751257,-0.000617460830772086,
4.63236849138271));
#45796=CARTESIAN_POINT('Ctrl Pts',(6.5925341535754,-0.532336898979176,4.34139325430452));
#45797=CARTESIAN_POINT('Ctrl Pts',(6.64024998963824,-0.575010046738857,
3.73693099107234));
#45798=CARTESIAN_POINT('Ctrl Pts',(6.68796582570108,-0.0897448725589052,
3.37403863313417));
#45799=CARTESIAN_POINT('Ctrl Pts',(6.73568166176391,0.477988548433368,3.58598174571673));
#45800=CARTESIAN_POINT('Ctrl Pts',(6.78339749782676,0.606749053262868,4.17812127049189));
#45801=CARTESIAN_POINT('Ctrl Pts',(6.83111333388958,0.178337754027021,4.60669083891839));
#45802=CARTESIAN_POINT('Ctrl Pts',(6.87882916995244,-0.413851892207341,
4.47812605548031));
#45803=CARTESIAN_POINT('Ctrl Pts',(6.92654500601527,-0.625990718083913,
3.91049119230943));
#45804=CARTESIAN_POINT('Ctrl Pts',(6.97426084207811,-0.263274891453005,
3.42505341469988));
#45805=CARTESIAN_POINT('Ctrl Pts',(7.02197667814094,0.341211513798207,3.46759805477058));
#45806=CARTESIAN_POINT('Ctrl Pts',(7.06969251420378,0.63235750294684,3.99905552874491));
#45807=CARTESIAN_POINT('Ctrl Pts',(7.11740835026662,0.342800202184808,4.53138035934227));
#45808=CARTESIAN_POINT('Ctrl Pts',(7.16512418632946,-0.261555976381552,
4.57573041153878));
#45809=CARTESIAN_POINT('Ctrl Pts',(7.2128400223923,-0.625721183287191,4.0913783776429));
#45810=CARTESIAN_POINT('Ctrl Pts',(7.26055585845514,-0.41527704940159,3.52311216844965));
#45811=CARTESIAN_POINT('Ctrl Pts',(7.30827169451797,0.176522415171576,3.39277939551711));
#45812=CARTESIAN_POINT('Ctrl Pts',(7.35598753058081,0.606218615784068,3.8200666455489));
#45813=CARTESIAN_POINT('Ctrl Pts',(7.40370336664364,0.479214941044062,4.4125894643569));
#45814=CARTESIAN_POINT('Ctrl Pts',(7.4514192027065,-0.0878591916424711,
4.62622502914213));
#45815=CARTESIAN_POINT('Ctrl Pts',(7.49913503876932,-0.574250874682306,
4.26478851416677));
#45816=CARTESIAN_POINT('Ctrl Pts',(7.54685087483217,-0.53329914461431,3.6601926322252));
#45817=CARTESIAN_POINT('Ctrl Pts',(7.594566710895,-0.00261060360317682,
3.36764708477891));
#45818=CARTESIAN_POINT('Ctrl Pts',(7.64228254695784,0.530475294557976,3.65580094934904));
#45819=CARTESIAN_POINT('Ctrl Pts',(7.68999838302067,0.576417567478113,4.26003809833172));
#45820=CARTESIAN_POINT('Ctrl Pts',(7.73771421908353,0.093026718772369,4.62547826040714));
#45821=CARTESIAN_POINT('Ctrl Pts',(7.78543005514634,-0.475791997136335,
4.41653211173522));
#45822=CARTESIAN_POINT('Ctrl Pts',(7.8331458912092,-0.607683601098078,3.82507811568403));
#45823=CARTESIAN_POINT('Ctrl Pts',(7.88086172727203,-0.181530003744534,
3.39425757752065));
#45824=CARTESIAN_POINT('Ctrl Pts',(7.92857756333487,0.411325389238953,3.51969962646458));
#45825=CARTESIAN_POINT('Ctrl Pts',(7.97629339939771,0.626454348233276,4.08620889879763));
#45826=CARTESIAN_POINT('Ctrl Pts',(8.02400923546054,0.266300640003926,4.57355121287022));
#45827=CARTESIAN_POINT('Ctrl Pts',(8.07172507152339,-0.338401043502061,
4.5341926229444));
#45828=CARTESIAN_POINT('Ctrl Pts',(8.11944090758622,-0.632343841791292,
4.00427672775865));
#45829=CARTESIAN_POINT('Ctrl Pts',(8.16715674364906,-0.345595560302635,
3.47043344766624));
#45830=CARTESIAN_POINT('Ctrl Pts',(8.2148725797119,0.258518441882999,3.42289928101069));
#45831=CARTESIAN_POINT('Ctrl Pts',(8.26258841577473,0.625230981070026,3.90532558443901));
#45832=CARTESIAN_POINT('Ctrl Pts',(8.31030425183758,0.417784289925175,4.47469286043008));
#45833=CARTESIAN_POINT('Ctrl Pts',(8.35802008790041,-0.173320143095541,
4.60814237859973));
#45834=CARTESIAN_POINT('Ctrl Pts',(8.40573592396325,-0.605262021838435,
4.18312539302794));
#45835=CARTESIAN_POINT('Ctrl Pts',(8.45345176002609,-0.481382472773795,
3.58994154129225));
#45836=CARTESIAN_POINT('Ctrl Pts',(8.50116759608892,0.0845580080604409,
3.37332068174828));
#45837=CARTESIAN_POINT('Ctrl Pts',(8.54888343215178,0.572847569000584,3.73218908285563));
#45838=CARTESIAN_POINT('Ctrl Pts',(8.59659926821459,0.535082392934658,4.33699236997728));
#45839=CARTESIAN_POINT('Ctrl Pts',(8.64431510427745,0.00594282213592907,
4.6323303784547));
#45840=CARTESIAN_POINT('Ctrl Pts',(8.69203094034027,-0.528654133672296,
4.34698967074364));
#45841=CARTESIAN_POINT('Ctrl Pts',(8.73974677640312,-0.577779864139828,
3.74300300926635));
#45842=CARTESIAN_POINT('Ctrl Pts',(8.78746261246595,-0.0963214550818077,
3.37502063878676));
#45843=CARTESIAN_POINT('Ctrl Pts',(8.8351784485288,0.473590428273928,3.58096643225285));
#45844=CARTESIAN_POINT('Ctrl Pts',(8.88289428459164,0.608596934220305,4.17171719864135));
#45845=CARTESIAN_POINT('Ctrl Pts',(8.93061012065447,0.184719511004659,4.60477741930878));
#45846=CARTESIAN_POINT('Ctrl Pts',(8.97832595671731,-0.408788681441581,
4.48246123012823));
#45847=CARTESIAN_POINT('Ctrl Pts',(9.02604179278014,-0.626899937697651,
3.91709346970068));
#45848=CARTESIAN_POINT('Ctrl Pts',(9.07375762884299,-0.269319335070538,
3.42786005172794));
#45849=CARTESIAN_POINT('Ctrl Pts',(9.12147346490582,0.335581356962483,3.46403155175812));
#45850=CARTESIAN_POINT('Ctrl Pts',(9.16918930096866,0.632312525313962,3.99239112474344));
#45851=CARTESIAN_POINT('Ctrl Pts',(9.21690513703149,0.348381372290835,4.52773804495445));
#45852=CARTESIAN_POINT('Ctrl Pts',(9.26462097309434,-0.255473755443411,
4.5784549981902));
#45853=CARTESIAN_POINT('Ctrl Pts',(9.31233680915717,-0.624723402584967,
4.09796782591368));
#45854=CARTESIAN_POINT('Ctrl Pts',(9.36005264522002,-0.420279936527615,
3.52751529167185));
#45855=CARTESIAN_POINT('Ctrl Pts',(9.40776848128285,0.170113062081096,3.39095273519949));
#45856=CARTESIAN_POINT('Ctrl Pts',(9.45548431734569,0.604288618254829,3.81368765339017));
#45857=CARTESIAN_POINT('Ctrl Pts',(9.50320015340853,0.483536638109595,4.40751606625661));
#45858=CARTESIAN_POINT('Ctrl Pts',(9.55091598947137,-0.0812544769791981,
4.62711620503893));
#45859=CARTESIAN_POINT('Ctrl Pts',(9.5986318255342,-0.571428355597161,4.27082588331087));
#45860=CARTESIAN_POINT('Ctrl Pts',(9.64634766159704,-0.536850782714826,
3.66583198574659));
#45861=CARTESIAN_POINT('Ctrl Pts',(9.69406349765987,-0.0092748755543832,
3.36770971750703));
#45862=CARTESIAN_POINT('Ctrl Pts',(9.74177933372272,0.52681829253995,3.65022934471732));
#45863=CARTESIAN_POINT('Ctrl Pts',(9.78949516978555,0.579126116453474,4.253948746587));
#45864=CARTESIAN_POINT('Ctrl Pts',(9.83721100584839,0.099613516627068,4.62446310696212));
#45865=CARTESIAN_POINT('Ctrl Pts',(9.88492684191123,-0.471375708268938,
4.42152338761395));
#45866=CARTESIAN_POINT('Ctrl Pts',(9.93264267797408,-0.609493367214024,
3.83149225544889));
#45867=CARTESIAN_POINT('Ctrl Pts',(9.9803585140369,-0.187903888785556,3.39620437793004));
#45868=CARTESIAN_POINT('Ctrl Pts',(10.0280743500997,0.406240621987656,3.51539131074786));
#45869=CARTESIAN_POINT('Ctrl Pts',(10.0757901861626,0.627328118774167,4.07960185956908));
#45870=CARTESIAN_POINT('Ctrl Pts',(10.1235060222254,0.27233055140652,4.57071279591595));
#45871=CARTESIAN_POINT('Ctrl Pts',(10.1712218582883,-0.332752351661881,
4.5377293902281));
#45872=CARTESIAN_POINT('Ctrl Pts',(10.2189376943511,-0.632263650146131,
4.01094081146358));
#45873=CARTESIAN_POINT('Ctrl Pts',(10.2666535304139,-0.351157510074434,
3.47410511718603));
#45874=CARTESIAN_POINT('Ctrl Pts',(10.3143693664768,0.252421974751429,3.42020678572945));
#45875=CARTESIAN_POINT('Ctrl Pts',(10.3620852025396,0.624198476151732,3.89874148420283));
#45876=CARTESIAN_POINT('Ctrl Pts',(10.4098010386024,0.422763912373798,4.47026343579529));
#45877=CARTESIAN_POINT('Ctrl Pts',(10.4575168746653,-0.166901257195935,
4.60993523836389));
#45878=CARTESIAN_POINT('Ctrl Pts',(10.5052327107281,-0.603298434176698,
4.18949412648294));
#45879=CARTESIAN_POINT('Ctrl Pts',(10.552948546791,-0.485677376113382,3.5950376425108));
#45880=CARTESIAN_POINT('Ctrl Pts',(10.6006643828538,0.0779486895418537,
3.3724643225678));
#45881=CARTESIAN_POINT('Ctrl Pts',(10.6483802189166,0.569993274196054,3.72616667108832));
#45882=CARTESIAN_POINT('Ctrl Pts',(10.6960960549795,0.538604264682155,4.3313343790158));
#45883=CARTESIAN_POINT('Ctrl Pts',(10.7438118910423,0.0126066714187673,
4.63223262845832));
#45884=CARTESIAN_POINT('Ctrl Pts',(10.7915277271052,-0.524967822187051,
4.35254192703816));
#45885=CARTESIAN_POINT('Ctrl Pts',(10.839243563168,-0.580456287010268,3.74910654946403));
#45886=CARTESIAN_POINT('Ctrl Pts',(10.8869593992308,-0.102902812003948,
3.37607048800905));
#45887=CARTESIAN_POINT('Ctrl Pts',(10.9346752352937,0.469147898628881,3.5759984978049));
#45888=CARTESIAN_POINT('Ctrl Pts',(10.9823910713565,0.610372875182502,4.16529361116822));
#45889=CARTESIAN_POINT('Ctrl Pts',(11.0301069074193,0.191083048662156,4.60279705802663));
#45890=CARTESIAN_POINT('Ctrl Pts',(11.0778227434822,-0.403681281635282,
4.48674269127424));
#45891=CARTESIAN_POINT('Ctrl Pts',(11.125538579545,-0.627738879572117,3.92370502162571));
#45892=CARTESIAN_POINT('Ctrl Pts',(11.1732544156079,-0.275334205393669,
3.43073020456744));
#45893=CARTESIAN_POINT('Ctrl Pts',(11.2209702516707,0.329914106159097,3.46052459999659));
#45894=CARTESIAN_POINT('Ctrl Pts',(11.2686860877335,0.632197217644931,3.98572755614488));
#45895=CARTESIAN_POINT('Ctrl Pts',(11.3164019237964,0.353923896562866,4.52403711709511));
#45896=CARTESIAN_POINT('Ctrl Pts',(11.3641177598592,-0.24936318455202,4.58111533006939));
#45897=CARTESIAN_POINT('Ctrl Pts',(11.411833595922,-0.623656216347001,4.10454639383227));
#45898=CARTESIAN_POINT('Ctrl Pts',(11.4595494319849,-0.425236148486169,
3.53197089548594));
#45899=CARTESIAN_POINT('Ctrl Pts',(11.5072652680477,0.163684817628688,3.3891937253683));
#45900=CARTESIAN_POINT('Ctrl Pts',(11.5549811041106,0.602291497100466,3.80732935570755));
#45901=CARTESIAN_POINT('Ctrl Pts',(11.6026969401734,0.487804627338989,4.40239740331947));
#45902=CARTESIAN_POINT('Ctrl Pts',(11.6504127762363,-0.0746407375468588,
4.62793772378323));
#45903=CARTESIAN_POINT('Ctrl Pts',(11.6981286122991,-0.568542364648052,
4.276833170433));
#45904=CARTESIAN_POINT('Ctrl Pts',(11.7458444483619,-0.540342790144192,
3.67150845704832));
#45905=CARTESIAN_POINT('Ctrl Pts',(11.7935602844247,-0.0159381172083995,
3.36784258204823));
#45906=CARTESIAN_POINT('Ctrl Pts',(11.8412761204876,0.523102773999324,3.64469659094542));
#45907=CARTESIAN_POINT('Ctrl Pts',(11.8889919565504,0.581770338872691,4.24783118742311));
#45908=CARTESIAN_POINT('Ctrl Pts',(11.9367077926133,0.106189249871976,4.62337859111715));
#45909=CARTESIAN_POINT('Ctrl Pts',(11.9844236286761,-0.466907061217805,
4.4264678426758));
#45910=CARTESIAN_POINT('Ctrl Pts',(12.0321394647389,-0.611235433702689,
3.83792511225401));
#45911=CARTESIAN_POINT('Ctrl Pts',(12.0798553008018,-0.19425690235234,3.39821824509208));
#45912=CARTESIAN_POINT('Ctrl Pts',(12.1275711368646,0.401110731454808,3.51113682306459));
#45913=CARTESIAN_POINT('Ctrl Pts',(12.1752869729275,0.628132208685083,4.07298597854376));
#45914=CARTESIAN_POINT('Ctrl Pts',(12.2230028089903,0.27833021362349,4.56781098689255));
#45915=CARTESIAN_POINT('Ctrl Pts',(12.2707186450531,-0.327066699269377,
4.54120642908287));
#45916=CARTESIAN_POINT('Ctrl Pts',(12.3184344811159,-0.632113229655128,
4.01760367991507));
#45917=CARTESIAN_POINT('Ctrl Pts',(12.3661503171788,-0.356680454936339,
3.47783520061383));
#45918=CARTESIAN_POINT('Ctrl Pts',(12.4138661532416,0.246297469784735,3.4175786911271));
#45919=CARTESIAN_POINT('Ctrl Pts',(12.4615819893045,0.623096638228782,3.89216863128209));
#45920=CARTESIAN_POINT('Ctrl Pts',(12.5092978253673,0.427696576213203,4.46578177652963));
#45921=CARTESIAN_POINT('Ctrl Pts',(12.5570136614302,-0.16046383269669,4.61166034941614));
#45922=CARTESIAN_POINT('Ctrl Pts',(12.604729497493,-0.601267834987779,4.1958418118296));
#45923=CARTESIAN_POINT('Ctrl Pts',(12.6524453335558,-0.489918332714758,
3.60017872502631));
#45924=CARTESIAN_POINT('Ctrl Pts',(12.7001611696187,0.0713307128527425,
3.37167766707246));
#45925=CARTESIAN_POINT('Ctrl Pts',(12.7478770056815,0.56707566724347,3.72017467542775));
#45926=CARTESIAN_POINT('Ctrl Pts',(12.7955928417444,0.542066310823814,4.32563958500381));
#45927=CARTESIAN_POINT('Ctrl Pts',(12.8433086778072,0.0192691204123526,
4.63206465306178));
#45928=CARTESIAN_POINT('Ctrl Pts',(12.89102451387,-0.521223199767296,4.35805502464836));
#45929=CARTESIAN_POINT('Ctrl Pts',(12.9387403499329,-0.583068235550835,
3.7552379577156));
#45930=CARTESIAN_POINT('Ctrl Pts',(12.9864561859957,-0.109472738970043,
3.37718964036075));
#45931=CARTESIAN_POINT('Ctrl Pts',(13.0341720220585,0.464653258261548,3.57107765943178));
#45932=CARTESIAN_POINT('Ctrl Pts',(13.0818878581214,0.612081018822183,4.15885166366515));
#45933=CARTESIAN_POINT('Ctrl Pts',(13.1296036941842,0.197425361721354,4.6007497409078));
#45934=CARTESIAN_POINT('Ctrl Pts',(13.177319530247,-0.398529042827853,4.49097008735187));
#45935=CARTESIAN_POINT('Ctrl Pts',(13.2250353663099,-0.628508095190705,
3.93032504803489));
#45936=CARTESIAN_POINT('Ctrl Pts',(13.2727512023727,-0.281318492899819,
3.4336635891944));
#45937=CARTESIAN_POINT('Ctrl Pts',(13.3204670384356,0.324210210062374,3.45707757060249));
#45938=CARTESIAN_POINT('Ctrl Pts',(13.3681828744984,0.632011688508986,3.97906557286167));
#45939=CARTESIAN_POINT('Ctrl Pts',(13.4158987105612,0.359427108647973,4.52027798167956));
#45940=CARTESIAN_POINT('Ctrl Pts',(13.4636145466241,-0.243224915581421,
4.58371111441534));
#45941=CARTESIAN_POINT('Ctrl Pts',(13.5113303826869,-0.622519757336015,
4.11111334923356));
#45942=CARTESIAN_POINT('Ctrl Pts',(13.5590462187498,-0.430145127231255,
3.53647848575196));
#45943=CARTESIAN_POINT('Ctrl Pts',(13.6067620548126,0.157238391843492,3.38750256099959));
#45944=CARTESIAN_POINT('Ctrl Pts',(13.6544778908755,0.600227476264717,3.8009924589658));
#45945=CARTESIAN_POINT('Ctrl Pts',(13.7021937269383,0.492018433545193,4.39723404398833));
#45946=CARTESIAN_POINT('Ctrl Pts',(13.7499095630011,-0.0680187073756014,
4.62868949418496));
#45947=CARTESIAN_POINT('Ctrl Pts',(13.797625399064,-0.565593222711038,4.28280970824024));
#45948=CARTESIAN_POINT('Ctrl Pts',(13.8453412351268,-0.543774778860562,
3.67722141563181));
#45949=CARTESIAN_POINT('Ctrl Pts',(13.8930570711896,-0.0225995885319848,
3.36804566363559));
#45950=CARTESIAN_POINT('Ctrl Pts',(13.9407729072525,0.519329151684885,3.63920330259016));
#45951=CARTESIAN_POINT('Ctrl Pts',(13.9884887433153,0.584349941003394,4.24168610034696));
#45952=CARTESIAN_POINT('Ctrl Pts',(14.0362045793781,0.112753188118911,4.62222483333648));
#45953=CARTESIAN_POINT('Ctrl Pts',(14.083920415441,-0.462386552345973,4.43136492771341));
#45954=CARTESIAN_POINT('Ctrl Pts',(14.1316362515038,-0.612909607059929,
3.84437597156854));
#45955=CARTESIAN_POINT('Ctrl Pts',(14.1793520875667,-0.200588338784227,
3.40029895531576));
#45956=CARTESIAN_POINT('Ctrl Pts',(14.2270679236295,0.395936287445344,3.50693663598317));
#45957=CARTESIAN_POINT('Ctrl Pts',(14.2747837596923,0.628866528650988,4.06636199058228));
#45958=CARTESIAN_POINT('Ctrl Pts',(14.3224995957552,0.284298960241116,4.5648461081192));
#45959=CARTESIAN_POINT('Ctrl Pts',(14.370215431818,-0.321344717859966,4.54462335329573));
#45960=CARTESIAN_POINT('Ctrl Pts',(14.4179312678809,-0.631892597026201,
4.02426459303334));
#45961=CARTESIAN_POINT('Ctrl Pts',(14.4656471039437,-0.362163781425906,
3.48162328362967));
#45962=CARTESIAN_POINT('Ctrl Pts',(14.5133629400065,0.240145607263868,3.41501528911991));
#45963=CARTESIAN_POINT('Ctrl Pts',(14.5610787760693,0.6219255896881,3.8856077557581));
#45964=CARTESIAN_POINT('Ctrl Pts',(14.6087946121322,0.432581733546503,4.46124838043455));
#45965=CARTESIAN_POINT('Ctrl Pts',(14.656510448195,-0.154008584636381,4.61331752013935));
#45966=CARTESIAN_POINT('Ctrl Pts',(14.7042262842579,-0.599170449821005,
4.20216774399712));
#45967=CARTESIAN_POINT('Ctrl Pts',(14.7519421203207,-0.494104871512583,
3.60536421779174));
#45968=CARTESIAN_POINT('Ctrl Pts',(14.7996579563836,0.0647048130865326,
3.37096080264023));
#45969=CARTESIAN_POINT('Ctrl Pts',(14.8473737924464,0.564095072216763,3.71421376143635));
#45970=CARTESIAN_POINT('Ctrl Pts',(14.8950896285093,0.545468146811986,4.319908620492));
#45971=CARTESIAN_POINT('Ctrl Pts',(14.942805464572,0.0259294290834894,4.63182647092298));
#45972=CARTESIAN_POINT('Ctrl Pts',(14.9905213006349,-0.517420682347921,
4.36352835120552));
#45973=CARTESIAN_POINT('Ctrl Pts',(15.0382371366977,-0.585615419638682,
3.76139655297334));
#45974=CARTESIAN_POINT('Ctrl Pts',(15.0859529727606,-0.116030506223773,
3.3783779715317));
#45975=CARTESIAN_POINT('Ctrl Pts',(15.1336688088234,0.460107006415252,3.56620446371685));
#45976=CARTESIAN_POINT('Ctrl Pts',(15.1813846448862,0.613721175406852,4.15239207167311));
#45977=CARTESIAN_POINT('Ctrl Pts',(15.2291004809491,0.203745745708236,4.59863569535852));
#45978=CARTESIAN_POINT('Ctrl Pts',(15.2768163170119,-0.393332537305518,
4.49514294880206));
#45979=CARTESIAN_POINT('Ctrl Pts',(15.3245321530748,-0.629207499112597,
3.93695281360709));
#45980=CARTESIAN_POINT('Ctrl Pts',(15.3722479891376,-0.287271532882751,
3.43665987978239));
#45981=CARTESIAN_POINT('Ctrl Pts',(15.4199638252004,0.318470302234025,3.45369084645546));
#45982=CARTESIAN_POINT('Ctrl Pts',(15.4676796612633,0.631755958513824,3.97240591487529));
#45983=CARTESIAN_POINT('Ctrl Pts',(15.5153954973261,0.364890397275464,4.51646105625472));
#45984=CARTESIAN_POINT('Ctrl Pts',(15.563111333389,-0.237059630341402,4.58624206290064));
#45985=CARTESIAN_POINT('Ctrl Pts',(15.6108271694518,-0.621314151784485,
4.11766796269128));
#45986=CARTESIAN_POINT('Ctrl Pts',(15.6585430055147,-0.435006327496808,
3.54103756178819));
#45987=CARTESIAN_POINT('Ctrl Pts',(15.7062588415774,0.150774500763906,3.38587942993986));
#45988=CARTESIAN_POINT('Ctrl Pts',(15.7539746776403,0.598096785009218,3.79467766703735));
#45989=CARTESIAN_POINT('Ctrl Pts',(15.8016905137032,0.496177588678611,4.39202656178461));
#45990=CARTESIAN_POINT('Ctrl Pts',(15.849406349766,-0.0613891220090978,
4.62937143274106));
#45991=CARTESIAN_POINT('Ctrl Pts',(15.8971221858288,-0.562581257362808,
4.28875483288714));
#45992=CARTESIAN_POINT('Ctrl Pts',(15.9448380218917,-0.547146367654922,
3.68297022692873));
#45993=CARTESIAN_POINT('Ctrl Pts',(15.9925538579545,-0.0292585496004989,
3.36831893971177));
#45994=CARTESIAN_POINT('Ctrl Pts',(16.0402696940173,0.515497844752703,3.63375008981994));
#45995=CARTESIAN_POINT('Ctrl Pts',(16.0879855300802,0.586864636315616,4.23551416792571));
#45996=CARTESIAN_POINT('Ctrl Pts',(16.135701366143,0.119304602276749,4.62100196177401));
#45997=CARTESIAN_POINT('Ctrl Pts',(16.1834172022059,-0.457814683770117,
4.43621409878185));
#45998=CARTESIAN_POINT('Ctrl Pts',(16.2311330382687,-0.614515701326505,
3.85084411686165));
#45999=CARTESIAN_POINT('Ctrl Pts',(16.2788488743316,-0.206897494815317,
3.40244627748567));
#46000=CARTESIAN_POINT('Ctrl Pts',(16.3265647103943,0.390717864711932,3.50279121604045));
#46001=CARTESIAN_POINT('Ctrl Pts',(16.3742805464572,0.629530997107116,4.05973063144581));
#46002=CARTESIAN_POINT('Ctrl Pts',(16.42199638252,0.290236128279341,4.56181848892059));
#46003=CARTESIAN_POINT('Ctrl Pts',(16.4697122185829,-0.315587043004215,
4.54797978333095));
#46004=CARTESIAN_POINT('Ctrl Pts',(16.5174280546457,-0.631601776766168,
4.03092281095576));
#46005=CARTESIAN_POINT('Ctrl Pts',(16.5651438907086,-0.367606880481235,
3.48546894547127));
#46006=CARTESIAN_POINT('Ctrl Pts',(16.6128597267714,0.233967070508539,3.41251686443844));
#46007=CARTESIAN_POINT('Ctrl Pts',(16.6605755628343,0.620685460604191,3.87905958638177));
#46008=CARTESIAN_POINT('Ctrl Pts',(16.7082913988971,0.437418841753611,4.45666375105816));
#46009=CARTESIAN_POINT('Ctrl Pts',(16.7560072349599,-0.147536230033309,
4.61490656646286));
#46010=CARTESIAN_POINT('Ctrl Pts',(16.8037230710227,-0.597006511643959,
4.20847122033102));
#46011=CARTESIAN_POINT('Ctrl Pts',(16.8514389070856,-0.498236527486006,
3.61059354482716));
#46012=CARTESIAN_POINT('Ctrl Pts',(16.8991547431484,0.058071726216741,3.37031380889701));
#46013=CARTESIAN_POINT('Ctrl Pts',(16.9468705792113,0.561051820186282,3.70828459122417));
#46014=CARTESIAN_POINT('Ctrl Pts',(16.9945864152741,0.548809394786867,4.31414212204871));
#46015=CARTESIAN_POINT('Ctrl Pts',(17.0423022513369,0.0325868576366809,
4.63151810849805));
#46016=CARTESIAN_POINT('Ctrl Pts',(17.0900180873998,-0.513560692294518,
4.3689612987585));
#46017=CARTESIAN_POINT('Ctrl Pts',(17.1377339234626,-0.588097556344686,
3.76758165116972));
#46018=CARTESIAN_POINT('Ctrl Pts',(17.1854497595255,-0.122575385359494,
3.37963534952775));
#46019=CARTESIAN_POINT('Ctrl Pts',(17.2331655955883,0.455509648066065,3.56137945195155));
#46020=CARTESIAN_POINT('Ctrl Pts',(17.2808814316511,0.615293162755707,4.14591555269289));
#46021=CARTESIAN_POINT('Ctrl Pts',(17.328597267714,0.210043498584534,4.59645515619697));
#46022=CARTESIAN_POINT('Ctrl Pts',(17.3763131037768,-0.388092342271454,
4.49926081212312));
#46023=CARTESIAN_POINT('Ctrl Pts',(17.4240289398397,-0.629837013651323,
3.94358758216158));
#46024=CARTESIAN_POINT('Ctrl Pts',(17.4717447759025,-0.293192664107019,
3.43971874351766));
#46025=CARTESIAN_POINT('Ctrl Pts',(17.5194606119653,0.312695020235776,3.45036480373676));
#46026=CARTESIAN_POINT('Ctrl Pts',(17.5671764480282,0.631430056064715,3.96574932190893));
#46027=CARTESIAN_POINT('Ctrl Pts',(17.614892284091,0.370313155609181,4.51258676478657));
#46028=CARTESIAN_POINT('Ctrl Pts',(17.6626081201539,-0.230868013642575,
4.58870789439952));
#46029=CARTESIAN_POINT('Ctrl Pts',(17.7103239562166,-0.620039533605355,
4.12420950615009));
#46030=CARTESIAN_POINT('Ctrl Pts',(17.7580397922796,-0.43981920932378,3.54564761719411));
#46031=CARTESIAN_POINT('Ctrl Pts',(17.8057556283423,0.144293862368219,3.38432451247882));
#46032=CARTESIAN_POINT('Ctrl Pts',(17.8534714644052,0.595899660001039,3.78838568133928));
#46033=CARTESIAN_POINT('Ctrl Pts',(17.901187300468,0.500281630760053,4.38677553513073));
#46034=CARTESIAN_POINT('Ctrl Pts',(17.9489031365309,-0.0547527178302441,
4.62998346370502));
#46035=CARTESIAN_POINT('Ctrl Pts',(17.9966189725937,-0.559506803158163,
4.29466788401745));
#46036=CARTESIAN_POINT('Ctrl Pts',(18.0443348086565,-0.550457182027191,
3.68875425238845));
#46037=CARTESIAN_POINT('Ctrl Pts',(18.0920506447194,-0.0359142607682062,
3.36866237992255));
#46038=CARTESIAN_POINT('Ctrl Pts',(18.1397664807822,0.511609278766163,3.62833755835171));
#46039=CARTESIAN_POINT('Ctrl Pts',(18.187482316845,0.589314145488933,4.22931607570827));
#46040=CARTESIAN_POINT('Ctrl Pts',(18.2351981529079,0.12584276464555,4.61971011226051));
#46041=CARTESIAN_POINT('Ctrl Pts',(18.2829139889707,-0.453191963311679,
4.44101481725822));
#46042=CARTESIAN_POINT('Ctrl Pts',(18.3306298250336,-0.616053538105107,
3.85732882968247));
#46043=CARTESIAN_POINT('Ctrl Pts',(18.3783456610964,-0.213183669654489,
3.40465997308746));
#46044=CARTESIAN_POINT('Ctrl Pts',(18.4260614971592,0.385456042892229,3.49870102369));
#46045=CARTESIAN_POINT('Ctrl Pts',(18.4737773332221,0.630125540247444,4.05309263771424));
#46046=CARTESIAN_POINT('Ctrl Pts',(18.5214931692849,0.296141058265729,4.55872846559028));
#46047=CARTESIAN_POINT('Ctrl Pts',(18.5692090053478,-0.309794314237323,
4.55127534637221));
#46048=CARTESIAN_POINT('Ctrl Pts',(18.6169248414106,-0.631240801177943,
4.0375775941191));
#46049=CARTESIAN_POINT('Ctrl Pts',(18.6646406774734,-0.373009147508776,
3.4893717589807));
#46050=CARTESIAN_POINT('Ctrl Pts',(18.7123565135363,0.227762545801372,3.41008369459593));
#46051=CARTESIAN_POINT('Ctrl Pts',(18.7600723495991,0.619376388724522,3.87252485049244));
#46052=CARTESIAN_POINT('Ctrl Pts',(18.8077881856619,0.442207363551868,4.45202839763978));
#46053=CARTESIAN_POINT('Ctrl Pts',(18.8555040217248,-0.141047487806633,
4.61642731188217));
#46054=CARTESIAN_POINT('Ctrl Pts',(18.9032198577876,-0.594776260815313,
4.21475154067248));
#46055=CARTESIAN_POINT('Ctrl Pts',(18.9509356938505,-0.502312841712761,
3.615866125281));
#46056=CARTESIAN_POINT('Ctrl Pts',(18.9986515299133,0.0514321890198641,
3.36973675771293));
#46057=CARTESIAN_POINT('Ctrl Pts',(19.0463673659762,0.557946249173174,3.70238782336559));
#46058=CARTESIAN_POINT('Ctrl Pts',(19.0940832020389,0.552089683635207,4.30834073020757));
#46059=CARTESIAN_POINT('Ctrl Pts',(19.1417990381018,0.0392406665648073,
4.63113960000379));
#46060=CARTESIAN_POINT('Ctrl Pts',(19.1895148741646,-0.509643658296843,
4.3743532639067));
#46061=CARTESIAN_POINT('Ctrl Pts',(19.2372307102275,-0.590514370077448,
3.77379256516987));
#46062=CARTESIAN_POINT('Ctrl Pts',(19.2849465462903,-0.129106649190522,
3.38096163491845));
#46063=CARTESIAN_POINT('Ctrl Pts',(19.3326623823532,0.450861693465423,3.55660315963506));
#46064=CARTESIAN_POINT('Ctrl Pts',(19.380378218416,0.616796807017627,4.1394228269368));
#46065=CARTESIAN_POINT('Ctrl Pts',(19.4280940544789,0.216317919394901,4.59420836405745));
#46066=CARTESIAN_POINT('Ctrl Pts',(19.4758098905416,-0.382809037079938,
4.50332322288615));
#46067=CARTESIAN_POINT('Ctrl Pts',(19.5235257266046,-0.630396573984801,
3.95022861114352));
#46068=CARTESIAN_POINT('Ctrl Pts',(19.5712415626673,-0.299081219248977,
3.44283985120298));
#46069=CARTESIAN_POINT('Ctrl Pts',(19.6189573987302,0.306884987370396,3.44709979193512));
#46070=CARTESIAN_POINT('Ctrl Pts',(19.666673234793,0.631034051704256,3.95909657101937));
#46071=CARTESIAN_POINT('Ctrl Pts',(19.7143890708559,0.375694716468479,4.50865546647685));
#46072=CARTESIAN_POINT('Ctrl Pts',(19.7621049069187,-0.224650630777236,
4.59110846933868));
#46073=CARTESIAN_POINT('Ctrl Pts',(19.8098207429815,-0.618696275574682,
4.13073699938377));
#46074=CARTESIAN_POINT('Ctrl Pts',(19.8575365790444,-0.44458280157215,3.55030861879767));
#46075=CARTESIAN_POINT('Ctrl Pts',(19.9052524151072,0.13779637220375,3.3828370770856));
#46076=CARTESIAN_POINT('Ctrl Pts',(19.9529682511701,0.593637901716091,3.7821189081517));
#46077=CARTESIAN_POINT('Ctrl Pts',(20.0006840872329,0.504327165075627,4.38147832337345));
#46078=CARTESIAN_POINT('Ctrl Pts',(20.0483999232957,-0.0481046828163007,
4.63053160650705));
#46079=CARTESIAN_POINT('Ctrl Pts',(20.0961157593586,-0.556380679578279,
4.30053671048834));
#46080=CARTESIAN_POINT('Ctrl Pts',(20.1438315954214,-0.553687069357429,
3.69459455385474));
#46081=CARTESIAN_POINT('Ctrl Pts',(20.1915474314843,-0.0426033430871586,
3.36903495876776));
#46082=CARTESIAN_POINT('Ctrl Pts',(20.2392632675471,0.507734449822709,3.62304374442814));
#46083=CARTESIAN_POINT('Ctrl Pts',(20.2869791036099,0.591564791291533,4.22294595084339));
#46084=CARTESIAN_POINT('Ctrl Pts',(20.3346949396728,0.132620199007312,4.618629012875));
#46085=CARTESIAN_POINT('Ctrl Pts',(20.3824107757356,-0.449008129734859,
4.44521533979349));
#46086=CARTESIAN_POINT('Ctrl Pts',(20.4221739724547,-0.588594799935545,
3.96175478680276));
#46087=CARTESIAN_POINT('Ctrl Pts',(20.4539845298298,-0.419131055782338,
3.63395025773895));
#46088=CARTESIAN_POINT('Ctrl Pts',(20.4778424478613,-0.194099195253748,
3.47709810398663));
#46089=CARTESIAN_POINT('Ctrl Pts',(20.5017003658927,0.0810471032980313,
3.44846366347126));
#46090=CARTESIAN_POINT('Ctrl Pts',(20.5255582839241,0.334940048200093,3.55449674151986));
#46091=CARTESIAN_POINT('Ctrl Pts',(20.5494162019556,0.507694843328107,3.76957374638464));
#46092=CARTESIAN_POINT('Ctrl Pts',(20.5732741199869,0.555899439471162,4.04093981905292));
#46093=CARTESIAN_POINT('Ctrl Pts',(20.5971320380184,0.468386015874758,4.30232489481291));
#46094=CARTESIAN_POINT('Ctrl Pts',(20.6209899560498,0.266225827016684,4.48976745893774));
#46095=CARTESIAN_POINT('Ctrl Pts',(20.6448478740812,-0.000973650874560818,
4.55745692740964));
#46096=CARTESIAN_POINT('Ctrl Pts',(20.6687057921126,-0.267966914960919,
4.48882854939535));
#46097=CARTESIAN_POINT('Ctrl Pts',(20.6925637101441,-0.469418090387657,
4.30067062862012));
#46098=CARTESIAN_POINT('Ctrl Pts',(20.7164216281755,-0.556092695039732,
4.03898930289119));
#46099=CARTESIAN_POINT('Ctrl Pts',(20.7402795462069,-0.506782753954552,
3.7677746905255));
#46100=CARTESIAN_POINT('Ctrl Pts',(20.7641374642383,-0.333553132261349,
3.55334514249538));
#46101=CARTESIAN_POINT('Ctrl Pts',(20.7879953822697,-0.0787593560922578,
3.44813505886707));
#46102=CARTESIAN_POINT('Ctrl Pts',(20.8118533003012,0.19529252477751,3.47787088781106));
#46103=CARTESIAN_POINT('Ctrl Pts',(20.8357112183325,0.421590436108717,3.63528155911584));
#46104=CARTESIAN_POINT('Ctrl Pts',(20.859569136364,0.544797804677434,3.8818757964511));
#46105=CARTESIAN_POINT('Ctrl Pts',(20.8834270543954,0.534787374467886,4.15735463375504));
#46106=CARTESIAN_POINT('Ctrl Pts',(20.9072849724269,0.394006808563119,4.39435596913946));
#46107=CARTESIAN_POINT('Ctrl Pts',(20.9311428904582,0.156880874733563,4.53492653211281));
#46108=CARTESIAN_POINT('Ctrl Pts',(20.9550008084897,-0.118606721834374,
4.54469298471526));
#46109=CARTESIAN_POINT('Ctrl Pts',(20.9788587265211,-0.365091735913813,
4.42126716656144));
#46110=CARTESIAN_POINT('Ctrl Pts',(21.0027166445525,-0.522301880015273,
4.19483005048941));
#46111=CARTESIAN_POINT('Ctrl Pts',(21.0265745625839,-0.55179498493052,3.92075168033001));
#46112=CARTESIAN_POINT('Ctrl Pts',(21.0504324806153,-0.446359186657349,
3.66605168284066));
#46113=CARTESIAN_POINT('Ctrl Pts',(21.0742903986468,-0.231776408019839,
3.49301114555638));
#46114=CARTESIAN_POINT('Ctrl Pts',(21.0981483166782,0.0394820154987394,
3.44394319323497));
#46115=CARTESIAN_POINT('Ctrl Pts',(21.1220062347096,0.301086010940692,3.5308462768762));
#46116=CARTESIAN_POINT('Ctrl Pts',(21.145864152741,0.489066275193333,3.73247022529863));
#46117=CARTESIAN_POINT('Ctrl Pts',(21.1697220707724,0.557456513314207,3.9995124910074));
#46118=CARTESIAN_POINT('Ctrl Pts',(21.1935799888039,0.489533449092281,4.26667396594056));
#46119=CARTESIAN_POINT('Ctrl Pts',(21.2174379068352,0.30190612195814,4.46862639215028));
#46120=CARTESIAN_POINT('Ctrl Pts',(21.2412958248667,0.0404545242400231,
4.55598690035157));
#46121=CARTESIAN_POINT('Ctrl Pts',(21.2651537428981,-0.230889306609896,
4.50739346663836));
#46122=CARTESIAN_POINT('Ctrl Pts',(21.2890116609295,-0.445774412697373,
4.33472850921124));
#46123=CARTESIAN_POINT('Ctrl Pts',(21.312869578961,-0.551655532228011,4.08021331346062));
#46124=CARTESIAN_POINT('Ctrl Pts',(21.3367274969923,-0.522641847334507,
3.80608377760199));
#46125=CARTESIAN_POINT('Ctrl Pts',(21.3605854150238,-0.365827994289322,
3.57937204029158));
#46126=CARTESIAN_POINT('Ctrl Pts',(21.3844433330552,-0.119559231686077,
3.45551529680541));
#46127=CARTESIAN_POINT('Ctrl Pts',(21.4083012510867,0.155945019792583,3.46479989471587));
#46128=CARTESIAN_POINT('Ctrl Pts',(21.432159169118,0.393316466074861,3.60495549692644));
#46129=CARTESIAN_POINT('Ctrl Pts',(21.4560170871495,0.534511322676435,3.84171024093472));
#46130=CARTESIAN_POINT('Ctrl Pts',(21.4798750051809,0.545003601087511,4.11717114276091));
#46131=CARTESIAN_POINT('Ctrl Pts',(21.5037329232123,0.422227653432673,4.36398050850424));
#46132=CARTESIAN_POINT('Ctrl Pts',(21.5275908412437,0.196205543263173,4.52178672528827));
#46133=CARTESIAN_POINT('Ctrl Pts',(21.5514487592751,-0.0777941667658609,
4.5520018745543));
#46134=CARTESIAN_POINT('Ctrl Pts',(21.5753066773066,-0.332771083950078,
4.44723752926263));
#46135=CARTESIAN_POINT('Ctrl Pts',(21.5991645953379,-0.506376406606172,
4.23311142556056));
#46136=CARTESIAN_POINT('Ctrl Pts',(21.6230225133694,-0.556158904430687,
3.96198322848119));
#46137=CARTESIAN_POINT('Ctrl Pts',(21.6468804314008,-0.469945400657515,
3.70015116759423));
#46138=CARTESIAN_POINT('Ctrl Pts',(21.6707383494323,-0.268817445367881,
3.51164031394868));
#46139=CARTESIAN_POINT('Ctrl Pts',(21.6945962674636,-0.00195630224560004,
3.44254670619344));
#46140=CARTESIAN_POINT('Ctrl Pts',(21.7184541854951,0.26538321006433,3.50976561349676));
#46141=CARTESIAN_POINT('Ctrl Pts',(21.7423121035264,0.467829298620023,3.6968601820167));
#46142=CARTESIAN_POINT('Ctrl Pts',(21.766170021558,0.555878380248887,3.95808069339639));
#46143=CARTESIAN_POINT('Ctrl Pts',(21.7900279395893,0.508000056083844,4.22955161709966));
#46144=CARTESIAN_POINT('Ctrl Pts',(21.8138858576208,0.335901880562604,4.44489091756156));
#46145=CARTESIAN_POINT('Ctrl Pts',(21.8377437756521,0.0816665454602928,
4.55144227009437));
#46146=CARTESIAN_POINT('Ctrl Pts',(21.8616016936836,-0.192538484559094,
4.52315096660328));
#46147=CARTESIAN_POINT('Ctrl Pts',(21.885459611715,-0.419662610460766,4.36693500143146));
#46148=CARTESIAN_POINT('Ctrl Pts',(21.9093175297464,-0.544167796724789,
4.12099343330092));
#46149=CARTESIAN_POINT('Ctrl Pts',(21.9331754477779,-0.535609133856441,
3.84546567493331));
#46150=CARTESIAN_POINT('Ctrl Pts',(21.9570333658092,-0.396079448060293,
3.60772576847503));
#46151=CARTESIAN_POINT('Ctrl Pts',(21.9808912838407,-0.159697548225882,
3.46590759696012));
#46152=CARTESIAN_POINT('Ctrl Pts',(22.0047492018721,0.115734752223676,3.45468956637345));
#46153=CARTESIAN_POINT('Ctrl Pts',(22.0286071199035,0.362866753203085,3.5768147907664));
#46154=CARTESIAN_POINT('Ctrl Pts',(22.0524650379349,0.521267948732644,3.80242032615069));
#46155=CARTESIAN_POINT('Ctrl Pts',(22.0763229559664,0.552204931742854,4.07633947375325));
#46156=CARTESIAN_POINT('Ctrl Pts',(22.1001808739978,0.448112767182329,4.33159154057792));
#46157=CARTESIAN_POINT('Ctrl Pts',(22.1240387920292,0.23444482469764,4.5057604433585));
#46158=CARTESIAN_POINT('Ctrl Pts',(22.1478967100606,-0.0365512635718279,
4.55625714110116));
#46159=CARTESIAN_POINT('Ctrl Pts',(22.171754628092,-0.298609572266455,4.47073381570218));
#46160=CARTESIAN_POINT('Ctrl Pts',(22.1956125461234,-0.487649706571227,
4.2701032498363));
#46161=CARTESIAN_POINT('Ctrl Pts',(22.2194704641549,-0.557446204325542,
4.00342508191314));
#46162=CARTESIAN_POINT('Ctrl Pts',(22.2433283821863,-0.490931920559466,
3.73590938817905));
#46163=CARTESIAN_POINT('Ctrl Pts',(22.2671863002177,-0.304371409562025,
3.53297104269219));
#46164=CARTESIAN_POINT('Ctrl Pts',(22.2910442182491,-0.0433837978980346,
3.44423399893113));
#46165=CARTESIAN_POINT('Ctrl Pts',(22.3149021362806,0.228212333880327,3.49139688109763));
#46166=CARTESIAN_POINT('Ctrl Pts',(22.3387600543119,0.444004334066149,3.66292708008725));
#46167=CARTESIAN_POINT('Ctrl Pts',(22.3626179723434,0.551225179343846,3.91688078933633));
#46168=CARTESIAN_POINT('Ctrl Pts',(22.3864758903748,0.523656454698273,4.19115941035881));
#46169=CARTESIAN_POINT('Ctrl Pts',(22.4103338084062,0.368039459933637,4.41869434725418));
#46170=CARTESIAN_POINT('Ctrl Pts',(22.4341917264376,0.122426797365049,4.54384711353805));
#46171=CARTESIAN_POINT('Ctrl Pts',(22.458049644469,-0.153122562087755,4.53601444212637));
#46172=CARTESIAN_POINT('Ctrl Pts',(22.4819075625005,-0.391229265084309,
4.39711164706476));
#46173=CARTESIAN_POINT('Ctrl Pts',(22.5057654805319,-0.533669791868601,
4.16110422172694));
#46174=CARTESIAN_POINT('Ctrl Pts',(22.5296233985633,-0.545613449745194,
3.88570245498666));
#46175=CARTESIAN_POINT('Ctrl Pts',(22.5534813165947,-0.424139885198736,
3.63824949626794));
#46176=CARTESIAN_POINT('Ctrl Pts',(22.5773392346261,-0.198952323217499,
3.47925449370713));
#46177=CARTESIAN_POINT('Ctrl Pts',(22.6011971526576,0.0748840438856019,
3.44759575567767));
#46178=CARTESIAN_POINT('Ctrl Pts',(22.625055070689,0.330410085854462,3.55101527375816));
#46179=CARTESIAN_POINT('Ctrl Pts',(22.6489129887204,0.505140231362423,3.7642230866287));
#46180=CARTESIAN_POINT('Ctrl Pts',(22.6727709067518,0.556352908954721,4.03508610068096));
#46181=CARTESIAN_POINT('Ctrl Pts',(22.6966288247833,0.471516332128332,4.29736710820476));
#46182=CARTESIAN_POINT('Ctrl Pts',(22.7204867428146,0.27139215166714,4.48693847894857));
#46183=CARTESIAN_POINT('Ctrl Pts',(22.7443446608461,0.00488440565515616,
4.55743119390072));
#46184=CARTESIAN_POINT('Ctrl Pts',(22.7682025788775,-0.262778018495442,
4.49163382183027));
#46185=CARTESIAN_POINT('Ctrl Pts',(22.7920604969089,-0.466262514422727,
4.30558517247789));
#46186=CARTESIAN_POINT('Ctrl Pts',(22.8079657755965,-0.525793678117208,
4.1317859159904));
#46187=CARTESIAN_POINT('Ctrl Pts',(22.8159184149403,-0.532958495437544,
4.04301651477895));
#46188=CARTESIAN_POINT('Ctrl Pts',(3.98408158505965,-0.251304309929533,
3.59658905474035));
#46189=CARTESIAN_POINT('Ctrl Pts',(3.99203422440346,-0.184112308377066,
3.5547318870523));
#46190=CARTESIAN_POINT('Ctrl Pts',(4.00793950309107,-0.0284797076443847,
3.50528009766423));
#46191=CARTESIAN_POINT('Ctrl Pts',(4.03179742112249,0.212077873916637,3.55216010213054));
#46192=CARTESIAN_POINT('Ctrl Pts',(4.05565533915392,0.400711255741927,3.70851080938071));
#46193=CARTESIAN_POINT('Ctrl Pts',(4.07951325718533,0.49139298320592,3.93615790384083));
#46194=CARTESIAN_POINT('Ctrl Pts',(4.10337117521676,0.461898357851897,4.17940600742409));
#46195=CARTESIAN_POINT('Ctrl Pts',(4.12722909324816,0.319466186301668,4.37878980142624));
#46196=CARTESIAN_POINT('Ctrl Pts',(4.15108701127959,0.0989109688445654,
4.48554634140719));
#46197=CARTESIAN_POINT('Ctrl Pts',(4.174944929311,-0.145828100556353,4.47357507321567));
#46198=CARTESIAN_POINT('Ctrl Pts',(4.19880284734243,-0.354909590370033,
4.34580100620849));
#46199=CARTESIAN_POINT('Ctrl Pts',(4.22266076537384,-0.477205295803391,
4.13346959398438));
#46200=CARTESIAN_POINT('Ctrl Pts',(4.24651868340526,-0.482811689970624,
3.88850100783657));
#46201=CARTESIAN_POINT('Ctrl Pts',(4.27037660143669,-0.370357271909554,
3.67079708031066));
#46202=CARTESIAN_POINT('Ctrl Pts',(4.2942345194681,-0.167340519784032,3.53359217153378));
#46203=CARTESIAN_POINT('Ctrl Pts',(4.31809243749953,0.0765956044913427,
3.51043671457025));
#46204=CARTESIAN_POINT('Ctrl Pts',(4.34195035553093,0.301801986965541,3.60699279882218));
#46205=CARTESIAN_POINT('Ctrl Pts',(4.36580827356237,0.453209578636439,3.79964985833574));
#46206=CARTESIAN_POINT('Ctrl Pts',(4.38966619159377,0.493795074712635,4.04129798000377));
#46207=CARTESIAN_POINT('Ctrl Pts',(4.4135241096252,0.413634228782107,4.27284762322724));
#46208=CARTESIAN_POINT('Ctrl Pts',(4.43738202765661,0.23232854437776,4.43767858897425));
#46209=CARTESIAN_POINT('Ctrl Pts',(4.46123994568804,-0.00578779637616802,
4.49548521832112));
#46210=CARTESIAN_POINT('Ctrl Pts',(4.48509786371945,-0.242488863923451,
4.43213221465579));
#46211=CARTESIAN_POINT('Ctrl Pts',(4.50895578175088,-0.419894798625899,
4.26311111366653));
#46212=CARTESIAN_POINT('Ctrl Pts',(4.53281369978229,-0.494625017545811,
4.02975217827461));
#46213=CARTESIAN_POINT('Ctrl Pts',(4.55667161781372,-0.448405946262215,
3.78911802491887));
#46214=CARTESIAN_POINT('Ctrl Pts',(4.58052953584513,-0.292539406836986,
3.60005025874973));
#46215=CARTESIAN_POINT('Ctrl Pts',(4.60438745387655,-0.0651390137990107,
3.50878109874461));
#46216=CARTESIAN_POINT('Ctrl Pts',(4.62824537190797,0.178189642449287,3.53762834062211));
#46217=CARTESIAN_POINT('Ctrl Pts',(4.65210328993938,0.377946077338085,3.67953804797316));
#46218=CARTESIAN_POINT('Ctrl Pts',(4.67596120797081,0.485284401269169,3.89980943180067));
#46219=CARTESIAN_POINT('Ctrl Pts',(4.69981912600222,0.473957470210434,4.14458013869048));
#46220=CARTESIAN_POINT('Ctrl Pts',(4.72367704403364,0.34673502734182,4.35399706338589));
#46221=CARTESIAN_POINT('Ctrl Pts',(4.74753496206506,0.134726425416229,4.47685206339739));
#46222=CARTESIAN_POINT('Ctrl Pts',(4.77139288009648,-0.110226457398098,
4.48310374471865));
#46223=CARTESIAN_POINT('Ctrl Pts',(4.7952507981279,-0.328225968870003,4.37122340097448));
#46224=CARTESIAN_POINT('Ctrl Pts',(4.81910871615932,-0.465965290257402,
4.16856882376961));
#46225=CARTESIAN_POINT('Ctrl Pts',(4.84296663419074,-0.489763405537152,
3.92469457743051));
#46226=CARTESIAN_POINT('Ctrl Pts',(4.86682455222216,-0.393801027275785,
3.69923455818817));
#46227=CARTESIAN_POINT('Ctrl Pts',(4.89068247025357,-0.201543570920867,
3.54731988215497));
#46228=CARTESIAN_POINT('Ctrl Pts',(4.914540388285,0.039996778460842,3.50609782569371));
#46229=CARTESIAN_POINT('Ctrl Pts',(4.93839830631641,0.271756826018508,3.58564830447545));
#46230=CARTESIAN_POINT('Ctrl Pts',(4.96225622434784,0.437064927107334,3.76651905952651));
#46231=CARTESIAN_POINT('Ctrl Pts',(4.98611414237925,0.495498748108838,4.00448226441646));
#46232=CARTESIAN_POINT('Ctrl Pts',(5.00997206041068,0.432769628082826,4.24134943356216));
#46233=CARTESIAN_POINT('Ctrl Pts',(5.03382997844209,0.26421654558258,4.41920009197534));
#46234=CARTESIAN_POINT('Ctrl Pts',(5.05768789647352,0.031055320573195,4.49454490911931));
#46235=CARTESIAN_POINT('Ctrl Pts',(5.08154581450493,-0.209699776246285,
4.44896002485074));
#46236=CARTESIAN_POINT('Ctrl Pts',(5.10540373253635,-0.399177565666329,
4.29359218508065));
#46237=CARTESIAN_POINT('Ctrl Pts',(5.12926165056777,-0.491045566902382,
4.06643305876778));
#46238=CARTESIAN_POINT('Ctrl Pts',(5.15311956859918,-0.462839551218119,
3.823029239986));
#46239=CARTESIAN_POINT('Ctrl Pts',(5.17697748663061,-0.321456657764784,
3.62289959261435));
#46240=CARTESIAN_POINT('Ctrl Pts',(5.20083540466202,-0.101468855184408,
3.51498126685736));
#46241=CARTESIAN_POINT('Ctrl Pts',(5.22469332269345,0.143330846444675,3.52566323299877));
#46242=CARTESIAN_POINT('Ctrl Pts',(5.24855124072486,0.353082251864168,3.6523334593461));
#46243=CARTESIAN_POINT('Ctrl Pts',(5.27240915875629,0.476495428935435,3.86401762512973));
#46244=CARTESIAN_POINT('Ctrl Pts',(5.2962670767877,0.483392494157105,4.10895318565465));
#46245=CARTESIAN_POINT('Ctrl Pts',(5.32012499481913,0.372086927210194,4.32724672446184));
#46246=CARTESIAN_POINT('Ctrl Pts',(5.34398291285054,0.169795971115995,4.46551952511629));
#46247=CARTESIAN_POINT('Ctrl Pts',(5.36784083088196,-0.0740147250654609,
4.48996012138256));
#46248=CARTESIAN_POINT('Ctrl Pts',(5.39169874891337,-0.299726804847767,
4.39459212172504));
#46249=CARTESIAN_POINT('Ctrl Pts',(5.4155566669448,-0.452147516450583,4.20273559983216));
#46250=CARTESIAN_POINT('Ctrl Pts',(5.43941458497621,-0.494005844030112,
3.96130470137348));
#46251=CARTESIAN_POINT('Ctrl Pts',(5.46327250300764,-0.415066286295368,
3.72933585746768));
#46252=CARTESIAN_POINT('Ctrl Pts',(5.48713042103905,-0.234631715382576,
3.56355176915442));
#46253=CARTESIAN_POINT('Ctrl Pts',(5.51098833907048,0.00317670118048804,
3.50449116189365));
#46254=CARTESIAN_POINT('Ctrl Pts',(5.53484625710188,0.240208327774024,3.56659596294035));
#46255=CARTESIAN_POINT('Ctrl Pts',(5.55870417513332,0.418502475082003,3.73467985673571));
#46256=CARTESIAN_POINT('Ctrl Pts',(5.58256209316472,0.494461367456411,3.96764175273735));
#46257=CARTESIAN_POINT('Ctrl Pts',(5.60642001119615,0.449510986625754,4.20851612161082));
#46258=CARTESIAN_POINT('Ctrl Pts',(5.63027792922757,0.294642925140636,4.39840261889448));
#46259=CARTESIAN_POINT('Ctrl Pts',(5.65413584725899,0.0677266425295592,
4.49086882357174));
#46260=CARTESIAN_POINT('Ctrl Pts',(5.6779937652904,-0.17575064898472,4.46330422991997));
#46261=CARTESIAN_POINT('Ctrl Pts',(5.70185168332183,-0.376252119531055,
4.32244913183746));
#46262=CARTESIAN_POINT('Ctrl Pts',(5.72570960135325,-0.48474969783608,4.10274643779879));
#46263=CARTESIAN_POINT('Ctrl Pts',(5.74956751938466,-0.474712770918799,
3.85791944074229));
#46264=CARTESIAN_POINT('Ctrl Pts',(5.77342543741608,-0.348595640189148,
3.64783501103505));
#46265=CARTESIAN_POINT('Ctrl Pts',(5.7972833554475,-0.13723738064616,3.52386451312966));
#46266=CARTESIAN_POINT('Ctrl Pts',(5.82114127347893,0.1076791581852,3.5163221129105));
#46267=CARTESIAN_POINT('Ctrl Pts',(5.84499919151033,0.326265206982528,3.62705212841851));
#46268=CARTESIAN_POINT('Ctrl Pts',(5.86885710954176,0.465070530553655,3.82897806268729));
#46269=CARTESIAN_POINT('Ctrl Pts',(5.89271502757317,0.490153431381492,4.07272350923538));
#46270=CARTESIAN_POINT('Ctrl Pts',(5.9165729456046,0.395380485146506,4.29868609559117));
#46271=CARTESIAN_POINT('Ctrl Pts',(5.94043086363601,0.203926205561759,4.45161176009809));
#46272=CARTESIAN_POINT('Ctrl Pts',(5.96428878166744,-0.0373935204432717,
4.49410611450448));
#46273=CARTESIAN_POINT('Ctrl Pts',(5.98814669969885,-0.26956963613406,4.41577793841189));
#46274=CARTESIAN_POINT('Ctrl Pts',(6.01200461773027,-0.435828398698505,
4.23578096933615));
#46275=CARTESIAN_POINT('Ctrl Pts',(6.0358625357617,-0.495515688199628,3.99812868033461));
#46276=CARTESIAN_POINT('Ctrl Pts',(6.0597204537931,-0.434035059498629,3.76093483037113));
#46277=CARTESIAN_POINT('Ctrl Pts',(6.08357837182454,-0.266422612259865,
3.58219732064663));
#46278=CARTESIAN_POINT('Ctrl Pts',(6.10743628985594,-0.0336596025775484,
3.50562697870369));
#46279=CARTESIAN_POINT('Ctrl Pts',(6.13129420788738,0.207328476491996,3.54993858195554));
#46280=CARTESIAN_POINT('Ctrl Pts',(6.15515212591877,0.397629707835022,3.70431327123879));
#46281=CARTESIAN_POINT('Ctrl Pts',(6.17901004395022,0.490679606253205,3.93097100878581));
#46282=CARTESIAN_POINT('Ctrl Pts',(6.20286796198161,0.463782811036945,4.17454675550933));
#46283=CARTESIAN_POINT('Ctrl Pts',(6.22672588001306,0.323407044622774,4.3753682944706));
#46284=CARTESIAN_POINT('Ctrl Pts',(6.25058379804445,0.104084330837213,4.48453946106473));
#46285=CARTESIAN_POINT('Ctrl Pts',(6.27444171607588,-0.140944443623038,
4.4749681472433));
#46286=CARTESIAN_POINT('Ctrl Pts',(6.29829963410731,-0.351028389709017,
4.349743491311));
#46287=CARTESIAN_POINT('Ctrl Pts',(6.32215755213872,-0.476177279109797,
4.13807688197341));
#46288=CARTESIAN_POINT('Ctrl Pts',(6.34601547017014,-0.483231738207782,
3.89435343878414));
#46289=CARTESIAN_POINT('Ctrl Pts',(6.37782602754537,-0.338784024988664,
3.5998542259592));
#46290=CARTESIAN_POINT('Ctrl Pts',(6.41758922426439,0.0803770223010952,
3.44371490521648));
#46291=CARTESIAN_POINT('Ctrl Pts',(6.46530506032724,0.512014121509362,3.7673575683149));
#46292=CARTESIAN_POINT('Ctrl Pts',(6.51302089639006,0.472271980317209,4.30452828893312));
#46293=CARTESIAN_POINT('Ctrl Pts',(6.56073673245292,-0.000548856210248058,
4.56210751581942));
#46294=CARTESIAN_POINT('Ctrl Pts',(6.60845256851575,-0.473190198344468,
4.30346185287483));
#46295=CARTESIAN_POINT('Ctrl Pts',(6.65616840457859,-0.511122033036262,
3.76615996983968));
#46296=CARTESIAN_POINT('Ctrl Pts',(6.70388424064142,-0.0797735308749388,
3.44358772816382));
#46297=CARTESIAN_POINT('Ctrl Pts',(6.75160007670426,0.424880365184703,3.63198234005898));
#46298=CARTESIAN_POINT('Ctrl Pts',(6.7993159127671,0.539334593204737,4.15833063512042));
#46299=CARTESIAN_POINT('Ctrl Pts',(6.84703174882994,0.158523065679302,4.53928284691909));
#46300=CARTESIAN_POINT('Ctrl Pts',(6.89474758489278,-0.367869781963911,
4.42500259414721));
#46301=CARTESIAN_POINT('Ctrl Pts',(6.94246342095561,-0.556438361909488,
3.92043630538129));
#46302=CARTESIAN_POINT('Ctrl Pts',(6.99017925701846,-0.234023037562683,
3.48893437735136));
#46303=CARTESIAN_POINT('Ctrl Pts',(7.03789509308128,0.303300305128555,3.52675198254107));
#46304=CARTESIAN_POINT('Ctrl Pts',(7.08561092914413,0.562097748282813,3.99916046672433));
#46305=CARTESIAN_POINT('Ctrl Pts',(7.13332676520696,0.304712478085684,4.47233993757656));
#46306=CARTESIAN_POINT('Ctrl Pts',(7.18104260126981,-0.232495107101315,
4.51176235979777));
#46307=CARTESIAN_POINT('Ctrl Pts',(7.22875843733264,-0.556198774489988,
4.08122554105153));
#46308=CARTESIAN_POINT('Ctrl Pts',(7.27647427339549,-0.369136593294786,
3.57609805363465));
#46309=CARTESIAN_POINT('Ctrl Pts',(7.32419010945832,0.156909424853758,3.46024624852207));
#46310=CARTESIAN_POINT('Ctrl Pts',(7.37190594552116,0.538863091386428,3.84005861730642));
#46311=CARTESIAN_POINT('Ctrl Pts',(7.41962178158399,0.425970496197337,4.36674761950234));
#46312=CARTESIAN_POINT('Ctrl Pts',(7.46733761764684,-0.0780973635293338,
4.55664663921719));
#46313=CARTESIAN_POINT('Ctrl Pts',(7.51505345370967,-0.510447210801067,
4.2353684852172));
#46314=CARTESIAN_POINT('Ctrl Pts',(7.56276928977251,-0.474045531130633,
3.69794782953315));
#46315=CARTESIAN_POINT('Ctrl Pts',(7.61048512583535,-0.00232054557778912,
3.43790632971152));
#46316=CARTESIAN_POINT('Ctrl Pts',(7.65820096189818,0.471535432411473,3.69404409621074));
#46317=CARTESIAN_POINT('Ctrl Pts',(7.70591679796103,0.512373167457076,4.23114587691112));
#46318=CARTESIAN_POINT('Ctrl Pts',(7.75363263402387,0.0826907388754792,
4.55598284219971));
#46319=CARTESIAN_POINT('Ctrl Pts',(7.80134847008669,-0.422927867535356,
4.3702522086048));
#46320=CARTESIAN_POINT('Ctrl Pts',(7.84906430614955,-0.540165305628305,
3.84451327478339));
#46321=CARTESIAN_POINT('Ctrl Pts',(7.89678014221237,-0.161360632039799,
3.46156019320034));
#46322=CARTESIAN_POINT('Ctrl Pts',(7.94449597827521,0.365623992797271,3.57306467116217));
#46323=CARTESIAN_POINT('Ctrl Pts',(7.99221181433806,0.556850479203549,4.07663043084052));
#46324=CARTESIAN_POINT('Ctrl Pts',(8.03992765040089,0.236712602309549,4.50982528676712));
#46325=CARTESIAN_POINT('Ctrl Pts',(8.08764348646373,-0.300802099575971,
4.47483973718518));
#46326=CARTESIAN_POINT('Ctrl Pts',(8.13535932252656,-0.562085604986122,
4.00380155059756));
#46327=CARTESIAN_POINT('Ctrl Pts',(8.18307515858941,-0.307197250538534,
3.52927234160183));
#46328=CARTESIAN_POINT('Ctrl Pts',(8.23079099465223,0.229795065915734,3.48701958438918));
#46329=CARTESIAN_POINT('Ctrl Pts',(8.27850683071509,0.555763037488074,3.91584463605021));
#46330=CARTESIAN_POINT('Ctrl Pts',(8.32622266677791,0.371365260221553,4.42195085332305));
#46331=CARTESIAN_POINT('Ctrl Pts',(8.37393850284076,-0.154062949695418,
4.54057310944092));
#46332=CARTESIAN_POINT('Ctrl Pts',(8.4216543389036,-0.538012782343907,4.16277876137275));
#46333=CARTESIAN_POINT('Ctrl Pts',(8.46937017496643,-0.427897198575242,
3.6355021720628));
#46334=CARTESIAN_POINT('Ctrl Pts',(8.51708601102927,0.0751629666897603,
3.44294954666756));
#46335=CARTESIAN_POINT('Ctrl Pts',(8.56480184709211,0.50919982311266,3.76194492389047));
#46336=CARTESIAN_POINT('Ctrl Pts',(8.61251768315494,0.475630646924824,4.29954994045293));
#46337=CARTESIAN_POINT('Ctrl Pts',(8.66023351921779,0.00528252914771292,
4.56207363752918));
#46338=CARTESIAN_POINT('Ctrl Pts',(8.70794935528062,-0.469916616427902,
4.30843646464781));
#46339=CARTESIAN_POINT('Ctrl Pts',(8.75566519134346,-0.513584102541225,
3.7715573403753));
#46340=CARTESIAN_POINT('Ctrl Pts',(8.8033810274063,-0.0856194047837525,
3.44446062547832));
#46341=CARTESIAN_POINT('Ctrl Pts',(8.85109686346913,0.420970909810523,3.6275242662766));
#46342=CARTESIAN_POINT('Ctrl Pts',(8.89881269953199,0.540977160455745,4.15263810462895));
#46343=CARTESIAN_POINT('Ctrl Pts',(8.9465285355948,0.1641957606509,4.5375820228614));
#46344=CARTESIAN_POINT('Ctrl Pts',(8.99424437165766,-0.363369132636193,
4.42885609773758));
#46345=CARTESIAN_POINT('Ctrl Pts',(9.04196020772048,-0.557246560270691,
3.92630501926208));
#46346=CARTESIAN_POINT('Ctrl Pts',(9.08967604378333,-0.239395897268157,
3.49142917554125));
#46347=CARTESIAN_POINT('Ctrl Pts',(9.13739187984617,0.298295701775085,3.52358174528888));
#46348=CARTESIAN_POINT('Ctrl Pts',(9.18510771590899,0.562057768008922,3.99323652897485));
#46349=CARTESIAN_POINT('Ctrl Pts',(9.23282355197185,0.309673537509763,4.46910231217259));
#46350=CARTESIAN_POINT('Ctrl Pts',(9.28053938803466,-0.227088667424462,
4.51418422403538));
#46351=CARTESIAN_POINT('Ctrl Pts',(9.32825522409753,-0.555311854854516,
4.08708285122523));
#46352=CARTESIAN_POINT('Ctrl Pts',(9.37597106016035,-0.373583621400482,
3.58001195619306));
#46353=CARTESIAN_POINT('Ctrl Pts',(9.4236868962232,0.151212199908504,3.45862254413551));
#46354=CARTESIAN_POINT('Ctrl Pts',(9.47140273228603,0.537147531342748,3.83438837996121));
#46355=CARTESIAN_POINT('Ctrl Pts',(9.51911856834887,0.429812019667804,4.36223791473086));
#46356=CARTESIAN_POINT('Ctrl Pts',(9.5668344044117,-0.0722264831760907,
4.5574387986564));
#46357=CARTESIAN_POINT('Ctrl Pts',(9.61455024047456,-0.507938295172089,
4.24073505647735));
#46358=CARTESIAN_POINT('Ctrl Pts',(9.66226607653738,-0.477202555076283,
3.70296060775017));
#46359=CARTESIAN_POINT('Ctrl Pts',(9.70998191260023,-0.00824436594879979,
3.43796200346455));
#46360=CARTESIAN_POINT('Ctrl Pts',(9.75769774866306,0.46828475128534,3.68909153946361));
#46361=CARTESIAN_POINT('Ctrl Pts',(9.80541358472589,0.514780775927077,4.22573309871483));
#46362=CARTESIAN_POINT('Ctrl Pts',(9.85312942078874,0.0885456931146035,
4.55508048006603));
#46363=CARTESIAN_POINT('Ctrl Pts',(9.90084525685159,-0.419002262135622,
4.37468891556157));
#46364=CARTESIAN_POINT('Ctrl Pts',(9.9485610929144,-0.541773992888202,3.8502147545669));
#46365=CARTESIAN_POINT('Ctrl Pts',(9.99627692897727,-0.167026329707142,
3.46329068919569));
#46366=CARTESIAN_POINT('Ctrl Pts',(10.0439927650401,0.361104182074418,3.56923504227033));
#46367=CARTESIAN_POINT('Ctrl Pts',(10.0917086011029,0.557627167155001,4.07075748419897));
#46368=CARTESIAN_POINT('Ctrl Pts',(10.1394244371657,0.242072544440304,4.50730223964386));
#46369=CARTESIAN_POINT('Ctrl Pts',(10.1871402732286,-0.295781020598791,
4.47798354257549));
#46370=CARTESIAN_POINT('Ctrl Pts',(10.2348561092914,-0.56201432324602,4.00972520363789));
#46371=CARTESIAN_POINT('Ctrl Pts',(10.2825719453543,-0.312141225154507,
3.53253606055812));
#46372=CARTESIAN_POINT('Ctrl Pts',(10.3302877814171,0.224375962906492,3.48462624592509));
#46373=CARTESIAN_POINT('Ctrl Pts',(10.37800361748,0.554845251762499,3.90999207970357));
#46374=CARTESIAN_POINT('Ctrl Pts',(10.4257194535428,0.375791608533427,4.41801357164013));
#46375=CARTESIAN_POINT('Ctrl Pts',(10.4734352896056,-0.148357251109035,
4.54216676877402));
#46376=CARTESIAN_POINT('Ctrl Pts',(10.5211511256685,-0.536267364288337,
4.16843987983467));
#46377=CARTESIAN_POINT('Ctrl Pts',(10.5688669617313,-0.431714905307627,
3.64003205746247));
#46378=CARTESIAN_POINT('Ctrl Pts',(10.6165827977942,0.0692879940047382,
3.44218833554121));
#46379=CARTESIAN_POINT('Ctrl Pts',(10.664298633857,0.50666266228973,3.75659164812817));
#46380=CARTESIAN_POINT('Ctrl Pts',(10.7120144699198,0.478761211786921,4.29452059555793));
#46381=CARTESIAN_POINT('Ctrl Pts',(10.7597303059827,0.0112059738120427,
4.56198674830498));
#46382=CARTESIAN_POINT('Ctrl Pts',(10.8074461420455,-0.466639882340508,
4.31337182280594));
#46383=CARTESIAN_POINT('Ctrl Pts',(10.8551619781083,-0.515963154362253,
3.77698273057893));
#46384=CARTESIAN_POINT('Ctrl Pts',(10.9028778141712,-0.0914695226195351,
3.44539382842306));
#46385=CARTESIAN_POINT('Ctrl Pts',(10.950593650234,0.417021979184216,3.62310830733915));
#46386=CARTESIAN_POINT('Ctrl Pts',(10.9983094862969,0.542555780795161,4.14692822684982));
#46387=CARTESIAN_POINT('Ctrl Pts',(11.0460253223597,0.169852260608159,4.53582169486292));
#46388=CARTESIAN_POINT('Ctrl Pts',(11.0937411584225,-0.358829204008283,
4.43266185580689));
#46389=CARTESIAN_POINT('Ctrl Pts',(11.1414569944853,-0.55799228928692,3.93218197720501));
#46390=CARTESIAN_POINT('Ctrl Pts',(11.1891728305482,-0.244742469498405,
3.49398043245019));
#46391=CARTESIAN_POINT('Ctrl Pts',(11.236888666611,0.293258125877444,3.5204644426882));
#46392=CARTESIAN_POINT('Ctrl Pts',(11.2846045026739,0.561955271903759,3.98731333380864));
#46393=CARTESIAN_POINT('Ctrl Pts',(11.3323203387367,0.314600244947554,4.46581258570203));
#46394=CARTESIAN_POINT('Ctrl Pts',(11.3800361747996,-0.221657027690976,
4.51654897269734));
#46395=CARTESIAN_POINT('Ctrl Pts',(11.4277520108624,-0.554363241169119,
4.0929304899371));
#46396=CARTESIAN_POINT('Ctrl Pts',(11.4754678469252,-0.377989160306769,
3.58397250834823));
#46397=CARTESIAN_POINT('Ctrl Pts',(11.5231836829881,0.145498182576105,3.45705897374896));
#46398=CARTESIAN_POINT('Ctrl Pts',(11.5708995190509,0.535372305622036,3.82873653777755));
#46399=CARTESIAN_POINT('Ctrl Pts',(11.6186153551137,0.43360580265347,4.35768797439208));
#46400=CARTESIAN_POINT('Ctrl Pts',(11.6663311911766,-0.0663475807746441,
4.55816904038548));
#46401=CARTESIAN_POINT('Ctrl Pts',(11.7140470272394,-0.505372959888646,
4.24607488805821));
#46402=CARTESIAN_POINT('Ctrl Pts',(11.7617628633023,-0.480306573774387,
3.70800637967828));
#46403=CARTESIAN_POINT('Ctrl Pts',(11.8094786993651,-0.0141672704965164,
3.43808010573911));
#46404=CARTESIAN_POINT('Ctrl Pts',(11.8571945354279,0.464982055269784,3.68417351694868));
#46405=CARTESIAN_POINT('Ctrl Pts',(11.9049103714908,0.517131205013274,4.22029524715934));
#46406=CARTESIAN_POINT('Ctrl Pts',(11.9526262075536,0.0943908121067024,
4.55411646222552));
#46407=CARTESIAN_POINT('Ctrl Pts',(12.0003420436165,-0.415030115946784,
4.37908400385228));
#46408=CARTESIAN_POINT('Ctrl Pts',(12.0480578796793,-0.543322502467158,
3.85593287178435));
#46409=CARTESIAN_POINT('Ctrl Pts',(12.0957737157421,-0.172673474880652,
3.46508080031456));
#46410=CARTESIAN_POINT('Ctrl Pts',(12.143489551805,0.356544261611682,3.56545326070575));
#46411=CARTESIAN_POINT('Ctrl Pts',(12.1912053878678,0.558341916527368,4.06487667815191));
#46412=CARTESIAN_POINT('Ctrl Pts',(12.2389212239306,0.247405598301292,4.50472284379514));
#46413=CARTESIAN_POINT('Ctrl Pts',(12.2866370599935,-0.290727087669313,
4.48107425582212));
#46414=CARTESIAN_POINT('Ctrl Pts',(12.3343528960563,-0.56188061562194,4.01564777644873));
#46415=CARTESIAN_POINT('Ctrl Pts',(12.3820687321191,-0.317050528604376,
3.5358517031905));
#46416=CARTESIAN_POINT('Ctrl Pts',(12.429784568182,0.218931937280033,3.48229015273196));
#46417=CARTESIAN_POINT('Ctrl Pts',(12.4775004042448,0.553865836459325,3.90414952100961));
#46418=CARTESIAN_POINT('Ctrl Pts',(12.5252162403077,0.380176215696692,4.4140298589933));
#46419=CARTESIAN_POINT('Ctrl Pts',(12.5729320763705,-0.142635073703209,
4.54370020679522));
#46420=CARTESIAN_POINT('Ctrl Pts',(12.6206479124333,-0.53446238019874,4.17408228879405));
#46421=CARTESIAN_POINT('Ctrl Pts',(12.6683637484962,-0.435484659196984,
3.644601926393));
#46422=CARTESIAN_POINT('Ctrl Pts',(12.716079584559,0.0634053251381518,3.44148908348752));
#46423=CARTESIAN_POINT('Ctrl Pts',(12.7637954206219,0.504069223782589,3.75126540901054));
#46424=CARTESIAN_POINT('Ctrl Pts',(12.8115112566847,0.481838598125516,4.2894585367128));
#46425=CARTESIAN_POINT('Ctrl Pts',(12.8592270927475,0.0171281737699642,
4.56183743625962));
#46426=CARTESIAN_POINT('Ctrl Pts',(12.9069429288104,-0.463311316109371,
4.31827237310907));
#46427=CARTESIAN_POINT('Ctrl Pts',(12.9546587648732,-0.518284895444539,
3.78243289248252));
#46428=CARTESIAN_POINT('Ctrl Pts',(13.0023746009361,-0.0973094804548018,
3.44638863438952));
#46429=CARTESIAN_POINT('Ctrl Pts',(13.0500904369989,0.413026727735397,3.61873421174243));
#46430=CARTESIAN_POINT('Ctrl Pts',(13.0978062730617,0.544074136613086,4.14120202898048));
#46431=CARTESIAN_POINT('Ctrl Pts',(13.1455221091246,0.17548989418231,4.53400185033327));
#46432=CARTESIAN_POINT('Ctrl Pts',(13.1932379451874,-0.354249418335187,
4.4364195558504));
#46433=CARTESIAN_POINT('Ctrl Pts',(13.2409537812502,-0.558676039167545,
3.93806646805208));
#46434=CARTESIAN_POINT('Ctrl Pts',(13.2886696173131,-0.250061856896528,
3.49658789561142));
#46435=CARTESIAN_POINT('Ctrl Pts',(13.3363854533759,0.288187976258808,3.51740040462167));
#46436=CARTESIAN_POINT('Ctrl Pts',(13.3841012894388,0.56179035647369,3.9813915478171));
#46437=CARTESIAN_POINT('Ctrl Pts',(13.4318171255016,0.319492008083037,4.46247111897993));
#46438=CARTESIAN_POINT('Ctrl Pts',(13.4795329615644,-0.21620076734671,4.51885634555065));
#46439=CARTESIAN_POINT('Ctrl Pts',(13.5272487976273,-0.553353051445561,
4.09876780637113));
#46440=CARTESIAN_POINT('Ctrl Pts',(13.5749646336901,-0.382352713970831,
3.58797927086295));
#46441=CARTESIAN_POINT('Ctrl Pts',(13.6226804697529,0.139768003996038,3.45555571067516));
#46442=CARTESIAN_POINT('Ctrl Pts',(13.6703963058158,0.53353761328617,3.82310371872654));
#46443=CARTESIAN_POINT('Ctrl Pts',(13.7181121418786,0.437351422764197,4.35309830377052));
#46444=CARTESIAN_POINT('Ctrl Pts',(13.7658279779415,-0.0604613087987784,
4.55883728334624));
#46445=CARTESIAN_POINT('Ctrl Pts',(13.8135438140043,-0.502751490175015,
4.25138738680826));
#46446=CARTESIAN_POINT('Ctrl Pts',(13.8612596500671,-0.483357242297515,
3.71308458487209));
#46447=CARTESIAN_POINT('Ctrl Pts',(13.90897548613,-0.0200886014110514,3.43826062340902));
#46448=CARTESIAN_POINT('Ctrl Pts',(13.9566913221928,0.461627711254046,3.67929057494076));
#46449=CARTESIAN_POINT('Ctrl Pts',(14.0044071582557,0.519424193619207,4.21483292625321));
#46450=CARTESIAN_POINT('Ctrl Pts',(14.0521229943185,0.100225446615308,4.55309089575788));
#46451=CARTESIAN_POINT('Ctrl Pts',(14.0998388303813,-0.411011870182152,
4.38343698529073));
#46452=CARTESIAN_POINT('Ctrl Pts',(14.1475546664441,-0.544810662360815,
3.86166699129474));
#46453=CARTESIAN_POINT('Ctrl Pts',(14.195270502507,-0.178301440303968,3.46693032771971));
#46454=CARTESIAN_POINT('Ctrl Pts',(14.2429863385698,0.351944737904315,3.5617197465309));
#46455=CARTESIAN_POINT('Ctrl Pts',(14.2907021746327,0.558994647929194,4.05898866591129));
#46456=CARTESIAN_POINT('Ctrl Pts',(14.3384180106955,0.252711171522458,4.50208738572805));
#46457=CARTESIAN_POINT('Ctrl Pts',(14.3861338467583,-0.28564086215454,4.48411153362329));
#46458=CARTESIAN_POINT('Ctrl Pts',(14.4338496828212,-0.561684496965419,
4.02156861117883));
#46459=CARTESIAN_POINT('Ctrl Pts',(14.481565518884,-0.321924615586062,3.53921890121312));
#46460=CARTESIAN_POINT('Ctrl Pts',(14.5292813549469,0.213463593732893,3.48001156429194));
#46461=CARTESIAN_POINT('Ctrl Pts',(14.5769971910097,0.552824900367352,3.89831760893199));
#46462=CARTESIAN_POINT('Ctrl Pts',(14.6247130270725,0.384518594689996,4.4100001578745));
#46463=CARTESIAN_POINT('Ctrl Pts',(14.6724288631354,-0.136897053070264,
4.54517325317752));
#46464=CARTESIAN_POINT('Ctrl Pts',(14.7201446991982,-0.532598030564186,
4.17970536151887));
#46465=CARTESIAN_POINT('Ctrl Pts',(14.7678605352611,-0.439206041516937,
3.64921127125505));
#46466=CARTESIAN_POINT('Ctrl Pts',(14.8155763713239,0.0575156135089261,
3.44085186817608));
#46467=CARTESIAN_POINT('Ctrl Pts',(14.8632922073868,0.501419795658073,3.74596679815093));
#46468=CARTESIAN_POINT('Ctrl Pts',(14.9110080434496,0.484862464119148,4.284364326187));
#46469=CARTESIAN_POINT('Ctrl Pts',(14.9587238795124,0.0230484712116303,
4.56162571797798));
#46470=CARTESIAN_POINT('Ctrl Pts',(15.0064397155752,-0.459931287455839,
4.32313757122732));
#46471=CARTESIAN_POINT('Ctrl Pts',(15.0541555516381,-0.5205490679001,3.78790722070797));
#46472=CARTESIAN_POINT('Ctrl Pts',(15.1018713877009,-0.103138629614742,
3.44744493287938));
#46473=CARTESIAN_POINT('Ctrl Pts',(15.1495872237638,0.40898559923764,3.61440246534021));
#46474=CARTESIAN_POINT('Ctrl Pts',(15.1973030598266,0.545532059257757,4.13546014705983));
#46475=CARTESIAN_POINT('Ctrl Pts',(15.2450188958894,0.181108035171788,4.53212269141213));
#46476=CARTESIAN_POINT('Ctrl Pts',(15.2927347319523,-0.349630284317748,
4.44012878048063));
#46477=CARTESIAN_POINT('Ctrl Pts',(15.3404505680151,-0.559297733964875,
3.94395783818199));
#46478=CARTESIAN_POINT('Ctrl Pts',(15.3881664040779,-0.255353468610234,
3.49925127540033));
#46479=CARTESIAN_POINT('Ctrl Pts',(15.4358822401408,0.283085816087337,3.51438997142805));
#46480=CARTESIAN_POINT('Ctrl Pts',(15.4835980762036,0.561563040036739,3.97547182876414));
#46481=CARTESIAN_POINT('Ctrl Pts',(15.5313139122665,0.324348283562367,4.45907828316053));
#46482=CARTESIAN_POINT('Ctrl Pts',(15.5790297483293,-0.210720492447169,
4.52110608630326));
#46483=CARTESIAN_POINT('Ctrl Pts',(15.6267455843921,-0.552281397890927,
4.10459415214592));
#46484=CARTESIAN_POINT('Ctrl Pts',(15.674461420455,-0.386673797709831,3.59203179868507));
#46485=CARTESIAN_POINT('Ctrl Pts',(15.7221772565178,0.134022300649356,3.45411292188939));
#46486=CARTESIAN_POINT('Ctrl Pts',(15.7698930925807,0.531643658124066,3.81749054847505));
#46487=CARTESIAN_POINT('Ctrl Pts',(15.8176089286435,0.441048463954279,4.34846941266494));
#46488=CARTESIAN_POINT('Ctrl Pts',(15.8653247647064,-0.054568321067637,
4.5594434533135));
#46489=CARTESIAN_POINT('Ctrl Pts',(15.9130406007692,-0.500074177211609,
4.25667196264028));
#46490=CARTESIAN_POINT('Ctrl Pts',(15.960756436832,-0.486354221791887,3.71819465926869));
#46491=CARTESIAN_POINT('Ctrl Pts',(16.0084722728949,-0.0260077009790528,
3.4385035364232));
#46492=CARTESIAN_POINT('Ctrl Pts',(16.0561881089577,0.458222091822753,3.6744432558139));
#46493=CARTESIAN_POINT('Ctrl Pts',(16.1039039450206,0.52165948705058,4.2093467427251));
#46494=CARTESIAN_POINT('Ctrl Pts',(16.1516197810833,0.106048948556897,4.55200389457816));
#46495=CARTESIAN_POINT('Ctrl Pts',(16.1993356171462,-0.406947971169398,
4.38774737636841));
#46496=CARTESIAN_POINT('Ctrl Pts',(16.247051453209,-0.546238307271431,3.86741647617928));
#46497=CARTESIAN_POINT('Ctrl Pts',(16.2947672892719,-0.183909600849411,
3.46883906597446));
#46498=CARTESIAN_POINT('Ctrl Pts',(16.3424831253347,0.347306121845567,3.55803491444678));
#46499=CARTESIAN_POINT('Ctrl Pts',(16.3901989613975,0.559585288858183,4.05309410148958));
#46500=CARTESIAN_POINT('Ctrl Pts',(16.4379147974604,0.257988674785898,4.49939615817675));
#46501=CARTESIAN_POINT('Ctrl Pts',(16.4856306335232,-0.280522909008289,
4.4870950386126));
#46502=CARTESIAN_POINT('Ctrl Pts',(16.5333464695861,-0.561425989060384,
4.02748705016995));
#46503=CARTESIAN_POINT('Ctrl Pts',(16.5810623056489,-0.326762944709103,
3.54263728061361));
#46504=CARTESIAN_POINT('Ctrl Pts',(16.6287781417117,0.207971539662738,3.4777907336998));
#46505=CARTESIAN_POINT('Ctrl Pts',(16.6764939777746,0.551722559108811,3.89249699125187));
#46506=CARTESIAN_POINT('Ctrl Pts',(16.7242098138374,0.388818263182495,4.40592491588375));
#46507=CARTESIAN_POINT('Ctrl Pts',(16.7719256499003,-0.131143826562283,
4.54658574430191));
#46508=CARTESIAN_POINT('Ctrl Pts',(16.8196414859631,-0.53067452246778,4.18530847342493));
#46509=CARTESIAN_POINT('Ctrl Pts',(16.8673573220259,-0.442878638914007,
3.65385958006445));
#46510=CARTESIAN_POINT('Ctrl Pts',(16.9150731580888,0.0516195133182915,
3.44027676038576));
#46511=CARTESIAN_POINT('Ctrl Pts',(16.9627889941516,0.498714672202087,3.74069640409388));
#46512=CARTESIAN_POINT('Ctrl Pts',(17.0105048302145,0.487832473891125,4.27923852982128));
#46513=CARTESIAN_POINT('Ctrl Pts',(17.0582206662773,0.0289662085384809,
4.56135161697672));
#46514=CARTESIAN_POINT('Ctrl Pts',(17.1059365023401,-0.456500171817451,
4.32796687675757));
#46515=CARTESIAN_POINT('Ctrl Pts',(17.1536523384029,-0.522755420235406,
3.79340510719289));
#46516=CARTESIAN_POINT('Ctrl Pts',(17.2013681744658,-0.108956322625149,
3.44856260656401));
#46517=CARTESIAN_POINT('Ctrl Pts',(17.2490840105286,0.404899042560309,3.61011354928233));
#46518=CARTESIAN_POINT('Ctrl Pts',(17.2967998465915,0.54692938679005,4.12970321886885));
#46519=CARTESIAN_POINT('Ctrl Pts',(17.3445156826543,0.186706059540143,4.53018442682757));
#46520=CARTESIAN_POINT('Ctrl Pts',(17.3922315187172,-0.344972315027459,
4.4437891176945));
#46521=CARTESIAN_POINT('Ctrl Pts',(17.43994735478,-0.559857304624004,3.94985543320929));
#46522=CARTESIAN_POINT('Ctrl Pts',(17.4876631908428,-0.260616716872392,
3.5019702759813));
#46523=CARTESIAN_POINT('Ctrl Pts',(17.5353790269057,0.277952212086773,3.51143347749201));
#46524=CARTESIAN_POINT('Ctrl Pts',(17.5830948629685,0.561273347842132,3.96955483418404));
#46525=CARTESIAN_POINT('Ctrl Pts',(17.6308106990313,0.329168531973526,4.45563445510394));
#46526=CARTESIAN_POINT('Ctrl Pts',(17.6785265350942,-0.205216811715269,
4.52329794506467));
#46527=CARTESIAN_POINT('Ctrl Pts',(17.726242371157,-0.551148399539408,4.11040888009862));
#46528=CARTESIAN_POINT('Ctrl Pts',(17.7739582072198,-0.390951931558304,
3.59612964167903));
#46529=CARTESIAN_POINT('Ctrl Pts',(17.8216740432827,0.128261710741471,3.45273076764982));
#46530=CARTESIAN_POINT('Ctrl Pts',(17.8693898793456,0.529690650507269,3.81189765050732));
#46531=CARTESIAN_POINT('Ctrl Pts',(17.9171057154083,0.44469651557395,4.34380181523062));
#46532=CARTESIAN_POINT('Ctrl Pts',(17.9648215514712,-0.0486692721463468,
4.55998748295674));
#46533=CARTESIAN_POINT('Ctrl Pts',(18.012537387534,-0.497341318381634,4.26192802856871));
#46534=CARTESIAN_POINT('Ctrl Pts',(18.0602532235969,-0.489297179367249,
3.72333603526529));
#46535=CARTESIAN_POINT('Ctrl Pts',(18.1079690596597,-0.0319239117350811,
3.43880881780002));
#46536=CARTESIAN_POINT('Ctrl Pts',(18.1556848957225,0.454765575255941,3.66963209798526));
#46537=CARTESIAN_POINT('Ctrl Pts',(18.2034007317854,0.523836837021606,4.20383730595423));
#46538=CARTESIAN_POINT('Ctrl Pts',(18.2511165678483,0.111860671084556,4.5508555794253));
#46539=CARTESIAN_POINT('Ctrl Pts',(18.298832403911,-0.402838870307115,4.39201469830757));
#46540=CARTESIAN_POINT('Ctrl Pts',(18.346548239974,-0.547605278623001,3.87318068781251));
#46541=CARTESIAN_POINT('Ctrl Pts',(18.3942640760367,-0.189497333589109,
3.47080680306518));
#46542=CARTESIAN_POINT('Ctrl Pts',(18.4419799120997,0.342628928670919,3.55439917374707));
#46543=CARTESIAN_POINT('Ctrl Pts',(18.4896957481624,0.560113773708727,4.04719363962704));
#46544=CARTESIAN_POINT('Ctrl Pts',(18.5374115842253,0.263237521891608,4.49664946007004));
#46545=CARTESIAN_POINT('Ctrl Pts',(18.5851274202881,-0.275373796708506,
4.49002443939646));
#46546=CARTESIAN_POINT('Ctrl Pts',(18.632843256351,-0.561105120620647,4.03340243603));
#46547=CARTESIAN_POINT('Ctrl Pts',(18.6805590924138,-0.331564978554912,
3.54610646169455));
#46548=CARTESIAN_POINT('Ctrl Pts',(18.7282749284766,0.202456385100939,3.47562790763498));
#46549=CARTESIAN_POINT('Ctrl Pts',(18.7759907645394,0.550558935126376,3.8866883144956));
#46550=CARTESIAN_POINT('Ctrl Pts',(18.8237066006023,0.393074743587739,4.40180458567998));
#46551=CARTESIAN_POINT('Ctrl Pts',(18.8714224366651,-0.125376033221007,
4.54793752327491));
#46552=CARTESIAN_POINT('Ctrl Pts',(18.919138272728,-0.528692069562509,4.19089100214638));
#46553=CARTESIAN_POINT('Ctrl Pts',(18.9668541087908,-0.4465020434557,3.6585463365067));
#46554=CARTESIAN_POINT('Ctrl Pts',(19.0145699448537,0.0457176794812401,
3.43976382400136));
#46555=CARTESIAN_POINT('Ctrl Pts',(19.0622857809165,0.495954153879041,3.73545481224116));
#46556=CARTESIAN_POINT('Ctrl Pts',(19.1100016169793,0.490748297561716,4.27408171698104));
#46557=CARTESIAN_POINT('Ctrl Pts',(19.1577174530421,0.0348807284082936,
4.5610151636709));
#46558=CARTESIAN_POINT('Ctrl Pts',(19.205433289105,-0.453018350253257,4.33275975334162));
#46559=CARTESIAN_POINT('Ctrl Pts',(19.2531491251678,-0.524903707479367,
3.79892594114836));
#46560=CARTESIAN_POINT('Ctrl Pts',(19.3008649612307,-0.11476191309534,3.44974153150476));
#46561=CARTESIAN_POINT('Ctrl Pts',(19.3485807972935,0.400767511262006,3.60586793956989));
#46562=CARTESIAN_POINT('Ctrl Pts',(19.3962966333564,0.548265964675035,4.12393188459875));
#46563=CARTESIAN_POINT('Ctrl Pts',(19.4440124694192,0.192283344213529,4.52818727047755));
#46564=CARTESIAN_POINT('Ctrl Pts',(19.491728305482,-0.340276025447905,4.44740016355363));
#46565=CARTESIAN_POINT('Ctrl Pts',(19.5394441415448,-0.560354693525076,
3.95575859308266));
#46566=CARTESIAN_POINT('Ctrl Pts',(19.5871599776077,-0.265851008504119,
3.50474460473346));
#46567=CARTESIAN_POINT('Ctrl Pts',(19.6348758136705,0.272787718306182,3.5085312334714));
#46568=CARTESIAN_POINT('Ctrl Pts',(19.6825916497334,0.560921342594646,3.96364125479661));
#46569=CARTESIAN_POINT('Ctrl Pts',(19.7303074857962,0.33395216026474,4.45213995410186));
#46570=CARTESIAN_POINT('Ctrl Pts',(19.7780233218591,-0.199690227635008,
4.52543179776919));
#46571=CARTESIAN_POINT('Ctrl Pts',(19.8257391579219,-0.549954387748789,
4.11621111891367));
#46572=CARTESIAN_POINT('Ctrl Pts',(19.8734549939848,-0.395186252277308,
3.60027277035845));
#46573=CARTESIAN_POINT('Ctrl Pts',(19.9211708300475,0.122486141425193,3.45140859770427));
#46574=CARTESIAN_POINT('Ctrl Pts',(19.9688866661104,0.527680190865048,3.80632716374734));
#46575=CARTESIAN_POINT('Ctrl Pts',(20.0166025021732,0.448292560087992,4.33909316421112));
#46576=CARTESIAN_POINT('Ctrl Pts',(20.0643183382361,-0.0427598846646947,
4.56047472290141));
#46577=CARTESIAN_POINT('Ctrl Pts',(20.1120341742989,-0.49456253103916,4.26714478353561));
#46578=CARTESIAN_POINT('Ctrl Pts',(20.1597500103618,-0.492168201513856,
3.72852743457374));
#46579=CARTESIAN_POINT('Ctrl Pts',(20.2074658464246,-0.0378697858522375,
3.43914000028616));
#46580=CARTESIAN_POINT('Ctrl Pts',(20.2551816824874,0.451321269441671,3.66492646727415));
#46581=CARTESIAN_POINT('Ctrl Pts',(20.3028975185503,0.52583741886325,4.1981749506787));
#46582=CARTESIAN_POINT('Ctrl Pts',(20.3506133546131,0.117885080656874,4.54989459844945));
#46583=CARTESIAN_POINT('Ctrl Pts',(20.398329190676,-0.399119892637424,4.39574851066478));
#46584=CARTESIAN_POINT('Ctrl Pts',(20.438092387395,-0.523197416260526,3.96600412247733));
#46585=CARTESIAN_POINT('Ctrl Pts',(20.4699029447702,-0.3725623900923,3.67462118354637));
#46586=CARTESIAN_POINT('Ctrl Pts',(20.4937608628016,-0.172533290246804,
3.53519650363565));
#46587=CARTESIAN_POINT('Ctrl Pts',(20.5176187808331,0.0720421502968434,
3.50974356844941));
#46588=CARTESIAN_POINT('Ctrl Pts',(20.5414766988645,0.297725647320748,3.60399556061657));
#46589=CARTESIAN_POINT('Ctrl Pts',(20.5653346168959,0.451286063531533,3.79517586539437));
#46590=CARTESIAN_POINT('Ctrl Pts',(20.5891925349273,0.494134760388362,4.03639109206021));
#46591=CARTESIAN_POINT('Ctrl Pts',(20.6130504529587,0.416344747430809,4.26873428690612));
#46592=CARTESIAN_POINT('Ctrl Pts',(20.6369083709901,0.23664610161733,4.43535054865035));
#46593=CARTESIAN_POINT('Ctrl Pts',(20.6607662890216,-0.000865470816140784,
4.49551919950567));
#46594=CARTESIAN_POINT('Ctrl Pts',(20.684624207053,-0.238193741375527,4.43451595913869));
#46595=CARTESIAN_POINT('Ctrl Pts',(20.7084821250844,-0.417262150572256,
4.26726382233879));
#46596=CARTESIAN_POINT('Ctrl Pts',(20.7323400431158,-0.494306543785295,
4.03465729316116));
#46597=CARTESIAN_POINT('Ctrl Pts',(20.7561979611472,-0.45047531426282,3.79357669839993));
#46598=CARTESIAN_POINT('Ctrl Pts',(20.7800558791787,-0.296492828349621,
3.60297191305088));
#46599=CARTESIAN_POINT('Ctrl Pts',(20.80391379721,-0.0700085893017688,3.50945147432983));
#46600=CARTESIAN_POINT('Ctrl Pts',(20.8277717152415,0.173594031734132,3.53588342526713));
#46601=CARTESIAN_POINT('Ctrl Pts',(20.8516296332729,0.374748514455718,3.6758045671588));
#46602=CARTESIAN_POINT('Ctrl Pts',(20.8754875513043,0.484266602122282,3.89500029884494));
#46603=CARTESIAN_POINT('Ctrl Pts',(20.8993454693358,0.475368407265908,4.13987133054223));
#46604=CARTESIAN_POINT('Ctrl Pts',(20.9232033873671,0.350229638882089,4.35054000504804));
#46605=CARTESIAN_POINT('Ctrl Pts',(20.9470613053986,0.139450209771325,4.47549210343221));
#46606=CARTESIAN_POINT('Ctrl Pts',(20.97091922343,-0.105428607968738,4.48417342845956));
#46607=CARTESIAN_POINT('Ctrl Pts',(20.9947771414615,-0.324527251938122,
4.37446116262749));
#46608=CARTESIAN_POINT('Ctrl Pts',(21.0186350594928,-0.464270146732381,
4.17318294187641));
#46609=CARTESIAN_POINT('Ctrl Pts',(21.0424929775243,-0.490486342136868,
3.92955677471355));
#46610=CARTESIAN_POINT('Ctrl Pts',(21.0663508955557,-0.396765267394252,
3.7031558948169));
#46611=CARTESIAN_POINT('Ctrl Pts',(21.0902088135871,-0.206024276530194,
3.54934148458869));
#46612=CARTESIAN_POINT('Ctrl Pts',(21.1140667316185,0.0350952616297792,
3.50572535702762));
#46613=CARTESIAN_POINT('Ctrl Pts',(21.1379246496499,0.267633052506714,3.58297284346672));
#46614=CARTESIAN_POINT('Ctrl Pts',(21.1617825676814,0.434727271782411,3.76219482925797));
#46615=CARTESIAN_POINT('Ctrl Pts',(21.1856404857128,0.495518831419392,3.99956665698474));
#46616=CARTESIAN_POINT('Ctrl Pts',(21.2094984037442,0.43514253908843,4.23704444887943));
#46617=CARTESIAN_POINT('Ctrl Pts',(21.2333563217756,0.268362042918248,4.41655841606373));
#46618=CARTESIAN_POINT('Ctrl Pts',(21.257214239807,0.0359597172125542,4.49421250369607));
#46619=CARTESIAN_POINT('Ctrl Pts',(21.2810721578384,-0.205235738871087,
4.45101817209691));
#46620=CARTESIAN_POINT('Ctrl Pts',(21.3049300758699,-0.396245466293343,
4.29753761193144));
#46621=CARTESIAN_POINT('Ctrl Pts',(21.3287879939013,-0.490362383696085,
4.07130100088706));
#46622=CARTESIAN_POINT('Ctrl Pts',(21.3526459119327,-0.464572341082516,
3.82762935292545));
#46623=CARTESIAN_POINT('Ctrl Pts',(21.3765038299641,-0.325181706377507,
3.62610702345576));
#46624=CARTESIAN_POINT('Ctrl Pts',(21.4003617479955,-0.106275286691508,
3.51601171139131));
#46625=CARTESIAN_POINT('Ctrl Pts',(21.424219666027,0.138618335471326,3.52426471946798));
#46626=CARTESIAN_POINT('Ctrl Pts',(21.4480775840584,0.349615998723735,3.64884796240357));
#46627=CARTESIAN_POINT('Ctrl Pts',(21.4719355020898,0.475123026939619,3.85929744372095));
#46628=CARTESIAN_POINT('Ctrl Pts',(21.4957934201212,0.484449532977353,4.10415253270923));
#46629=CARTESIAN_POINT('Ctrl Pts',(21.5196513381527,0.375314932061802,4.32353949039209));
#46630=CARTESIAN_POINT('Ctrl Pts',(21.543509256184,0.174405606883644,4.4638122296353));
#46631=CARTESIAN_POINT('Ctrl Pts',(21.5673671742155,-0.069150639890911,
4.49067024474121));
#46632=CARTESIAN_POINT('Ctrl Pts',(21.5912250922469,-0.29579767158652,4.39754601941878));
#46633=CARTESIAN_POINT('Ctrl Pts',(21.6150830102783,-0.450114115212426,
4.20721096341231));
#46634=CARTESIAN_POINT('Ctrl Pts',(21.6389409283097,-0.494365396806572,
3.96620718253823));
#46635=CARTESIAN_POINT('Ctrl Pts',(21.6627988463412,-0.417730872638478,
3.73346666603139));
#46636=CARTESIAN_POINT('Ctrl Pts',(21.6866567643726,-0.238949771349764,
3.56590080990214));
#46637=CARTESIAN_POINT('Ctrl Pts',(21.710514682404,-0.00173894210493873,
3.50448403037633));
#46638=CARTESIAN_POINT('Ctrl Pts',(21.7343726004354,0.235897105852373,3.56423440300754));
#46639=CARTESIAN_POINT('Ctrl Pts',(21.7582305184669,0.415849885720624,3.73054133411992));
#46640=CARTESIAN_POINT('Ctrl Pts',(21.7820884364982,0.49411604100673,3.96273824894669));
#46641=CARTESIAN_POINT('Ctrl Pts',(21.8059463545297,0.451557364815975,4.20404667689569));
#46642=CARTESIAN_POINT('Ctrl Pts',(21.8298042725611,0.29858061275206,4.39546013422383));
#46643=CARTESIAN_POINT('Ctrl Pts',(21.8536621905925,0.0725927676976751,
4.49017281661646));
#46644=CARTESIAN_POINT('Ctrl Pts',(21.8775201086239,-0.171145986446082,
4.46502489330693));
#46645=CARTESIAN_POINT('Ctrl Pts',(21.9013780266554,-0.373034884980705,
4.32616571656009));
#46646=CARTESIAN_POINT('Ctrl Pts',(21.9252359446868,-0.483706592871294,
4.10755013753858));
#46647=CARTESIAN_POINT('Ctrl Pts',(21.9490938627182,-0.476098862901817,
3.86263562028194));
#46648=CARTESIAN_POINT('Ctrl Pts',(21.9729517807496,-0.352071992280181,
3.65131043559696));
#46649=CARTESIAN_POINT('Ctrl Pts',(21.996809698781,-0.141953929297546,3.52524934752154));
#46650=CARTESIAN_POINT('Ctrl Pts',(22.0206676168125,0.102875736145779,3.51527772592526));
#46651=CARTESIAN_POINT('Ctrl Pts',(22.0445255348438,0.322549481822576,3.62383390390986));
#46652=CARTESIAN_POINT('Ctrl Pts',(22.0683834528753,0.46335109312246,3.82437293894729));
#46653=CARTESIAN_POINT('Ctrl Pts',(22.0922413709067,0.490850740723195,4.06785757439707));
#46654=CARTESIAN_POINT('Ctrl Pts',(22.1160992889381,0.398324011712033,4.29474918450382));
#46655=CARTESIAN_POINT('Ctrl Pts',(22.1399572069695,0.208396211707814,4.44956659019228));
#46656=CARTESIAN_POINT('Ctrl Pts',(22.163815125001,-0.0324901386554863,
4.49445271863166));
#46657=CARTESIAN_POINT('Ctrl Pts',(22.1876730430324,-0.265431765108271,
4.41843168874211));
#46658=CARTESIAN_POINT('Ctrl Pts',(22.2115309610638,-0.433468094767725,
4.24009271310828));
#46659=CARTESIAN_POINT('Ctrl Pts',(22.2353888790952,-0.495509667838209,
4.00304452911861));
#46660=CARTESIAN_POINT('Ctrl Pts',(22.2592467971266,-0.436385629680506,
3.76525187484075));
#46661=CARTESIAN_POINT('Ctrl Pts',(22.2831047151581,-0.270553418215538,
3.58486153155103));
#46662=CARTESIAN_POINT('Ctrl Pts',(22.3069626331895,-0.0385635261649252,
3.50598385198694));
#46663=CARTESIAN_POINT('Ctrl Pts',(22.3308205512209,0.202856198284482,3.54790657725669));
#46664=CARTESIAN_POINT('Ctrl Pts',(22.3546784692523,0.394672056935096,3.70037845932536));
#46665=CARTESIAN_POINT('Ctrl Pts',(22.3785363872837,0.489979846308564,3.9261159693126));
#46666=CARTESIAN_POINT('Ctrl Pts',(22.4023943053151,0.465474217808745,4.1699201379362));
#46667=CARTESIAN_POINT('Ctrl Pts',(22.4262522233466,0.327147461276091,4.37217420322137));
#46668=CARTESIAN_POINT('Ctrl Pts',(22.450110141378,0.108824243893236,4.4834215400391));
#46669=CARTESIAN_POINT('Ctrl Pts',(22.4739680594094,-0.136109474402841,
4.47645913832327));
#46670=CARTESIAN_POINT('Ctrl Pts',(22.4978259774408,-0.347760701725541,
4.3529895060813));
#46671=CARTESIAN_POINT('Ctrl Pts',(22.5216838954723,-0.474374996640319,
4.1432043106148));
#46672=CARTESIAN_POINT('Ctrl Pts',(22.5455418135036,-0.484991622785221,
3.89840178635216));
#46673=CARTESIAN_POINT('Ctrl Pts',(22.5693997315351,-0.377014700254462,
3.67844274379546));
#46674=CARTESIAN_POINT('Ctrl Pts',(22.5932576495665,-0.176847198578467,
3.53711330196678));
#46675=CARTESIAN_POINT('Ctrl Pts',(22.6171155675979,0.0665638539184235,
3.50897209184919));
#46676=CARTESIAN_POINT('Ctrl Pts',(22.6409734856293,0.293698998435555,3.60090091054846));
#46677=CARTESIAN_POINT('Ctrl Pts',(22.6648314036608,0.449015288492166,3.79041970485759));
#46678=CARTESIAN_POINT('Ctrl Pts',(22.6886893216922,0.494537845944295,4.03118776656693));
#46679=CARTESIAN_POINT('Ctrl Pts',(22.7125472397236,0.419127261608858,4.26432734830583));
#46680=CARTESIAN_POINT('Ctrl Pts',(22.736405157755,0.241238408088568,4.43283588997321));
#46681=CARTESIAN_POINT('Ctrl Pts',(22.7602630757865,0.00434171083240793,
4.49549632518638));
#46682=CARTESIAN_POINT('Ctrl Pts',(22.7841209938178,-0.233581370990537,
4.43700954435219));
#46683=CARTESIAN_POINT('Ctrl Pts',(22.8079789118493,-0.414457183229959,
4.27163232278894));
#46684=CARTESIAN_POINT('Ctrl Pts',(22.8238841905369,-0.46737397936094,4.11714349286348));
#46685=CARTESIAN_POINT('Ctrl Pts',(22.8318368298807,-0.473742730682552,
4.03823705100924));
#46686=CARTESIAN_POINT('Ctrl Pts',(4.,-0.219892372743211,3.64701365460636));
#46687=CARTESIAN_POINT('Ctrl Pts',(4.00795263934381,-0.161099076858729,
3.61038844940468));
#46688=CARTESIAN_POINT('Ctrl Pts',(4.02385791803142,-0.0249198690254346,
3.56711791692558));
#46689=CARTESIAN_POINT('Ctrl Pts',(4.04771583606284,0.185569069288609,3.60813812632505));
#46690=CARTESIAN_POINT('Ctrl Pts',(4.07157375409426,0.350624105231944,3.74494568050885));
#46691=CARTESIAN_POINT('Ctrl Pts',(4.09543167212568,0.429971014252744,3.94413788601839));
#46692=CARTESIAN_POINT('Ctrl Pts',(4.1192895901571,0.40416308778273,4.15698104289539));
#46693=CARTESIAN_POINT('Ctrl Pts',(4.14314750818851,0.279534313346206,4.3314427366163));
#46694=CARTESIAN_POINT('Ctrl Pts',(4.16700542621994,0.0865475313004802,
4.42485517705098));
#46695=CARTESIAN_POINT('Ctrl Pts',(4.19086334425134,-0.127600227202394,
4.41438026490915));
#46696=CARTESIAN_POINT('Ctrl Pts',(4.21472126228278,-0.310547447266788,
4.30257739619942));
#46697=CARTESIAN_POINT('Ctrl Pts',(4.23857918031418,-0.417556725585918,
4.11678647978038));
#46698=CARTESIAN_POINT('Ctrl Pts',(4.26243709834561,-0.422462345057068,
3.90243789311793));
#46699=CARTESIAN_POINT('Ctrl Pts',(4.28629501637703,-0.324064236326554,
3.71194600226016));
#46700=CARTESIAN_POINT('Ctrl Pts',(4.31015293440845,-0.146423688323203,
3.59189110566319));
#46701=CARTESIAN_POINT('Ctrl Pts',(4.33401085243986,0.0670214896752265,
3.5716299793216));
#46702=CARTESIAN_POINT('Ctrl Pts',(4.35786877047129,0.264078061498623,3.65611697628114));
#46703=CARTESIAN_POINT('Ctrl Pts',(4.38172668850271,0.396560367883193,3.82469274783887));
#46704=CARTESIAN_POINT('Ctrl Pts',(4.40558460653412,0.432072854850341,4.03613591352675));
#46705=CARTESIAN_POINT('Ctrl Pts',(4.42944252456555,0.361931763288092,4.23874286631049));
#46706=CARTESIAN_POINT('Ctrl Pts',(4.45330044259696,0.203288494707987,4.382970683851));
#46707=CARTESIAN_POINT('Ctrl Pts',(4.47715836062838,-0.00506434719902249,
4.43355173791626));
#46708=CARTESIAN_POINT('Ctrl Pts',(4.5010162786598,-0.212178818846594,4.37811758201071));
#46709=CARTESIAN_POINT('Ctrl Pts',(4.52487419669122,-0.367409789343613,
4.23022337776645));
#46710=CARTESIAN_POINT('Ctrl Pts',(4.54873211472264,-0.432799058467291,
4.02603328640456));
#46711=CARTESIAN_POINT('Ctrl Pts',(4.57259003275406,-0.392357168499796,
3.8154773474345));
#46712=CARTESIAN_POINT('Ctrl Pts',(4.59644795078547,-0.255973263285106,
3.65004222328625));
#46713=CARTESIAN_POINT('Ctrl Pts',(4.6203058688169,-0.0569969226013119,
3.57018130821703));
#46714=CARTESIAN_POINT('Ctrl Pts',(4.64416378684831,0.155916718210686,3.59542277130738));
#46715=CARTESIAN_POINT('Ctrl Pts',(4.66802170487973,0.330704474340828,3.71959438727947));
#46716=CARTESIAN_POINT('Ctrl Pts',(4.69187962291115,0.424625978282027,3.91233281365517));
#46717=CARTESIAN_POINT('Ctrl Pts',(4.71573754094257,0.41471486395576,4.1265082550995));
#46718=CARTESIAN_POINT('Ctrl Pts',(4.73959545897399,0.303394668785218,4.30974898215573));
#46719=CARTESIAN_POINT('Ctrl Pts',(4.76345337700541,0.117886212792376,4.41724764568232));
#46720=CARTESIAN_POINT('Ctrl Pts',(4.78731129503683,-0.0964486333844469,
4.42271789424177));
#46721=CARTESIAN_POINT('Ctrl Pts',(4.81116921306824,-0.287199161490599,
4.32482210305491));
#46722=CARTESIAN_POINT('Ctrl Pts',(4.83502713109967,-0.407721671464292,
4.14749845969467));
#46723=CARTESIAN_POINT('Ctrl Pts',(4.85888504913109,-0.42854512664958,3.93410742516172));
#46724=CARTESIAN_POINT('Ctrl Pts',(4.8827429671625,-0.344577625034195,3.73682892005441));
#46725=CARTESIAN_POINT('Ctrl Pts',(4.90660088519393,-0.176351507991885,
3.60390291263011));
#46726=CARTESIAN_POINT('Ctrl Pts',(4.93045880322534,0.0349973564730633,
3.56783343253575));
#46727=CARTESIAN_POINT('Ctrl Pts',(4.95431672125677,0.237788413971502,3.63744045016736));
#46728=CARTESIAN_POINT('Ctrl Pts',(4.97817463928818,0.382433727027559,3.79570315365689));
#46729=CARTESIAN_POINT('Ctrl Pts',(5.0020325573196,0.433563576539811,4.00392200101168));
#46730=CARTESIAN_POINT('Ctrl Pts',(5.02589047535102,0.378675321553375,4.21118181228595));
#46731=CARTESIAN_POINT('Ctrl Pts',(5.04974839338244,0.231190635538481,4.36680191797922));
#46732=CARTESIAN_POINT('Ctrl Pts',(5.07360631141386,0.0271735416279573,
4.43272896324296));
#46733=CARTESIAN_POINT('Ctrl Pts',(5.09746422944527,-0.183488223403015,
4.39284198969348));
#46734=CARTESIAN_POINT('Ctrl Pts',(5.1213221474767,-0.349282119693095,4.256894448863));
#46735=CARTESIAN_POINT('Ctrl Pts',(5.1451800655081,-0.4296670234643,4.05812921762123));
#46736=CARTESIAN_POINT('Ctrl Pts',(5.16903798353954,-0.404986636103755,
3.84514980926298));
#46737=CARTESIAN_POINT('Ctrl Pts',(5.19289590157095,-0.281275984601366,
3.67003549057442));
#46738=CARTESIAN_POINT('Ctrl Pts',(5.21675381960238,-0.0887856930599551,
3.5756064824932));
#46739=CARTESIAN_POINT('Ctrl Pts',(5.24061173763379,0.125415118908336,3.58495324968971));
#46740=CARTESIAN_POINT('Ctrl Pts',(5.26446965566521,0.308948518064291,3.69579025298356));
#46741=CARTESIAN_POINT('Ctrl Pts',(5.28832757369662,0.416935588964862,3.88101482593007));
#46742=CARTESIAN_POINT('Ctrl Pts',(5.31218549172805,0.422970551266107,4.09533451502773));
#46743=CARTESIAN_POINT('Ctrl Pts',(5.33604340975946,0.325577692296299,4.28634231834109));
#46744=CARTESIAN_POINT('Ctrl Pts',(5.35990132779089,0.148572219001774,4.40733162501188));
#46745=CARTESIAN_POINT('Ctrl Pts',(5.3837592458223,-0.0647632088646815,
4.42871725387658));
#46746=CARTESIAN_POINT('Ctrl Pts',(5.40761716385372,-0.26226226804932,4.34526983614494));
#46747=CARTESIAN_POINT('Ctrl Pts',(5.43147508188515,-0.395631058815178,
4.17739453851434));
#46748=CARTESIAN_POINT('Ctrl Pts',(5.45533299991656,-0.432257278927009,
3.96614144408682));
#46749=CARTESIAN_POINT('Ctrl Pts',(5.47919091794798,-0.363184819889405,
3.76316768886851));
#46750=CARTESIAN_POINT('Ctrl Pts',(5.5030488359794,-0.205303779432806,3.61810588490468));
#46751=CARTESIAN_POINT('Ctrl Pts',(5.52690675401082,0.00277962745745752,
3.56642759466814));
#46752=CARTESIAN_POINT('Ctrl Pts',(5.55076467204224,0.210183339719457,3.62076956781107));
#46753=CARTESIAN_POINT('Ctrl Pts',(5.57462259007365,0.36619150013966,3.76784371165257));
#46754=CARTESIAN_POINT('Ctrl Pts',(5.59848050810508,0.432655863921731,3.97168639180759));
#46755=CARTESIAN_POINT('Ctrl Pts',(5.62233842613649,0.393324083661671,4.18245252040861));
#46756=CARTESIAN_POINT('Ctrl Pts',(5.64619634416792,0.257813851021257,4.34860403787086));
#46757=CARTESIAN_POINT('Ctrl Pts',(5.67005426219933,0.0592611090830247,
4.42951237227525));
#46758=CARTESIAN_POINT('Ctrl Pts',(5.69391218023075,-0.153782588238227,
4.40539323200473));
#46759=CARTESIAN_POINT('Ctrl Pts',(5.71777009826218,-0.329222253834466,
4.28214440376531));
#46760=CARTESIAN_POINT('Ctrl Pts',(5.74162801629359,-0.424158110434281,
4.08990358344764));
#46761=CARTESIAN_POINT('Ctrl Pts',(5.76548593432501,-0.415375755386326,
3.8756788878607));
#46762=CARTESIAN_POINT('Ctrl Pts',(5.78934385235642,-0.305022713182347,
3.69185409099321));
#46763=CARTESIAN_POINT('Ctrl Pts',(5.81320177038785,-0.120083309624962,
3.58337936191985));
#46764=CARTESIAN_POINT('Ctrl Pts',(5.83705968841926,0.0942197354074567,
3.57677972866706));
#46765=CARTESIAN_POINT('Ctrl Pts',(5.86091760645069,0.285483486244351,3.673668977605));
#46766=CARTESIAN_POINT('Ctrl Pts',(5.8847755244821,0.406938752801468,3.85035505520226));
#46767=CARTESIAN_POINT('Ctrl Pts',(5.90863344251353,0.428886400972996,4.06363338935351));
#46768=CARTESIAN_POINT('Ctrl Pts',(5.93249136054494,0.345959657594393,4.261351642888));
#46769=CARTESIAN_POINT('Ctrl Pts',(5.95634927857636,0.178436323746589,4.39516226965834));
#46770=CARTESIAN_POINT('Ctrl Pts',(5.98020719660778,-0.0327194942966983,
4.4323450160316));
#46771=CARTESIAN_POINT('Ctrl Pts',(6.0040651146392,-0.23587461323539,4.36380751861078));
#46772=CARTESIAN_POINT('Ctrl Pts',(6.02792303267061,-0.381351759249696,
4.20630938167977));
#46773=CARTESIAN_POINT('Ctrl Pts',(6.05178095070204,-0.433578399193506,
3.9983625870902));
#46774=CARTESIAN_POINT('Ctrl Pts',(6.07563886873346,-0.379782579589031,
3.79081692866841));
#46775=CARTESIAN_POINT('Ctrl Pts',(6.09949678676487,-0.233120953551068,
3.63442082419035));
#46776=CARTESIAN_POINT('Ctrl Pts',(6.12335470479629,-0.0294522997972467,
3.5674214393556));
#46777=CARTESIAN_POINT('Ctrl Pts',(6.14721262282771,0.181413325723775,3.60619428643423));
#46778=CARTESIAN_POINT('Ctrl Pts',(6.17107054085913,0.347927737305898,3.74127281623538));
#46779=CARTESIAN_POINT('Ctrl Pts',(6.19492845889055,0.429346806292137,3.93959933010928));
#46780=CARTESIAN_POINT('Ctrl Pts',(6.21878637692197,0.405811992579865,4.15272917617017));
#46781=CARTESIAN_POINT('Ctrl Pts',(6.24264429495339,0.282982581651336,4.32844890303245));
#46782=CARTESIAN_POINT('Ctrl Pts',(6.26650221298481,0.0910742457207041,
4.42397415233781));
#46783=CARTESIAN_POINT('Ctrl Pts',(6.29036013101623,-0.123327005978964,
4.41559921078967));
#46784=CARTESIAN_POINT('Ctrl Pts',(6.31421804904765,-0.307151379675736,
4.3060270879454));
#46785=CARTESIAN_POINT('Ctrl Pts',(6.33807596707907,-0.416657206472865,
4.12081787696614));
#46786=CARTESIAN_POINT('Ctrl Pts',(6.36193388511048,-0.422829889105799,
3.9075587958503));
#46787=CARTESIAN_POINT('Ctrl Pts',(6.39374444248571,-0.296437506874183,
3.64987069373525));
#46788=CARTESIAN_POINT('Ctrl Pts',(6.43350763920474,0.0703302468340302,
3.51324810367198));
#46789=CARTESIAN_POINT('Ctrl Pts',(6.48122347526758,0.448014600657906,3.7964368525222));
#46790=CARTESIAN_POINT('Ctrl Pts',(6.52893931133042,0.413240052911115,4.26646358767058));
#46791=CARTESIAN_POINT('Ctrl Pts',(6.57665514739325,-0.000480251589724132,
4.49184654025612));
#46792=CARTESIAN_POINT('Ctrl Pts',(6.62437098345609,-0.41404349770976,4.26553045144514));
#46793=CARTESIAN_POINT('Ctrl Pts',(6.67208681951894,-0.447234019333667,
3.79538894860702));
#46794=CARTESIAN_POINT('Ctrl Pts',(6.71980265558177,-0.0698021891909718,
3.51313682319347));
#46795=CARTESIAN_POINT('Ctrl Pts',(6.76751849164461,0.371772181936036,3.67798293440124));
#46796=CARTESIAN_POINT('Ctrl Pts',(6.81523432770745,0.471920133146607,4.13853999974893));
#46797=CARTESIAN_POINT('Ctrl Pts',(6.86295016377028,0.138708377331583,4.4718748549198));
#46798=CARTESIAN_POINT('Ctrl Pts',(6.91066599983312,-0.32188767172048,4.37187913281409));
#46799=CARTESIAN_POINT('Ctrl Pts',(6.95838183589596,-0.486886005735063,
3.93038141845316));
#46800=CARTESIAN_POINT('Ctrl Pts',(7.0060976719588,-0.204771183672361,3.55281534000283));
#46801=CARTESIAN_POINT('Ctrl Pts',(7.05381350802163,0.265389096458903,3.58590591031157));
#46802=CARTESIAN_POINT('Ctrl Pts',(7.10152934408448,0.491837993618785,3.99926540470374));
#46803=CARTESIAN_POINT('Ctrl Pts',(7.14924518014731,0.266624753986561,4.41329951581085));
#46804=CARTESIAN_POINT('Ctrl Pts',(7.19696101621015,-0.203434237821079,
4.44779430805676));
#46805=CARTESIAN_POINT('Ctrl Pts',(7.24467685227299,-0.486676365692783,
4.07107270446015));
#46806=CARTESIAN_POINT('Ctrl Pts',(7.29239268833582,-0.322996137187983,
3.62908393881966));
#46807=CARTESIAN_POINT('Ctrl Pts',(7.34010852439867,0.137296434535941,3.52771310152703));
#46808=CARTESIAN_POINT('Ctrl Pts',(7.3878243604615,0.471507566988788,3.86005058906394));
#46809=CARTESIAN_POINT('Ctrl Pts',(7.43554019652434,0.372726051350611,4.32090577464778));
#46810=CARTESIAN_POINT('Ctrl Pts',(7.48325603258718,-0.0683355354161961,
4.48706824929225));
#46811=CARTESIAN_POINT('Ctrl Pts',(7.53097186865002,-0.44664354691983,4.20594845626764));
#46812=CARTESIAN_POINT('Ctrl Pts',(7.57868770471286,-0.414791917646955,
3.73570302684109));
#46813=CARTESIAN_POINT('Ctrl Pts',(7.62640354077569,-0.00203048755240202,
3.50816557464413));
#46814=CARTESIAN_POINT('Ctrl Pts',(7.67411937683853,0.412595570264971,3.73228724307244));
#46815=CARTESIAN_POINT('Ctrl Pts',(7.72183521290137,0.448328767436039,4.20225365549051));
#46816=CARTESIAN_POINT('Ctrl Pts',(7.7695510489642,0.0723547589785895,4.48648742399228));
#46817=CARTESIAN_POINT('Ctrl Pts',(7.81726688502705,-0.370063737934377,
4.32397230547438));
#46818=CARTESIAN_POINT('Ctrl Pts',(7.86498272108989,-0.472647010158531,
3.86394843388276));
#46819=CARTESIAN_POINT('Ctrl Pts',(7.91269855715272,-0.141191260335066,
3.52886280888004));
#46820=CARTESIAN_POINT('Ctrl Pts',(7.96041439321556,0.31992259635559,3.62642971585976));
#46821=CARTESIAN_POINT('Ctrl Pts',(8.0081302292784,0.48724661017382,4.0670519628834));
#46822=CARTESIAN_POINT('Ctrl Pts',(8.05584606534124,0.207124564615173,4.44609936066402));
#46823=CARTESIAN_POINT('Ctrl Pts',(8.10356190140407,-0.263203155649882,
4.41548685142597));
#46824=CARTESIAN_POINT('Ctrl Pts',(8.15127773746691,-0.491827368180951,
4.00332637343646));
#46825=CARTESIAN_POINT('Ctrl Pts',(8.19899357352975,-0.268798940774433,
3.58811123553743));
#46826=CARTESIAN_POINT('Ctrl Pts',(8.24670940959259,0.201071689948468,3.55113988776764));
#46827=CARTESIAN_POINT('Ctrl Pts',(8.29442524565542,0.486295093906121,3.92636368766143));
#46828=CARTESIAN_POINT('Ctrl Pts',(8.34214108171827,0.324946230517931,4.36920884621601));
#46829=CARTESIAN_POINT('Ctrl Pts',(8.3898569177811,-0.134805756295296,4.47300384028212));
#46830=CARTESIAN_POINT('Ctrl Pts',(8.43757275384394,-0.470763542849379,
4.14243212971755));
#46831=CARTESIAN_POINT('Ctrl Pts',(8.48528858990678,-0.37441192437669,3.68106280283335));
#46832=CARTESIAN_POINT('Ctrl Pts',(8.53300442596962,0.0657679253190804,
3.51257841158684));
#46833=CARTESIAN_POINT('Ctrl Pts',(8.58072026203246,0.445552077224736,3.79170076492532));
#46834=CARTESIAN_POINT('Ctrl Pts',(8.62843609809529,0.41617890091499,4.26210751092856));
#46835=CARTESIAN_POINT('Ctrl Pts',(8.67615193415813,0.0046222361594965,
4.49181689660367));
#46836=CARTESIAN_POINT('Ctrl Pts',(8.72386777022097,-0.411179099183508,
4.26988325855195));
#46837=CARTESIAN_POINT('Ctrl Pts',(8.7715836062838,-0.449388340942622,3.80011167148426));
#46838=CARTESIAN_POINT('Ctrl Pts',(8.81929944234665,-0.0749173544856965,
3.51390061216986));
#46839=CARTESIAN_POINT('Ctrl Pts',(8.86701527840948,0.368351391347115,3.67408210030036));
#46840=CARTESIAN_POINT('Ctrl Pts',(8.91473111447233,0.473357386691186,4.13355901061654));
#46841=CARTESIAN_POINT('Ctrl Pts',(8.96244695053515,0.14367201029714,4.47038662641401));
#46842=CARTESIAN_POINT('Ctrl Pts',(9.01016278659801,-0.317949583830803,
4.37525096534692));
#46843=CARTESIAN_POINT('Ctrl Pts',(9.05787862266083,-0.487593182843731,
3.93551656882348));
#46844=CARTESIAN_POINT('Ctrl Pts',(9.10559445872368,-0.209472459465777,
3.55499829935456));
#46845=CARTESIAN_POINT('Ctrl Pts',(9.15331029478651,0.261010046587687,3.58313193881964));
#46846=CARTESIAN_POINT('Ctrl Pts',(9.20102613084934,0.491803010703882,3.99408193320625));
#46847=CARTESIAN_POINT('Ctrl Pts',(9.2487419669122,0.270965702728691,4.41046657939073));
#46848=CARTESIAN_POINT('Ctrl Pts',(9.29645780297501,-0.198703579405513,
4.44991344988054));
#46849=CARTESIAN_POINT('Ctrl Pts',(9.34417363903789,-0.485900307124067,
4.07619787653679));
#46850=CARTESIAN_POINT('Ctrl Pts',(9.39188947510068,-0.326887306273347,
3.63250862071426));
#46851=CARTESIAN_POINT('Ctrl Pts',(9.43960531116356,0.13231133773591,3.52629235307153));
#46852=CARTESIAN_POINT('Ctrl Pts',(9.48732114722637,0.470006444430667,3.85508910653225));
#46853=CARTESIAN_POINT('Ctrl Pts',(9.53503698328922,0.376087401226012,4.31695976320512));
#46854=CARTESIAN_POINT('Ctrl Pts',(9.58275281935206,-0.0631984893729827,
4.48776139227388));
#46855=CARTESIAN_POINT('Ctrl Pts',(9.63046865541489,-0.444448234747017,
4.21064422964382));
#46856=CARTESIAN_POINT('Ctrl Pts',(9.67818449147773,-0.41755432743774,3.74008922975375));
#46857=CARTESIAN_POINT('Ctrl Pts',(9.72590032754057,-0.00721385634321597,
3.50821428942208));
#46858=CARTESIAN_POINT('Ctrl Pts',(9.77361616360341,0.40975121003073,3.72795373420991));
#46859=CARTESIAN_POINT('Ctrl Pts',(9.82133199966624,0.450435435400681,4.19751745084266));
#46860=CARTESIAN_POINT('Ctrl Pts',(9.86904783572909,0.077477869602138,4.48569785316993));
#46861=CARTESIAN_POINT('Ctrl Pts',(9.91676367179192,-0.366628816002305,
4.3278544435092));
#46862=CARTESIAN_POINT('Ctrl Pts',(9.96447950785476,-0.474054618562381,
3.8689372536849));
#46863=CARTESIAN_POINT('Ctrl Pts',(10.0121953439176,-0.146148770628728,
3.53037700046135));
#46864=CARTESIAN_POINT('Ctrl Pts',(10.0599111799804,0.315967742161179,3.62307877379278));
#46865=CARTESIAN_POINT('Ctrl Pts',(10.1076270160433,0.487926215535836,4.06191310882887));
#46866=CARTESIAN_POINT('Ctrl Pts',(10.1553428521061,0.211814537474087,4.44389168337175));
#46867=CARTESIAN_POINT('Ctrl Pts',(10.203058688169,-0.258809689535701,4.4182376949229));
#46868=CARTESIAN_POINT('Ctrl Pts',(10.2507745242318,-0.491764996345908,
4.00850959581219));
#46869=CARTESIAN_POINT('Ctrl Pts',(10.2984903602946,-0.273124940234581,
3.59096700393021));
#46870=CARTESIAN_POINT('Ctrl Pts',(10.3462061963575,0.196329951061554,3.54904570612073));
#46871=CARTESIAN_POINT('Ctrl Pts',(10.3939220324203,0.485492027373267,3.92124267520431));
#46872=CARTESIAN_POINT('Ctrl Pts',(10.4416378684831,0.328819304693055,4.36576370748498));
#46873=CARTESIAN_POINT('Ctrl Pts',(10.489353704546,-0.129813245022134,4.47439829918413));
#46874=CARTESIAN_POINT('Ctrl Pts',(10.5370695406088,-0.469236294399976,
4.14738563318641));
#46875=CARTESIAN_POINT('Ctrl Pts',(10.5847853766716,-0.377752434501872,
3.68502647241413));
#46876=CARTESIAN_POINT('Ctrl Pts',(10.6325012127345,0.0606272984676223,
3.51191234851464));
#46877=CARTESIAN_POINT('Ctrl Pts',(10.6802170487973,0.443332050383407,3.78701662516801));
#46878=CARTESIAN_POINT('Ctrl Pts',(10.7279328848602,0.418918158891686,4.25770681210006));
#46879=CARTESIAN_POINT('Ctrl Pts',(10.775648720923,0.00980527620531799,
4.49174086815163));
#46880=CARTESIAN_POINT('Ctrl Pts',(10.8233645569858,-0.408311942493964,
4.27420171857372));
#46881=CARTESIAN_POINT('Ctrl Pts',(10.8710803930487,-0.451470021714238,
3.80485891169382));
#46882=CARTESIAN_POINT('Ctrl Pts',(10.9187962291115,-0.080036233235122,
3.51471716883706));
#46883=CARTESIAN_POINT('Ctrl Pts',(10.9665120651743,0.364896059739551,3.6702181168734));
#46884=CARTESIAN_POINT('Ctrl Pts',(11.0142279012372,0.47473868640782,4.1285628425314));
#46885=CARTESIAN_POINT('Ctrl Pts',(11.0619437373,0.148621472554162,4.46884633169921));
#46886=CARTESIAN_POINT('Ctrl Pts',(11.1096595733629,-0.313977126381285,
4.37858102033954));
#46887=CARTESIAN_POINT('Ctrl Pts',(11.1573754094257,-0.488245699001722,
3.94065893278431));
#46888=CARTESIAN_POINT('Ctrl Pts',(11.2050912454886,-0.214150733603143,
3.55723066033293));
#46889=CARTESIAN_POINT('Ctrl Pts',(11.2528070815514,0.256602145595791,3.58040428537983));
#46890=CARTESIAN_POINT('Ctrl Pts',(11.3005229176142,0.491713326162588,3.98889911147238));
#46891=CARTESIAN_POINT('Ctrl Pts',(11.3482387536771,0.275276593332242,4.40758805430897));
#46892=CARTESIAN_POINT('Ctrl Pts',(11.3959545897399,-0.193950870829933,
4.45198261532529));
#46893=CARTESIAN_POINT('Ctrl Pts',(11.4436704258028,-0.485070265991237,
4.08131458604192));
#46894=CARTESIAN_POINT('Ctrl Pts',(11.4913862618656,-0.330742172127369,
3.63597412121053));
#46895=CARTESIAN_POINT('Ctrl Pts',(11.5391020979284,0.127311547523522,3.52492422212962));
#46896=CARTESIAN_POINT('Ctrl Pts',(11.5868179339912,0.468453114143607,3.85014371984754));
#46897=CARTESIAN_POINT('Ctrl Pts',(11.6345337700541,0.379406977967949,4.31297854546471));
#46898=CARTESIAN_POINT('Ctrl Pts',(11.6822496061169,-0.0580544240024287,
4.48840035698771));
#46899=CARTESIAN_POINT('Ctrl Pts',(11.7299654421798,-0.44220355512924,4.21531660568344));
#46900=CARTESIAN_POINT('Ctrl Pts',(11.7776812782426,-0.420270357404582,
3.74450430230823));
#46901=CARTESIAN_POINT('Ctrl Pts',(11.8253971143054,-0.0123964237846327,
3.50831762943));
#46902=CARTESIAN_POINT('Ctrl Pts',(11.8731129503683,0.406861336540243,3.72365044295193));
#46903=CARTESIAN_POINT('Ctrl Pts',(11.9208287864311,0.452492071153857,4.1927593068956));
#46904=CARTESIAN_POINT('Ctrl Pts',(11.968544622494,0.0825923743414284,4.48485433333386));
#46905=CARTESIAN_POINT('Ctrl Pts',(12.0162604585568,-0.363153170675764,
4.33170016502878));
#46906=CARTESIAN_POINT('Ctrl Pts',(12.0639762946196,-0.475409571231627,
3.87394063131468));
#46907=CARTESIAN_POINT('Ctrl Pts',(12.1116921306825,-0.151090047408964,
3.53194335553704));
#46908=CARTESIAN_POINT('Ctrl Pts',(12.1594079667453,0.311977791768556,3.61976969834691));
#46909=CARTESIAN_POINT('Ctrl Pts',(12.2071238028081,0.488551624369653,4.05676737776005));
#46910=CARTESIAN_POINT('Ctrl Pts',(12.254839638871,0.216480982979095,4.44163470069774));
#46911=CARTESIAN_POINT('Ctrl Pts',(12.3025554749338,-0.254387476069249,
4.42094208256136));
#46912=CARTESIAN_POINT('Ctrl Pts',(12.3502713109967,-0.49164800158875,4.0136918729824));
#46913=CARTESIAN_POINT('Ctrl Pts',(12.3979871470595,-0.277420602272412,
3.59386820576715));
#46914=CARTESIAN_POINT('Ctrl Pts',(12.4457029831224,0.191566404775332,3.54700161433684));
#46915=CARTESIAN_POINT('Ctrl Pts',(12.4934188191852,0.484635034689867,3.91613041073711));
#46916=CARTESIAN_POINT('Ctrl Pts',(12.541134655248,0.332655855180181,4.362277941457));
#46917=CARTESIAN_POINT('Ctrl Pts',(12.5888504913109,-0.124806314709729,
4.47574006417428));
#46918=CARTESIAN_POINT('Ctrl Pts',(12.6365663273737,-0.4676569254097,4.15232276575852));
#46919=CARTESIAN_POINT('Ctrl Pts',(12.6842821634365,-0.381050985679211,
3.68902512775968));
#46920=CARTESIAN_POINT('Ctrl Pts',(12.7319979994994,0.0554799374235607,
3.5113004999026));
#46921=CARTESIAN_POINT('Ctrl Pts',(12.7797138355622,0.441062780321708,3.78235614259331));
#46922=CARTESIAN_POINT('Ctrl Pts',(12.8274296716251,0.421610885427219,4.2532774884218));
#46923=CARTESIAN_POINT('Ctrl Pts',(12.8751455076879,0.0149872271275763,
4.49161021945745));
#46924=CARTESIAN_POINT('Ctrl Pts',(12.9228613437507,-0.405399432451448,
4.27848972156979));
#46925=CARTESIAN_POINT('Ctrl Pts',(12.9705771798136,-0.453501555338242,
3.80962782724943));
#46926=CARTESIAN_POINT('Ctrl Pts',(13.0182930158764,-0.0851462219395619,
3.51558762841831));
#46927=CARTESIAN_POINT('Ctrl Pts',(13.0660088519392,0.361400197209248,3.66639076405307));
#46928=CARTESIAN_POINT('Ctrl Pts',(13.1137246880021,0.476067254403989,4.1235523942958));
#46929=CARTESIAN_POINT('Ctrl Pts',(13.1614405240649,0.153554426643267,4.46725395975876));
#46930=CARTESIAN_POINT('Ctrl Pts',(13.2091563601278,-0.30996979384252,4.38186902434892));
#46931=CARTESIAN_POINT('Ctrl Pts',(13.2568721961906,-0.488843983144383,
3.94580788806928));
#46932=CARTESIAN_POINT('Ctrl Pts',(13.3045880322534,-0.218805220893238,
3.55951220202843));
#46933=CARTESIAN_POINT('Ctrl Pts',(13.3523038683163,0.252165742455243,3.57772323864086));
#46934=CARTESIAN_POINT('Ctrl Pts',(13.4000197043791,0.491569024438394,3.98371752277252));
#46935=CARTESIAN_POINT('Ctrl Pts',(13.447735540442,0.279556907518101,4.40466425628032));
#46936=CARTESIAN_POINT('Ctrl Pts',(13.4954513765048,-0.189176619112,4.45400157668594));
#46937=CARTESIAN_POINT('Ctrl Pts',(13.5431672125676,-0.484186345555107,
4.08642226350871));
#46938=CARTESIAN_POINT('Ctrl Pts',(13.5908830486304,-0.334560300710407,
3.63948005597396));
#46939=CARTESIAN_POINT('Ctrl Pts',(13.6385988846933,0.122297616148583,3.52360886035071));
#46940=CARTESIAN_POINT('Ctrl Pts',(13.6863147207561,0.466847750307624,3.8452149784873));
#46941=CARTESIAN_POINT('Ctrl Pts',(13.734030556819,0.3826844119832,4.30896256355269));
#46942=CARTESIAN_POINT('Ctrl Pts',(13.7817463928818,-0.0529039102219543,
4.48898507250754));
#46943=CARTESIAN_POINT('Ctrl Pts',(13.8294622289446,-0.439909757638992,
4.21996506537626));
#46944=CARTESIAN_POINT('Ctrl Pts',(13.8771780650075,-0.422939705734467,
3.74894775411238));
#46945=CARTESIAN_POINT('Ctrl Pts',(13.9248939010703,-0.0175776142901187,
3.50847558318244));
#46946=CARTESIAN_POINT('Ctrl Pts',(13.9726097371332,0.403926270823208,3.71937784729135));
#46947=CARTESIAN_POINT('Ctrl Pts',(14.020325573196,0.454498446235019,4.18797975215946));
#46948=CARTESIAN_POINT('Ctrl Pts',(14.0680414092588,0.0876977051117048,
4.48395695817926));
#46949=CARTESIAN_POINT('Ctrl Pts',(14.1157572453217,-0.359637188018331,
4.33550904286807));
#46950=CARTESIAN_POINT('Ctrl Pts',(14.1634730813845,-0.476711717661702,
3.87895801102093));
#46951=CARTESIAN_POINT('Ctrl Pts',(14.2111889174473,-0.156014541823709,
3.53356170012368));
#46952=CARTESIAN_POINT('Ctrl Pts',(14.2589047535102,0.307953188363286,3.61650285707861));
#46953=CARTESIAN_POINT('Ctrl Pts',(14.306620589573,0.4891227672074,4.05161534124029));
#46954=CARTESIAN_POINT('Ctrl Pts',(14.3543364256359,0.2211233828038,4.4393286633369));
#46955=CARTESIAN_POINT('Ctrl Pts',(14.4020522616987,-0.249937006449114,
4.42359971395084));
#46956=CARTESIAN_POINT('Ctrl Pts',(14.4497680977616,-0.491476396904638,
4.01887262932433));
#46957=CARTESIAN_POINT('Ctrl Pts',(14.4974839338244,-0.281685449746218,
3.59681451879656));
#46958=CARTESIAN_POINT('Ctrl Pts',(14.5451997698872,0.186781580201919,3.54500783946397));
#46959=CARTESIAN_POINT('Ctrl Pts',(14.59291560595,0.483724211046603,3.91102746210588));
#46960=CARTESIAN_POINT('Ctrl Pts',(14.6406314420129,0.33645545583349,4.35875193531444));
#46961=CARTESIAN_POINT('Ctrl Pts',(14.6883472780757,-0.119785521504147,
4.47702898621568));
#46962=CARTESIAN_POINT('Ctrl Pts',(14.7360631141386,-0.466025611307368,
4.15724297904063));
#46963=CARTESIAN_POINT('Ctrl Pts',(14.7837789502014,-0.38430721152129,3.69305832471834));
#46964=CARTESIAN_POINT('Ctrl Pts',(14.8314947862642,0.0503264139313189,
3.51074293371195));
#46965=CARTESIAN_POINT('Ctrl Pts',(14.8792106223271,0.438744519099385,3.77771983486548));
#46966=CARTESIAN_POINT('Ctrl Pts',(14.9269264583899,0.42425678142631,4.24882003188202));
#46967=CARTESIAN_POINT('Ctrl Pts',(14.9746422944528,0.0201675133397715,
4.49142496503298));
#46968=CARTESIAN_POINT('Ctrl Pts',(15.0223581305156,-0.402441892563756,
4.28274679124913));
#46969=CARTESIAN_POINT('Ctrl Pts',(15.0700739665785,-0.455482716161518,
3.8144178884426));
#46970=CARTESIAN_POINT('Ctrl Pts',(15.1177898026413,-0.0902467530057116,
3.51651189422706));
#46971=CARTESIAN_POINT('Ctrl Pts',(15.1655056387041,0.357864192060027,3.66260046696357));
#46972=CARTESIAN_POINT('Ctrl Pts',(15.2132214747669,0.47734294310866,4.11852822244656));
#46973=CARTESIAN_POINT('Ctrl Pts',(15.2609373108298,0.15847032463534,4.46560968746574));
#46974=CARTESIAN_POINT('Ctrl Pts',(15.3086531468926,-0.305928031329979,
4.38511461215921));
#46975=CARTESIAN_POINT('Ctrl Pts',(15.3563689829555,-0.489387968817152,
3.95096286275689));
#46976=CARTESIAN_POINT('Ctrl Pts',(15.4040848190183,-0.223435404337718,
3.56184267101825));
#46977=CARTESIAN_POINT('Ctrl Pts',(15.4518006550811,0.24770132994065,3.57508909640066));
#46978=CARTESIAN_POINT('Ctrl Pts',(15.499516491144,0.491370121559653,3.97853774265298));
#46979=CARTESIAN_POINT('Ctrl Pts',(15.5472323272068,0.283806169849271,4.40169551006635));
#46980=CARTESIAN_POINT('Ctrl Pts',(15.5949481632697,-0.184381354552937,
4.4559701097059));
#46981=CARTESIAN_POINT('Ctrl Pts',(15.6426639993325,-0.483248643997369,
4.09152034160055));
#46982=CARTESIAN_POINT('Ctrl Pts',(15.6903798353953,-0.338341267922855,
3.64302603558196));
#46983=CARTESIAN_POINT('Ctrl Pts',(15.7380956714582,0.117270100534806,3.52234641383892));
#46984=CARTESIAN_POINT('Ctrl Pts',(15.785811507521,0.465190531238913,3.84030342991275));
#46985=CARTESIAN_POINT('Ctrl Pts',(15.8335273435838,0.385919339229949,4.30491226354526));
#46986=CARTESIAN_POINT('Ctrl Pts',(15.8812431796467,-0.0477475201261761,
4.48951547388594));
#46987=CARTESIAN_POINT('Ctrl Pts',(15.9289590157095,-0.437567097060412,
4.22458909239344));
#46988=CARTESIAN_POINT('Ctrl Pts',(15.9766748517724,-0.425562075928853,
3.75341909160864));
#46989=CARTESIAN_POINT('Ctrl Pts',(16.0243906878352,-0.0227568523576073,
3.50868813313462));
#46990=CARTESIAN_POINT('Ctrl Pts',(16.072106523898,0.400946338892803,3.71513642180785));
#46991=CARTESIAN_POINT('Ctrl Pts',(16.1198223599609,0.456454337785543,4.1831793175245));
#46992=CARTESIAN_POINT('Ctrl Pts',(16.1675381960237,0.0927932948370443,
4.4830058273823));
#46993=CARTESIAN_POINT('Ctrl Pts',(16.2152540320865,-0.356081258568678,
4.33928065395499));
#46994=CARTESIAN_POINT('Ctrl Pts',(16.2629698681494,-0.477960913216358,
3.88398883549692));
#46995=CARTESIAN_POINT('Ctrl Pts',(16.3106857042122,-0.160921706883503,
3.53523185446324));
#46996=CARTESIAN_POINT('Ctrl Pts',(16.358401540275,0.303894378979202,3.6132786128531));
#46997=CARTESIAN_POINT('Ctrl Pts',(16.4061173763379,0.489639580609251,4.04645757153336));
#46998=CARTESIAN_POINT('Ctrl Pts',(16.4538332124007,0.225741221292456,4.43697382743292));
#46999=CARTESIAN_POINT('Ctrl Pts',(16.5015490484636,-0.245458775012363,
4.42621029389423));
#47000=CARTESIAN_POINT('Ctrl Pts',(16.5492648845264,-0.4912502013546,4.02405128938415));
#47001=CARTESIAN_POINT('Ctrl Pts',(16.5969807205893,-0.285919008936969,
3.59980561575594));
#47002=CARTESIAN_POINT('Ctrl Pts',(16.6446965566521,0.181976008816936,3.54306460296116));
#47003=CARTESIAN_POINT('Ctrl Pts',(16.6924123927149,0.482759657613431,3.90593439612197));
#47004=CARTESIAN_POINT('Ctrl Pts',(16.7401282287778,0.340217684611379,4.35518608070932));
#47005=CARTESIAN_POINT('Ctrl Pts',(16.7878440648406,-0.114751423091257,
4.47826492214097));
#47006=CARTESIAN_POINT('Ctrl Pts',(16.8355599009034,-0.464342533291602,
4.16214572651883));
#47007=CARTESIAN_POINT('Ctrl Pts',(16.8832757369663,-0.387520750342007,
3.69712561530174));
#47008=CARTESIAN_POINT('Ctrl Pts',(16.9309915730291,0.0451673004198413,
3.51023971187451));
#47009=CARTESIAN_POINT('Ctrl Pts',(16.978707409092,0.436377524217892,3.7731082169636));
#47010=CARTESIAN_POINT('Ctrl Pts',(17.0264232451548,0.426855552995382,4.24433493759383));
#47011=CARTESIAN_POINT('Ctrl Pts',(17.0741390812176,0.0253455594402812,
4.49118512545541));
#47012=CARTESIAN_POINT('Ctrl Pts',(17.1218549172805,-0.399439651340385,
4.28697245475663));
#47013=CARTESIAN_POINT('Ctrl Pts',(17.1695707533433,-0.457413284126125,
3.81922856321607));
#47014=CARTESIAN_POINT('Ctrl Pts',(17.2172865894061,-0.0953372598908034,
3.51748986360026));
#47015=CARTESIAN_POINT('Ctrl Pts',(17.265002425469,0.354288437054553,3.6588476466131));
#47016=CARTESIAN_POINT('Ctrl Pts',(17.3127182615318,0.478565610824392,4.11349088504481));
#47017=CARTESIAN_POINT('Ctrl Pts',(17.3604340975947,0.163368620495752,4.46391369745815));
#47018=CARTESIAN_POINT('Ctrl Pts',(17.4081499336575,-0.301852287783465,
4.38831742326589));
#47019=CARTESIAN_POINT('Ctrl Pts',(17.4558657697204,-0.489877595596684,
3.956123284257));
#47020=CARTESIAN_POINT('Ctrl Pts',(17.5035816057832,-0.228040769637767,
3.56422180844494));
#47021=CARTESIAN_POINT('Ctrl Pts',(17.551297441846,0.243209403937772,3.57250215124727));
#47022=CARTESIAN_POINT('Ctrl Pts',(17.5990132779089,0.491116639619549,3.97336034645914));
#47023=CARTESIAN_POINT('Ctrl Pts',(17.6467291139717,0.288023908337871,4.39868214542132));
#47024=CARTESIAN_POINT('Ctrl Pts',(17.6944449500345,-0.179565609787963,
4.45788799572981));
#47025=CARTESIAN_POINT('Ctrl Pts',(17.7421607860973,-0.48225726547346,4.09660825404716));
#47026=CARTESIAN_POINT('Ctrl Pts',(17.7898766221602,-0.342084653792828,
3.64661166616396));
#47027=CARTESIAN_POINT('Ctrl Pts',(17.837592458223,0.112229559114723,3.52113702282083));
#47028=CARTESIAN_POINT('Ctrl Pts',(17.8853082942859,0.463481641013499,3.83540961967535));
#47029=CARTESIAN_POINT('Ctrl Pts',(17.9330241303487,0.389111400387848,4.30082809533052));
#47030=CARTESIAN_POINT('Ctrl Pts',(17.9807399664116,-0.0425858264624495,
4.48999150220845));
#47031=CARTESIAN_POINT('Ctrl Pts',(18.0284558024744,-0.435175833605105,
4.22918817311999));
#47032=CARTESIAN_POINT('Ctrl Pts',(18.0761716385373,-0.428137176707308,
3.75791781814212));
#47033=CARTESIAN_POINT('Ctrl Pts',(18.1238874746,-0.0279335627019553,3.5089552556775));
#47034=CARTESIAN_POINT('Ctrl Pts',(18.1716033106629,0.397921871745719,3.71092663761881));
#47035=CARTESIAN_POINT('Ctrl Pts',(18.2193191467257,0.458359528554279,4.17835853620019));
#47036=CARTESIAN_POINT('Ctrl Pts',(18.2670349827886,0.097878577523561,4.48200104659009));
#47037=CARTESIAN_POINT('Ctrl Pts',(18.3147508188514,-0.352485777302551,
4.34301457935691));
#47038=CARTESIAN_POINT('Ctrl Pts',(18.3624666549143,-0.479157019140895,
3.88903254594255));
#47039=CARTESIAN_POINT('Ctrl Pts',(18.4101824909771,-0.165810997523729,
3.5369536330429));
#47040=CARTESIAN_POINT('Ctrl Pts',(18.4578983270399,0.299801814449608,3.61009732380414));
#47041=CARTESIAN_POINT('Ctrl Pts',(18.5056141631028,0.49010200717001,4.04129464153984));
#47042=CARTESIAN_POINT('Ctrl Pts',(18.5533299991656,0.230333985517487,4.43457045454981));
#47043=CARTESIAN_POINT('Ctrl Pts',(18.6010458352284,-0.24095327917969,4.42877353242069));
#47044=CARTESIAN_POINT('Ctrl Pts',(18.6487616712913,-0.49096944006335,4.0292272779409));
#47045=CARTESIAN_POINT('Ctrl Pts',(18.6964775073541,-0.290120809601049,
3.60284116440841));
#47046=CARTESIAN_POINT('Ctrl Pts',(18.744193343417,0.177150224400508,3.54117212067402));
#47047=CARTESIAN_POINT('Ctrl Pts',(18.7919091794797,0.481741481528227,3.90085177849878));
#47048=CARTESIAN_POINT('Ctrl Pts',(18.8396250155427,0.343942123623612,4.35158077372017));
#47049=CARTESIAN_POINT('Ctrl Pts',(18.8873408516054,-0.109704578635382,
4.47944773466767));
#47050=CARTESIAN_POINT('Ctrl Pts',(18.9350566876684,-0.462607878309702,
4.16703046362027));
#47051=CARTESIAN_POINT('Ctrl Pts',(18.9827725237311,-0.39069124519864,3.70122654773242));
#47052=CARTESIAN_POINT('Ctrl Pts',(19.030488359794,0.0400031699426168,3.50979089028978));
#47053=CARTESIAN_POINT('Ctrl Pts',(19.0782041958568,0.433962058584907,3.76852180111673));
#47054=CARTESIAN_POINT('Ctrl Pts',(19.1259200319197,0.429406911488226,4.23982270375453));
#47055=CARTESIAN_POINT('Ctrl Pts',(19.1736358679825,0.0305207902517796,
4.49089072733801));
#47056=CARTESIAN_POINT('Ctrl Pts',(19.2213517040454,-0.396393042209671,
4.29116624277653));
#47057=CARTESIAN_POINT('Ctrl Pts',(19.2690675401082,-0.459293044881286,
3.82405931712685));
#47058=CARTESIAN_POINT('Ctrl Pts',(19.316783376171,-0.100417177000157,3.51852142809106));
#47059=CARTESIAN_POINT('Ctrl Pts',(19.3644992122339,0.350673329058588,3.65513271950473));
#47060=CARTESIAN_POINT('Ctrl Pts',(19.4122150482967,0.479735122332443,4.10844094226069));
#47061=CARTESIAN_POINT('Ctrl Pts',(19.4599308843596,0.168248769032157,4.46216617689766));
#47062=CARTESIAN_POINT('Ctrl Pts',(19.5076467204224,-0.297743013815871,
4.39147710422109));
#47063=CARTESIAN_POINT('Ctrl Pts',(19.5553625564852,-0.490312813065352,
3.96128857502183));
#47064=CARTESIAN_POINT('Ctrl Pts',(19.603078392548,-0.232620797759261,3.56664935826393));
#47065=CARTESIAN_POINT('Ctrl Pts',(19.6507942286109,0.238690449241969,3.56996267500769));
#47066=CARTESIAN_POINT('Ctrl Pts',(19.6985100646737,0.490808633485035,3.96818593857384));
#47067=CARTESIAN_POINT('Ctrl Pts',(19.7462259007366,0.292209604061002,4.39562444172689));
#47068=CARTESIAN_POINT('Ctrl Pts',(19.7939417367994,-0.174729824492781,
4.45975512619968));
#47069=CARTESIAN_POINT('Ctrl Pts',(19.8416575728622,-0.481212499922896,
4.10168523844358));
#47070=CARTESIAN_POINT('Ctrl Pts',(19.8893734089251,-0.345789702982467,
3.65023692191923));
#47071=CARTESIAN_POINT('Ctrl Pts',(19.9370892449879,0.107175910646637,3.51998011832295));
#47072=CARTESIAN_POINT('Ctrl Pts',(19.9848050810508,0.461722480014006,3.83053541934297));
#47073=CARTESIAN_POINT('Ctrl Pts',(20.0325209171136,0.392257955100357,4.29670800504879));
#47074=CARTESIAN_POINT('Ctrl Pts',(20.0802367531764,-0.0374150865130887,
4.49041783929577));
#47075=CARTESIAN_POINT('Ctrl Pts',(20.1279525892393,-0.432744382500041,
4.23375285658289));
#47076=CARTESIAN_POINT('Ctrl Pts',(20.1756684253021,-0.430649333670284,
3.76246031529274));
#47077=CARTESIAN_POINT('Ctrl Pts',(20.223384261365,-0.033136228617316,3.50924504180455));
#47078=CARTESIAN_POINT('Ctrl Pts',(20.2711000974278,0.394908089060633,3.70680919012016));
#47079=CARTESIAN_POINT('Ctrl Pts',(20.3188159334906,0.460110046434968,4.17340395051402));
#47080=CARTESIAN_POINT('Ctrl Pts',(20.3665317695535,0.103149962306437,4.48116018402389));
#47081=CARTESIAN_POINT('Ctrl Pts',(20.4142476056163,-0.34923165553999,4.34628168153608));
#47082=CARTESIAN_POINT('Ctrl Pts',(20.4540108023354,-0.457800032585507,
3.97025345815189));
#47083=CARTESIAN_POINT('Ctrl Pts',(20.4858213597105,-0.325993724402262,
3.71529210935379));
#47084=CARTESIAN_POINT('Ctrl Pts',(20.509679277742,-0.15096738523986,3.59329490328468));
#47085=CARTESIAN_POINT('Ctrl Pts',(20.5335371957734,0.0630371972956549,
3.57102347342756));
#47086=CARTESIAN_POINT('Ctrl Pts',(20.5573951138048,0.260511246441404,3.65349437971329));
#47087=CARTESIAN_POINT('Ctrl Pts',(20.5812530318362,0.394877283734959,3.82077798440408));
#47088=CARTESIAN_POINT('Ctrl Pts',(20.6051109498677,0.432370081305563,4.03184236506754));
#47089=CARTESIAN_POINT('Ctrl Pts',(20.6289688678991,0.364303478986858,4.23514367899931));
#47090=CARTESIAN_POINT('Ctrl Pts',(20.6528267859305,0.207066376217976,4.38093363836299));
#47091=CARTESIAN_POINT('Ctrl Pts',(20.6766847039619,-0.000757290757721993,
4.43358147160167));
#47092=CARTESIAN_POINT('Ctrl Pts',(20.7005426219933,-0.208420567790133,
4.38020336888205));
#47093=CARTESIAN_POINT('Ctrl Pts',(20.7244005400248,-0.365106210756856,
4.23385701605743));
#47094=CARTESIAN_POINT('Ctrl Pts',(20.7482584580562,-0.432520392530856,
4.03032528343114));
#47095=CARTESIAN_POINT('Ctrl Pts',(20.7721163760876,-0.394167874571092,
3.81937870627435));
#47096=CARTESIAN_POINT('Ctrl Pts',(20.795974294119,-0.259432524437891,3.65259868360638));
#47097=CARTESIAN_POINT('Ctrl Pts',(20.8198322121504,-0.0612578225112809,
3.57076788979259));
#47098=CARTESIAN_POINT('Ctrl Pts',(20.8436901301819,0.151895538690754,3.5938959627232));
#47099=CARTESIAN_POINT('Ctrl Pts',(20.8675480482132,0.327906592802717,3.71632757520176));
#47100=CARTESIAN_POINT('Ctrl Pts',(20.8914059662447,0.423735399567132,3.90812480123879));
#47101=CARTESIAN_POINT('Ctrl Pts',(20.9152638842761,0.415949440063929,4.12238802732943));
#47102=CARTESIAN_POINT('Ctrl Pts',(20.9391218023075,0.30645246920106,4.30672404095661));
#47103=CARTESIAN_POINT('Ctrl Pts',(20.962979720339,0.122019544809087,4.41605767475162));
#47104=CARTESIAN_POINT('Ctrl Pts',(20.9868376383703,-0.0922504941031022,
4.42365387220386));
#47105=CARTESIAN_POINT('Ctrl Pts',(21.0106955564018,-0.28396276796243,4.32765515869354));
#47106=CARTESIAN_POINT('Ctrl Pts',(21.0345534744332,-0.40623841344949,4.15153583326342));
#47107=CARTESIAN_POINT('Ctrl Pts',(21.0584113924646,-0.429177699343215,
3.93836186909709));
#47108=CARTESIAN_POINT('Ctrl Pts',(21.082269310496,-0.347171348131155,3.74026010679315));
#47109=CARTESIAN_POINT('Ctrl Pts',(21.1061272285274,-0.180272145040548,
3.605671823621));
#47110=CARTESIAN_POINT('Ctrl Pts',(21.1299851465589,0.0307085077608185,
3.56750752082027));
#47111=CARTESIAN_POINT('Ctrl Pts',(21.1538430645903,0.234180094072738,3.63509941005724));
#47112=CARTESIAN_POINT('Ctrl Pts',(21.1777009826217,0.380388268371489,3.79191943321731));
#47113=CARTESIAN_POINT('Ctrl Pts',(21.2015589006531,0.433581149524578,3.99962082296209));
#47114=CARTESIAN_POINT('Ctrl Pts',(21.2254168186846,0.380751629084578,4.2074149318183));
#47115=CARTESIAN_POINT('Ctrl Pts',(21.2492747367159,0.234817963878357,4.36449043997717));
#47116=CARTESIAN_POINT('Ctrl Pts',(21.2731326547474,0.0314649101850846,
4.43243810704058));
#47117=CARTESIAN_POINT('Ctrl Pts',(21.2969905727788,-0.179582171132277,
4.39464287755545));
#47118=CARTESIAN_POINT('Ctrl Pts',(21.3208484908102,-0.346716519889314,
4.26034671465164));
#47119=CARTESIAN_POINT('Ctrl Pts',(21.3447064088417,-0.429069235164158,
4.0623886883135));
#47120=CARTESIAN_POINT('Ctrl Pts',(21.368564326873,-0.406502834830527,3.8491749282489));
#47121=CARTESIAN_POINT('Ctrl Pts',(21.3924222449045,-0.284535418465691,
3.67284200661995));
#47122=CARTESIAN_POINT('Ctrl Pts',(21.4162801629359,-0.0929913416969399,
3.5765081259772));
#47123=CARTESIAN_POINT('Ctrl Pts',(21.4401380809674,0.121291651150069,3.58372954422009));
#47124=CARTESIAN_POINT('Ctrl Pts',(21.4639959989987,0.305915531372611,3.69274042788069));
#47125=CARTESIAN_POINT('Ctrl Pts',(21.4878539170302,0.415734731202803,3.87688464650718));
#47126=CARTESIAN_POINT('Ctrl Pts',(21.5117118350615,0.423895464867194,4.09113392265755));
#47127=CARTESIAN_POINT('Ctrl Pts',(21.535569753093,0.328402210690932,4.28309847227994));
#47128=CARTESIAN_POINT('Ctrl Pts',(21.5594276711244,0.152605670504114,4.40583773398234));
#47129=CARTESIAN_POINT('Ctrl Pts',(21.5832855891559,-0.0605071130159612,
4.42933861492812));
#47130=CARTESIAN_POINT('Ctrl Pts',(21.6071435071872,-0.258824259222961,
4.34785450957493));
#47131=CARTESIAN_POINT('Ctrl Pts',(21.6310014252187,-0.39385182381868,4.18131050126406));
#47132=CARTESIAN_POINT('Ctrl Pts',(21.6548593432501,-0.432571889182456,
3.97043113659525));
#47133=CARTESIAN_POINT('Ctrl Pts',(21.6787172612815,-0.365516344619441,
3.76678216446856));
#47134=CARTESIAN_POINT('Ctrl Pts',(21.702575179313,-0.209082097331647,3.62016130585559));
#47135=CARTESIAN_POINT('Ctrl Pts',(21.7264330973443,-0.00152158196427748,
3.56642135455923));
#47136=CARTESIAN_POINT('Ctrl Pts',(21.7502910153758,0.206411001640417,3.61870319251831));
#47137=CARTESIAN_POINT('Ctrl Pts',(21.7741489334072,0.363870472821225,3.76422248622317));
#47138=CARTESIAN_POINT('Ctrl Pts',(21.7980068514386,0.432353701764573,3.96739580449697));
#47139=CARTESIAN_POINT('Ctrl Pts',(21.82186476947,0.395114673548107,4.17854173669174));
#47140=CARTESIAN_POINT('Ctrl Pts',(21.8457226875014,0.261259344941517,4.3460293508861));
#47141=CARTESIAN_POINT('Ctrl Pts',(21.8695806055329,0.0635189899350569,
4.42890336313855));
#47142=CARTESIAN_POINT('Ctrl Pts',(21.8934385235643,-0.14975348833307,4.40689882001058));
#47143=CARTESIAN_POINT('Ctrl Pts',(21.9172964415957,-0.326407159500644,
4.28539643168872));
#47144=CARTESIAN_POINT('Ctrl Pts',(21.9411543596271,-0.423245389017799,
4.09410684177624));
#47145=CARTESIAN_POINT('Ctrl Pts',(21.9650122776585,-0.416588591947193,
3.87980556563057));
#47146=CARTESIAN_POINT('Ctrl Pts',(21.98887019569,-0.30806453650007,3.69489510271888));
#47147=CARTESIAN_POINT('Ctrl Pts',(22.0127281137213,-0.12421031036921,3.58459109808296));
#47148=CARTESIAN_POINT('Ctrl Pts',(22.0365860317528,0.0900167200678817,
3.57586588547707));
#47149=CARTESIAN_POINT('Ctrl Pts',(22.0604439497842,0.282232210442068,3.67085301705332));
#47150=CARTESIAN_POINT('Ctrl Pts',(22.0843018678157,0.405434237512275,3.8463255517439));
#47151=CARTESIAN_POINT('Ctrl Pts',(22.108159785847,0.429496549703537,4.05937567504088));
#47152=CARTESIAN_POINT('Ctrl Pts',(22.1320177038785,0.348535256241736,4.25790682842971));
#47153=CARTESIAN_POINT('Ctrl Pts',(22.1558756219099,0.182347598717988,4.39337273702606));
#47154=CARTESIAN_POINT('Ctrl Pts',(22.1797335399413,-0.0284290137391457,
4.43264829616218));
#47155=CARTESIAN_POINT('Ctrl Pts',(22.2035914579727,-0.232253957950086,
4.36612956178204));
#47156=CARTESIAN_POINT('Ctrl Pts',(22.2274493760041,-0.379286482964224,
4.21008217638027));
#47157=CARTESIAN_POINT('Ctrl Pts',(22.2513072940356,-0.433573131350875,
4.00266397632408));
#47158=CARTESIAN_POINT('Ctrl Pts',(22.275165212067,-0.381839338801546,3.79459436150246));
#47159=CARTESIAN_POINT('Ctrl Pts',(22.2990231300984,-0.236735426869051,
3.63675202040985));
#47160=CARTESIAN_POINT('Ctrl Pts',(22.3228810481298,-0.0337432544318164,
3.56773370504276));
#47161=CARTESIAN_POINT('Ctrl Pts',(22.3467389661613,0.177500062688638,3.60441627341574));
#47162=CARTESIAN_POINT('Ctrl Pts',(22.3705968841926,0.345339779804043,3.73782983856348));
#47163=CARTESIAN_POINT('Ctrl Pts',(22.3944548022241,0.428734513273282,3.93535114928888));
#47164=CARTESIAN_POINT('Ctrl Pts',(22.4183127202555,0.407291980919218,4.1486808655136));
#47165=CARTESIAN_POINT('Ctrl Pts',(22.4421706382869,0.286255462618544,4.32565405918856));
#47166=CARTESIAN_POINT('Ctrl Pts',(22.4660285563183,0.0952216904214238,
4.42299596654013));
#47167=CARTESIAN_POINT('Ctrl Pts',(22.4898864743497,-0.119096386717928,
4.41690383452019));
#47168=CARTESIAN_POINT('Ctrl Pts',(22.5137443923812,-0.304292138366774,
4.30886736509782));
#47169=CARTESIAN_POINT('Ctrl Pts',(22.5376023104126,-0.415080201412036,
4.12530439950267));
#47170=CARTESIAN_POINT('Ctrl Pts',(22.561460228444,-0.424369795825249,3.91110111771763));
#47171=CARTESIAN_POINT('Ctrl Pts',(22.5853181464754,-0.329889515310188,
3.71863599132299));
#47172=CARTESIAN_POINT('Ctrl Pts',(22.6091760645068,-0.154742073939436,
3.59497211022641));
#47173=CARTESIAN_POINT('Ctrl Pts',(22.6330339825383,0.0582436639512456,
3.57034842802071));
#47174=CARTESIAN_POINT('Ctrl Pts',(22.6568919005697,0.256987911016647,3.65078654733876));
#47175=CARTESIAN_POINT('Ctrl Pts',(22.6807498186011,0.39289034562191,3.81661632308649));
#47176=CARTESIAN_POINT('Ctrl Pts',(22.7046077366325,0.432722782933869,4.02728943245291));
#47177=CARTESIAN_POINT('Ctrl Pts',(22.7284656546639,0.366738191089385,4.2312875884069));
#47178=CARTESIAN_POINT('Ctrl Pts',(22.7523235726953,0.211084664509997,4.37873330099785));
#47179=CARTESIAN_POINT('Ctrl Pts',(22.7761814907268,0.00379901600965994,
4.43356145647204));
#47180=CARTESIAN_POINT('Ctrl Pts',(22.8000394087582,-0.204384723485633,
4.3823852668741));
#47181=CARTESIAN_POINT('Ctrl Pts',(22.8238973267896,-0.36265185203719,4.2376794731));
#47182=CARTESIAN_POINT('Ctrl Pts',(22.8398026054772,-0.408954280604672,
4.10250106973657));
#47183=CARTESIAN_POINT('Ctrl Pts',(22.847755244821,-0.414526965927561,4.03345758723954));
#47184=CARTESIAN_POINT('',(22.8,-0.592174260192535,4.04779597854866));
#47185=CARTESIAN_POINT('Ctrl Pts',(22.8,-0.19576256658266,4.36695865185836));
#47186=CARTESIAN_POINT('Ctrl Pts',(22.8,-0.195886593570853,4.36694806728808));
#47187=CARTESIAN_POINT('Ctrl Pts',(22.8,-0.196010613870461,4.36693742279878));
#47188=CARTESIAN_POINT('Ctrl Pts',(22.8,-0.196134627427637,4.36692671841166));
#47189=CARTESIAN_POINT('Ctrl Pts',(22.8,-0.216622178843513,4.36515830948628));
#47190=CARTESIAN_POINT('Ctrl Pts',(22.8,-0.236921239981942,4.36175743074964));
#47191=CARTESIAN_POINT('Ctrl Pts',(22.8,-0.256857422940798,4.35688458679081));
#47192=CARTESIAN_POINT('Ctrl Pts',(22.8,-0.271809560159941,4.35322995382169));
#47193=CARTESIAN_POINT('Ctrl Pts',(22.8,-0.286558947067823,4.34874691155445));
#47194=CARTESIAN_POINT('Ctrl Pts',(22.8,-0.301048271828705,4.34349077646485));
#47195=CARTESIAN_POINT('Ctrl Pts',(22.8,-0.310003423377303,4.3402422133286));
#47196=CARTESIAN_POINT('Ctrl Pts',(22.8,-0.318859482942331,4.33669811041118));
#47197=CARTESIAN_POINT('Ctrl Pts',(22.8,-0.327604744452034,4.33286912874946));
#47198=CARTESIAN_POINT('Ctrl Pts',(22.8,-0.333457186121174,4.33030672489195));
#47199=CARTESIAN_POINT('Ctrl Pts',(22.8,-0.33926207870774,4.32761569029118));
#47200=CARTESIAN_POINT('Ctrl Pts',(22.8,-0.345009487597299,4.32480202294401));
#47201=CARTESIAN_POINT('Ctrl Pts',(22.8,-0.365309066997251,4.31486428146495));
#47202=CARTESIAN_POINT('Ctrl Pts',(22.8,-0.384828901796994,4.30343044333042));
#47203=CARTESIAN_POINT('Ctrl Pts',(22.8,-0.403416958856431,4.29067119823496));
#47204=CARTESIAN_POINT('Ctrl Pts',(22.8,-0.409874425773003,4.28623865303559));
#47205=CARTESIAN_POINT('Ctrl Pts',(22.8,-0.416219739836017,4.28164578247975));
#47206=CARTESIAN_POINT('Ctrl Pts',(22.8,-0.422447327171508,4.27689854297234));
#47207=CARTESIAN_POINT('Ctrl Pts',(22.8,-0.43500295340691,4.2673274905416));
#47208=CARTESIAN_POINT('Ctrl Pts',(22.8,-0.447079966647781,4.25712966465555));
#47209=CARTESIAN_POINT('Ctrl Pts',(22.8,-0.458660056443695,4.24636133358853));
#47210=CARTESIAN_POINT('Ctrl Pts',(22.8,-0.465333929961841,4.24015529539631));
#47211=CARTESIAN_POINT('Ctrl Pts',(22.8,-0.471842796551704,4.23375955955572));
#47212=CARTESIAN_POINT('Ctrl Pts',(22.8,-0.478183280583292,4.22718326898633));
#47213=CARTESIAN_POINT('Ctrl Pts',(22.8,-0.48330469601013,4.22187138494));
#47214=CARTESIAN_POINT('Ctrl Pts',(22.8,-0.488310096860405,4.21644792156372));
#47215=CARTESIAN_POINT('Ctrl Pts',(22.8,-0.49319389770791,4.21092357737429));
#47216=CARTESIAN_POINT('Ctrl Pts',(22.8,-0.509882204568999,4.19204648678071));
#47217=CARTESIAN_POINT('Ctrl Pts',(22.8,-0.525164669297395,4.17198027236651));
#47218=CARTESIAN_POINT('Ctrl Pts',(22.8,-0.538985569877159,4.15095378743758));
#47219=CARTESIAN_POINT('Ctrl Pts',(22.8,-0.553292287721507,4.12918820238033));
#47220=CARTESIAN_POINT('Ctrl Pts',(22.8,-0.566034197593199,4.10639346234103));
#47221=CARTESIAN_POINT('Ctrl Pts',(22.8,-0.577149101532509,4.08276767497818));
#47222=CARTESIAN_POINT('Ctrl Pts',(22.8,-0.582543745751794,4.07130084468266));
#47223=CARTESIAN_POINT('Ctrl Pts',(22.8,-0.587554988912119,4.05963744408228));
#47224=CARTESIAN_POINT('Ctrl Pts',(22.8,-0.592174260192535,4.04779597854866));
#47225=CARTESIAN_POINT('Ctrl Pts',(22.8,-0.592174260192532,4.04779597854869));
#47226=CARTESIAN_POINT('Ctrl Pts',(22.7920473606562,-0.584213376873468,
4.14642833911734));
#47227=CARTESIAN_POINT('Ctrl Pts',(22.7840947213124,-0.551140611244481,
4.24298318064208));
#47228=CARTESIAN_POINT('Ctrl Pts',(22.7761420819686,-0.496922031827459,
4.32571394759471));
#47229=CARTESIAN_POINT('Ctrl Pts',(22.7681894426248,-0.442703452410443,
4.40844471454734));
#47230=CARTESIAN_POINT('Ctrl Pts',(22.760236803281,-0.367339059205388,4.47735140692785));
#47231=CARTESIAN_POINT('Ctrl Pts',(22.7522841639372,-0.280089901523161,
4.52398941366922));
#47232=CARTESIAN_POINT('Ctrl Pts',(22.7444712463773,-0.194373644734646,
4.56980802634291));
#47233=CARTESIAN_POINT('Ctrl Pts',(22.7366583288174,-0.0971865673270821,
4.59413356703531));
#47234=CARTESIAN_POINT('Ctrl Pts',(22.7288454112575,-7.11440487624268E-7,
4.59414971000239));
#47235=CARTESIAN_POINT('Origin',(27.2,0.3,2.9));
#47236=CARTESIAN_POINT('',(29.2,0.3,3.04606079858305));
#47237=CARTESIAN_POINT('',(27.2,0.3,3.04606079858305));
#47238=CARTESIAN_POINT('',(23.3,0.3,3.04606079858305));
#47239=CARTESIAN_POINT('',(29.2,0.3,3.35));
#47240=CARTESIAN_POINT('',(29.2,0.3,2.9));
#47241=CARTESIAN_POINT('',(27.2,0.3,3.35));
#47242=CARTESIAN_POINT('',(27.2,0.3,3.35));
#47243=CARTESIAN_POINT('',(27.2,0.3,2.9));
#47244=CARTESIAN_POINT('Origin',(27.2,0.,3.125));
#47245=CARTESIAN_POINT('',(27.2,-0.3,3.04606079858305));
#47246=CARTESIAN_POINT('Origin',(27.2,0.,4.));
#47247=CARTESIAN_POINT('',(27.2,-0.3,3.35));
#47248=CARTESIAN_POINT('',(27.2,0.3,3.35));
#47249=CARTESIAN_POINT('',(27.2,-0.3,3.35));
#47250=CARTESIAN_POINT('Origin',(27.2,0.3,3.35));
#47251=CARTESIAN_POINT('',(29.2,-0.3,3.35));
#47252=CARTESIAN_POINT('',(29.2,0.3,3.35));
#47253=CARTESIAN_POINT('',(27.2,-0.3,3.35));
#47254=CARTESIAN_POINT('Origin',(27.2,-0.3,3.35));
#47255=CARTESIAN_POINT('',(29.2,-0.3,3.04606079858305));
#47256=CARTESIAN_POINT('',(23.3,-0.3,3.04606079858305));
#47257=CARTESIAN_POINT('',(29.2,-0.3,3.35));
#47258=CARTESIAN_POINT('Origin',(29.2,0.,3.125));
#47259=CARTESIAN_POINT('Origin',(29.2,0.,4.));
#47260=CARTESIAN_POINT('Origin',(23.3,0.,4.));
#47261=CARTESIAN_POINT('',(29.4,-1.22464679914735E-16,5.));
#47262=CARTESIAN_POINT('Origin',(29.4,0.,4.));
#47263=CARTESIAN_POINT('',(23.3,-1.22464679914735E-16,5.));
#47264=CARTESIAN_POINT('',(23.3,-1.22464679914735E-16,5.));
#47265=CARTESIAN_POINT('Origin',(23.3,0.,4.));
#47266=CARTESIAN_POINT('Origin',(29.4,0.,4.));
#47267=CARTESIAN_POINT('Origin',(22.8,0.,4.));
#47268=CARTESIAN_POINT('',(22.8,-1.65327317884893E-16,5.35));
#47269=CARTESIAN_POINT('Origin',(22.8,0.,4.));
#47270=CARTESIAN_POINT('Origin',(22.8,0.,4.));
#47271=CARTESIAN_POINT('Origin',(22.8,0.,4.));
#47272=CARTESIAN_POINT('',(23.3,-1.65327317884893E-16,5.35));
#47273=CARTESIAN_POINT('Origin',(23.3,0.,4.));
#47274=CARTESIAN_POINT('',(22.8,-1.65327317884893E-16,5.35));
#47275=CARTESIAN_POINT('Origin',(23.3,0.,4.));
#47276=CARTESIAN_POINT('Origin',(4.,0.,4.));
#62827=UNCERTAINTY_MEASURE_WITH_UNIT(LENGTH_MEASURE(0.001),#62985,
'DISTANCE_ACCURACY_VALUE',
'Maximum model space distance between geometric entities at asserted c
onnectivities');
#62885=UNCERTAINTY_MEASURE_WITH_UNIT(LENGTH_MEASURE(0.001),#62985,
'DISTANCE_ACCURACY_VALUE',
'Maximum model space distance between geometric entities at asserted c
onnectivities');
#62926=(
GEOMETRIC_REPRESENTATION_CONTEXT(3)
GLOBAL_UNCERTAINTY_ASSIGNED_CONTEXT((#62827))
GLOBAL_UNIT_ASSIGNED_CONTEXT((#62985,#62987,#62988))
REPRESENTATION_CONTEXT('','3D')
);
#62984=(
GEOMETRIC_REPRESENTATION_CONTEXT(3)
GLOBAL_UNCERTAINTY_ASSIGNED_CONTEXT((#62885))
GLOBAL_UNIT_ASSIGNED_CONTEXT((#62985,#62987,#62988))
REPRESENTATION_CONTEXT('','3D')
);
#62985=(
LENGTH_UNIT()
NAMED_UNIT(*)
SI_UNIT(.CENTI.,.METRE.)
);
#62987=(
NAMED_UNIT(*)
PLANE_ANGLE_UNIT()
SI_UNIT($,.RADIAN.)
);
#62988=(
NAMED_UNIT(*)
SI_UNIT($,.STERADIAN.)
SOLID_ANGLE_UNIT()
);
#63029=SHAPE_DEFINITION_REPRESENTATION(#63160,#63389);
#63160=PRODUCT_DEFINITION_SHAPE('',$,#63488);
#63389=SHAPE_REPRESENTATION('',(#24870),#62926);
#63447=PRODUCT_DEFINITION_CONTEXT('part definition',#63743,'design');
#63488=PRODUCT_DEFINITION('X Stage - 01 Supported TR12x3 screw',
'X Stage - 01 Supported TR12x3 screw',#63586,#63447);
#63586=PRODUCT_DEFINITION_FORMATION('',$,#63785);
#63743=APPLICATION_CONTEXT(
'Core Data for Automotive Mechanical Design Process');
#63744=PRODUCT_CONTEXT('part definition',#63743,'mechanical');
#63785=PRODUCT('X Stage - 01 Supported TR12x3 screw',
'X Stage - 01 Supported TR12x3 screw',
'X Stage - 01 Supported TR12x3 screw',(#63744));
#63913=COLOUR_RGB('Black',0.12,0.14,0.17);
#63914=FILL_AREA_STYLE_COLOUR('',#63913);
#63915=FILL_AREA_STYLE('',(#63914));
#63916=SURFACE_STYLE_FILL_AREA(#63915);
#63917=SURFACE_SIDE_STYLE('',(#63916));
#63918=SURFACE_STYLE_USAGE(.BOTH.,#63917);
#63919=PRESENTATION_STYLE_ASSIGNMENT((#63918));
ENDSEC;
END-ISO-10303-21;
